ISO-10303-21;
HEADER;
FILE_DESCRIPTION (('STEP AP214'),
    '1' );
FILE_NAME ('MirrorTreadle Extension Return Springs.step',
    '2026-10-21T17:07:05',
    ( '' ),
    ( '' ),
    'SwSTEP 2.0',
    'SolidWorks 2025',
    '' );
FILE_SCHEMA (( 'AUTOMOTIVE_DESIGN' ));
ENDSEC;

DATA;
#3=CARTESIAN_POINT ( 'NONE',  ( 745.1769319972822814, -209.8055962898687881, 346.2694204179732083 ) ) ;
#4=CARTESIAN_POINT ( 'NONE',  ( 797.8594530101009923, -13.54369356751140963, 322.1405469898982119 ) ) ;
#6=VERTEX_POINT ( 'NONE', #33122 ) ;
#8=CARTESIAN_POINT ( 'NONE',  ( 781.8018195045266339, -190.2709662947835909, 365.1927285166406705 ) ) ;
#10=CARTESIAN_POINT ( 'NONE',  ( 757.8323909638828582, -314.6346026584195101, 352.1044303154654358 ) ) ;
#13=CARTESIAN_POINT ( 'NONE',  ( 755.8398074228967971, -67.44195992623289726, 333.4516893846970333 ) ) ;
#15=CARTESIAN_POINT ( 'NONE',  ( 812.7932403749906598, -255.1800572038742700, 327.7687537140311633 ) ) ;
#16=CARTESIAN_POINT ( 'NONE',  ( 748.3538107759620743, 7.285312801039605546, 355.8262568251490165 ) ) ;
#21=CARTESIAN_POINT ( 'NONE',  ( 808.0189434323515343, -278.0891481129651197, 319.0252816721025511 ) ) ;
#22=CARTESIAN_POINT ( 'NONE',  ( 798.6699377194444196, -457.0491014588743042, 363.8754770338464368 ) ) ;
#23=CARTESIAN_POINT ( 'NONE',  ( 756.1348686366196716, -329.2601417444138860, 347.5531968255698416 ) ) ;
#25=CARTESIAN_POINT ( 'NONE',  ( 800.9840315886518738, -148.9181544815166092, 354.1144889064786412 ) ) ;
#26=CARTESIAN_POINT ( 'NONE',  ( 788.7366044899766848, -11.90732993114778182, 316.5762568750059813 ) ) ;
#30=CARTESIAN_POINT ( 'NONE',  ( 745.7194118038753459, -229.6454272087890729, 348.7631598425976449 ) ) ;
#31=CARTESIAN_POINT ( 'NONE',  ( 776.9566956441375396, -180.8965053807779952, 364.8461984189686405 ) ) ;
#33=CARTESIAN_POINT ( 'NONE',  ( 772.4999999999993179, -512.9681489794448908, 339.9999999999999432 ) ) ;
#35=CARTESIAN_POINT ( 'NONE',  ( 759.0252816721024374, -0.9982390220569063999, 368.0189434323527280 ) ) ;
#36=CARTESIAN_POINT ( 'NONE',  ( 801.4587497624105481, -452.9681489794446634, 353.8271441104080282 ) ) ;
#40=CARTESIAN_POINT ( 'NONE',  ( 814.2805881961230625, -337.6454272087888171, 331.2368401574024119 ) ) ;
#42=CARTESIAN_POINT ( 'NONE',  ( 814.9108240113580450, -328.2709662947831362, 337.5031285880265273 ) ) ;
#46=CARTESIAN_POINT ( 'NONE',  ( 781.8018195045266339, -430.2709662947827383, 365.1927285166406705 ) ) ;
#47=CARTESIAN_POINT ( 'NONE',  ( 799.2566176426618085, -168.0090635724256458, 324.0069404352559559 ) ) ;
#50=CARTESIAN_POINT ( 'NONE',  ( 815.0009284576459549, -102.3510508353236901, 338.7629533639073429 ) ) ;
#51=CARTESIAN_POINT ( 'NONE',  ( 795.1360043628808398, -404.0891481129646650, 360.2193346964456282 ) ) ;
#53=CARTESIAN_POINT ( 'NONE',  ( 771.2368401574024119, -157.4419599262326130, 374.2805881961240857 ) ) ;
#54=CARTESIAN_POINT ( 'NONE',  ( 804.9363028652555840, -448.2709662947827951, 338.2165204200192079 ) ) ;
#56=VERTEX_POINT ( 'NONE', #45682 ) ;
#59=EDGE_CURVE ( 'NONE', #755, #21705, #14891, .T. ) ;
#60=CARTESIAN_POINT ( 'NONE',  ( 767.8955696845333705, -240.4527844766015221, 362.1676090361162323 ) ) ;
#61=CARTESIAN_POINT ( 'NONE',  ( 797.8594530101009923, -229.5436935675107009, 322.1405469898982119 ) ) ;
#63=CARTESIAN_POINT ( 'NONE',  ( 812.6845335610512393, -439.9874144716862929, 353.5525998758768651 ) ) ;
#68=CARTESIAN_POINT ( 'NONE',  ( 767.7687537140311633, -143.9073299311473590, 372.7932403749916830 ) ) ;
#70=CARTESIAN_POINT ( 'NONE',  ( 752.4576283171824116, -189.0783235625961822, 317.7880784355627952 ) ) ;
#75=CARTESIAN_POINT ( 'NONE',  ( 763.2154366446407039, -213.6237781080506011, 321.4292242960311228 ) ) ;
#84=CARTESIAN_POINT ( 'NONE',  ( 802.2119215644370342, -150.0090635724257027, 367.5423716828165084 ) ) ;
#91=CARTESIAN_POINT ( 'NONE',  ( 781.2370466360911223, -380.7363362996977116, 304.9990715423533629 ) ) ;
#96=CARTESIAN_POINT ( 'NONE',  ( 788.7366044899766848, -11.90732993114778182, 316.5762568750059813 ) ) ;
#98=CARTESIAN_POINT ( 'NONE',  ( 786.2694204179717872, -261.2817908451526705, 305.1769319972829067 ) ) ;
#100=CARTESIAN_POINT ( 'NONE',  ( 814.2001403089898304, -209.3618753856926276, 347.4397851343538264 ) ) ;
#103=CARTESIAN_POINT ( 'NONE',  ( 804.9363028652555840, -304.2709662947832499, 338.2165204200192079 ) ) ;
#104=CARTESIAN_POINT ( 'NONE',  ( 802.9823548866075953, -97.09997266333496668, 330.0799878456151077 ) ) ;
#108=CARTESIAN_POINT ( 'NONE',  ( 799.9999999999993179, 205.0000000000000568, 319.9999999999999432 ) ) ;
#110=CARTESIAN_POINT ( 'NONE',  ( 776.9566956441375396, -132.8965053807781374, 364.8461984189686405 ) ) ;
#111=CARTESIAN_POINT ( 'NONE',  ( 768.0187753319979720, -368.6346026584193964, 318.0580252608186242 ) ) ;
#115=CARTESIAN_POINT ( 'NONE',  ( 795.1360043628807261, -140.0891481129654892, 360.2193346964456282 ) ) ;
#116=CARTESIAN_POINT ( 'NONE',  ( 788.7366044899766848, -107.9073299311474727, 316.5762568750059813 ) ) ;
#119=CARTESIAN_POINT ( 'NONE',  ( 788.7631598425961101, -409.4419599262317320, 305.7194118038759143 ) ) ;
#121=CARTESIAN_POINT ( 'NONE',  ( 805.1927285166397041, -328.8164208402375834, 341.8018195045277707 ) ) ;
#125=CARTESIAN_POINT ( 'NONE',  ( 794.9819416627830151, -420.9982390220555999, 319.9864689768909898 ) ) ;
#133=CARTESIAN_POINT ( 'NONE',  ( 763.0428371773158460, -443.4636090269702322, 358.7617431975195359 ) ) ;
#134=CARTESIAN_POINT ( 'NONE',  ( 800.7704444035546203, -124.1692326535054463, 326.0291762391768771 ) ) ;
#135=DIRECTION ( 'NONE',  ( 0.000000000000000000, 1.110223024625155554E-15, -1.000000000000000000 ) ) ;
#137=CARTESIAN_POINT ( 'NONE',  ( 801.9858362298568863, -387.0783235625955285, 312.7379699480935642 ) ) ;
#138=EDGE_CURVE ( 'NONE', #11154, #34810, #22920, .T. ) ;
#143=CARTESIAN_POINT ( 'NONE',  ( 797.8822607201568644, -30.55451811788062244, 370.1134526219340160 ) ) ;
#152=CARTESIAN_POINT ( 'NONE',  ( 755.3028492785439312, -351.2817908451523294, 335.9200461376539693 ) ) ;
#153=CARTESIAN_POINT ( 'NONE',  ( 805.6418435158337843, -341.4636090269705733, 363.8556311672236916 ) ) ;
#157=CARTESIAN_POINT ( 'NONE',  ( 778.7629533639073998, -152.7363362996983938, 375.0009284576466371 ) ) ;
#159=CARTESIAN_POINT ( 'NONE',  ( 792.3570229623688874, -117.1800572038746964, 373.1304606946836202 ) ) ;
#163=CARTESIAN_POINT ( 'NONE',  ( 768.0187753319979720, -200.6346026584199365, 318.0580252608186242 ) ) ;
#165=CARTESIAN_POINT ( 'NONE',  ( 776.9254006560222479, 3.809118245755632959, 314.8983024940802125 ) ) ;
#170=CARTESIAN_POINT ( 'NONE',  ( 808.7758568127978833, -4.169232653505813069, 320.0363995740631822 ) ) ;
#173=CARTESIAN_POINT ( 'NONE',  ( 791.1614460488616487, -323.2601417444138860, 373.5763878283158874 ) ) ;
#174=CARTESIAN_POINT ( 'NONE',  ( 754.8072714833583632, -124.8164208402383366, 338.1981804954721156 ) ) ;
#176=CARTESIAN_POINT ( 'NONE',  ( 785.3141322388236176, -309.7255117493287457, 364.4286716492789537 ) ) ;
#179=CARTESIAN_POINT ( 'NONE',  ( 792.2312462859673587, -83.90732993114754379, 307.2067596250082602 ) ) ;
#180=ORIENTED_EDGE ( 'NONE', *, *, #7452, .F. ) ;
#185=CARTESIAN_POINT ( 'NONE',  ( 778.2165204200184689, -22.81642084023865280, 364.9363028652563230 ) ) ;
#187=CARTESIAN_POINT ( 'NONE',  ( 805.0032342141413437, -349.5436935675103314, 314.9967657858572352 ) ) ;
#188=CARTESIAN_POINT ( 'NONE',  ( 747.3154664389472828, -283.9874144716867477, 326.4474001241230781 ) ) ;
#190=CARTESIAN_POINT ( 'NONE',  ( 808.7758568127978833, -76.16923265350557415, 320.0363995740631822 ) ) ;
#196=CARTESIAN_POINT ( 'NONE',  ( 782.4968714119720516, -394.8164208402374697, 305.0891759886411023 ) ) ;
#202=EDGE_CURVE ( 'NONE', #18957, #27321, #40211, .T. ) ;
#203=CARTESIAN_POINT ( 'NONE',  ( 780.5236548040995785, -260.7363362996981095, 314.9735926884559944 ) ) ;
#204=CARTESIAN_POINT ( 'NONE',  ( 788.8264449731200330, -117.1800572038746964, 363.6646147819171233 ) ) ;
#208=CARTESIAN_POINT ( 'NONE',  ( 801.3366627262608972, -296.5328690171411949, 353.0897708529566899 ) ) ;
#210=CARTESIAN_POINT ( 'NONE',  ( 814.4686193811664907, -51.28179084515328867, 346.2056067578752732 ) ) ;
#212=CARTESIAN_POINT ( 'NONE',  ( 814.5518280994195948, -183.7255117493290015, 332.4837098697145734 ) ) ;
#213=CARTESIAN_POINT ( 'NONE',  ( 774.6312213355099630, -71.36187538569302546, 364.6798772138717482 ) ) ;
#217=CARTESIAN_POINT ( 'NONE',  ( 802.2119215644370342, -438.0090635724247932, 367.5423716828165084 ) ) ;
#220=CARTESIAN_POINT ( 'NONE',  ( 787.6308680596127942, -347.2601417444138860, 364.1105419155492768 ) ) ;
#221=CARTESIAN_POINT ( 'NONE',  ( 745.7998596910086917, -53.36187538569310362, 332.5602148656461168 ) ) ;
#223=CARTESIAN_POINT ( 'NONE',  ( 776.9566956441375396, -60.89650538077837894, 364.8461984189686405 ) ) ;
#226=CARTESIAN_POINT ( 'NONE',  ( 773.7943932421234194, -215.8055962898687881, 305.5313806188329409 ) ) ;
#227=CARTESIAN_POINT ( 'NONE',  ( 781.7834795799800531, -10.81642084023869543, 315.0636971347436202 ) ) ;
#230=CARTESIAN_POINT ( 'NONE',  ( 791.9812246680005501, -212.6346026584198796, 361.9419747391813189 ) ) ;
#232=CARTESIAN_POINT ( 'NONE',  ( 756.3353852180820240, -317.9073299311467622, 331.1735550268787733 ) ) ;
#236=CARTESIAN_POINT ( 'NONE',  ( 789.9200121543843807, -49.98741447168749374, 317.0176451133914384 ) ) ;
#238=CARTESIAN_POINT ( 'NONE',  ( 759.0252816721024374, -264.9982390220561115, 368.0189434323527280 ) ) ;
#239=CARTESIAN_POINT ( 'NONE',  ( 746.7653713866222915, 6.739858255585061464, 351.0478386215610271 ) ) ;
#246=CARTESIAN_POINT ( 'NONE',  ( 763.0537975583475827, -288.4527844766014937, 371.0346526505627480 ) ) ;
#248=CARTESIAN_POINT ( 'NONE',  ( 794.1144889064781864, -322.1692326535048210, 360.9840315886528401 ) ) ;
#250=CARTESIAN_POINT ( 'NONE',  ( 799.2566176426618085, -168.0090635724256458, 324.0069404352559559 ) ) ;
#251=CARTESIAN_POINT ( 'NONE',  ( 759.9864689768902508, -26.08914811296592262, 354.9819416627836404 ) ) ;
#255=CARTESIAN_POINT ( 'NONE',  ( 750.9282345327678740, -232.9181544815163249, 319.8311093483690115 ) ) ;
#256=CARTESIAN_POINT ( 'NONE',  ( 786.6156483768007774, -193.4419599262325278, 315.5913626894246136 ) ) ;
#259=CARTESIAN_POINT ( 'NONE',  ( 781.7834795799800531, 13.18357915976123174, 315.0636971347436202 ) ) ;
#262=CARTESIAN_POINT ( 'NONE',  ( 767.6429770376289525, -9.180057203875058747, 306.8695393053162093 ) ) ;
#263=CARTESIAN_POINT ( 'NONE',  ( 782.4968714119720516, -82.81642084023846451, 305.0891759886411023 ) ) ;
#268=CARTESIAN_POINT ( 'NONE',  ( 793.5525998758768083, -367.0999726633342561, 372.6845335610516941 ) ) ;
#270=CARTESIAN_POINT ( 'NONE',  ( 767.7687537140311633, -335.9073299311468190, 372.7932403749916830 ) ) ;
#274=CARTESIAN_POINT ( 'NONE',  ( 759.9864689768902508, -434.0891481129646081, 354.9819416627836404 ) ) ;
#275=CARTESIAN_POINT ( 'NONE',  ( 755.1538015810308480, -206.1908817542437191, 343.0433043558613804 ) ) ;
#278=CARTESIAN_POINT ( 'NONE',  ( 786.2056067578752163, -107.8055962898691433, 374.4686193811670023 ) ) ;
#279=CARTESIAN_POINT ( 'NONE',  ( 778.2165204200184689, -406.8164208402375266, 364.9363028652563230 ) ) ;
#281=CARTESIAN_POINT ( 'NONE',  ( 801.9419747391806368, -450.4527844766009821, 351.9812246680014027 ) ) ;
#285=CARTESIAN_POINT ( 'NONE',  ( 762.3223304703356007, -223.5436935675107577, 322.3223304703362828 ) ) ;
#286=CARTESIAN_POINT ( 'NONE',  ( 778.1981804954715471, -226.2709662947834488, 314.8072714833591021 ) ) ;
#290=CARTESIAN_POINT ( 'NONE',  ( 765.0180583372156207, -432.9982390220555999, 360.0135310231089534 ) ) ;
#294=CARTESIAN_POINT ( 'NONE',  ( 804.7487373415286811, -163.5436935675109567, 364.7487373415288516 ) ) ;
#295=CARTESIAN_POINT ( 'NONE',  ( 759.0159684113467620, -280.9181544815162965, 325.8855110935213020 ) ) ;
#297=CARTESIAN_POINT ( 'NONE',  ( 783.7566961878529810, -192.8965053807779668, 305.1792804349288417 ) ) ;
#302=CARTESIAN_POINT ( 'NONE',  ( 790.8726784830453198, -226.7146871989596661, 362.5472867521010585 ) ) ;
#311=CARTESIAN_POINT ( 'NONE',  ( 762.1177392798416577, -138.5545181178802636, 309.8865473780659272 ) ) ;
#322=CARTESIAN_POINT ( 'NONE',  ( 795.1360043628807261, 3.910851887033985896, 360.2193346964456282 ) ) ;
#324=CARTESIAN_POINT ( 'NONE',  ( 814.2805881961230625, -265.6454272087889876, 331.2368401574024119 ) ) ;
#326=CARTESIAN_POINT ( 'NONE',  ( 746.8695393053150156, -221.9073299311470464, 327.6429770376306010 ) ) ;
#330=CARTESIAN_POINT ( 'NONE',  ( 795.1360043628807261, -308.0891481129650629, 360.2193346964456282 ) ) ;
#331=CARTESIAN_POINT ( 'NONE',  ( 772.4468031744293057, -81.82724539060772884, 363.8651313633793620 ) ) ;
#332=CARTESIAN_POINT ( 'NONE',  ( 802.5472867521000353, -76.37269993606228979, 350.8726784830461156 ) ) ;
#336=CARTESIAN_POINT ( 'NONE',  ( 773.3843516231979720, -109.4419599262327836, 364.4086373105754433 ) ) ;
#337=CARTESIAN_POINT ( 'NONE',  ( 797.8594530101008786, -373.5436935675101040, 322.1405469898980982 ) ) ;
#341=CARTESIAN_POINT ( 'NONE',  ( 803.4237431249931660, -111.1800572038747532, 331.2633955100225194 ) ) ;
#345=CARTESIAN_POINT ( 'NONE',  ( 800.1688906516307043, -418.1692326535044799, 369.0717654672308186 ) ) ;
#347=CARTESIAN_POINT ( 'NONE',  ( 774.6312213355099630, -311.3618753856922581, 364.6798772138717482 ) ) ;
#351=CARTESIAN_POINT ( 'NONE',  ( 803.4237431249931660, -423.1800572038737300, 331.2633955100225194 ) ) ;
#360=CARTESIAN_POINT ( 'NONE',  ( 762.3223304703356007, -127.5436935675110561, 322.3223304703362828 ) ) ;
#361=CARTESIAN_POINT ( 'NONE',  ( 758.4439275373578084, -444.5545181178792973, 353.2243759319684386 ) ) ;
#362=CARTESIAN_POINT ( 'NONE',  ( 761.2382568024794409, -135.6237781080508853, 356.9571628226838129 ) ) ;
#365=CARTESIAN_POINT ( 'NONE',  ( 745.1769319972822814, -377.8055962898682765, 346.2694204179732083 ) ) ;
#371=CARTESIAN_POINT ( 'NONE',  ( 795.8262568251477660, -22.37269993606246743, 308.3538107759623585 ) ) ;
#379=CARTESIAN_POINT ( 'NONE',  ( 759.0159684113467620, -376.9181544815159555, 325.8855110935213020 ) ) ;
#381=CARTESIAN_POINT ( 'NONE',  ( 766.4474001241216001, -331.0999726633342561, 307.3154664389482491 ) ) ;
#387=CARTESIAN_POINT ( 'NONE',  ( 788.6739635108323228, -151.6454272087892718, 373.9316612368139090 ) ) ;
#389=CARTESIAN_POINT ( 'NONE',  ( 792.2312462859673587, -131.9073299311473875, 307.2067596250082602 ) ) ;
#393=CARTESIAN_POINT ( 'NONE',  ( 764.8639956371174549, -224.0891481129653187, 319.7806653035542013 ) ) ;
#394=CARTESIAN_POINT ( 'NONE',  ( 790.9844846989617508, 1.627300063937458408, 317.2208543904092721 ) ) ;
#399=CARTESIAN_POINT ( 'NONE',  ( 776.2433038121456548, -12.89650538077851216, 374.8207195650711014 ) ) ;
#400=EDGE_LOOP ( 'NONE', ( #17798, #30805, #15022, #180 ) ) ;
#405=CARTESIAN_POINT ( 'NONE',  ( 754.0944755984390895, -327.6237781080502600, 364.1009440267246760 ) ) ;
#406=CARTESIAN_POINT ( 'NONE',  ( 794.9819416627830151, -108.9982390220565804, 319.9864689768909898 ) ) ;
#408=CARTESIAN_POINT ( 'NONE',  ( 771.1735550268778070, -297.1800572038740711, 316.3353852180827630 ) ) ;
#411=CARTESIAN_POINT ( 'NONE',  ( 813.1304606946831655, -65.90732993114760063, 352.3570229623691716 ) ) ;
#416=SHAPE_DEFINITION_REPRESENTATION ( #10394, #2289 ) ;
#417=CARTESIAN_POINT ( 'NONE',  ( 759.9864689768902508, -26.08914811296592262, 354.9819416627836404 ) ) ;
#419=CARTESIAN_POINT ( 'NONE',  ( 759.0252816721024374, -384.9982390220556567, 368.0189434323527280 ) ) ;
#420=CARTESIAN_POINT ( 'NONE',  ( 746.0683387631852383, -283.4419599262321867, 331.3260364891676204 ) ) ;
#421=CARTESIAN_POINT ( 'NONE',  ( 754.0944755984390895, -87.62377810805102740, 364.1009440267246760 ) ) ;
#428=CARTESIAN_POINT ( 'NONE',  ( 782.5225473063381969, -406.2709662947829088, 375.2698199232970637 ) ) ;
#429=CARTESIAN_POINT ( 'NONE',  ( 762.3515768340985232, 20.87080523294372014, 315.3598267498177847 ) ) ;
#430=CARTESIAN_POINT ( 'NONE',  ( 792.3126160409814247, -458.0040092590086260, 368.0749526239440570 ) ) ;
#434=CYLINDRICAL_SURFACE ( 'NONE', #9840, 10.00000000000000888 ) ;
#436=CARTESIAN_POINT ( 'NONE',  ( 772.4468031744293057, -273.8272453906071746, 363.8651313633793620 ) ) ;
#437=CARTESIAN_POINT ( 'NONE',  ( 805.1927285166397041, -136.8164208402382371, 341.8018195045277707 ) ) ;
#441=CARTESIAN_POINT ( 'NONE',  ( 798.7617431975189675, -315.6237781080503169, 323.0428371773161871 ) ) ;
#443=CARTESIAN_POINT ( 'NONE',  ( 814.2805881961230625, -25.64542720878973014, 331.2368401574024119 ) ) ;
#444=CARTESIAN_POINT ( 'NONE',  ( 772.4837098697144029, -215.3618753856925423, 374.5518280994205611 ) ) ;
#445=CARTESIAN_POINT ( 'NONE',  ( 771.2633955100217236, -71.90732993114760063, 363.4237431249939618 ) ) ;
#450=CARTESIAN_POINT ( 'NONE',  ( 778.7629533639073998, -440.7363362996975980, 375.0009284576466371 ) ) ;
#453=CARTESIAN_POINT ( 'NONE',  ( 761.2382568024794409, -375.6237781080501463, 356.9571628226838129 ) ) ;
#455=CARTESIAN_POINT ( 'NONE',  ( 792.2312462859673587, -59.90732993114762905, 307.2067596250082602 ) ) ;
#458=CARTESIAN_POINT ( 'NONE',  ( 805.1016975059191054, -54.89650538077837183, 343.0745993439771837 ) ) ;
#460=CARTESIAN_POINT ( 'NONE',  ( 815.0009284576459549, -222.3510508353233206, 338.7629533639073429 ) ) ;
#461=CARTESIAN_POINT ( 'NONE',  ( 758.0580252608178853, -6.452784476602343666, 328.0187753319985404 ) ) ;
#465=CARTESIAN_POINT ( 'NONE',  ( 785.3141322388236176, -189.7255117493290300, 364.4286716492789537 ) ) ;
#467=ADVANCED_FACE ( 'NONE', ( #17609 ), #13685, .F. ) ;
#469=CARTESIAN_POINT ( 'NONE',  ( 804.4286716492782716, -329.3618753856922581, 345.3141322388244703 ) ) ;
#471=CARTESIAN_POINT ( 'NONE',  ( 758.9356612065449781, 18.10977687916123813, 318.6379319222613731 ) ) ;
#473=CARTESIAN_POINT ( 'NONE',  ( 804.1601925771018387, -55.44195992623293989, 346.5483106153029098 ) ) ;
#475=CARTESIAN_POINT ( 'NONE',  ( 808.0189434323515343, -302.0891481129650629, 319.0252816721025511 ) ) ;
#476=CARTESIAN_POINT ( 'NONE',  ( 754.0944755984390895, 8.376221891948691933, 364.1009440267246760 ) ) ;
#482=CARTESIAN_POINT ( 'NONE',  ( 801.6550554848130332, -456.5036469134198001, 360.7619500998734452 ) ) ;
#483=CARTESIAN_POINT ( 'NONE',  ( 770.0799878456142551, -349.9874144716865771, 362.9823548866085616 ) ) ;
#486=CARTESIAN_POINT ( 'NONE',  ( 804.1105419155481968, -171.8272453906074304, 347.6308680596136469 ) ) ;
#487=CARTESIAN_POINT ( 'NONE',  ( 800.0135310231082713, -38.08914811296587999, 325.0180583372163028 ) ) ;
#488=ORIENTED_EDGE ( 'NONE', *, *, #35724, .T. ) ;
#492=CARTESIAN_POINT ( 'NONE',  ( 746.4236121716829757, -279.8272453906071746, 328.8385539511384650 ) ) ;
#493=CARTESIAN_POINT ( 'NONE',  ( 790.8726784830453198, -370.7146871989592114, 362.5472867521010585 ) ) ;
#494=CARTESIAN_POINT ( 'NONE',  ( 756.1348686366196716, -185.2601417444143692, 347.5531968255698416 ) ) ;
#496=CARTESIAN_POINT ( 'NONE',  ( 804.9363028652555840, 7.729033705215793582, 338.2165204200192079 ) ) ;
#499=CARTESIAN_POINT ( 'NONE',  ( 746.8695393053150156, -5.907329931147798696, 327.6429770376306010 ) ) ;
#500=CARTESIAN_POINT ( 'NONE',  ( 746.8695393053150156, -101.9073299311474727, 327.6429770376306010 ) ) ;
#504=CARTESIAN_POINT ( 'NONE',  ( 813.5763878283155464, -363.8272453906068336, 351.1614460488615350 ) ) ;
#505=CYLINDRICAL_SURFACE ( 'NONE', #16137, 30.00000000000008171 ) ;
#506=CARTESIAN_POINT ( 'NONE',  ( 744.7301800767019131, -340.8164208402376971, 337.4774526936615757 ) ) ;
#510=CARTESIAN_POINT ( 'NONE',  ( 764.8639956371174549, -440.0891481129644944, 319.7806653035542013 ) ) ;
#511=CARTESIAN_POINT ( 'NONE',  ( 772.4468031744293057, -177.8272453906074304, 363.8651313633793620 ) ) ;
#514=CARTESIAN_POINT ( 'NONE',  ( 745.1769319972822814, -89.80559628986918597, 346.2694204179732083 ) ) ;
#515=CARTESIAN_POINT ( 'NONE',  ( 781.8018195045267476, -406.2709662947828519, 365.1927285166407273 ) ) ;
#523=CARTESIAN_POINT ( 'NONE',  ( 759.9864689768902508, -218.0891481129653187, 354.9819416627836404 ) ) ;
#524=CARTESIAN_POINT ( 'NONE',  ( 762.3223304703356007, -223.5436935675107577, 322.3223304703362828 ) ) ;
#528=CARTESIAN_POINT ( 'NONE',  ( 757.8323909638827445, -410.6346026584191122, 352.1044303154654358 ) ) ;
#529=CIRCLE ( 'NONE', #15277, 10.00000000000000888 ) ;
#533=CARTESIAN_POINT ( 'NONE',  ( 787.4397851343537695, -165.7255117493291152, 374.2001403089903988 ) ) ;
#534=CARTESIAN_POINT ( 'NONE',  ( 755.3028492785439312, -255.2817908451526705, 335.9200461376539693 ) ) ;
#537=CARTESIAN_POINT ( 'NONE',  ( 793.4146539503750546, -193.9874144716870319, 307.6481478633938877 ) ) ;
#542=CARTESIAN_POINT ( 'NONE',  ( 783.0433043558608688, -240.8965053807777963, 315.1538015810313027 ) ) ;
#551=CARTESIAN_POINT ( 'NONE',  ( 748.6759233522253680, -184.3726999360619629, 324.3348316497537098 ) ) ;
#557=CARTESIAN_POINT ( 'NONE',  ( 745.5313806188320314, -375.2817908451523294, 333.7943932421247268 ) ) ;
#561=CARTESIAN_POINT ( 'NONE',  ( 800.2193346964447755, 5.001760977943074948, 355.1360043628815788 ) ) ;
#563=CARTESIAN_POINT ( 'NONE',  ( 778.7629533639073998, -248.7363362996981380, 375.0009284576466371 ) ) ;
#565=CARTESIAN_POINT ( 'NONE',  ( 782.5225473063381969, -214.2709662947834488, 375.2698199232970637 ) ) ;
#568=CARTESIAN_POINT ( 'NONE',  ( 805.1927285166397041, -328.8164208402375834, 341.8018195045277707 ) ) ;
#570=CARTESIAN_POINT ( 'NONE',  ( 760.7433823573367135, -84.00906357242590161, 355.9930595647440441 ) ) ;
#571=CARTESIAN_POINT ( 'NONE',  ( 804.6971507214547046, -75.28179084515321051, 344.0799538623459739 ) ) ;
#575=CARTESIAN_POINT ( 'NONE',  ( 766.7756240680305382, -158.5328690171417065, 361.5560724626415663 ) ) ;
#576=CARTESIAN_POINT ( 'NONE',  ( 756.5762568750052424, -363.1800572038739006, 348.7366044899774238 ) ) ;
#579=CARTESIAN_POINT ( 'NONE',  ( 756.3353852180819104, -125.9073299311474159, 331.1735550268788302 ) ) ;
#582=CARTESIAN_POINT ( 'NONE',  ( 752.4576283171824116, -429.0783235625953580, 317.7880784355627952 ) ) ;
#584=CARTESIAN_POINT ( 'NONE',  ( 801.9419747391806368, -330.4527844766013231, 351.9812246680014027 ) ) ;
#588=CARTESIAN_POINT ( 'NONE',  ( 762.1405469898971887, -433.5436935675099903, 357.8594530101015607 ) ) ;
#595=CARTESIAN_POINT ( 'NONE',  ( 785.3687786644884454, 12.63812461430668321, 315.3201227861279676 ) ) ;
#596=CARTESIAN_POINT ( 'NONE',  ( 782.4968714119720516, -226.8164208402380098, 305.0891759886411023 ) ) ;
#597=CARTESIAN_POINT ( 'NONE',  ( 779.4709603349208464, -120.3510508353236048, 314.7162404726379918 ) ) ;
#600=CARTESIAN_POINT ( 'NONE',  ( 746.0683387631852383, -403.4419599262317888, 331.3260364891676204 ) ) ;
#605=CARTESIAN_POINT ( 'NONE',  ( 805.6418435158337843, -29.46360902697153250, 363.8556311672236916 ) ) ;
#613=CARTESIAN_POINT ( 'NONE',  ( 784.1219089521767955, -381.2817908451523294, 315.0488828828318333 ) ) ;
#614=CARTESIAN_POINT ( 'NONE',  ( 755.8990559732751535, -347.4636090269705733, 365.9055244015606831 ) ) ;
#618=CARTESIAN_POINT ( 'NONE',  ( 755.8990559732751535, -131.4636090269711985, 365.9055244015606831 ) ) ;
#620=CARTESIAN_POINT ( 'NONE',  ( 813.1304606946830518, -113.9073299311474301, 352.3570229623690580 ) ) ;
#625=CARTESIAN_POINT ( 'NONE',  ( 771.1735550268778070, -225.1800572038743269, 316.3353852180827630 ) ) ;
#626=CARTESIAN_POINT ( 'NONE',  ( 776.2046728542105711, -452.1908817542428665, 304.8212110874238761 ) ) ;
#631=CARTESIAN_POINT ( 'NONE',  ( 766.5853460496234675, 10.01258552831232329, 372.3518521366060554 ) ) ;
#633=CARTESIAN_POINT ( 'NONE',  ( 764.8639956371174549, -32.08914811296588709, 319.7806653035542013 ) ) ;
#635=CARTESIAN_POINT ( 'NONE',  ( 773.7943932421234194, -311.8055962898685038, 305.5313806188329409 ) ) ;
#636=CARTESIAN_POINT ( 'NONE',  ( 755.0636971347428243, -172.2709662947836478, 341.7834795799807353 ) ) ;
#638=CARTESIAN_POINT ( 'NONE',  ( 756.5762568750052424, -291.1800572038741848, 348.7366044899774238 ) ) ;
#641=CARTESIAN_POINT ( 'NONE',  ( 751.6929314249750860, -78.99823902205665149, 318.8095938919659034 ) ) ;
#644=ORIENTED_EDGE ( 'NONE', *, *, #14195, .F. ) ;
#646=CARTESIAN_POINT ( 'NONE',  ( 755.0636971347428243, -76.27096629478394618, 341.7834795799807353 ) ) ;
#647=CARTESIAN_POINT ( 'NONE',  ( 758.4439275373578084, -324.5545181178796952, 353.2243759319684386 ) ) ;
#649=CARTESIAN_POINT ( 'NONE',  ( 746.8695393053151292, -389.9073299311465917, 327.6429770376306578 ) ) ;
#650=CARTESIAN_POINT ( 'NONE',  ( 778.7502325331095108, -288.3510508353231216, 304.6391490659818828 ) ) ;
#651=CARTESIAN_POINT ( 'NONE',  ( 803.8556311672234642, -81.62377810805104161, 365.6418435158340117 ) ) ;
#659=CARTESIAN_POINT ( 'NONE',  ( 800.9747183278959710, -396.9982390220556567, 311.9810565676471583 ) ) ;
#666=CARTESIAN_POINT ( 'NONE',  ( 796.9571628226829034, -263.4636090269708006, 321.2382568024804641 ) ) ;
#667=CARTESIAN_POINT ( 'NONE',  ( 804.4286716492782716, -161.3618753856927697, 345.3141322388244703 ) ) ;
#671=CARTESIAN_POINT ( 'NONE',  ( 787.6308680596127942, -323.2601417444138860, 364.1105419155492768 ) ) ;
#673=CARTESIAN_POINT ( 'NONE',  ( 783.7953271457878373, -56.19088175424417386, 375.1787889125761239 ) ) ;
#676=CARTESIAN_POINT ( 'NONE',  ( 811.0346526505616112, -206.6346026584198512, 323.0537975583477532 ) ) ;
#677=CARTESIAN_POINT ( 'NONE',  ( 785.3141322388236176, -117.7255117493292715, 364.4286716492789537 ) ) ;
#680=CARTESIAN_POINT ( 'NONE',  ( 771.3260364891663130, -451.6454272087884192, 306.0683387631859773 ) ) ;
#683=CARTESIAN_POINT ( 'NONE',  ( 760.5453621957607311, -357.0783235625956422, 323.8424801807151425 ) ) ;
#684=CARTESIAN_POINT ( 'NONE',  ( 758.8095938919644823, -56.08914811296581604, 311.6929314249762797 ) ) ;
#686=CARTESIAN_POINT ( 'NONE',  ( 754.8983024940795303, -42.89650538077842157, 336.9254006560228163 ) ) ;
#690=CARTESIAN_POINT ( 'NONE',  ( 815.0009284576459549, -198.3510508353234059, 338.7629533639073429 ) ) ;
#691=CARTESIAN_POINT ( 'NONE',  ( 797.6776695296629214, -67.54369356751125508, 357.6776695296636603 ) ) ;
#696=CARTESIAN_POINT ( 'NONE',  ( 804.9363028652555840, -208.2709662947835341, 338.2165204200192079 ) ) ;
#698=CARTESIAN_POINT ( 'NONE',  ( 765.0180583372156207, -312.9982390220559409, 360.0135310231089534 ) ) ;
#702=CARTESIAN_POINT ( 'NONE',  ( 756.1348686366196716, -65.26014174441471027, 347.5531968255698416 ) ) ;
#704=CARTESIAN_POINT ( 'NONE',  ( 812.7932403749906598, -303.1800572038740711, 327.7687537140311633 ) ) ;
#705=CARTESIAN_POINT ( 'NONE',  ( 815.0009284576459549, -6.351050835323991173, 338.7629533639073429 ) ) ;
#710=CARTESIAN_POINT ( 'NONE',  ( 777.4774526936600978, -274.2709662947833067, 304.7301800767027657 ) ) ;
#713=CARTESIAN_POINT ( 'NONE',  ( 795.9930595647434757, -363.0783235625955854, 320.7433823573372820 ) ) ;
#716=CARTESIAN_POINT ( 'NONE',  ( 763.8424801807145741, -162.0090635724256742, 320.5453621957614700 ) ) ;
#717=CARTESIAN_POINT ( 'NONE',  ( 754.8072714833581358, -52.81642084023856398, 338.1981804954720587 ) ) ;
#721=CARTESIAN_POINT ( 'NONE',  ( 745.1792804349281596, -278.1908817542434917, 343.7566961878542884 ) ) ;
#722=CARTESIAN_POINT ( 'NONE',  ( 780.5290396650775619, -228.3510508353232922, 365.2837595273619513 ) ) ;
#725=CARTESIAN_POINT ( 'NONE',  ( 802.5472867521000353, -460.3726999360611103, 350.8726784830461156 ) ) ;
#729=CARTESIAN_POINT ( 'NONE',  ( 744.7301800767019131, -4.816420840238714085, 337.4774526936615757 ) ) ;
#730=CARTESIAN_POINT ( 'NONE',  ( 796.9462024416508257, -108.4527844766019911, 308.9653473494370246 ) ) ;
#734=CARTESIAN_POINT ( 'NONE',  ( 745.5313806188320314, -375.2817908451523294, 333.7943932421247268 ) ) ;
#736=CARTESIAN_POINT ( 'NONE',  ( 747.2067596250078623, -339.1800572038740142, 352.2312462859687230 ) ) ;
#740=CARTESIAN_POINT ( 'NONE',  ( 800.0135310231082713, -422.0891481129647218, 325.0180583372163028 ) ) ;
#741=CARTESIAN_POINT ( 'NONE',  ( 790.9844846989617508, -190.3726999360619629, 317.2208543904092721 ) ) ;
#744=CARTESIAN_POINT ( 'NONE',  ( 748.3538107759620743, -88.71468719896009247, 355.8262568251490165 ) ) ;
#745=CARTESIAN_POINT ( 'NONE',  ( 800.0135310231082713, -422.0891481129647218, 325.0180583372163028 ) ) ;
#752=CARTESIAN_POINT ( 'NONE',  ( 797.8594530101008786, -277.5436935675105019, 322.1405469898980982 ) ) ;
#753=CARTESIAN_POINT ( 'NONE',  ( 788.7366044899766848, -227.9073299311471033, 316.5762568750059813 ) ) ;
#755=VERTEX_POINT ( 'NONE', #43223 ) ;
#756=CARTESIAN_POINT ( 'NONE',  ( 802.1676090361156639, -422.6346026584192259, 327.8955696845344505 ) ) ;
#758=CARTESIAN_POINT ( 'NONE',  ( 755.2512626584698410, -175.5436935675108998, 315.2512626584710915 ) ) ;
#759=CARTESIAN_POINT ( 'NONE',  ( 800.9840315886518738, -268.9181544815162397, 354.1144889064786412 ) ) ;
#762=CARTESIAN_POINT ( 'NONE',  ( 745.1769319972822814, -233.8055962898687028, 346.2694204179732083 ) ) ;
#768=CARTESIAN_POINT ( 'NONE',  ( 756.1348686366196716, -281.2601417444139997, 347.5531968255698416 ) ) ;
#776=CARTESIAN_POINT ( 'NONE',  ( 813.5763878283155464, -171.8272453906074304, 351.1614460488615350 ) ) ;
#781=CARTESIAN_POINT ( 'NONE',  ( 810.7187646348534145, -18.45278447660230725, 356.7737145352016341 ) ) ;
#785=CARTESIAN_POINT ( 'NONE',  ( 804.4286716492782716, 6.638124614306706306, 345.3141322388244703 ) ) ;
#786=CARTESIAN_POINT ( 'NONE',  ( 748.6759233522253680, -280.3726999360616787, 324.3348316497537098 ) ) ;
#788=CARTESIAN_POINT ( 'NONE',  ( 815.2698199232961542, -208.8164208402380666, 342.5225473063383106 ) ) ;
#792=CARTESIAN_POINT ( 'NONE',  ( 781.8018195045266339, -310.2709662947832499, 365.1927285166406705 ) ) ;
#793=CARTESIAN_POINT ( 'NONE',  ( 798.5707757039680246, -77.46360902697138329, 356.7845633553585003 ) ) ;
#797=CARTESIAN_POINT ( 'NONE',  ( 780.5290396650775619, -156.3510508353235480, 365.2837595273619513 ) ) ;
#798=CARTESIAN_POINT ( 'NONE',  ( 792.1044303154645831, -372.4527844766010958, 317.8323909638837677 ) ) ;
#803=CARTESIAN_POINT ( 'NONE',  ( 804.7487373415286811, 4.456306432488530866, 364.7487373415288516 ) ) ;
#805=CARTESIAN_POINT ( 'NONE',  ( 774.6312213355099630, -335.3618753856920307, 364.6798772138717482 ) ) ;
#807=CARTESIAN_POINT ( 'NONE',  ( 802.1676090361156639, -446.6346026584189985, 327.8955696845344505 ) ) ;
#814=CARTESIAN_POINT ( 'NONE',  ( 802.1676090361156639, 9.365397341579420498, 327.8955696845344505 ) ) ;
#815=CARTESIAN_POINT ( 'NONE',  ( 814.5518280994195948, -231.7255117493288310, 332.4837098697145734 ) ) ;
#816=CARTESIAN_POINT ( 'NONE',  ( 775.9200461376533440, -119.8055962898690865, 315.3028492785443291 ) ) ;
#817=FACE_OUTER_BOUND ( 'NONE', #10229, .T. ) ;
#819=CARTESIAN_POINT ( 'NONE',  ( 756.1443688327750579, -381.6237781080500326, 314.3581564841659315 ) ) ;
#825=CARTESIAN_POINT ( 'NONE',  ( 747.6481478633932056, -61.09997266333506616, 353.4146539503763620 ) ) ;
#833=CARTESIAN_POINT ( 'NONE',  ( 783.0745993439762742, -392.1908817542432075, 365.1016975059196739 ) ) ;
#837=CARTESIAN_POINT ( 'NONE',  ( 757.7880784355613741, -138.0090635724257311, 312.4576283171834916 ) ) ;
#839=CARTESIAN_POINT ( 'NONE',  ( 814.2001403089898304, -113.3618753856929260, 347.4397851343538264 ) ) ;
#841=CARTESIAN_POINT ( 'NONE',  ( 772.4999999999993179, -512.9681489794448908, 370.0000000000000000 ) ) ;
#843=CARTESIAN_POINT ( 'NONE',  ( 788.7366044899766848, -227.9073299311471033, 316.5762568750059813 ) ) ;
#844=CARTESIAN_POINT ( 'NONE',  ( 769.9779781133707957, 4.900027336664720679, 316.7813123517150871 ) ) ;
#848=CARTESIAN_POINT ( 'NONE',  ( 751.2241431872005251, -16.16923265350578021, 359.9636004259367610 ) ) ;
#851=CARTESIAN_POINT ( 'NONE',  ( 774.6858677611749044, -33.72551174932952733, 315.5713283507209894 ) ) ;
#854=CARTESIAN_POINT ( 'NONE',  ( 764.3348316497523456, -358.7146871989592114, 308.6759233522265617 ) ) ;
#855=CARTESIAN_POINT ( 'NONE',  ( 762.3223304703356007, -151.5436935675109851, 322.3223304703362828 ) ) ;
#857=CARTESIAN_POINT ( 'NONE',  ( 773.7943932421234194, -431.8055962898681059, 305.5313806188329409 ) ) ;
#858=CARTESIAN_POINT ( 'NONE',  ( 756.5762568750052424, -339.1800572038740142, 348.7366044899774238 ) ) ;
#864=CARTESIAN_POINT ( 'NONE',  ( 778.1981804954714335, -58.27096629478398171, 314.8072714833589885 ) ) ;
#865=CARTESIAN_POINT ( 'NONE',  ( 796.9571628226829034, -359.4636090269705164, 321.2382568024804641 ) ) ;
#866=CARTESIAN_POINT ( 'NONE',  ( 755.2512626584698410, -391.5436935675101608, 315.2512626584710915 ) ) ;
#867=CARTESIAN_POINT ( 'NONE',  ( 813.2346286133761168, -293.2601417444139429, 328.9521613784389160 ) ) ;
#868=CARTESIAN_POINT ( 'NONE',  ( 744.8212110874229666, -66.89650538077835051, 336.2046728542121627 ) ) ;
#875=CARTESIAN_POINT ( 'NONE',  ( 751.6929314249748586, -438.9982390220553157, 318.8095938919659034 ) ) ;
#881=CARTESIAN_POINT ( 'NONE',  ( 772.4468031744293057, -249.8272453906072315, 363.8651313633793620 ) ) ;
#882=CARTESIAN_POINT ( 'NONE',  ( 801.9419747391806368, -162.4527844766018632, 351.9812246680014027 ) ) ;
#886=CARTESIAN_POINT ( 'NONE',  ( 775.9200461376533440, -311.8055962898685038, 315.3028492785443291 ) ) ;
#888=CARTESIAN_POINT ( 'NONE',  ( 768.9521613784389729, -33.82724539060788516, 373.2346286133773106 ) ) ;
#890=CARTESIAN_POINT ( 'NONE',  ( 755.0636971347428243, -100.2709662947838609, 341.7834795799807353 ) ) ;
#893=CARTESIAN_POINT ( 'NONE',  ( 811.3240766477731540, -436.3726999360612240, 355.6651683502462902 ) ) ;
#896=CARTESIAN_POINT ( 'NONE',  ( 798.7617431975189675, -411.6237781080499758, 323.0428371773161871 ) ) ;
#902=CARTESIAN_POINT ( 'NONE',  ( 812.6845335610512393, -199.9874144716870603, 353.5525998758768651 ) ) ;
#903=CARTESIAN_POINT ( 'NONE',  ( 792.1044303154646968, -36.45278447660224685, 317.8323909638837677 ) ) ;
#906=CARTESIAN_POINT ( 'NONE',  ( 778.1981804954714335, -226.2709662947834204, 314.8072714833589885 ) ) ;
#908=CARTESIAN_POINT ( 'NONE',  ( 803.4237431249931660, -351.1800572038740142, 331.2633955100225194 ) ) ;
#914=CARTESIAN_POINT ( 'NONE',  ( 745.0891759886404770, -292.2709662947831930, 342.4968714119734159 ) ) ;
#915=CARTESIAN_POINT ( 'NONE',  ( 803.8556311672234642, 14.37622189194867417, 365.6418435158340117 ) ) ;
#922=CARTESIAN_POINT ( 'NONE',  ( 772.4837098697144029, -287.3618753856923718, 374.5518280994205611 ) ) ;
#923=CARTESIAN_POINT ( 'NONE',  ( 787.4999999999992042, -512.9681489794448908, 309.9999999999998863 ) ) ;
#924=CARTESIAN_POINT ( 'NONE',  ( 790.9844846989617508, -214.3726999360618493, 317.2208543904092721 ) ) ;
#926=CARTESIAN_POINT ( 'NONE',  ( 754.7162404726377645, -158.7363362996984222, 339.4709603349214717 ) ) ;
#927=CARTESIAN_POINT ( 'NONE',  ( 803.4237431249931660, -39.18005720387496638, 331.2633955100225194 ) ) ;
#932=CARTESIAN_POINT ( 'NONE',  ( 749.5768839229115201, -276.5545181178798657, 358.0661480581553064 ) ) ;
#933=CARTESIAN_POINT ( 'NONE',  ( 756.1348686366196716, -209.2601417444142839, 347.5531968255698416 ) ) ;
#936=CARTESIAN_POINT ( 'NONE',  ( 798.5707757039680246, -461.4636090269701754, 356.7845633553585003 ) ) ;
#939=CARTESIAN_POINT ( 'NONE',  ( 808.3070685750230950, -42.99823902205675807, 361.1904061080339261 ) ) ;
#940=CARTESIAN_POINT ( 'NONE',  ( 787.4397851343537695, -117.7255117493292715, 374.2001403089903988 ) ) ;
#942=CARTESIAN_POINT ( 'NONE',  ( 799.9999999999993179, -512.9681489794448908, 339.9999999999999432 ) ) ;
#944=CARTESIAN_POINT ( 'NONE',  ( 811.3240766477731540, -388.3726999360613945, 355.6651683502462902 ) ) ;
#946=CARTESIAN_POINT ( 'NONE',  ( 782.5225473063381969, -358.2709662947829088, 375.2698199232970637 ) ) ;
#949=CARTESIAN_POINT ( 'NONE',  ( 802.1676090361156639, -446.6346026584189985, 327.8955696845344505 ) ) ;
#950=CARTESIAN_POINT ( 'NONE',  ( 755.5913626894240451, -205.6454272087891297, 346.6156483768012890 ) ) ;
#953=CARTESIAN_POINT ( 'NONE',  ( 749.8865473780648472, -92.53286901714190549, 322.1177392798429082 ) ) ;
#954=CARTESIAN_POINT ( 'NONE',  ( 804.4286716492782716, -425.3618753856919170, 345.3141322388244703 ) ) ;
#962=CARTESIAN_POINT ( 'NONE',  ( 803.4237431249931660, -255.1800572038742700, 331.2633955100225194 ) ) ;
#963=CARTESIAN_POINT ( 'NONE',  ( 797.6776695296629214, -259.5436935675106156, 357.6776695296636603 ) ) ;
#967=CARTESIAN_POINT ( 'NONE',  ( 764.8639956371174549, -440.0891481129644944, 319.7806653035542013 ) ) ;
#969=( NAMED_UNIT ( * ) SI_UNIT ( $, .STERADIAN. ) SOLID_ANGLE_UNIT ( ) );
#971=CARTESIAN_POINT ( 'NONE',  ( 787.4397851343537695, -189.7255117493290300, 374.2001403089903988 ) ) ;
#972=CARTESIAN_POINT ( 'NONE',  ( 784.1219089521767955, -261.2817908451526705, 315.0488828828318333 ) ) ;
#975=CARTESIAN_POINT ( 'NONE',  ( 766.5853460496234675, -205.9874144716870035, 372.3518521366060554 ) ) ;
#981=CARTESIAN_POINT ( 'NONE',  ( 776.9566956441375396, -276.8965053807776258, 364.8461984189686405 ) ) ;
#989=CARTESIAN_POINT ( 'NONE',  ( 812.3518521366052028, -169.0999726633347393, 326.5853460496235243 ) ) ;
#995=AXIS2_PLACEMENT_3D ( 'NONE', #25421, #31508, #45374 ) ;
#1000=CARTESIAN_POINT ( 'NONE',  ( 762.1405469898971887, -25.54369356751136877, 357.8594530101015607 ) ) ;
#1002=CARTESIAN_POINT ( 'NONE',  ( 811.3240766477731540, -292.3726999360616219, 355.6651683502462902 ) ) ;
#1004=CARTESIAN_POINT ( 'NONE',  ( 772.4837098697144029, -215.3618753856925423, 374.5518280994205611 ) ) ;
#1008=CARTESIAN_POINT ( 'NONE',  ( 781.7834795799800531, -322.8164208402377540, 315.0636971347436202 ) ) ;
#1010=CARTESIAN_POINT ( 'NONE',  ( 790.9844846989617508, -94.37269993606224716, 317.2208543904092721 ) ) ;
#1016=CARTESIAN_POINT ( 'NONE',  ( 764.0069404352550464, -159.0783235625962391, 359.2566176426627180 ) ) ;
#1017=CARTESIAN_POINT ( 'NONE',  ( 791.9812246680005501, -356.6346026584193964, 361.9419747391813189 ) ) ;
#1021=CARTESIAN_POINT ( 'NONE',  ( 788.7366044899766848, -155.9073299311473306, 316.5762568750059813 ) ) ;
#1025=CARTESIAN_POINT ( 'NONE',  ( 808.0189434323515343, 9.910851887033969021, 319.0252816721025511 ) ) ;
#1026=CARTESIAN_POINT ( 'NONE',  ( 800.0135310231082713, -302.0891481129650629, 325.0180583372163028 ) ) ;
#1027=ORIENTED_EDGE ( 'NONE', *, *, #7837, .T. ) ;
#1028=CARTESIAN_POINT ( 'NONE',  ( 755.3201227861273992, -339.7255117493285184, 345.3687786644892981 ) ) ;
#1038=CARTESIAN_POINT ( 'NONE',  ( 781.8018195045266339, 1.729033705215812011, 365.1927285166406705 ) ) ;
#1039=CARTESIAN_POINT ( 'NONE',  ( 796.7845633553578182, -153.6237781080508000, 358.5707757039688204 ) ) ;
#1046=CARTESIAN_POINT ( 'NONE',  ( 799.9636004259356241, -70.91815448151683654, 311.2241431872006956 ) ) ;
#1049=DIRECTION ( 'NONE',  ( -0.000000000000000000, 1.000000000000000000, -0.000000000000000000 ) ) ;
#1055=CARTESIAN_POINT ( 'NONE',  ( 757.4527132478984868, -400.3726999360612808, 329.1273215169538844 ) ) ;
#1060=CARTESIAN_POINT ( 'NONE',  ( 805.6418435158337843, -173.4636090269710849, 363.8556311672236916 ) ) ;
#1062=CARTESIAN_POINT ( 'NONE',  ( 811.0346526505616112, -134.6346026584201070, 323.0537975583477532 ) ) ;
#1066=CARTESIAN_POINT ( 'NONE',  ( 797.6776695296629214, -211.5436935675107861, 357.6776695296636603 ) ) ;
#1069=CARTESIAN_POINT ( 'NONE',  ( 800.9840315886518738, -28.91815448151699286, 354.1144889064786412 ) ) ;
#1072=CARTESIAN_POINT ( 'NONE',  ( 779.9999999999992042, 126.4563064324884465, 339.9999999999999432 ) ) ;
#1073=CARTESIAN_POINT ( 'NONE',  ( 793.4146539503750546, -25.98741447168755769, 307.6481478633938877 ) ) ;
#1076=CARTESIAN_POINT ( 'NONE',  ( 781.7834795799800531, -10.81642084023869543, 315.0636971347436202 ) ) ;
#1078=CARTESIAN_POINT ( 'NONE',  ( 761.9338519418445230, -350.5328690171411381, 370.4231160770881957 ) ) ;
#1079=CARTESIAN_POINT ( 'NONE',  ( 785.3141322388236176, -165.7255117493291152, 364.4286716492789537 ) ) ;
#1081=CARTESIAN_POINT ( 'NONE',  ( 744.9990715423526808, -426.3510508353226669, 341.2370466360926002 ) ) ;
#1083=CARTESIAN_POINT ( 'NONE',  ( 803.4237431249931660, -351.1800572038740142, 331.2633955100225194 ) ) ;
#1091=CARTESIAN_POINT ( 'NONE',  ( 785.3141322388236176, -69.72551174932942786, 364.4286716492789537 ) ) ;
#1092=CARTESIAN_POINT ( 'NONE',  ( 801.5560724626406000, -360.5545181178796383, 326.7756240680316182 ) ) ;
#1094=CARTESIAN_POINT ( 'NONE',  ( 767.7687537140311633, -383.9073299311466485, 372.7932403749916830 ) ) ;
#1095=CARTESIAN_POINT ( 'NONE',  ( 786.2056067578752163, -275.8055962898685038, 374.4686193811670023 ) ) ;
#1096=CARTESIAN_POINT ( 'NONE',  ( 788.7631598425961101, -97.44195992623281199, 305.7194118038759143 ) ) ;
#1105=CARTESIAN_POINT ( 'NONE',  ( 767.9999999999992042, 205.0000000000000568, 319.9999999999999432 ) ) ;
#1109=CARTESIAN_POINT ( 'NONE',  ( 760.7433823573367135, -300.0090635724252479, 355.9930595647440441 ) ) ;
#1110=CARTESIAN_POINT ( 'NONE',  ( 785.3141322388236176, -165.7255117493291152, 364.4286716492789537 ) ) ;
#1113=CARTESIAN_POINT ( 'NONE',  ( 786.6156483768007774, -337.4419599262319593, 315.5913626894246136 ) ) ;
#1116=CARTESIAN_POINT ( 'NONE',  ( 786.2694204179717872, -69.28179084515321051, 305.1769319972829067 ) ) ;
#1120=CARTESIAN_POINT ( 'NONE',  ( 758.0580252608178853, -102.4527844766020337, 328.0187753319985404 ) ) ;
#1123=CARTESIAN_POINT ( 'NONE',  ( 805.2837595273609850, -2.736336299698892027, 340.5290396650784714 ) ) ;
#1126=CARTESIAN_POINT ( 'NONE',  ( 760.5453621957607311, -405.0783235625954148, 323.8424801807151425 ) ) ;
#1135=CARTESIAN_POINT ( 'NONE',  ( 801.9858362298568863, -243.0783235625959833, 312.7379699480935642 ) ) ;
#1136=CARTESIAN_POINT ( 'NONE',  ( 803.4237431249931660, -63.18005720387488822, 331.2633955100225194 ) ) ;
#1140=CARTESIAN_POINT ( 'NONE',  ( 771.2633955100217236, -239.9073299311470748, 363.4237431249939618 ) ) ;
#1146=CARTESIAN_POINT ( 'NONE',  ( 765.8855110935204493, -70.16923265350563099, 319.0159684113471599 ) ) ;
#1150=CARTESIAN_POINT ( 'NONE',  ( 754.9967657858570647, -289.5436935675105019, 365.0032342141425943 ) ) ;
#1151=CARTESIAN_POINT ( 'NONE',  ( 778.7502325331095108, -24.35105083532392811, 304.6391490659818828 ) ) ;
#1158=CARTESIAN_POINT ( 'NONE',  ( 763.0537975583475827, -312.4527844766012663, 371.0346526505627480 ) ) ;
#1160=CARTESIAN_POINT ( 'NONE',  ( 803.2186876482843445, -367.9874144716865203, 350.0220218866286928 ) ) ;
#1162=CARTESIAN_POINT ( 'NONE',  ( 802.5472867521000353, -196.3726999360619061, 350.8726784830461156 ) ) ;
#1163=CARTESIAN_POINT ( 'NONE',  ( 767.8955696845333705, -48.45278447660219712, 362.1676090361162323 ) ) ;
#1167=CARTESIAN_POINT ( 'NONE',  ( 773.3843516231979720, -205.4419599262324425, 364.4086373105754433 ) ) ;
#1171=CARTESIAN_POINT ( 'NONE',  ( 799.2566176426618085, -456.0090635724247932, 324.0069404352559559 ) ) ;
#1175=CARTESIAN_POINT ( 'NONE',  ( 759.0252816721024374, -48.99823902205675807, 368.0189434323527280 ) ) ;
#1176=CARTESIAN_POINT ( 'NONE',  ( 804.7487373415286811, -91.54369356751116982, 364.7487373415288516 ) ) ;
#1177=FACE_BOUND ( 'NONE', #29400, .T. ) ;
#1179=CARTESIAN_POINT ( 'NONE',  ( 813.5763878283155464, -387.8272453906067767, 351.1614460488615350 ) ) ;
#1181=CARTESIAN_POINT ( 'NONE',  ( 814.9108240113580450, -352.2709662947830225, 337.5031285880265273 ) ) ;
#1185=CARTESIAN_POINT ( 'NONE',  ( 789.9200121543843807, 22.01258552831228599, 317.0176451133914384 ) ) ;
#1186=CARTESIAN_POINT ( 'NONE',  ( 755.3028492785439312, -183.2817908451528695, 335.9200461376539693 ) ) ;
#1189=CARTESIAN_POINT ( 'NONE',  ( 773.7943932421234194, -143.8055962898690154, 305.5313806188329409 ) ) ;
#1190=CARTESIAN_POINT ( 'NONE',  ( 768.0187753319979720, -440.6346026584191122, 318.0580252608186242 ) ) ;
#1191=CARTESIAN_POINT ( 'NONE',  ( 746.7653713866222915, -161.2601417444143976, 351.0478386215610271 ) ) ;
#1196=CARTESIAN_POINT ( 'NONE',  ( 781.8018195045266339, -262.2709662947831930, 365.1927285166406705 ) ) ;
#1197=CARTESIAN_POINT ( 'NONE',  ( 781.8018195045267476, -262.2709662947832499, 365.1927285166407273 ) ) ;
#1198=PLANE ( 'NONE',  #4293 ) ;
#1200=CARTESIAN_POINT ( 'NONE',  ( 804.9511171171677688, 18.19440371013048008, 335.8780910478229202 ) ) ;
#1204=CARTESIAN_POINT ( 'NONE',  ( 745.0891759886404770, -196.2709662947835909, 342.4968714119734159 ) ) ;
#1205=CARTESIAN_POINT ( 'NONE',  ( 760.7433823573367135, -276.0090635724253048, 355.9930595647440441 ) ) ;
#1208=CARTESIAN_POINT ( 'NONE',  ( 793.4146539503750546, -217.9874144716870035, 307.6481478633938877 ) ) ;
#1213=CARTESIAN_POINT ( 'NONE',  ( 757.2208543904082489, -256.7146871989595525, 350.9844846989624330 ) ) ;
#1215=FACE_OUTER_BOUND ( 'NONE', #4489, .T. ) ;
#1216=AXIS2_PLACEMENT_3D ( 'NONE', #36940, #8992, #29784 ) ;
#1221=CARTESIAN_POINT ( 'NONE',  ( 750.9282345327678740, -160.9181544815165807, 319.8311093483690115 ) ) ;
#1222=DIRECTION ( 'NONE',  ( -1.000000000000000000, -0.000000000000000000, 0.000000000000000000 ) ) ;
#1227=CARTESIAN_POINT ( 'NONE',  ( 792.2312462859673587, -11.90732993114778182, 307.2067596250082602 ) ) ;
#1232=CARTESIAN_POINT ( 'NONE',  ( 774.6858677611749044, -33.72551174932952733, 315.5713283507209894 ) ) ;
#1233=CARTESIAN_POINT ( 'NONE',  ( 773.7305795820266212, -297.2817908451526137, 374.8230680027170365 ) ) ;
#1236=CARTESIAN_POINT ( 'NONE',  ( 747.2067596250078623, -243.1800572038743269, 352.2312462859687230 ) ) ;
#1242=CARTESIAN_POINT ( 'NONE',  ( 792.1044303154645831, -324.4527844766013231, 317.8323909638837677 ) ) ;
#1244=CARTESIAN_POINT ( 'NONE',  ( 801.5560724626406000, -72.55451811788049099, 326.7756240680316182 ) ) ;
#1248=CARTESIAN_POINT ( 'NONE',  ( 799.9999999999993179, 166.4563064324884465, 360.0000000000000000 ) ) ;
#1249=CARTESIAN_POINT ( 'NONE',  ( 755.0488828828309806, -161.8055962898689870, 344.1219089521771934 ) ) ;
#1250=CARTESIAN_POINT ( 'NONE',  ( 774.6858677611749044, -393.7255117493283478, 315.5713283507209894 ) ) ;
#1254=CARTESIAN_POINT ( 'NONE',  ( 792.1044303154645831, -156.4527844766018916, 317.8323909638837677 ) ) ;
#1257=CARTESIAN_POINT ( 'NONE',  ( 798.0661480581538854, -434.5328690171407970, 309.5768839229118043 ) ) ;
#1260=CARTESIAN_POINT ( 'NONE',  ( 804.6798772138708955, -375.7255117493283478, 334.6312213355107019 ) ) ;
#1261=EDGE_CURVE ( 'NONE', #23899, #3360, #19287, .T. ) ;
#1267=EDGE_LOOP ( 'NONE', ( #32695, #4959, #6707, #37329 ) ) ;
#1272=CARTESIAN_POINT ( 'NONE',  ( 758.0580252608178853, -6.452784476602343666, 328.0187753319985404 ) ) ;
#1273=CARTESIAN_POINT ( 'NONE',  ( 803.8651313633788504, -149.2601417444144261, 332.4468031744301015 ) ) ;
#1281=CARTESIAN_POINT ( 'NONE',  ( 814.2805881961230625, -73.64542720878957027, 331.2368401574024119 ) ) ;
#1290=CARTESIAN_POINT ( 'NONE',  ( 804.8461984189677878, -410.1908817542430370, 336.9566956441385628 ) ) ;
#1293=CARTESIAN_POINT ( 'NONE',  ( 776.9254006560222479, -236.1908817542436338, 314.8983024940802125 ) ) ;
#1296=CARTESIAN_POINT ( 'NONE',  ( 773.7305795820266212, -177.2817908451528695, 374.8230680027170365 ) ) ;
#1298=CARTESIAN_POINT ( 'NONE',  ( 747.2067596250078623, -171.1800572038745543, 352.2312462859687230 ) ) ;
#1301=EDGE_CURVE ( 'NONE', #20106, #32443, #42354, .T. ) ;
#1303=DIRECTION ( 'NONE',  ( 0.000000000000000000, -1.000000000000000000, 0.000000000000000000 ) ) ;
#1304=CARTESIAN_POINT ( 'NONE',  ( 801.9419747391806368, -210.4527844766016926, 351.9812246680014027 ) ) ;
#1305=CARTESIAN_POINT ( 'NONE',  ( 755.3028492785439312, -39.28179084515331709, 335.9200461376539693 ) ) ;
#1309=CARTESIAN_POINT ( 'NONE',  ( 810.1134526219336749, -32.53286901714208312, 357.8822607201570349 ) ) ;
#1310=ORIENTED_EDGE ( 'NONE', *, *, #3849, .F. ) ;
#1312=CARTESIAN_POINT ( 'NONE',  ( 803.4237431249931660, -15.18005720387504631, 331.2633955100225194 ) ) ;
#1314=CARTESIAN_POINT ( 'NONE',  ( 788.7631598425961101, -361.4419599262319593, 305.7194118038759143 ) ) ;
#1315=ORIENTED_EDGE ( 'NONE', *, *, #3538, .F. ) ;
#1316=CARTESIAN_POINT ( 'NONE',  ( 747.3154664389472828, -427.9874144716862929, 326.4474001241230781 ) ) ;
#1318=CARTESIAN_POINT ( 'NONE',  ( 804.6798772138708955, -327.7255117493285184, 334.6312213355107019 ) ) ;
#1324=CARTESIAN_POINT ( 'NONE',  ( 788.7366044899766848, -59.90732993114762905, 316.5762568750059813 ) ) ;
#1325=CARTESIAN_POINT ( 'NONE',  ( 755.3028492785439312, -375.2817908451523294, 335.9200461376539693 ) ) ;
#1327=CARTESIAN_POINT ( 'NONE',  ( 745.0891759886404770, -412.2709662947829088, 342.4968714119734159 ) ) ;
#1328=CARTESIAN_POINT ( 'NONE',  ( 815.1787889125755555, -318.8965053807775121, 343.7953271457877804 ) ) ;
#1329=CARTESIAN_POINT ( 'NONE',  ( 801.9858362298568863, -99.07832356259642381, 312.7379699480935642 ) ) ;
#1335=CARTESIAN_POINT ( 'NONE',  ( 814.2001403089898304, -425.3618753856919170, 347.4397851343538264 ) ) ;
#1342=CARTESIAN_POINT ( 'NONE',  ( 754.7162404726377645, -302.7363362996979959, 339.4709603349214717 ) ) ;
#1344=CARTESIAN_POINT ( 'NONE',  ( 785.3687786644884454, -155.3618753856927128, 315.3201227861279676 ) ) ;
#1347=CARTESIAN_POINT ( 'NONE',  ( 804.9511171171677688, -341.8055962898683333, 335.8780910478229202 ) ) ;
#1351=CARTESIAN_POINT ( 'NONE',  ( 814.8207195650702488, -74.19088175424410281, 336.2433038121456548 ) ) ;
#1353=CARTESIAN_POINT ( 'NONE',  ( 785.3687786644884454, -131.3618753856928834, 315.3201227861279676 ) ) ;
#1356=CARTESIAN_POINT ( 'NONE',  ( 766.9102291470427417, -18.55451811788065797, 318.6633372737382501 ) ) ;
#1359=CARTESIAN_POINT ( 'NONE',  ( 765.8855110935204493, -382.1692326535045936, 319.0159684113471599 ) ) ;
#1361=CARTESIAN_POINT ( 'NONE',  ( 784.0799538623451781, -83.80559628986920018, 364.6971507214555572 ) ) ;
#1365=CARTESIAN_POINT ( 'NONE',  ( 798.0661480581538854, -242.5328690171414507, 309.5768839229118043 ) ) ;
#1366=CARTESIAN_POINT ( 'NONE',  ( 762.3223304703356007, -55.54369356751127640, 322.3223304703362828 ) ) ;
#1369=CARTESIAN_POINT ( 'NONE',  ( 781.7834795799800531, -250.8164208402379245, 315.0636971347436202 ) ) ;
#1373=VERTEX_POINT ( 'NONE', #14187 ) ;
#1377=CARTESIAN_POINT ( 'NONE',  ( 813.1304606946831655, -281.9073299311469327, 352.3570229623691716 ) ) ;
#1378=CARTESIAN_POINT ( 'NONE',  ( 746.7653713866222915, -41.26014174441479554, 351.0478386215610271 ) ) ;
#1384=CARTESIAN_POINT ( 'NONE',  ( 772.5602148656447525, -321.7255117493286320, 305.7998596910095443 ) ) ;
#1388=CARTESIAN_POINT ( 'NONE',  ( 758.4439275373578084, -204.5545181178800931, 353.2243759319684386 ) ) ;
#1389=CARTESIAN_POINT ( 'NONE',  ( 778.1981804954714335, -34.27096629478407408, 314.8072714833589885 ) ) ;
#1393=CARTESIAN_POINT ( 'NONE',  ( 758.6633372737375112, -212.5328690171415076, 326.9102291470432533 ) ) ;
#1396=CARTESIAN_POINT ( 'NONE',  ( 814.9108240113580450, -448.2709662947827951, 337.5031285880265273 ) ) ;
#1400=CARTESIAN_POINT ( 'NONE',  ( 767.7687537140311633, -47.90732993114767169, 372.7932403749916830 ) ) ;
#1401=CARTESIAN_POINT ( 'NONE',  ( 754.9967657858570647, -121.5436935675110419, 365.0032342141425374 ) ) ;
#1404=CIRCLE ( 'NONE', #34609, 30.00000000000008171 ) ;
#1405=CARTESIAN_POINT ( 'NONE',  ( 778.7629533639073998, -392.7363362996977116, 375.0009284576466371 ) ) ;
#1407=CARTESIAN_POINT ( 'NONE',  ( 812.7932403749906598, -351.1800572038740142, 327.7687537140311633 ) ) ;
#1409=CARTESIAN_POINT ( 'NONE',  ( 794.1144889064781864, 13.83076734649413098, 360.9840315886528401 ) ) ;
#1412=CARTESIAN_POINT ( 'NONE',  ( 808.7758568127978833, -148.1692326535053610, 320.0363995740631822 ) ) ;
#1413=CARTESIAN_POINT ( 'NONE',  ( 762.1405469898973024, -433.5436935675100472, 357.8594530101016176 ) ) ;
#1417=CARTESIAN_POINT ( 'NONE',  ( 800.0135310231082713, -134.0891481129655745, 325.0180583372163028 ) ) ;
#1420=CARTESIAN_POINT ( 'NONE',  ( 785.3687786644884454, -251.3618753856923149, 315.3201227861279676 ) ) ;
#1421=CARTESIAN_POINT ( 'NONE',  ( 755.3201227861273992, -267.7255117493287457, 345.3687786644892981 ) ) ;
#1422=CARTESIAN_POINT ( 'NONE',  ( 779.9999999999992042, 16.45630643248849267, 339.9999999999999432 ) ) ;
#1424=CARTESIAN_POINT ( 'NONE',  ( 800.2193346964447755, -450.9982390220554294, 355.1360043628815788 ) ) ;
#1426=CARTESIAN_POINT ( 'NONE',  ( 800.9747183278959710, -180.9982390220563389, 311.9810565676471583 ) ) ;
#1427=CARTESIAN_POINT ( 'NONE',  ( 793.9708237608222134, -310.9181544815160123, 319.2295555964448681 ) ) ;
#1428=CARTESIAN_POINT ( 'NONE',  ( 783.0433043558608688, -384.8965053807772847, 315.1538015810313027 ) ) ;
#1436=CARTESIAN_POINT ( 'NONE',  ( 765.8855110935204493, -262.1692326535049347, 319.0159684113471599 ) ) ;
#1443=CARTESIAN_POINT ( 'NONE',  ( 748.6759233522253680, -160.3726999360620482, 324.3348316497537098 ) ) ;
#1447=CARTESIAN_POINT ( 'NONE',  ( 772.5602148656447525, -9.725511749329603717, 305.7998596910095443 ) ) ;
#1452=CARTESIAN_POINT ( 'NONE',  ( 781.7834795799800531, -34.81642084023861372, 315.0636971347436202 ) ) ;
#1453=CARTESIAN_POINT ( 'NONE',  ( 754.3581564841646241, -281.4636090269706870, 316.1443688327762516 ) ) ;
#1455=CARTESIAN_POINT ( 'NONE',  ( 749.2812353651451076, -246.4527844766016074, 323.2262854647983090 ) ) ;
#1457=DIRECTION ( 'NONE',  ( 0.000000000000000000, 1.000000000000000000, 0.000000000000000000 ) ) ;
#1459=CARTESIAN_POINT ( 'NONE',  ( 762.3223304703356007, -367.5436935675102745, 322.3223304703362828 ) ) ;
#1460=CARTESIAN_POINT ( 'NONE',  ( 755.1538015810308480, -134.1908817542439181, 343.0433043558613804 ) ) ;
#1464=CARTESIAN_POINT ( 'NONE',  ( 754.8072714833581358, -388.8164208402374129, 338.1981804954720587 ) ) ;
#1467=CARTESIAN_POINT ( 'NONE',  ( 774.6312213355099630, -143.3618753856927697, 364.6798772138717482 ) ) ;
#1472=CARTESIAN_POINT ( 'NONE',  ( 758.0580252608178853, -366.4527844766012095, 328.0187753319985404 ) ) ;
#1474=CARTESIAN_POINT ( 'NONE',  ( 765.0180583372156207, -432.9982390220555999, 360.0135310231089534 ) ) ;
#1477=CARTESIAN_POINT ( 'NONE',  ( 746.8695393053151292, -77.90732993114757221, 327.6429770376306578 ) ) ;
#1478=ORIENTED_EDGE ( 'NONE', *, *, #31981, .T. ) ;
#1482=CARTESIAN_POINT ( 'NONE',  ( 801.5560724626406000, -456.5545181178792404, 326.7756240680316182 ) ) ;
#1483=CARTESIAN_POINT ( 'NONE',  ( 796.9462024416508257, -228.4527844766015789, 308.9653473494370246 ) ) ;
#1484=CARTESIAN_POINT ( 'NONE',  ( 754.9735926884551418, -162.3510508353235196, 340.5236548041000333 ) ) ;
#1492=CARTESIAN_POINT ( 'NONE',  ( 773.7305795820266212, -57.28179084515326736, 374.8230680027170365 ) ) ;
#1496=CARTESIAN_POINT ( 'NONE',  ( 791.7608162188021197, 205.0000000000000568, 339.9999999999999432 ) ) ;
#1501=CARTESIAN_POINT ( 'NONE',  ( 800.9840315886518738, -412.9181544815157281, 354.1144889064786412 ) ) ;
#1503=CARTESIAN_POINT ( 'NONE',  ( 801.5560724626406000, -240.5545181178798941, 326.7756240680316182 ) ) ;
#1506=CARTESIAN_POINT ( 'NONE',  ( 804.1009440267234822, -167.4636090269711133, 314.0944755984392600 ) ) ;
#1507=EDGE_CURVE ( 'NONE', #45297, #13477, #40147, .T. ) ;
#1510=CARTESIAN_POINT ( 'NONE',  ( 754.9967657858570647, -145.5436935675109851, 365.0032342141425374 ) ) ;
#1514=CARTESIAN_POINT ( 'NONE',  ( 781.7834795799800531, -250.8164208402379245, 315.0636971347436202 ) ) ;
#1515=CARTESIAN_POINT ( 'NONE',  ( 769.9779781133707957, -19.09997266333520116, 316.7813123517150871 ) ) ;
#1520=CARTESIAN_POINT ( 'NONE',  ( 803.2186876482843445, -55.98741447168748664, 350.0220218866286928 ) ) ;
#1523=CARTESIAN_POINT ( 'NONE',  ( 774.6312213355099630, -23.36187538569318889, 364.6798772138717482 ) ) ;
#1526=CARTESIAN_POINT ( 'NONE',  ( 746.7653713866222915, -329.2601417444138860, 351.0478386215610271 ) ) ;
#1529=CARTESIAN_POINT ( 'NONE',  ( 759.9864689768902508, -338.0891481129649492, 354.9819416627836404 ) ) ;
#1537=CARTESIAN_POINT ( 'NONE',  ( 768.0187753319979720, -56.63460265842036279, 318.0580252608186242 ) ) ;
#1538=CARTESIAN_POINT ( 'NONE',  ( 757.4527132478984868, -376.3726999360614514, 329.1273215169538844 ) ) ;
#1540=CARTESIAN_POINT ( 'NONE',  ( 767.6429770376291799, -417.1800572038736732, 306.8695393053162093 ) ) ;
#1541=CARTESIAN_POINT ( 'NONE',  ( 799.9999999999993179, 205.0000000000000568, 360.0000000000000000 ) ) ;
#1542=CARTESIAN_POINT ( 'NONE',  ( 748.3538107759620743, -328.7146871989592682, 355.8262568251490165 ) ) ;
#1544=CARTESIAN_POINT ( 'NONE',  ( 756.1443688327750579, -93.62377810805098477, 314.3581564841659315 ) ) ;
#1548=CARTESIAN_POINT ( 'NONE',  ( 811.0346526505616112, -422.6346026584192259, 323.0537975583477532 ) ) ;
#1549=CARTESIAN_POINT ( 'NONE',  ( 755.2512626584698410, 16.45630643248849267, 315.2512626584710915 ) ) ;
#1550=FACE_BOUND ( 'NONE', #35499, .T. ) ;
#1554=CARTESIAN_POINT ( 'NONE',  ( 766.9102291470427417, -282.5545181178798657, 318.6633372737382501 ) ) ;
#1555=CARTESIAN_POINT ( 'NONE',  ( 759.7806653035534055, -174.9982390220563673, 324.8639956371180801 ) ) ;
#1560=CARTESIAN_POINT ( 'NONE',  ( 748.6759233522253680, -88.37269993606226137, 324.3348316497537098 ) ) ;
#1564=CARTESIAN_POINT ( 'NONE',  ( 801.9419747391806368, -114.4527844766020053, 351.9812246680014027 ) ) ;
#1568=CARTESIAN_POINT ( 'NONE',  ( 804.1105419155481968, -27.82724539060790292, 347.6308680596136469 ) ) ;
#1570=FACE_BOUND ( 'NONE', #43424, .T. ) ;
#1571=CARTESIAN_POINT ( 'NONE',  ( 793.2243759319678702, -386.5328690171409676, 318.4439275373583200 ) ) ;
#1573=CARTESIAN_POINT ( 'NONE',  ( 805.1016975059191054, -78.89650538077832209, 343.0745993439771837 ) ) ;
#1576=CARTESIAN_POINT ( 'NONE',  ( 781.2497674668890113, -252.3510508353232353, 375.3608509340180603 ) ) ;
#1577=CARTESIAN_POINT ( 'NONE',  ( 754.8072714833583632, -52.81642084023856398, 338.1981804954721156 ) ) ;
#1580=CARTESIAN_POINT ( 'NONE',  ( 804.6798772138708955, -231.7255117493288310, 334.6312213355107019 ) ) ;
#1590=CARTESIAN_POINT ( 'NONE',  ( 744.7301800767020268, -316.8164208402377540, 337.4774526936615189 ) ) ;
#1591=CARTESIAN_POINT ( 'NONE',  ( 807.5423716828161105, -33.07832356259662987, 362.2119215644372048 ) ) ;
#1597=CARTESIAN_POINT ( 'NONE',  ( 757.8323909638827445, -218.6346026584197944, 352.1044303154654358 ) ) ;
#1600=CARTESIAN_POINT ( 'NONE',  ( 759.0252816721024374, -336.9982390220558273, 368.0189434323527280 ) ) ;
#1602=CARTESIAN_POINT ( 'NONE',  ( 805.0264073115434940, -366.3510508353228374, 339.4763451958999099 ) ) ;
#1605=CARTESIAN_POINT ( 'NONE',  ( 769.0155153010367712, -202.3726999360618777, 362.7791456095907279 ) ) ;
#1606=CARTESIAN_POINT ( 'NONE',  ( 785.3141322388236176, -69.72551174932942786, 364.4286716492789537 ) ) ;
#1610=CARTESIAN_POINT ( 'NONE',  ( 779.4709603349208464, -216.3510508353233490, 314.7162404726379918 ) ) ;
#1613=CARTESIAN_POINT ( 'NONE',  ( 745.4481719005789273, -435.7255117493282341, 347.5162901302853129 ) ) ;
#1617=CARTESIAN_POINT ( 'NONE',  ( 792.2312462859673587, -35.90732993114770011, 307.2067596250082602 ) ) ;
#1618=CARTESIAN_POINT ( 'NONE',  ( 814.2001403089898304, -137.3618753856928265, 347.4397851343538264 ) ) ;
#1622=CARTESIAN_POINT ( 'NONE',  ( 792.2312462859673587, -371.9073299311465917, 307.2067596250082602 ) ) ;
#1624=CARTESIAN_POINT ( 'NONE',  ( 764.0069404352550464, 8.921676437403235127, 359.2566176426627180 ) ) ;
#1627=CARTESIAN_POINT ( 'NONE',  ( 805.9055244015594326, -147.6237781080508285, 315.8990559732753240 ) ) ;
#1628=CARTESIAN_POINT ( 'NONE',  ( 764.8639956371174549, -440.0891481129645513, 319.7806653035542581 ) ) ;
#1632=CARTESIAN_POINT ( 'NONE',  ( 797.8594530101008786, -133.5436935675110135, 322.1405469898980982 ) ) ;
#1634=CARTESIAN_POINT ( 'NONE',  ( 774.6858677611749044, -273.7255117493288026, 315.5713283507209894 ) ) ;
#1635=CARTESIAN_POINT ( 'NONE',  ( 755.3201227861273992, -243.7255117493288310, 345.3687786644892981 ) ) ;
#1638=CARTESIAN_POINT ( 'NONE',  ( 797.8594530101008786, -445.5436935675098766, 322.1405469898980982 ) ) ;
#1642=CARTESIAN_POINT ( 'NONE',  ( 808.0189434323515343, -206.0891481129653471, 319.0252816721025511 ) ) ;
#1643=CARTESIAN_POINT ( 'NONE',  ( 802.5472867521000353, -292.3726999360616219, 350.8726784830461156 ) ) ;
#1644=CARTESIAN_POINT ( 'NONE',  ( 801.3366627262608972, -392.5328690171409107, 353.0897708529566899 ) ) ;
#1651=CARTESIAN_POINT ( 'NONE',  ( 766.7756240680305382, -278.5328690171412518, 361.5560724626415663 ) ) ;
#1652=CARTESIAN_POINT ( 'NONE',  ( 772.4999999999993179, -462.9681489794448339, 369.0473750965555837 ) ) ;
#1663=CARTESIAN_POINT ( 'NONE',  ( 754.9967657858570647, -25.54369356751136877, 365.0032342141425374 ) ) ;
#1666=CARTESIAN_POINT ( 'NONE',  ( 805.1927285166397041, -40.81642084023859951, 341.8018195045277707 ) ) ;
#1667=CARTESIAN_POINT ( 'NONE',  ( 807.2620300519052989, -288.0090635724252479, 318.0141637701419768 ) ) ;
#1668=CARTESIAN_POINT ( 'NONE',  ( 772.5602148656447525, -249.7255117493288594, 305.7998596910095443 ) ) ;
#1672=CARTESIAN_POINT ( 'NONE',  ( 758.0580252608178853, -342.4527844766013231, 328.0187753319985404 ) ) ;
#1674=CARTESIAN_POINT ( 'NONE',  ( 773.4516893846965786, -115.6454272087894424, 315.8398074228977066 ) ) ;
#1676=PRODUCT_DEFINITION_FORMATION_WITH_SPECIFIED_SOURCE ( 'ANY', '', #9267, .NOT_KNOWN. ) ;
#1679=CARTESIAN_POINT ( 'NONE',  ( 800.2193346964447755, -378.9982390220555999, 355.1360043628815788 ) ) ;
#1682=CARTESIAN_POINT ( 'NONE',  ( 754.8072714833581358, -148.8164208402382656, 338.1981804954720587 ) ) ;
#1686=CARTESIAN_POINT ( 'NONE',  ( 762.3223304703356007, -367.5436935675102745, 322.3223304703362828 ) ) ;
#1690=CARTESIAN_POINT ( 'NONE',  ( 796.9462024416508257, -84.45278447660207632, 308.9653473494370246 ) ) ;
#1695=CARTESIAN_POINT ( 'NONE',  ( 744.7301800767019131, -268.8164208402378108, 337.4774526936615757 ) ) ;
#1696=CARTESIAN_POINT ( 'NONE',  ( 805.1016975059191054, -150.8965053807781089, 343.0745993439771837 ) ) ;
#1699=CARTESIAN_POINT ( 'NONE',  ( 788.7631598425961101, -409.4419599262317320, 305.7194118038759143 ) ) ;
#1703=AXIS2_PLACEMENT_3D ( 'NONE', #5254, #19345, #33429 ) ;
#1706=CARTESIAN_POINT ( 'NONE',  ( 813.5763878283155464, -51.82724539060782121, 351.1614460488615350 ) ) ;
#1715=CARTESIAN_POINT ( 'NONE',  ( 786.5483106153019435, -391.6454272087885897, 364.1601925771022366 ) ) ;
#1717=CARTESIAN_POINT ( 'NONE',  ( 805.2837595273609850, -242.7363362996980811, 340.5290396650784714 ) ) ;
#1719=CARTESIAN_POINT ( 'NONE',  ( 759.9999999999992042, 166.4563064324884465, 319.9999999999999432 ) ) ;
#1721=CARTESIAN_POINT ( 'NONE',  ( 804.1009440267234822, -191.4636090269709996, 314.0944755984392600 ) ) ;
#1723=CARTESIAN_POINT ( 'NONE',  ( 751.6929314249748586, -150.9982390220563957, 318.8095938919659034 ) ) ;
#1726=CARTESIAN_POINT ( 'NONE',  ( 756.3353852180819104, -245.9073299311469896, 331.1735550268788302 ) ) ;
#1727=CARTESIAN_POINT ( 'NONE',  ( 790.0220218866281812, -31.09997266333516919, 363.2186876482849129 ) ) ;
#1733=CARTESIAN_POINT ( 'NONE',  ( 803.8651313633788504, -77.26014174441466764, 332.4468031744301015 ) ) ;
#1738=CARTESIAN_POINT ( 'NONE',  ( 767.8955696845333705, -48.45278447660219712, 362.1676090361162323 ) ) ;
#1742=CARTESIAN_POINT ( 'NONE',  ( 793.4146539503750546, -361.9874144716864635, 307.6481478633938877 ) ) ;
#1745=CARTESIAN_POINT ( 'NONE',  ( 794.9819416627830151, -348.9982390220558273, 319.9864689768909898 ) ) ;
#1752=CARTESIAN_POINT ( 'NONE',  ( 794.9819416627830151, -108.9982390220565804, 319.9864689768909898 ) ) ;
#1753=CARTESIAN_POINT ( 'NONE',  ( 760.7433823573367135, -372.0090635724250205, 355.9930595647440441 ) ) ;
#1754=CARTESIAN_POINT ( 'NONE',  ( 745.0891759886404770, -436.2709662947827951, 342.4968714119734159 ) ) ;
#1756=CARTESIAN_POINT ( 'NONE',  ( 781.2497674668890113, -324.3510508353229511, 375.3608509340180603 ) ) ;
#1757=CARTESIAN_POINT ( 'NONE',  ( 764.3348316497523456, -94.71468719896007826, 308.6759233522265617 ) ) ;
#1761=CARTESIAN_POINT ( 'NONE',  ( 748.9653473494363425, -434.6346026584190554, 356.9462024416521331 ) ) ;
#1762=CARTESIAN_POINT ( 'NONE',  ( 782.7696130847263021, 18.14353250567099707, 310.1281195208451322 ) ) ;
#1765=CARTESIAN_POINT ( 'NONE',  ( 779.9999999999992042, -462.9681489794448339, 370.0000000000000568 ) ) ;
#1767=CARTESIAN_POINT ( 'NONE',  ( 761.4292242960306112, -281.4636090269706870, 323.2154366446414429 ) ) ;
#1768=CARTESIAN_POINT ( 'NONE',  ( 781.7834795799800531, -178.8164208402381519, 315.0636971347436202 ) ) ;
#1770=CARTESIAN_POINT ( 'NONE',  ( 773.7305795820266212, -273.2817908451526137, 374.8230680027170365 ) ) ;
#1771=AXIS2_PLACEMENT_3D ( 'NONE', #16689, #8846, #40278 ) ;
#1774=CARTESIAN_POINT ( 'NONE',  ( 757.7880784355613741, -66.00906357242595845, 312.4576283171834916 ) ) ;
#1778=CARTESIAN_POINT ( 'NONE',  ( 755.0636971347428243, -148.2709662947837330, 341.7834795799807353 ) ) ;
#1779=ORIENTED_EDGE ( 'NONE', *, *, #1261, .T. ) ;
#1783=CARTESIAN_POINT ( 'NONE',  ( 799.2566176426618085, -0.009063572426172561425, 324.0069404352559559 ) ) ;
#1786=CARTESIAN_POINT ( 'NONE',  ( 790.8726784830453198, -394.7146871989591546, 362.5472867521010585 ) ) ;
#1793=CARTESIAN_POINT ( 'NONE',  ( 800.1688906516307043, -250.1692326535050199, 369.0717654672308186 ) ) ;
#1794=CARTESIAN_POINT ( 'NONE',  ( 794.9819416627830151, -84.99823902205663728, 319.9864689768909898 ) ) ;
#1797=CARTESIAN_POINT ( 'NONE',  ( 774.6312213355099630, -239.3618753856924570, 364.6798772138717482 ) ) ;
#1798=VECTOR ( 'NONE', #38745, 1000.000000000000000 ) ;
#1809=CARTESIAN_POINT ( 'NONE',  ( 767.6429770376291799, -321.1800572038740711, 306.8695393053162093 ) ) ;
#1810=CARTESIAN_POINT ( 'NONE',  ( 751.2241431872005251, -16.16923265350578021, 359.9636004259367610 ) ) ;
#1814=CARTESIAN_POINT ( 'NONE',  ( 788.8264449731200330, -213.1800572038743553, 363.6646147819171233 ) ) ;
#1817=CARTESIAN_POINT ( 'NONE',  ( 744.7301800767019131, -316.8164208402377540, 337.4774526936615757 ) ) ;
#1823=CARTESIAN_POINT ( 'NONE',  ( 776.9254006560222479, -188.1908817542437760, 314.8983024940802125 ) ) ;
#1824=CARTESIAN_POINT ( 'NONE',  ( 797.6776695296629214, -91.54369356751116982, 357.6776695296636603 ) ) ;
#1828=CARTESIAN_POINT ( 'NONE',  ( 805.1016975059191054, -246.8965053807777679, 343.0745993439771837 ) ) ;
#1832=CARTESIAN_POINT ( 'NONE',  ( 767.6429770376289525, -441.1800572038735027, 306.8695393053162093 ) ) ;
#1838=CARTESIAN_POINT ( 'NONE',  ( 777.4774526936600978, -34.27096629478407408, 304.7301800767027657 ) ) ;
#1839=CARTESIAN_POINT ( 'NONE',  ( 745.4481719005789273, -147.7255117493291152, 347.5162901302853129 ) ) ;
#1845=CARTESIAN_POINT ( 'NONE',  ( 792.2312462859673587, -347.9073299311467053, 307.2067596250082602 ) ) ;
#1849=CARTESIAN_POINT ( 'NONE',  ( 760.5453621957607311, 2.921676437403253779, 323.8424801807151425 ) ) ;
#1852=CARTESIAN_POINT ( 'NONE',  ( 783.7566961878529810, -120.8965053807781800, 305.1792804349288417 ) ) ;
#1853=CARTESIAN_POINT ( 'NONE',  ( 756.3353852180820240, -437.9073299311464211, 331.1735550268787733 ) ) ;
#1858=CARTESIAN_POINT ( 'NONE',  ( 774.6312213355099630, -143.3618753856927697, 364.6798772138717482 ) ) ;
#1861=CARTESIAN_POINT ( 'NONE',  ( 771.1735550268778070, -297.1800572038740711, 316.3353852180827630 ) ) ;
#1862=CARTESIAN_POINT ( 'NONE',  ( 803.6646147819162707, -257.9073299311469327, 348.8264449731211130 ) ) ;
#1865=CARTESIAN_POINT ( 'NONE',  ( 784.0799538623451781, 12.19440371013049784, 364.6971507214555572 ) ) ;
#1869=CARTESIAN_POINT ( 'NONE',  ( 808.3070685750232087, -234.9982390220561683, 361.1904061080339829 ) ) ;
#1870=CARTESIAN_POINT ( 'NONE',  ( 796.9571628226829034, -311.4636090269706870, 321.2382568024804641 ) ) ;
#1871=CARTESIAN_POINT ( 'NONE',  ( 763.2154366446407039, -405.6237781080500326, 321.4292242960311228 ) ) ;
#1879=CARTESIAN_POINT ( 'NONE',  ( 787.6308680596127942, -299.2601417444139997, 364.1105419155492768 ) ) ;
#1882=CARTESIAN_POINT ( 'NONE',  ( 772.4999999999993179, -462.9681489794447202, 270.0000000000000568 ) ) ;
#1886=CARTESIAN_POINT ( 'NONE',  ( 749.5768839229115201, -204.5545181178800931, 358.0661480581553064 ) ) ;
#1887=STYLED_ITEM('',(#45765),#31946);
#1890=EDGE_CURVE ( 'NONE', #10697, #34810, #20967, .T. ) ;
#1894=CARTESIAN_POINT ( 'NONE',  ( 758.8095938919642549, -32.08914811296588709, 311.6929314249763365 ) ) ;
#1897=CARTESIAN_POINT ( 'NONE',  ( 781.8018195045266339, -46.27096629478404566, 365.1927285166406705 ) ) ;
#1898=CARTESIAN_POINT ( 'NONE',  ( 786.2694204179717872, -309.2817908451525568, 305.1769319972829067 ) ) ;
#1899=CARTESIAN_POINT ( 'NONE',  ( 796.9462024416508257, -252.4527844766015789, 308.9653473494370246 ) ) ;
#1901=ADVANCED_FACE ( 'NONE', ( #34213 ), #44393, .F. ) ;
#1904=CARTESIAN_POINT ( 'NONE',  ( 800.0135310231082713, -350.0891481129648923, 325.0180583372163028 ) ) ;
#1905=CARTESIAN_POINT ( 'NONE',  ( 796.1575198192839480, -126.0090635724257737, 359.4546378042384163 ) ) ;
#1909=FACE_OUTER_BOUND ( 'NONE', #17632, .T. ) ;
#1910=CARTESIAN_POINT ( 'NONE',  ( 781.2497674668890113, -132.3510508353235764, 375.3608509340180603 ) ) ;
#1911=CARTESIAN_POINT ( 'NONE',  ( 759.9864689768902508, -410.0891481129647218, 354.9819416627836404 ) ) ;
#1916=CARTESIAN_POINT ( 'NONE',  ( 804.9363028652555840, -160.2709662947836762, 338.2165204200192079 ) ) ;
#1917=CARTESIAN_POINT ( 'NONE',  ( 778.2165204200184689, -142.8164208402382656, 364.9363028652563230 ) ) ;
#1918=UNCERTAINTY_MEASURE_WITH_UNIT (LENGTH_MEASURE( 1.000000000000000082E-05 ), #28708, 'distance_accuracy_value', 'NONE');
#1922=CARTESIAN_POINT ( 'NONE',  ( 768.0187753319979720, -344.6346026584195101, 318.0580252608186242 ) ) ;
#1928=CARTESIAN_POINT ( 'NONE',  ( 749.2812353651451076, -126.4527844766019626, 323.2262854647983090 ) ) ;
#1933=CARTESIAN_POINT ( 'NONE',  ( 815.2698199232961542, -256.8164208402379245, 342.5225473063383106 ) ) ;
#1934=CARTESIAN_POINT ( 'NONE',  ( 804.1601925771018387, -175.4419599262325562, 346.5483106153029098 ) ) ;
#1938=ORIENTED_EDGE ( 'NONE', *, *, #17991, .F. ) ;
#1943=CARTESIAN_POINT ( 'NONE',  ( 797.8822607201568644, -102.5545181178804057, 370.1134526219340160 ) ) ;
#1954=CARTESIAN_POINT ( 'NONE',  ( 784.1219089521767955, -429.2817908451521021, 315.0488828828318333 ) ) ;
#1957=CARTESIAN_POINT ( 'NONE',  ( 793.0897708529556667, -246.5545181178799510, 361.3366627262616362 ) ) ;
#1961=CIRCLE ( 'NONE', #14553, 4.999999999999982236 ) ;
#1962=CARTESIAN_POINT ( 'NONE',  ( 771.3260364891663130, -163.6454272087893003, 306.0683387631859773 ) ) ;
#1964=CARTESIAN_POINT ( 'NONE',  ( 804.7487373415286811, -163.5436935675109567, 364.7487373415288516 ) ) ;
#1968=CARTESIAN_POINT ( 'NONE',  ( 804.4286716492782716, -257.3618753856924286, 345.3141322388244703 ) ) ;
#1969=CARTESIAN_POINT ( 'NONE',  ( 763.0428371773158460, -11.46360902697159290, 358.7617431975195359 ) ) ;
#1974=CARTESIAN_POINT ( 'NONE',  ( 775.9200461376533440, -71.80559628986922860, 315.3028492785443291 ) ) ;
#1978=CARTESIAN_POINT ( 'NONE',  ( 788.7366044899766848, -59.90732993114762905, 316.5762568750059813 ) ) ;
#1980=CARTESIAN_POINT ( 'NONE',  ( 744.9990715423526808, -378.3510508353227806, 341.2370466360926002 ) ) ;
#1983=CARTESIAN_POINT ( 'NONE',  ( 772.5602148656447525, 14.27448825067031812, 305.7998596910095443 ) ) ;
#1985=CARTESIAN_POINT ( 'NONE',  ( 791.9812246680005501, -356.6346026584193964, 361.9419747391813189 ) ) ;
#1994=CARTESIAN_POINT ( 'NONE',  ( 756.3353852180819104, -77.90732993114757221, 331.1735550268788302 ) ) ;
#1995=CARTESIAN_POINT ( 'NONE',  ( 775.8780910478218402, -393.2817908451522726, 364.9511171171680530 ) ) ;
#1997=CARTESIAN_POINT ( 'NONE',  ( 805.0032342141413437, -445.5436935675099335, 314.9967657858572352 ) ) ;
#1999=CARTESIAN_POINT ( 'NONE',  ( 801.9858362298568863, -315.0783235625957559, 312.7379699480935642 ) ) ;
#2003=CARTESIAN_POINT ( 'NONE',  ( 744.6391490659812007, -14.73633629969885384, 338.7502325331110455 ) ) ;
#2004=DIRECTION ( 'NONE',  ( 0.000000000000000000, 1.000000000000000000, 1.110223024625155554E-15 ) ) ;
#2010=CARTESIAN_POINT ( 'NONE',  ( 798.5707757039680246, -293.4636090269707438, 356.7845633553585003 ) ) ;
#2011=CARTESIAN_POINT ( 'NONE',  ( 778.1981804954714335, -178.2709662947835625, 314.8072714833589885 ) ) ;
#2012=ORIENTED_EDGE ( 'NONE', *, *, #14906, .F. ) ;
#2013=CARTESIAN_POINT ( 'NONE',  ( 804.1009440267234822, -263.4636090269708006, 314.0944755984392600 ) ) ;
#2016=CARTESIAN_POINT ( 'NONE',  ( 809.0717654672305343, -76.91815448151683654, 360.1688906516309885 ) ) ;
#2018=VECTOR ( 'NONE', #9854, 1000.000000000000000 ) ;
#2019=CARTESIAN_POINT ( 'NONE',  ( 779.9999999999992042, 16.45630643248849267, 339.9999999999999432 ) ) ;
#2020=CARTESIAN_POINT ( 'NONE',  ( 805.1927285166397041, -160.8164208402382371, 341.8018195045277707 ) ) ;
#2025=CARTESIAN_POINT ( 'NONE',  ( 796.9571628226829034, -23.46360902697155026, 321.2382568024804641 ) ) ;
#2028=CARTESIAN_POINT ( 'NONE',  ( 794.1144889064781864, -418.1692326535044799, 360.9840315886528401 ) ) ;
#2033=CARTESIAN_POINT ( 'NONE',  ( 795.6651683502461765, -226.7146871989596661, 371.3240766477733814 ) ) ;
#2034=CARTESIAN_POINT ( 'NONE',  ( 762.1405469898973024, -73.54369356751121245, 357.8594530101016176 ) ) ;
#2038=CARTESIAN_POINT ( 'NONE',  ( 762.1405469898971887, -265.5436935675106156, 357.8594530101015607 ) ) ;
#2045=CARTESIAN_POINT ( 'NONE',  ( 748.9653473494365699, -338.6346026584195101, 356.9462024416520762 ) ) ;
#2046=CARTESIAN_POINT ( 'NONE',  ( 781.2497674668890113, -228.3510508353232922, 375.3608509340180603 ) ) ;
#2047=ADVANCED_FACE ( 'NONE', ( #2347 ), #8632, .F. ) ;
#2048=CARTESIAN_POINT ( 'NONE',  ( 761.9338519418445230, -38.53286901714206891, 370.4231160770881957 ) ) ;
#2053=CARTESIAN_POINT ( 'NONE',  ( 803.6646147819161570, -209.9073299311470748, 348.8264449731210561 ) ) ;
#2057=CARTESIAN_POINT ( 'NONE',  ( 758.8095938919642549, -320.0891481129648355, 311.6929314249763365 ) ) ;
#2062=CARTESIAN_POINT ( 'NONE',  ( 754.7162404726377645, -182.7363362996983369, 339.4709603349214717 ) ) ;
#2063=CARTESIAN_POINT ( 'NONE',  ( 759.9864689768902508, -74.08914811296577341, 354.9819416627836404 ) ) ;
#2067=CARTESIAN_POINT ( 'NONE',  ( 804.9511171171677688, -269.8055962898686175, 335.8780910478229202 ) ) ;
#2070=CARTESIAN_POINT ( 'NONE',  ( 755.2512626584698410, -415.5436935675102177, 315.2512626584710915 ) ) ;
#2074=CARTESIAN_POINT ( 'NONE',  ( 787.4397851343537695, -69.72551174932942786, 374.2001403089903988 ) ) ;
#2075=CARTESIAN_POINT ( 'NONE',  ( 744.7301800767019131, -148.8164208402382656, 337.4774526936615757 ) ) ;
#2078=EDGE_CURVE ( 'NONE', #27436, #32644, #12994, .T. ) ;
#2081=CARTESIAN_POINT ( 'NONE',  ( 800.9747183278959710, -396.9982390220556567, 311.9810565676471583 ) ) ;
#2082=CARTESIAN_POINT ( 'NONE',  ( 796.9462024416508257, -12.45278447660232324, 308.9653473494370246 ) ) ;
#2084=CARTESIAN_POINT ( 'NONE',  ( 775.9200461376533440, 24.19440371013046231, 315.3028492785443291 ) ) ;
#2088=CARTESIAN_POINT ( 'NONE',  ( 813.9316612368132837, -151.4419599262326415, 348.6739635108323228 ) ) ;
#2090=AXIS2_PLACEMENT_3D ( 'NONE', #42506, #28870, #17797 ) ;
#2091=CARTESIAN_POINT ( 'NONE',  ( 812.6845335610512393, -175.9874144716871172, 353.5525998758768651 ) ) ;
#2095=CARTESIAN_POINT ( 'NONE',  ( 754.8072714833581358, -148.8164208402382656, 338.1981804954720587 ) ) ;
#2097=CARTESIAN_POINT ( 'NONE',  ( 756.3353852180820240, -293.9073299311468759, 331.1735550268787733 ) ) ;
#2098=FACE_OUTER_BOUND ( 'NONE', #12227, .T. ) ;
#2100=CARTESIAN_POINT ( 'NONE',  ( 763.2154366446407039, 26.37622189194863509, 321.4292242960311228 ) ) ;
#2102=EDGE_CURVE ( 'NONE', #21705, #35766, #8461, .T. ) ;
#2105=CARTESIAN_POINT ( 'NONE',  ( 747.2067596250078623, -219.1800572038744122, 352.2312462859687230 ) ) ;
#2106=EDGE_CURVE ( 'NONE', #10247, #12793, #44588, .T. ) ;
#2107=CARTESIAN_POINT ( 'NONE',  ( 796.1575198192839480, -294.0090635724253048, 359.4546378042384163 ) ) ;
#2108=CARTESIAN_POINT ( 'NONE',  ( 794.1144889064781864, -394.1692326535045368, 360.9840315886528401 ) ) ;
#2116=CARTESIAN_POINT ( 'NONE',  ( 772.3691319403857278, -311.2601417444139429, 315.8894580844506663 ) ) ;
#2124=CARTESIAN_POINT ( 'NONE',  ( 750.9282345327678740, -208.9181544815164102, 319.8311093483690115 ) ) ;
#2129=CARTESIAN_POINT ( 'NONE',  ( 767.7687537140311633, -47.90732993114767169, 372.7932403749916830 ) ) ;
#2132=CARTESIAN_POINT ( 'NONE',  ( 792.1044303154645831, -60.45278447660215448, 317.8323909638837677 ) ) ;
#2133=CARTESIAN_POINT ( 'NONE',  ( 747.6481478633932056, -325.0999726633342561, 353.4146539503763620 ) ) ;
#2135=CARTESIAN_POINT ( 'NONE',  ( 745.0891759886404770, -268.2709662947833067, 342.4968714119734159 ) ) ;
#2139=CARTESIAN_POINT ( 'NONE',  ( 757.8323909638827445, -362.6346026584194533, 352.1044303154654358 ) ) ;
#2140=CARTESIAN_POINT ( 'NONE',  ( 757.4527132478984868, -112.3726999360621761, 329.1273215169538844 ) ) ;
#2142=CARTESIAN_POINT ( 'NONE',  ( 746.0683387631852383, -43.44195992623296831, 331.3260364891676204 ) ) ;
#2143=CARTESIAN_POINT ( 'NONE',  ( 755.3201227861273992, -387.7255117493284047, 345.3687786644892981 ) ) ;
#2144=CARTESIAN_POINT ( 'NONE',  ( 769.9999999999992042, 178.9475563372491251, 320.0000000000000000 ) ) ;
#2145=CARTESIAN_POINT ( 'NONE',  ( 799.9999999999993179, -512.9681489794448908, 339.9999999999999432 ) ) ;
#2146=CARTESIAN_POINT ( 'NONE',  ( 762.3223304703356007, -391.5436935675101608, 322.3223304703362828 ) ) ;
#2149=CARTESIAN_POINT ( 'NONE',  ( 805.1927285166397041, -208.8164208402380666, 341.8018195045277707 ) ) ;
#2150=CARTESIAN_POINT ( 'NONE',  ( 759.9864689768902508, -146.0891481129655176, 354.9819416627836404 ) ) ;
#2154=CARTESIAN_POINT ( 'NONE',  ( 785.3687786644884454, -371.3618753856919739, 315.3201227861279676 ) ) ;
#2159=CARTESIAN_POINT ( 'NONE',  ( 801.1904061080338124, -116.0891481129656313, 368.3070685750236066 ) ) ;
#2166=CARTESIAN_POINT ( 'NONE',  ( 754.9967657858570647, -265.5436935675106156, 365.0032342141425374 ) ) ;
#2167=CARTESIAN_POINT ( 'NONE',  ( 759.2295555964440155, -184.1692326535052757, 353.9708237608231229 ) ) ;
#2177=CARTESIAN_POINT ( 'NONE',  ( 810.4231160770870019, -96.55451811788039151, 321.9338519418446936 ) ) ;
#2186=CARTESIAN_POINT ( 'NONE',  ( 759.0159684113467620, -424.9181544815158986, 325.8855110935213020 ) ) ;
#2193=CARTESIAN_POINT ( 'NONE',  ( 744.6391490659812007, -230.7363362996981664, 338.7502325331110455 ) ) ;
#2195=CARTESIAN_POINT ( 'NONE',  ( 813.1304606946830518, -137.9073299311473875, 352.3570229623690580 ) ) ;
#2198=CARTESIAN_POINT ( 'NONE',  ( 765.0180583372156207, -264.9982390220561115, 360.0135310231089534 ) ) ;
#2199=CARTESIAN_POINT ( 'NONE',  ( 802.9823548866075953, -49.09997266333511590, 330.0799878456151077 ) ) ;
#2203=CARTESIAN_POINT ( 'NONE',  ( 784.0799538623451781, -83.80559628986920018, 364.6971507214555572 ) ) ;
#2208=CARTESIAN_POINT ( 'NONE',  ( 771.2633955100217236, -47.90732993114767169, 363.4237431249939618 ) ) ;
#2211=CARTESIAN_POINT ( 'NONE',  ( 776.2433038121456548, -396.8965053807772847, 374.8207195650711014 ) ) ;
#2214=CARTESIAN_POINT ( 'NONE',  ( 800.2193346964447755, -378.9982390220555999, 355.1360043628815788 ) ) ;
#2221=CARTESIAN_POINT ( 'NONE',  ( 794.9819416627830151, -84.99823902205663728, 319.9864689768909898 ) ) ;
#2222=CARTESIAN_POINT ( 'NONE',  ( 790.9844846989617508, -406.3726999360612808, 317.2208543904092721 ) ) ;
#2223=CARTESIAN_POINT ( 'NONE',  ( 813.1304606946831655, -425.9073299311463643, 352.3570229623691716 ) ) ;
#2225=CARTESIAN_POINT ( 'NONE',  ( 756.1443688327750579, -309.6237781080502600, 314.3581564841659315 ) ) ;
#2229=CARTESIAN_POINT ( 'NONE',  ( 811.3240766477731540, -4.372699936062523385, 355.6651683502462902 ) ) ;
#2231=PLANE ( 'NONE',  #41075 ) ;
#2234=LINE ( 'NONE', #3629, #42598 ) ;
#2236=CARTESIAN_POINT ( 'NONE',  ( 804.4086373105744769, -337.6454272087888171, 333.3843516231986541 ) ) ;
#2237=CARTESIAN_POINT ( 'NONE',  ( 778.2165204200184689, -190.8164208402381234, 364.9363028652563230 ) ) ;
#2239=CARTESIAN_POINT ( 'NONE',  ( 745.7194118038753459, -301.6454272087889308, 348.7631598425976449 ) ) ;
#2242=CARTESIAN_POINT ( 'NONE',  ( 814.8207195650702488, -122.1908817542439749, 336.2433038121456548 ) ) ;
#2246=CARTESIAN_POINT ( 'NONE',  ( 781.7834795799800531, -154.8164208402382371, 315.0636971347436202 ) ) ;
#2248=CARTESIAN_POINT ( 'NONE',  ( 793.5525998758768083, -391.0999726633340288, 372.6845335610516941 ) ) ;
#2251=CARTESIAN_POINT ( 'NONE',  ( 769.0155153010367712, -34.37269993606243901, 362.7791456095907279 ) ) ;
#2254=CARTESIAN_POINT ( 'NONE',  ( 805.1016975059191054, -438.8965053807771710, 343.0745993439771837 ) ) ;
#2258=CARTESIAN_POINT ( 'NONE',  ( 771.2368401574024119, -277.4419599262322436, 374.2805881961240857 ) ) ;
#2259=CARTESIAN_POINT ( 'NONE',  ( 804.4286716492782716, -89.36187538569299704, 345.3141322388244703 ) ) ;
#2261=CARTESIAN_POINT ( 'NONE',  ( 803.6646147819161570, -281.9073299311468759, 348.8264449731210561 ) ) ;
#2268=CARTESIAN_POINT ( 'NONE',  ( 758.8095938919644823, -320.0891481129648923, 311.6929314249762797 ) ) ;
#2269=CARTESIAN_POINT ( 'NONE',  ( 744.9990715423526808, -210.3510508353233490, 341.2370466360926002 ) ) ;
#2274=CARTESIAN_POINT ( 'NONE',  ( 768.0187753319979720, -200.6346026584199365, 318.0580252608186242 ) ) ;
#2277=CARTESIAN_POINT ( 'NONE',  ( 751.9810565676468741, -362.0891481129648923, 360.9747183278973921 ) ) ;
#2280=CYLINDRICAL_SURFACE ( 'NONE', #12795, 10.00000000000000888 ) ;
#2281=CARTESIAN_POINT ( 'NONE',  ( 796.1575198192839480, -222.0090635724254184, 359.4546378042384163 ) ) ;
#2282=CARTESIAN_POINT ( 'NONE',  ( 803.6646147819161570, -89.90732993114750116, 348.8264449731210561 ) ) ;
#2286=CARTESIAN_POINT ( 'NONE',  ( 759.2295555964440155, -256.1692326535049915, 353.9708237608231229 ) ) ;
#2289=SHAPE_REPRESENTATION ( 'MirrorTreadle Extension Return Springs', ( #26858 ), #27503 ) ;
#2290=CARTESIAN_POINT ( 'NONE',  ( 777.4774526936600978, -442.2709662947826814, 304.7301800767027657 ) ) ;
#2294=CARTESIAN_POINT ( 'NONE',  ( 754.9967657858570647, -73.54369356751118403, 365.0032342141425374 ) ) ;
#2295=CARTESIAN_POINT ( 'NONE',  ( 800.9747183278959710, -156.9982390220564241, 311.9810565676471583 ) ) ;
#2299=CARTESIAN_POINT ( 'NONE',  ( 805.6418435158337843, -413.4636090269704027, 363.8556311672236916 ) ) ;
#2301=CARTESIAN_POINT ( 'NONE',  ( 745.4481719005789273, -411.7255117493282910, 347.5162901302853129 ) ) ;
#2302=CARTESIAN_POINT ( 'NONE',  ( 745.7998596910086917, -29.36187538569318178, 332.5602148656461168 ) ) ;
#2304=CARTESIAN_POINT ( 'NONE',  ( 803.8651313633788504, -5.260141744414903897, 332.4468031744301015 ) ) ;
#2307=CARTESIAN_POINT ( 'NONE',  ( 758.0141637701419768, -159.0783235625962391, 367.2620300519063790 ) ) ;
#2308=PLANE ( 'NONE',  #27667 ) ;
#2312=CARTESIAN_POINT ( 'NONE',  ( 792.1044303154645831, -180.4527844766017211, 317.8323909638837677 ) ) ;
#2315=CARTESIAN_POINT ( 'NONE',  ( 755.0636971347428243, -292.2709662947831930, 341.7834795799807353 ) ) ;
#2319=CARTESIAN_POINT ( 'NONE',  ( 756.1348686366196716, -17.26014174441486659, 347.5531968255698416 ) ) ;
#2323=CARTESIAN_POINT ( 'NONE',  ( 792.3570229623691148, -237.1800572038742985, 373.1304606946836770 ) ) ;
#2324=CARTESIAN_POINT ( 'NONE',  ( 805.2837595273609850, -290.7363362996980527, 340.5290396650784714 ) ) ;
#2325=CARTESIAN_POINT ( 'NONE',  ( 760.5453621957607311, -405.0783235625954148, 323.8424801807151425 ) ) ;
#2330=ORIENTED_EDGE ( 'NONE', *, *, #36798, .F. ) ;
#2332=CARTESIAN_POINT ( 'NONE',  ( 761.2382568024794409, -303.6237781080503169, 356.9571628226838129 ) ) ;
#2333=CARTESIAN_POINT ( 'NONE',  ( 793.4839952031973098, -454.3310370489100478, 372.1249834419284639 ) ) ;
#2335=CARTESIAN_POINT ( 'NONE',  ( 784.1219089521767955, -117.2817908451530684, 315.0488828828318333 ) ) ;
#2336=CARTESIAN_POINT ( 'NONE',  ( 781.7834795799800531, 13.18357915976123174, 315.0636971347436202 ) ) ;
#2339=CARTESIAN_POINT ( 'NONE',  ( 781.2370466360911223, -188.7363362996983085, 304.9990715423533629 ) ) ;
#2343=CARTESIAN_POINT ( 'NONE',  ( 777.4774526936600978, -58.27096629478398171, 304.7301800767027657 ) ) ;
#2347=FACE_OUTER_BOUND ( 'NONE', #400, .T. ) ;
#2349=CARTESIAN_POINT ( 'NONE',  ( 811.3240766477731540, -316.3726999360615082, 355.6651683502462902 ) ) ;
#2351=CARTESIAN_POINT ( 'NONE',  ( 811.0346526505616112, -302.6346026584196238, 323.0537975583477532 ) ) ;
#2356=CARTESIAN_POINT ( 'NONE',  ( 792.1044303154645831, -348.4527844766012663, 317.8323909638837677 ) ) ;
#2357=CARTESIAN_POINT ( 'NONE',  ( 793.0897708529556667, -126.5545181178803205, 361.3366627262616362 ) ) ;
#2359=CARTESIAN_POINT ( 'NONE',  ( 776.2433038121456548, -60.89650538077837894, 374.8207195650711014 ) ) ;
#2360=CARTESIAN_POINT ( 'NONE',  ( 803.6646147819162707, -353.9073299311467053, 348.8264449731211130 ) ) ;
#2361=CARTESIAN_POINT ( 'NONE',  ( 814.5518280994195948, 8.274488250670337663, 332.4837098697145166 ) ) ;
#2363=CARTESIAN_POINT ( 'NONE',  ( 798.0661480581538854, -146.5328690171417350, 309.5768839229118043 ) ) ;
#2364=CARTESIAN_POINT ( 'NONE',  ( 781.7834795799800531, -442.8164208402372992, 315.0636971347436202 ) ) ;
#2369=CARTESIAN_POINT ( 'NONE',  ( 765.0180583372156207, -192.9982390220562820, 360.0135310231089534 ) ) ;
#2370=CARTESIAN_POINT ( 'NONE',  ( 764.8639956371174549, -176.0891481129654039, 319.7806653035542581 ) ) ;
#2375=CARTESIAN_POINT ( 'NONE',  ( 762.3223304703356007, -391.5436935675101608, 322.3223304703362828 ) ) ;
#2378=CARTESIAN_POINT ( 'NONE',  ( 808.3070685750232087, -114.9982390220565378, 361.1904061080339829 ) ) ;
#2386=CARTESIAN_POINT ( 'NONE',  ( 751.9810565676468741, -242.0891481129652618, 360.9747183278973921 ) ) ;
#2387=CARTESIAN_POINT ( 'NONE',  ( 803.2186876482843445, -199.9874144716870603, 350.0220218866286928 ) ) ;
#2398=CARTESIAN_POINT ( 'NONE',  ( 766.4474001241216001, -91.09997266333496668, 307.3154664389482491 ) ) ;
#2406=CARTESIAN_POINT ( 'NONE',  ( 802.5472867521000353, -436.3726999360612240, 350.8726784830461156 ) ) ;
#2416=CARTESIAN_POINT ( 'NONE',  ( 814.4686193811664907, -219.2817908451527558, 346.2056067578752732 ) ) ;
#2418=CARTESIAN_POINT ( 'NONE',  ( 805.0032342141412300, -181.5436935675108145, 314.9967657858571783 ) ) ;
#2420=LINE ( 'NONE', #16757, #28339 ) ;
#2422=CARTESIAN_POINT ( 'NONE',  ( 758.0580252608178853, -270.4527844766014937, 328.0187753319985404 ) ) ;
#2423=CARTESIAN_POINT ( 'NONE',  ( 755.8894580844503253, -63.82724539060779279, 332.3691319403863531 ) ) ;
#2427=CARTESIAN_POINT ( 'NONE',  ( 766.7756240680305382, -86.53286901714194812, 361.5560724626415663 ) ) ;
#2428=CARTESIAN_POINT ( 'NONE',  ( 778.2165204200184689, -334.8164208402376403, 364.9363028652563230 ) ) ;
#2430=EDGE_CURVE ( 'NONE', #24420, #41138, #3963, .T. ) ;
#2432=CARTESIAN_POINT ( 'NONE',  ( 791.9812246680005501, -44.63460265842040542, 361.9419747391813189 ) ) ;
#2435=CARTESIAN_POINT ( 'NONE',  ( 768.8385539511368734, -383.2601417444137155, 306.4236121716840557 ) ) ;
#2437=CARTESIAN_POINT ( 'NONE',  ( 778.1981804954714335, -274.2709662947833067, 314.8072714833589885 ) ) ;
#2438=CARTESIAN_POINT ( 'NONE',  ( 793.9861285913068514, -442.9180389616178672, 372.1637643035757606 ) ) ;
#2440=CARTESIAN_POINT ( 'NONE',  ( 788.8264449731200330, -357.1800572038739006, 363.6646147819171233 ) ) ;
#2448=CARTESIAN_POINT ( 'NONE',  ( 765.0180583372156207, -96.99823902205660886, 360.0135310231089534 ) ) ;
#2449=CARTESIAN_POINT ( 'NONE',  ( 769.0155153010367712, -418.3726999360612808, 362.7791456095907279 ) ) ;
#2450=CARTESIAN_POINT ( 'NONE',  ( 755.0488828828309806, -89.80559628986918597, 344.1219089521771934 ) ) ;
#2453=CARTESIAN_POINT ( 'NONE',  ( 805.9055244015594326, -363.6237781080502032, 315.8990559732753240 ) ) ;
#2457=CARTESIAN_POINT ( 'NONE',  ( 804.7487373415286811, -451.5436935675099903, 364.7487373415288516 ) ) ;
#2465=CARTESIAN_POINT ( 'NONE',  ( 796.1575198192839480, -318.0090635724251911, 359.4546378042384163 ) ) ;
#2467=CARTESIAN_POINT ( 'NONE',  ( 804.1009440267234822, -287.4636090269708575, 314.0944755984392600 ) ) ;
#2470=CARTESIAN_POINT ( 'NONE',  ( 795.8262568251477660, -94.37269993606224716, 308.3538107759623585 ) ) ;
#2474=CARTESIAN_POINT ( 'NONE',  ( 795.1360043628807261, -140.0891481129654892, 360.2193346964456282 ) ) ;
#2477=CARTESIAN_POINT ( 'NONE',  ( 762.1177392798416577, -426.5545181178794678, 309.8865473780659272 ) ) ;
#2480=CARTESIAN_POINT ( 'NONE',  ( 772.4468031744293057, -57.82724539060780700, 363.8651313633793620 ) ) ;
#2483=CARTESIAN_POINT ( 'NONE',  ( 778.7502325331095108, 23.64894916467591912, 304.6391490659818828 ) ) ;
#2487=CARTESIAN_POINT ( 'NONE',  ( 801.9858362298568863, -291.0783235625957559, 312.7379699480935642 ) ) ;
#2488=CARTESIAN_POINT ( 'NONE',  ( 795.1360043628808398, -92.08914811296570235, 360.2193346964456282 ) ) ;
#2492=CARTESIAN_POINT ( 'NONE',  ( 800.2193346964447755, -258.9982390220561115, 355.1360043628815788 ) ) ;
#2499=CARTESIAN_POINT ( 'NONE',  ( 763.0537975583476964, -336.4527844766012663, 371.0346526505628617 ) ) ;
#2500=CARTESIAN_POINT ( 'NONE',  ( 805.9055244015594326, -267.6237781080504305, 315.8990559732753240 ) ) ;
#2506=CARTESIAN_POINT ( 'NONE',  ( 756.3353852180819104, -221.9073299311470464, 331.1735550268788302 ) ) ;
#2508=CARTESIAN_POINT ( 'NONE',  ( 755.2512626584698410, -343.5436935675103314, 315.2512626584710915 ) ) ;
#2509=LINE ( 'NONE', #26322, #33659 ) ;
#2511=CARTESIAN_POINT ( 'NONE',  ( 792.8389451398237497, 16.45630643248849978, 314.6345231965543121 ) ) ;
#2513=CARTESIAN_POINT ( 'NONE',  ( 799.2566176426618085, -240.0090635724253900, 324.0069404352559559 ) ) ;
#2514=CARTESIAN_POINT ( 'NONE',  ( 759.7806653035534055, -78.99823902205662307, 324.8639956371180801 ) ) ;
#2518=CARTESIAN_POINT ( 'NONE',  ( 770.0799878456142551, -253.9874144716868329, 362.9823548866085616 ) ) ;
#2522=CARTESIAN_POINT ( 'NONE',  ( 781.2370466360911223, -20.73633629969883430, 304.9990715423533629 ) ) ;
#2527=CARTESIAN_POINT ( 'NONE',  ( 777.4774526936600978, -82.27096629478388934, 304.7301800767027657 ) ) ;
#2528=CARTESIAN_POINT ( 'NONE',  ( 813.1304606946830518, -137.9073299311473875, 352.3570229623690580 ) ) ;
#2530=LINE ( 'NONE', #23760, #29132 ) ;
#2532=CARTESIAN_POINT ( 'NONE',  ( 776.2046728542105711, -404.1908817542431507, 304.8212110874238761 ) ) ;
#2535=CARTESIAN_POINT ( 'NONE',  ( 792.3570229623688874, -381.1800572038737869, 373.1304606946836202 ) ) ;
#2536=CARTESIAN_POINT ( 'NONE',  ( 800.9747183278959710, -12.99823902205686821, 311.9810565676471583 ) ) ;
#2539=CARTESIAN_POINT ( 'NONE',  ( 795.9930595647434757, -27.07832356259665474, 320.7433823573372820 ) ) ;
#2543=CARTESIAN_POINT ( 'NONE',  ( 805.9055244015594326, -171.6237781080507432, 315.8990559732753240 ) ) ;
#2544=CARTESIAN_POINT ( 'NONE',  ( 804.4286716492782716, 6.638124614306706306, 345.3141322388244703 ) ) ;
#2548=CARTESIAN_POINT ( 'NONE',  ( 804.4286716492782716, -161.3618753856927697, 345.3141322388244703 ) ) ;
#2550=CARTESIAN_POINT ( 'NONE',  ( 802.1676090361155502, -302.6346026584195670, 327.8955696845344505 ) ) ;
#2553=CARTESIAN_POINT ( 'NONE',  ( 804.1601925771018387, -7.441959926233078448, 346.5483106153029098 ) ) ;
#2558=CARTESIAN_POINT ( 'NONE',  ( 772.5602148656447525, -225.7255117493289163, 305.7998596910095443 ) ) ;
#2559=CARTESIAN_POINT ( 'NONE',  ( 755.5913626894240451, -349.6454272087887603, 346.6156483768012890 ) ) ;
#2560=CARTESIAN_POINT ( 'NONE',  ( 755.8398074228967971, -427.4419599262317888, 333.4516893846970333 ) ) ;
#2567=CARTESIAN_POINT ( 'NONE',  ( 755.0488828828309806, -305.8055962898684470, 344.1219089521771934 ) ) ;
#2568=CARTESIAN_POINT ( 'NONE',  ( 793.1217772804590140, -457.0129860853185733, 370.3581812299415787 ) ) ;
#2571=CARTESIAN_POINT ( 'NONE',  ( 763.0428371773158460, -107.4636090269713122, 358.7617431975195359 ) ) ;
#2572=CARTESIAN_POINT ( 'NONE',  ( 804.6798772138708955, 8.274488250670337663, 334.6312213355107019 ) ) ;
#2577=CARTESIAN_POINT ( 'NONE',  ( 814.2805881961230625, -217.6454272087891582, 331.2368401574024119 ) ) ;
#2583=CARTESIAN_POINT ( 'NONE',  ( 745.7998596910086917, -29.36187538569318178, 332.5602148656461168 ) ) ;
#2589=CARTESIAN_POINT ( 'NONE',  ( 812.3518521366052028, -337.0999726633342561, 326.5853460496235243 ) ) ;
#2591=CARTESIAN_POINT ( 'NONE',  ( 808.3070685750230950, -282.9982390220558841, 361.1904061080339261 ) ) ;
#2596=CARTESIAN_POINT ( 'NONE',  ( 792.1044303154645831, -396.4527844766010389, 317.8323909638837677 ) ) ;
#2597=CARTESIAN_POINT ( 'NONE',  ( 766.9102291470427417, -162.5545181178802352, 318.6633372737382501 ) ) ;
#2599=CARTESIAN_POINT ( 'NONE',  ( 814.8230680027162407, -77.80559628986920018, 333.7305795820267917 ) ) ;
#2600=CARTESIAN_POINT ( 'NONE',  ( 759.9864689768902508, -362.0891481129648923, 354.9819416627836404 ) ) ;
#2603=CARTESIAN_POINT ( 'NONE',  ( 764.8639956371174549, -416.0891481129645513, 319.7806653035542013 ) ) ;
#2604=ORIENTED_EDGE ( 'NONE', *, *, #1301, .F. ) ;
#2607=CARTESIAN_POINT ( 'NONE',  ( 791.9812246680005501, -188.6346026584199365, 361.9419747391813189 ) ) ;
#2608=CARTESIAN_POINT ( 'NONE',  ( 785.3141322388236176, -189.7255117493290300, 364.4286716492789537 ) ) ;
#2613=CARTESIAN_POINT ( 'NONE',  ( 804.4286716492782716, -377.3618753856920875, 345.3141322388244703 ) ) ;
#2618=CARTESIAN_POINT ( 'NONE',  ( 787.5162901302840055, -107.3618753856928976, 305.4481719005793252 ) ) ;
#2625=CARTESIAN_POINT ( 'NONE',  ( 756.1348686366196716, -209.2601417444142839, 347.5531968255698416 ) ) ;
#2626=CARTESIAN_POINT ( 'NONE',  ( 809.8718804791541288, -453.2309196406925480, 337.2303869152726179 ) ) ;
#2627=DIRECTION ( 'NONE',  ( -1.000000000000000000, -0.000000000000000000, -0.000000000000000000 ) ) ;
#2628=DIRECTION ( 'NONE',  ( -1.000000000000000000, -0.000000000000000000, 0.000000000000000000 ) ) ;
#2636=EDGE_LOOP ( 'NONE', ( #16416, #40742 ) ) ;
#2638=CARTESIAN_POINT ( 'NONE',  ( 786.2694204179717872, -117.2817908451530684, 305.1769319972829067 ) ) ;
#2646=EDGE_CURVE ( 'NONE', #19936, #44204, #25430, .T. ) ;
#2647=CARTESIAN_POINT ( 'NONE',  ( 790.0220218866281812, -439.0999726633339719, 363.2186876482849129 ) ) ;
#2648=CARTESIAN_POINT ( 'NONE',  ( 779.9999999999992042, 166.4563064324884465, 339.9999999999999432 ) ) ;
#2654=CARTESIAN_POINT ( 'NONE',  ( 793.5525998758768083, -223.0999726633346256, 372.6845335610516941 ) ) ;
#2656=CARTESIAN_POINT ( 'NONE',  ( 745.4481719005789273, -195.7255117493289731, 347.5162901302853129 ) ) ;
#2660=CARTESIAN_POINT ( 'NONE',  ( 788.7366044899766848, -275.9073299311469896, 316.5762568750059813 ) ) ;
#2661=CARTESIAN_POINT ( 'NONE',  ( 793.9708237608222134, -70.91815448151683654, 319.2295555964448681 ) ) ;
#2667=CARTESIAN_POINT ( 'NONE',  ( 798.7617431975189675, -99.62377810805098477, 323.0428371773161871 ) ) ;
#2668=CARTESIAN_POINT ( 'NONE',  ( 759.9864689768902508, -338.0891481129649492, 354.9819416627836404 ) ) ;
#2673=CARTESIAN_POINT ( 'NONE',  ( 804.9363028652555840, -64.27096629478397460, 338.2165204200192079 ) ) ;
#2676=CARTESIAN_POINT ( 'NONE',  ( 766.5853460496234675, -373.9874144716864066, 372.3518521366060554 ) ) ;
#2678=CARTESIAN_POINT ( 'NONE',  ( 781.8018195045266339, -286.2709662947833635, 365.1927285166406705 ) ) ;
#2679=CARTESIAN_POINT ( 'NONE',  ( 808.0189434323515343, 9.910851887033969021, 319.0252816721025511 ) ) ;
#2682=CARTESIAN_POINT ( 'NONE',  ( 755.0636971347428243, -364.2709662947830793, 341.7834795799807353 ) ) ;
#2688=EDGE_CURVE ( 'NONE', #33757, #23899, #35833, .T. ) ;
#2689=CARTESIAN_POINT ( 'NONE',  ( 788.7366044899766848, -107.9073299311474727, 316.5762568750059813 ) ) ;
#2690=CARTESIAN_POINT ( 'NONE',  ( 761.4292242960306112, -401.4636090269704027, 323.2154366446414429 ) ) ;
#2692=CARTESIAN_POINT ( 'NONE',  ( 814.9108240113580450, -448.2709662947827951, 337.5031285880265273 ) ) ;
#2694=CARTESIAN_POINT ( 'NONE',  ( 752.4576283171824116, -357.0783235625956422, 317.7880784355627952 ) ) ;
#2699=CARTESIAN_POINT ( 'NONE',  ( 760.0363995740630116, -10.91815448151704793, 368.7758568127991907 ) ) ;
#2709=CARTESIAN_POINT ( 'NONE',  ( 805.2837595273609850, -338.7363362996978822, 340.5290396650784714 ) ) ;
#2711=CARTESIAN_POINT ( 'NONE',  ( 804.1009440267234822, -311.4636090269706870, 314.0944755984392600 ) ) ;
#2714=CARTESIAN_POINT ( 'NONE',  ( 805.6418435158337843, -125.4636090269712412, 363.8556311672236916 ) ) ;
#2719=CARTESIAN_POINT ( 'NONE',  ( 759.9864689768902508, -146.0891481129655176, 354.9819416627836404 ) ) ;
#2721=CARTESIAN_POINT ( 'NONE',  ( 805.6418435158337843, -413.4636090269704027, 363.8556311672236916 ) ) ;
#2724=CARTESIAN_POINT ( 'NONE',  ( 760.7433823573367135, -60.00906357242598688, 355.9930595647440441 ) ) ;
#2727=CARTESIAN_POINT ( 'NONE',  ( 756.1348686366196716, -425.2601417444136018, 347.5531968255698416 ) ) ;
#2729=CARTESIAN_POINT ( 'NONE',  ( 755.3201227861273992, -267.7255117493286320, 345.3687786644892981 ) ) ;
#2730=AXIS2_PLACEMENT_3D ( 'NONE', #3897, #25127, #45243 ) ;
#2734=CARTESIAN_POINT ( 'NONE',  ( 800.1688906516307043, -274.1692326535049915, 369.0717654672308186 ) ) ;
#2735=CARTESIAN_POINT ( 'NONE',  ( 797.6776695296629214, -91.54369356751116982, 357.6776695296636603 ) ) ;
#2738=CARTESIAN_POINT ( 'NONE',  ( 774.6312213355099630, -263.3618753856924855, 364.6798772138717482 ) ) ;
#2740=CARTESIAN_POINT ( 'NONE',  ( 790.0208454995162128, -448.6851210678752864, 365.6426314972804903 ) ) ;
#2746=CARTESIAN_POINT ( 'NONE',  ( 759.0252816721024374, -360.9982390220557704, 368.0189434323527280 ) ) ;
#2747=CARTESIAN_POINT ( 'NONE',  ( 791.1614460488616487, -251.2601417444141134, 373.5763878283158874 ) ) ;
#2751=CARTESIAN_POINT ( 'NONE',  ( 788.8264449731200330, -237.1800572038742985, 363.6646147819171233 ) ) ;
#2754=CARTESIAN_POINT ( 'NONE',  ( 744.7301800767019131, -364.8164208402374697, 337.4774526936615757 ) ) ;
#2757=CARTESIAN_POINT ( 'NONE',  ( 783.6926022324497580, 16.45630643248849267, 313.7971720364932935 ) ) ;
#2760=CARTESIAN_POINT ( 'NONE',  ( 773.4516893846965786, -211.6454272087891582, 315.8398074228977066 ) ) ;
#2761=CARTESIAN_POINT ( 'NONE',  ( 801.9419747391806368, -114.4527844766020053, 351.9812246680014027 ) ) ;
#2765=CARTESIAN_POINT ( 'NONE',  ( 779.4709603349208464, -264.3510508353232353, 314.7162404726379918 ) ) ;
#2769=CARTESIAN_POINT ( 'NONE',  ( 810.7187646348534145, -450.4527844766009821, 356.7737145352016341 ) ) ;
#2772=CARTESIAN_POINT ( 'NONE',  ( 751.6929314249748586, -78.99823902205662307, 318.8095938919659034 ) ) ;
#2773=CARTESIAN_POINT ( 'NONE',  ( 813.1304606946830518, -185.9073299311472454, 352.3570229623690580 ) ) ;
#2777=CARTESIAN_POINT ( 'NONE',  ( 810.4231160770870019, -408.5545181178794110, 321.9338519418446936 ) ) ;
#2780=CARTESIAN_POINT ( 'NONE',  ( 767.6429770376289525, -393.1800572038737300, 306.8695393053162093 ) ) ;
#2781=CARTESIAN_POINT ( 'NONE',  ( 814.5518280994195948, -15.72551174932958951, 332.4837098697145166 ) ) ;
#2783=CARTESIAN_POINT ( 'NONE',  ( 805.1016975059191054, -30.89650538077846065, 343.0745993439771837 ) ) ;
#2786=CARTESIAN_POINT ( 'NONE',  ( 747.3154664389472828, -163.9874144716871456, 326.4474001241230781 ) ) ;
#2787=CARTESIAN_POINT ( 'NONE',  ( 803.4237431249931660, 8.819942796124882634, 331.2633955100225194 ) ) ;
#2788=CARTESIAN_POINT ( 'NONE',  ( 758.0141637701419768, -183.0783235625961538, 367.2620300519063790 ) ) ;
#2792=CARTESIAN_POINT ( 'NONE',  ( 778.2165204200184689, -166.8164208402382087, 364.9363028652563230 ) ) ;
#2794=CARTESIAN_POINT ( 'NONE',  ( 762.3223304703356007, -295.5436935675105588, 322.3223304703362828 ) ) ;
#2795=CARTESIAN_POINT ( 'NONE',  ( 756.5762568750052424, -291.1800572038741848, 348.7366044899774238 ) ) ;
#2798=CARTESIAN_POINT ( 'NONE',  ( 770.0799878456142551, -13.98741447168760033, 362.9823548866085616 ) ) ;
#2801=CARTESIAN_POINT ( 'NONE',  ( 796.9462024416508257, -252.4527844766015789, 308.9653473494370246 ) ) ;
#2802=CARTESIAN_POINT ( 'NONE',  ( 763.0428371773158460, -323.4636090269706301, 358.7617431975195359 ) ) ;
#2803=CARTESIAN_POINT ( 'NONE',  ( 772.3691319403857278, -431.2601417444136018, 315.8894580844506663 ) ) ;
#2809=CARTESIAN_POINT ( 'NONE',  ( 800.7704444035546203, -316.1692326535048210, 326.0291762391768771 ) ) ;
#2812=CARTESIAN_POINT ( 'NONE',  ( 758.4439275373578084, -132.5545181178802920, 353.2243759319684386 ) ) ;
#2813=CARTESIAN_POINT ( 'NONE',  ( 803.6646147819161570, 6.092670068852159559, 348.8264449731210561 ) ) ;
#2816=CARTESIAN_POINT ( 'NONE',  ( 755.1538015810308480, -230.1908817542436338, 343.0433043558613804 ) ) ;
#2817=CARTESIAN_POINT ( 'NONE',  ( 802.2119215644370342, -222.0090635724254184, 367.5423716828165084 ) ) ;
#2819=DIRECTION ( 'NONE',  ( 0.000000000000000000, 0.000000000000000000, -1.000000000000000000 ) ) ;
#2821=CARTESIAN_POINT ( 'NONE',  ( 744.7301800767019131, -52.81642084023856398, 337.4774526936615757 ) ) ;
#2825=CARTESIAN_POINT ( 'NONE',  ( 807.2620300519052989, -312.0090635724251911, 318.0141637701419768 ) ) ;
#2827=CARTESIAN_POINT ( 'NONE',  ( 815.2698199232961542, -304.8164208402376403, 342.5225473063383106 ) ) ;
#2831=CARTESIAN_POINT ( 'NONE',  ( 774.6312213355099630, -383.3618753856921444, 364.6798772138717482 ) ) ;
#2832=CARTESIAN_POINT ( 'NONE',  ( 754.7162404726377645, -158.7363362996984222, 339.4709603349214717 ) ) ;
#2835=CARTESIAN_POINT ( 'NONE',  ( 773.7943932421234194, -71.80559628986922860, 305.5313806188329409 ) ) ;
#2836=CARTESIAN_POINT ( 'NONE',  ( 797.8594530101009923, -373.5436935675102177, 322.1405469898982119 ) ) ;
#2838=DIRECTION ( 'NONE',  ( 0.000000000000000000, 0.000000000000000000, 1.000000000000000000 ) ) ;
#2839=CARTESIAN_POINT ( 'NONE',  ( 802.1676090361156639, -422.6346026584192259, 327.8955696845344505 ) ) ;
#2843=CARTESIAN_POINT ( 'NONE',  ( 804.4286716492782716, -209.3618753856926276, 345.3141322388244703 ) ) ;
#2844=CARTESIAN_POINT ( 'NONE',  ( 804.9363028652555840, -184.2709662947835909, 338.2165204200192079 ) ) ;
#2848=CARTESIAN_POINT ( 'NONE',  ( 802.1676090361156639, -398.6346026584193396, 327.8955696845344505 ) ) ;
#2852=CARTESIAN_POINT ( 'NONE',  ( 777.4774526936600978, -130.2709662947837614, 304.7301800767028226 ) ) ;
#2859=CARTESIAN_POINT ( 'NONE',  ( 800.7704444035546203, -196.1692326535052473, 326.0291762391768771 ) ) ;
#2869=CARTESIAN_POINT ( 'NONE',  ( 755.8990559732751535, -107.4636090269713122, 365.9055244015606831 ) ) ;
#2877=CARTESIAN_POINT ( 'NONE',  ( 776.9254006560222479, -428.1908817542430938, 314.8983024940802125 ) ) ;
#2884=CARTESIAN_POINT ( 'NONE',  ( 781.2370466360911223, -212.7363362996982232, 304.9990715423533629 ) ) ;
#2886=CARTESIAN_POINT ( 'NONE',  ( 792.2312462859673587, -203.9073299311471885, 307.2067596250082602 ) ) ;
#2889=CARTESIAN_POINT ( 'NONE',  ( 804.4286716492782716, -281.3618753856923718, 345.3141322388244703 ) ) ;
#2890=CARTESIAN_POINT ( 'NONE',  ( 804.1105419155481968, -75.82724539060775726, 347.6308680596136469 ) ) ;
#2895=CARTESIAN_POINT ( 'NONE',  ( 787.6308680596127942, -131.2601417444144829, 364.1105419155492768 ) ) ;
#2896=CARTESIAN_POINT ( 'NONE',  ( 756.3353852180819104, -341.9073299311465917, 331.1735550268788302 ) ) ;
#2900=CARTESIAN_POINT ( 'NONE',  ( 764.8639956371174549, -80.08914811296574499, 319.7806653035542013 ) ) ;
#2903=CARTESIAN_POINT ( 'NONE',  ( 801.9858362298568863, -363.0783235625955854, 312.7379699480935642 ) ) ;
#2905=CARTESIAN_POINT ( 'NONE',  ( 803.4237431249931660, -279.1800572038741848, 331.2633955100225194 ) ) ;
#2908=CARTESIAN_POINT ( 'NONE',  ( 765.0180583372156207, -408.9982390220556567, 360.0135310231089534 ) ) ;
#2915=CARTESIAN_POINT ( 'NONE',  ( 800.2193346964447755, -138.9982390220563957, 355.1360043628815788 ) ) ;
#2916=CARTESIAN_POINT ( 'NONE',  ( 780.5236548040995785, -404.7363362996975980, 314.9735926884559944 ) ) ;
#2917=CARTESIAN_POINT ( 'NONE',  ( 783.0433043558608688, -96.89650538077825104, 315.1538015810313027 ) ) ;
#2920=CARTESIAN_POINT ( 'NONE',  ( 758.0141637701419768, -351.0783235625955854, 367.2620300519063790 ) ) ;
#2921=CARTESIAN_POINT ( 'NONE',  ( 783.7566961878529810, -120.8965053807781800, 305.1792804349288417 ) ) ;
#2926=CARTESIAN_POINT ( 'NONE',  ( 799.9636004259356241, 1.081845518482914104, 311.2241431872006956 ) ) ;
#2934=CARTESIAN_POINT ( 'NONE',  ( 766.0291762391763086, -346.9181544815160123, 360.7704444035551319 ) ) ;
#2935=CARTESIAN_POINT ( 'NONE',  ( 747.6481478633932056, -301.0999726633342561, 353.4146539503763620 ) ) ;
#2938=CARTESIAN_POINT ( 'NONE',  ( 791.0478386215596629, -93.82724539060770041, 306.7653713866226326 ) ) ;
#2942=CARTESIAN_POINT ( 'NONE',  ( 755.3201227861273992, -195.7255117493289731, 345.3687786644892981 ) ) ;
#2944=CARTESIAN_POINT ( 'NONE',  ( 749.5768839229115201, -420.5545181178793541, 358.0661480581553064 ) ) ;
#2948=CARTESIAN_POINT ( 'NONE',  ( 798.5707757039680246, -53.46360902697146855, 356.7845633553585003 ) ) ;
#2951=CARTESIAN_POINT ( 'NONE',  ( 801.3366627262608972, -440.5328690171407970, 353.0897708529566899 ) ) ;
#2956=CARTESIAN_POINT ( 'NONE',  ( 795.6651683502461765, -274.7146871989594388, 371.3240766477733814 ) ) ;
#2957=CARTESIAN_POINT ( 'NONE',  ( 768.0187753319979720, -128.6346026584201354, 318.0580252608186242 ) ) ;
#2959=CARTESIAN_POINT ( 'NONE',  ( 762.3223304703356007, -271.5436935675106156, 322.3223304703362828 ) ) ;
#2962=DIRECTION ( 'NONE',  ( 0.000000000000000000, 1.000000000000000000, 0.000000000000000000 ) ) ;
#2967=CARTESIAN_POINT ( 'NONE',  ( 804.6798772138708955, -39.72551174932951312, 334.6312213355107019 ) ) ;
#2969=CARTESIAN_POINT ( 'NONE',  ( 796.9462024416508257, -372.4527844766012095, 308.9653473494370246 ) ) ;
#2970=CARTESIAN_POINT ( 'NONE',  ( 764.3348316497523456, -262.7146871989594956, 308.6759233522265617 ) ) ;
#2976=CARTESIAN_POINT ( 'NONE',  ( 788.7366044899766848, -251.9073299311470748, 316.5762568750059813 ) ) ;
#2978=CARTESIAN_POINT ( 'NONE',  ( 745.4481719005789273, -363.7255117493284047, 347.5162901302853129 ) ) ;
#2984=CARTESIAN_POINT ( 'NONE',  ( 755.3028492785439312, -231.2817908451527558, 335.9200461376539693 ) ) ;
#2985=CARTESIAN_POINT ( 'NONE',  ( 803.4237431249931660, -111.1800572038747532, 331.2633955100225194 ) ) ;
#2989=CARTESIAN_POINT ( 'NONE',  ( 756.1348686366196716, -281.2601417444139997, 347.5531968255698416 ) ) ;
#2992=CARTESIAN_POINT ( 'NONE',  ( 813.1304606946830518, -449.9073299311463643, 352.3570229623690580 ) ) ;
#2994=CARTESIAN_POINT ( 'NONE',  ( 744.7301800767019131, -172.8164208402381234, 337.4774526936615757 ) ) ;
#2995=CARTESIAN_POINT ( 'NONE',  ( 758.0580252608178853, -78.45278447660211896, 328.0187753319985404 ) ) ;
#2999=EDGE_CURVE ( 'NONE', #14626, #24474, #40884, .T. ) ;
#3000=CARTESIAN_POINT ( 'NONE',  ( 799.9636004259356241, -430.9181544815157849, 311.2241431872006956 ) ) ;
#3003=CARTESIAN_POINT ( 'NONE',  ( 787.4397851343537695, -405.7255117493283478, 374.2001403089903988 ) ) ;
#3004=CARTESIAN_POINT ( 'NONE',  ( 748.9653473494365699, -26.63460265842046226, 356.9462024416520762 ) ) ;
#3008=CARTESIAN_POINT ( 'NONE',  ( 787.6308680596127942, -35.26014174441480264, 364.1105419155492768 ) ) ;
#3011=CARTESIAN_POINT ( 'NONE',  ( 761.9338519418445230, -158.5328690171417065, 370.4231160770881957 ) ) ;
#3012=CARTESIAN_POINT ( 'NONE',  ( 762.1405469898973024, -25.54369356751137232, 357.8594530101016176 ) ) ;
#3013=CARTESIAN_POINT ( 'NONE',  ( 815.0009284576459549, -174.3510508353234627, 338.7629533639073429 ) ) ;
#3018=CARTESIAN_POINT ( 'NONE',  ( 774.6858677611749044, -177.7255117493290868, 315.5713283507209894 ) ) ;
#3020=CARTESIAN_POINT ( 'NONE',  ( 797.8594530101009923, -301.5436935675105588, 322.1405469898982119 ) ) ;
#3023=CARTESIAN_POINT ( 'NONE',  ( 798.7617431975189675, -27.62377810805120149, 323.0428371773161871 ) ) ;
#3025=CARTESIAN_POINT ( 'NONE',  ( 748.9653473494365699, -242.6346026584197659, 356.9462024416520762 ) ) ;
#3026=CARTESIAN_POINT ( 'NONE',  ( 786.5483106153019435, -319.6454272087888739, 364.1601925771022366 ) ) ;
#3027=CARTESIAN_POINT ( 'NONE',  ( 793.4146539503750546, 22.01258552831228599, 307.6481478633938877 ) ) ;
#3031=CARTESIAN_POINT ( 'NONE',  ( 761.2382568024794409, -351.6237781080502032, 356.9571628226838129 ) ) ;
#3033=CARTESIAN_POINT ( 'NONE',  ( 763.8424801807145741, -138.0090635724257311, 320.5453621957614700 ) ) ;
#3034=CARTESIAN_POINT ( 'NONE',  ( 785.3141322388236176, 2.274488250670355871, 364.4286716492789537 ) ) ;
#3038=CARTESIAN_POINT ( 'NONE',  ( 768.9521613784389729, -249.8272453906072315, 373.2346286133773106 ) ) ;
#3039=CARTESIAN_POINT ( 'NONE',  ( 755.8398074228967971, -187.4419599262325278, 333.4516893846970333 ) ) ;
#3043=CARTESIAN_POINT ( 'NONE',  ( 813.1304606946830518, -65.90732993114758642, 352.3570229623690580 ) ) ;
#3047=CARTESIAN_POINT ( 'NONE',  ( 762.1177392798416577, -354.5545181178796383, 309.8865473780659272 ) ) ;
#3049=CARTESIAN_POINT ( 'NONE',  ( 787.4397851343537695, -309.7255117493287457, 374.2001403089903988 ) ) ;
#3053=CARTESIAN_POINT ( 'NONE',  ( 758.0580252608178853, -390.4527844766011526, 328.0187753319985404 ) ) ;
#3055=CARTESIAN_POINT ( 'NONE',  ( 790.9844846989617508, -142.3726999360620766, 317.2208543904092721 ) ) ;
#3058=CARTESIAN_POINT ( 'NONE',  ( 807.5423716828161105, -57.07832356259658013, 362.2119215644372048 ) ) ;
#3059=CARTESIAN_POINT ( 'NONE',  ( 805.1927285166399315, -376.8164208402375834, 341.8018195045277707 ) ) ;
#3060=CARTESIAN_POINT ( 'NONE',  ( 772.5602148656447525, 14.27448825067031812, 305.7998596910095443 ) ) ;
#3062=CARTESIAN_POINT ( 'NONE',  ( 762.1405469898971887, -433.5436935675099903, 357.8594530101015607 ) ) ;
#3065=CARTESIAN_POINT ( 'NONE',  ( 803.6646147819161570, -185.9073299311472454, 348.8264449731210561 ) ) ;
#3066=CARTESIAN_POINT ( 'NONE',  ( 757.8323909638828582, -194.6346026584199080, 352.1044303154654358 ) ) ;
#3070=CARTESIAN_POINT ( 'NONE',  ( 791.9812246680005501, -380.6346026584192828, 361.9419747391813189 ) ) ;
#3071=ORIENTED_EDGE ( 'NONE', *, *, #44258, .T. ) ;
#3073=CARTESIAN_POINT ( 'NONE',  ( 772.5602148656447525, -153.7255117493291721, 305.7998596910095443 ) ) ;
#3075=CARTESIAN_POINT ( 'NONE',  ( 744.8212110874229666, -186.8965053807779668, 336.2046728542121627 ) ) ;
#3080=CARTESIAN_POINT ( 'NONE',  ( 790.8726784830453198, -202.7146871989597514, 362.5472867521010585 ) ) ;
#3090=CARTESIAN_POINT ( 'NONE',  ( 814.4686193811664907, -123.2817908451530542, 346.2056067578752732 ) ) ;
#3101=CARTESIAN_POINT ( 'NONE',  ( 778.1981804954714335, 13.72903370521577138, 314.8072714833589885 ) ) ;
#3103=CARTESIAN_POINT ( 'NONE',  ( 804.1009440267234822, -215.4636090269709712, 314.0944755984392600 ) ) ;
#3105=CARTESIAN_POINT ( 'NONE',  ( 808.0189434323515343, -206.0891481129653471, 319.0252816721025511 ) ) ;
#3108=CARTESIAN_POINT ( 'NONE',  ( 759.7806653035534055, -294.9982390220560546, 324.8639956371180801 ) ) ;
#3110=CARTESIAN_POINT ( 'NONE',  ( 804.1105419155481968, -51.82724539060782121, 347.6308680596136469 ) ) ;
#3114=CARTESIAN_POINT ( 'NONE',  ( 755.8398074228967971, -115.4419599262327409, 333.4516893846970333 ) ) ;
#3115=CARTESIAN_POINT ( 'NONE',  ( 781.7834795799800531, -322.8164208402377540, 315.0636971347436202 ) ) ;
#3118=CARTESIAN_POINT ( 'NONE',  ( 757.8323909638827445, -98.63460265842024910, 352.1044303154654358 ) ) ;
#3122=CARTESIAN_POINT ( 'NONE',  ( 759.8311093483677041, -406.1692326535045368, 310.9282345327691814 ) ) ;
#3123=VERTEX_POINT ( 'NONE', #20992 ) ;
#3124=CARTESIAN_POINT ( 'NONE',  ( 754.8072714833581358, -292.8164208402376971, 338.1981804954720587 ) ) ;
#3128=CARTESIAN_POINT ( 'NONE',  ( 800.2193346964447755, -402.9982390220555430, 355.1360043628815788 ) ) ;
#3135=CARTESIAN_POINT ( 'NONE',  ( 754.8072714833581358, -124.8164208402383508, 338.1981804954720587 ) ) ;
#3136=CARTESIAN_POINT ( 'NONE',  ( 798.5707757039680246, -437.4636090269703459, 356.7845633553585003 ) ) ;
#3139=CARTESIAN_POINT ( 'NONE',  ( 813.2346286133761168, -341.2601417444138292, 328.9521613784389160 ) ) ;
#3145=CARTESIAN_POINT ( 'NONE',  ( 799.9636004259356241, -46.91815448151694312, 311.2241431872006956 ) ) ;
#3153=CARTESIAN_POINT ( 'NONE',  ( 786.5483106153019435, -367.6454272087886466, 364.1601925771022366 ) ) ;
#3154=CARTESIAN_POINT ( 'NONE',  ( 809.0717654672305343, -316.9181544815160692, 360.1688906516309885 ) ) ;
#3156=EDGE_CURVE ( 'NONE', #29447, #23565, #7737, .T. ) ;
#3158=CARTESIAN_POINT ( 'NONE',  ( 795.8262568251477660, -118.3726999360621619, 308.3538107759623585 ) ) ;
#3160=EDGE_CURVE ( 'NONE', #24078, #3360, #45503, .T. ) ;
#3163=CARTESIAN_POINT ( 'NONE',  ( 797.8594530101008786, -181.5436935675108145, 322.1405469898980982 ) ) ;
#3165=CARTESIAN_POINT ( 'NONE',  ( 813.5763878283155464, -435.8272453906066062, 351.1614460488615350 ) ) ;
#3170=CARTESIAN_POINT ( 'NONE',  ( 773.7943932421234194, 0.1944037101305369775, 305.5313806188329409 ) ) ;
#3172=VECTOR ( 'NONE', #39419, 1000.000000000000000 ) ;
#3175=CARTESIAN_POINT ( 'NONE',  ( 810.1134526219336749, -320.5328690171411949, 357.8822607201570349 ) ) ;
#3176=CARTESIAN_POINT ( 'NONE',  ( 800.2193346964446619, -114.9982390220565378, 355.1360043628816925 ) ) ;
#3179=CARTESIAN_POINT ( 'NONE',  ( 759.7806653035534055, -294.9982390220560546, 324.8639956371180801 ) ) ;
#3188=CARTESIAN_POINT ( 'NONE',  ( 801.9419747391806368, -18.45278447660230725, 351.9812246680014027 ) ) ;
#3190=CARTESIAN_POINT ( 'NONE',  ( 814.5518280994195948, -375.7255117493284047, 332.4837098697145166 ) ) ;
#3191=CARTESIAN_POINT ( 'NONE',  ( 778.7502325331095108, -264.3510508353232353, 304.6391490659818828 ) ) ;
#3196=CARTESIAN_POINT ( 'NONE',  ( 804.4286716492782716, -257.3618753856924286, 345.3141322388244703 ) ) ;
#3197=CARTESIAN_POINT ( 'NONE',  ( 751.9810565676468741, -386.0891481129647786, 360.9747183278973921 ) ) ;
#3200=FACE_BOUND ( 'NONE', #2636, .T. ) ;
#3203=CARTESIAN_POINT ( 'NONE',  ( 763.0428371773158460, -227.4636090269709143, 358.7617431975195359 ) ) ;
#3204=CARTESIAN_POINT ( 'NONE',  ( 804.6798772138708955, -135.7255117493291152, 334.6312213355107019 ) ) ;
#3209=CARTESIAN_POINT ( 'NONE',  ( 784.0799538623451781, -299.8055962898685038, 364.6971507214555572 ) ) ;
#3211=CARTESIAN_POINT ( 'NONE',  ( 755.8990559732751535, -11.46360902697159290, 365.9055244015606831 ) ) ;
#3214=CARTESIAN_POINT ( 'NONE',  ( 811.0346526505616112, -182.6346026584199649, 323.0537975583477532 ) ) ;
#3215=CARTESIAN_POINT ( 'NONE',  ( 788.8264449731200330, -93.18005720387481006, 363.6646147819171233 ) ) ;
#3216=CARTESIAN_POINT ( 'NONE',  ( 779.9999999999997726, 16.45630643248849267, 339.9999999999994884 ) ) ;
#3220=CARTESIAN_POINT ( 'NONE',  ( 748.6759233522253680, -424.3726999360612808, 324.3348316497537098 ) ) ;
#3223=CARTESIAN_POINT ( 'NONE',  ( 754.9735926884551418, -378.3510508353227806, 340.5236548041000333 ) ) ;
#3224=CARTESIAN_POINT ( 'NONE',  ( 796.9462024416508257, -60.45278447660216159, 308.9653473494370246 ) ) ;
#3226=CARTESIAN_POINT ( 'NONE',  ( 804.9511171171677688, -5.805596289869448867, 335.8780910478229202 ) ) ;
#3231=CARTESIAN_POINT ( 'NONE',  ( 752.4576283171824116, -165.0783235625962391, 317.7880784355627952 ) ) ;
#3232=CARTESIAN_POINT ( 'NONE',  ( 767.8955696845334842, -24.45278447660228949, 362.1676090361161755 ) ) ;
#3233=EDGE_CURVE ( 'NONE', #44752, #8827, #2530, .T. ) ;
#3237=CARTESIAN_POINT ( 'NONE',  ( 788.7366044899766848, -203.9073299311471885, 316.5762568750059813 ) ) ;
#3239=CARTESIAN_POINT ( 'NONE',  ( 755.0636971347428243, -316.2709662947832499, 341.7834795799807353 ) ) ;
#3244=CARTESIAN_POINT ( 'NONE',  ( 755.0488828828309806, -41.80559628986934229, 344.1219089521771934 ) ) ;
#3246=CARTESIAN_POINT ( 'NONE',  ( 767.6429770376291799, -249.1800572038742700, 306.8695393053162093 ) ) ;
#3247=CARTESIAN_POINT ( 'NONE',  ( 758.4439275373578084, -348.5545181178796383, 353.2243759319684386 ) ) ;
#3248=CARTESIAN_POINT ( 'NONE',  ( 754.9735926884551418, -426.3510508353226669, 340.5236548041000333 ) ) ;
#3253=CARTESIAN_POINT ( 'NONE',  ( 767.7687537140311633, -239.9073299311470748, 372.7932403749916830 ) ) ;
#3256=CARTESIAN_POINT ( 'NONE',  ( 800.7704444035546203, -340.1692326535047641, 326.0291762391768771 ) ) ;
#3259=CARTESIAN_POINT ( 'NONE',  ( 802.9823548866075953, -121.0999726633348956, 330.0799878456151077 ) ) ;
#3260=CARTESIAN_POINT ( 'NONE',  ( 800.2193346964447755, -18.99823902205683979, 355.1360043628815788 ) ) ;
#3264=CARTESIAN_POINT ( 'NONE',  ( 748.6759233522253680, -232.3726999360617924, 324.3348316497537098 ) ) ;
#3265=CARTESIAN_POINT ( 'NONE',  ( 796.7845633553578182, -177.6237781080507148, 358.5707757039688204 ) ) ;
#3271=CARTESIAN_POINT ( 'NONE',  ( 800.9747183278959710, -12.99823902205686821, 311.9810565676471583 ) ) ;
#3272=CARTESIAN_POINT ( 'NONE',  ( 800.9747183278959710, -84.99823902205663728, 311.9810565676471583 ) ) ;
#3273=CARTESIAN_POINT ( 'NONE',  ( 802.7276637122909051, -452.9681489794449476, 352.0069550970126784 ) ) ;
#3277=CARTESIAN_POINT ( 'NONE',  ( 766.4474001241216001, -355.0999726633341993, 307.3154664389482491 ) ) ;
#3279=CARTESIAN_POINT ( 'NONE',  ( 812.7932403749906598, -279.1800572038741848, 327.7687537140311633 ) ) ;
#3283=CARTESIAN_POINT ( 'NONE',  ( 785.3141322388236176, -405.7255117493283478, 364.4286716492789537 ) ) ;
#3284=CARTESIAN_POINT ( 'NONE',  ( 804.1105419155481968, -147.8272453906075157, 347.6308680596136469 ) ) ;
#3287=CARTESIAN_POINT ( 'NONE',  ( 810.1134526219336749, -80.53286901714194812, 357.8822607201570349 ) ) ;
#3288=CARTESIAN_POINT ( 'NONE',  ( 803.4237431249931660, -399.1800572038738437, 331.2633955100225194 ) ) ;
#3289=DIRECTION ( 'NONE',  ( 0.000000000000000000, 0.000000000000000000, -1.000000000000000000 ) ) ;
#3291=CARTESIAN_POINT ( 'NONE',  ( 773.7943932421234194, -143.8055962898690154, 305.5313806188329409 ) ) ;
#3292=CARTESIAN_POINT ( 'NONE',  ( 788.8264449731200330, -429.1800572038737869, 363.6646147819171233 ) ) ;
#3297=CARTESIAN_POINT ( 'NONE',  ( 754.8072714833581358, -220.8164208402379529, 338.1981804954720587 ) ) ;
#3298=CARTESIAN_POINT ( 'NONE',  ( 800.0135310231082713, -206.0891481129653471, 325.0180583372163028 ) ) ;
#3303=CARTESIAN_POINT ( 'NONE',  ( 797.6776695296629214, -403.5436935675101608, 357.6776695296636603 ) ) ;
#3307=CARTESIAN_POINT ( 'NONE',  ( 763.0537975583476964, -144.4527844766018632, 371.0346526505628617 ) ) ;
#3309=CARTESIAN_POINT ( 'NONE',  ( 748.3538107759620743, -184.7146871989598083, 355.8262568251490165 ) ) ;
#3317=CARTESIAN_POINT ( 'NONE',  ( 794.1144889064781864, -226.1692326535051052, 360.9840315886528401 ) ) ;
#3319=DIRECTION ( 'NONE',  ( 0.000000000000000000, 0.000000000000000000, -1.000000000000000000 ) ) ;
#3328=CARTESIAN_POINT ( 'NONE',  ( 745.7194118038753459, -133.6454272087893571, 348.7631598425976449 ) ) ;
#3338=CARTESIAN_POINT ( 'NONE',  ( 748.6759233522253680, -376.3726999360614514, 324.3348316497537098 ) ) ;
#3339=DIRECTION ( 'NONE',  ( 0.000000000000000000, 1.000000000000000000, 0.000000000000000000 ) ) ;
#3345=CARTESIAN_POINT ( 'NONE',  ( 752.7379699480933368, -252.0090635724254184, 361.9858362298580232 ) ) ;
#3347=CARTESIAN_POINT ( 'NONE',  ( 792.2312462859673587, -179.9073299311472454, 307.2067596250082602 ) ) ;
#3351=CARTESIAN_POINT ( 'NONE',  ( 794.9819416627830151, -300.9982390220559409, 319.9864689768909898 ) ) ;
#3353=CARTESIAN_POINT ( 'NONE',  ( 802.5472867521000353, -76.37269993606228979, 350.8726784830461156 ) ) ;
#3358=CARTESIAN_POINT ( 'NONE',  ( 755.0488828828309806, -137.8055962898690154, 344.1219089521771934 ) ) ;
#3359=CARTESIAN_POINT ( 'NONE',  ( 757.8323909638827445, -314.6346026584194533, 352.1044303154654358 ) ) ;
#3360=VERTEX_POINT ( 'NONE', #22140 ) ;
#3362=CARTESIAN_POINT ( 'NONE',  ( 755.5713283507202505, -77.36187538569302546, 334.6858677611754729 ) ) ;
#3365=CARTESIAN_POINT ( 'NONE',  ( 761.9338519418445230, -398.5328690171409107, 370.4231160770881957 ) ) ;
#3366=ORIENTED_EDGE ( 'NONE', *, *, #17368, .F. ) ;
#3367=CARTESIAN_POINT ( 'NONE',  ( 768.0187753319979720, -296.6346026584195670, 318.0580252608186242 ) ) ;
#3368=AXIS2_PLACEMENT_3D ( 'NONE', #34752, #23660, #44938 ) ;
#3372=CARTESIAN_POINT ( 'NONE',  ( 805.1927285166397041, -400.8164208402373561, 341.8018195045277707 ) ) ;
#3378=CARTESIAN_POINT ( 'NONE',  ( 757.8323909638827445, -122.6346026584201354, 352.1044303154654358 ) ) ;
#3379=CARTESIAN_POINT ( 'NONE',  ( 776.9254006560222479, -428.1908817542430938, 314.8983024940802125 ) ) ;
#3380=CARTESIAN_POINT ( 'NONE',  ( 793.2243759319678702, -122.5328690171417918, 318.4439275373583200 ) ) ;
#3382=CYLINDRICAL_SURFACE ( 'NONE', #23994, 10.00000000000000888 ) ;
#3383=CARTESIAN_POINT ( 'NONE',  ( 746.0683387631852383, -355.4419599262319593, 331.3260364891676204 ) ) ;
#3390=CARTESIAN_POINT ( 'NONE',  ( 745.7194118038753459, -37.64542720878968396, 348.7631598425976449 ) ) ;
#3396=LINE ( 'NONE', #20922, #2018 ) ;
#3398=CARTESIAN_POINT ( 'NONE',  ( 804.4086373105744769, -361.6454272087887603, 333.3843516231986541 ) ) ;
#3399=CARTESIAN_POINT ( 'NONE',  ( 746.4236121716829757, -327.8272453906069472, 328.8385539511384650 ) ) ;
#3402=CARTESIAN_POINT ( 'NONE',  ( 810.4231160770870019, -144.5545181178802636, 321.9338519418446936 ) ) ;
#3407=CARTESIAN_POINT ( 'NONE',  ( 785.3141322388236176, -189.7255117493290300, 364.4286716492789537 ) ) ;
#3409=CARTESIAN_POINT ( 'NONE',  ( 778.7629533639073998, -416.7363362996975980, 375.0009284576466371 ) ) ;
#3414=CARTESIAN_POINT ( 'NONE',  ( 815.0009284576459549, 17.64894916467593688, 338.7629533639073429 ) ) ;
#3417=CARTESIAN_POINT ( 'NONE',  ( 744.8212110874229666, -306.8965053807775689, 336.2046728542121627 ) ) ;
#3418=CARTESIAN_POINT ( 'NONE',  ( 781.7834795799800531, -106.8164208402383935, 315.0636971347436202 ) ) ;
#3422=CARTESIAN_POINT ( 'NONE',  ( 788.7366044899766848, -299.9073299311468759, 316.5762568750059813 ) ) ;
#3428=CARTESIAN_POINT ( 'NONE',  ( 794.9819416627830151, -12.99823902205686821, 319.9864689768909898 ) ) ;
#3431=CARTESIAN_POINT ( 'NONE',  ( 763.0537975583476964, -360.4527844766011526, 371.0346526505628617 ) ) ;
#3432=CARTESIAN_POINT ( 'NONE',  ( 788.7631598425961101, -241.4419599262322720, 305.7194118038759143 ) ) ;
#3433=CARTESIAN_POINT ( 'NONE',  ( 795.6651683502461765, -58.71468719896019905, 371.3240766477733814 ) ) ;
#3438=CARTESIAN_POINT ( 'NONE',  ( 771.1735550268778070, -249.1800572038742416, 316.3353852180827630 ) ) ;
#3440=CARTESIAN_POINT ( 'NONE',  ( 782.5225473063381969, -382.2709662947828519, 375.2698199232970637 ) ) ;
#3444=DIRECTION ( 'NONE',  ( -1.000000000000000000, -0.000000000000000000, 0.000000000000000000 ) ) ;
#3445=CARTESIAN_POINT ( 'NONE',  ( 798.5707757039680246, -269.4636090269708006, 356.7845633553585003 ) ) ;
#3446=CARTESIAN_POINT ( 'NONE',  ( 755.5713283507202505, -101.3618753856929544, 334.6858677611754729 ) ) ;
#3450=CARTESIAN_POINT ( 'NONE',  ( 770.0799878456142551, -277.9874144716867477, 362.9823548866085616 ) ) ;
#3453=CARTESIAN_POINT ( 'NONE',  ( 781.2370466360911223, 3.263663700301089765, 304.9990715423533629 ) ) ;
#3456=CARTESIAN_POINT ( 'NONE',  ( 748.9653473494363425, -170.6346026584199649, 356.9462024416521331 ) ) ;
#3457=CARTESIAN_POINT ( 'NONE',  ( 803.6646147819161570, -65.90732993114758642, 348.8264449731210561 ) ) ;
#3462=CARTESIAN_POINT ( 'NONE',  ( 745.1792804349281596, -446.1908817542429802, 343.7566961878542884 ) ) ;
#3465=CARTESIAN_POINT ( 'NONE',  ( 799.4546378042377910, -345.0783235625956991, 356.1575198192848006 ) ) ;
#3466=CARTESIAN_POINT ( 'NONE',  ( 808.0189434323515343, -38.08914811296587999, 319.0252816721025511 ) ) ;
#3470=CARTESIAN_POINT ( 'NONE',  ( 805.0264073115434940, -54.35105083532383219, 339.4763451958999099 ) ) ;
#3473=CARTESIAN_POINT ( 'NONE',  ( 791.1614460488616487, -203.2601417444143124, 373.5763878283158874 ) ) ;
#3474=CARTESIAN_POINT ( 'NONE',  ( 804.9363028652555840, -16.27096629478413092, 338.2165204200192079 ) ) ;
#3475=ORIENTED_EDGE ( 'NONE', *, *, #35991, .F. ) ;
#3478=CARTESIAN_POINT ( 'NONE',  ( 755.5713283507202505, -197.3618753856926560, 334.6858677611754729 ) ) ;
#3481=CARTESIAN_POINT ( 'NONE',  ( 774.6312213355098493, -335.3618753856921444, 364.6798772138717482 ) ) ;
#3484=CARTESIAN_POINT ( 'NONE',  ( 798.7617431975189675, -51.62377810805111267, 323.0428371773161871 ) ) ;
#3489=CARTESIAN_POINT ( 'NONE',  ( 772.4837098697145166, -239.3618753856924855, 374.5518280994205611 ) ) ;
#3490=CARTESIAN_POINT ( 'NONE',  ( 763.2154366446407039, -429.6237781080499190, 321.4292242960311228 ) ) ;
#3496=CARTESIAN_POINT ( 'NONE',  ( 745.7998596910086917, -293.3618753856923718, 332.5602148656461168 ) ) ;
#3498=CARTESIAN_POINT ( 'NONE',  ( 755.0488828828309806, -329.8055962898683902, 344.1219089521771934 ) ) ;
#3501=CARTESIAN_POINT ( 'NONE',  ( 804.6971507214547046, -147.2817908451529547, 344.0799538623459739 ) ) ;
#3502=CARTESIAN_POINT ( 'NONE',  ( 767.8955696845333705, -24.45278447660229304, 362.1676090361162323 ) ) ;
#3505=DIRECTION ( 'NONE',  ( -0.000000000000000000, -1.000000000000000000, 0.000000000000000000 ) ) ;
#3507=CARTESIAN_POINT ( 'NONE',  ( 764.1737431748507561, -250.3726999360618208, 371.6461892240376415 ) ) ;
#3508=CARTESIAN_POINT ( 'NONE',  ( 798.7617431975189675, -171.6237781080507432, 323.0428371773161871 ) ) ;
#3513=CARTESIAN_POINT ( 'NONE',  ( 751.6929314249748586, -30.99823902205680071, 318.8095938919659034 ) ) ;
#3514=EDGE_CURVE ( 'NONE', #6763, #11154, #36229, .T. ) ;
#3515=CARTESIAN_POINT ( 'NONE',  ( 799.9999999999993179, 205.0000000000000568, 329.9999999999999432 ) ) ;
#3518=CARTESIAN_POINT ( 'NONE',  ( 815.3608509340175488, -362.7363362996977116, 341.2497674668889545 ) ) ;
#3520=CARTESIAN_POINT ( 'NONE',  ( 796.9462024416508257, -324.4527844766013231, 308.9653473494370246 ) ) ;
#3524=CARTESIAN_POINT ( 'NONE',  ( 757.8323909638827445, -386.6346026584191691, 352.1044303154654358 ) ) ;
#3525=CARTESIAN_POINT ( 'NONE',  ( 769.9779781133707957, -163.0999726633347677, 316.7813123517150871 ) ) ;
#3528=CARTESIAN_POINT ( 'NONE',  ( 754.0944755984390895, -111.6237781080509279, 364.1009440267246760 ) ) ;
#3529=CARTESIAN_POINT ( 'NONE',  ( 756.3353852180820240, -389.9073299311465917, 331.1735550268787733 ) ) ;
#3531=CARTESIAN_POINT ( 'NONE',  ( 804.7487373415286811, 4.456306432488530866, 364.7487373415288516 ) ) ;
#3534=CARTESIAN_POINT ( 'NONE',  ( 758.0141637701419768, -159.0783235625962391, 367.2620300519063790 ) ) ;
#3538=EDGE_CURVE ( 'NONE', #12793, #28817, #21458, .T. ) ;
#3540=CARTESIAN_POINT ( 'NONE',  ( 756.3353852180819104, -221.9073299311470464, 331.1735550268788302 ) ) ;
#3541=CARTESIAN_POINT ( 'NONE',  ( 765.0180583372156207, -216.9982390220562252, 360.0135310231089534 ) ) ;
#3544=CARTESIAN_POINT ( 'NONE',  ( 808.3070685750230950, 5.001760977943074948, 361.1904061080339261 ) ) ;
#3547=CARTESIAN_POINT ( 'NONE',  ( 788.7366044899766848, -443.9073299311464780, 316.5762568750059813 ) ) ;
#3552=CARTESIAN_POINT ( 'NONE',  ( 811.0346526505617248, -158.6346026584200217, 323.0537975583478101 ) ) ;
#3554=CARTESIAN_POINT ( 'NONE',  ( 745.1769319972822814, -185.8055962898689302, 346.2694204179732083 ) ) ;
#3559=CARTESIAN_POINT ( 'NONE',  ( 765.8855110935204493, -214.1692326535052189, 319.0159684113471599 ) ) ;
#3568=CARTESIAN_POINT ( 'NONE',  ( 809.0717654672305343, -148.9181544815166092, 360.1688906516309885 ) ) ;
#3582=CARTESIAN_POINT ( 'NONE',  ( 771.3260364891663130, -259.6454272087890445, 306.0683387631859773 ) ) ;
#3584=CARTESIAN_POINT ( 'NONE',  ( 787.4397851343537695, -213.7255117493289731, 374.2001403089903988 ) ) ;
#3587=CARTESIAN_POINT ( 'NONE',  ( 800.2193346964447755, -306.9982390220558273, 355.1360043628815788 ) ) ;
#3588=CARTESIAN_POINT ( 'NONE',  ( 758.4439275373578084, -84.55451811788046257, 353.2243759319684386 ) ) ;
#3593=CARTESIAN_POINT ( 'NONE',  ( 758.6633372737375112, -140.5328690171417634, 326.9102291470432533 ) ) ;
#3594=CARTESIAN_POINT ( 'NONE',  ( 758.0580252608178853, -366.4527844766012095, 328.0187753319985404 ) ) ;
#3599=CARTESIAN_POINT ( 'NONE',  ( 771.1735550268778070, -105.1800572038747248, 316.3353852180827630 ) ) ;
#3602=CARTESIAN_POINT ( 'NONE',  ( 744.8212110874229666, -402.8965053807773415, 336.2046728542121627 ) ) ;
#3604=CARTESIAN_POINT ( 'NONE',  ( 759.7806653035534055, -318.9982390220557704, 324.8639956371180801 ) ) ;
#3608=CARTESIAN_POINT ( 'NONE',  ( 764.8639956371174549, -416.0891481129645513, 319.7806653035542013 ) ) ;
#3614=CARTESIAN_POINT ( 'NONE',  ( 761.4292242960306112, -449.4636090269702322, 323.2154366446414429 ) ) ;
#3615=CARTESIAN_POINT ( 'NONE',  ( 780.5290396650775619, -108.3510508353236759, 365.2837595273619513 ) ) ;
#3618=CARTESIAN_POINT ( 'NONE',  ( 761.9338519418445230, -374.5328690171410813, 370.4231160770881957 ) ) ;
#3623=CARTESIAN_POINT ( 'NONE',  ( 786.2694204179717872, -21.28179084515337749, 305.1769319972829067 ) ) ;
#3629=CARTESIAN_POINT ( 'NONE',  ( 779.9999999999992042, 126.4563064324884465, 329.9999999999999432 ) ) ;
#3631=CARTESIAN_POINT ( 'NONE',  ( 796.9571628226829034, -359.4636090269705164, 321.2382568024804641 ) ) ;
#3632=CARTESIAN_POINT ( 'NONE',  ( 788.6739635108323228, -343.6454272087887603, 373.9316612368139090 ) ) ;
#3634=CARTESIAN_POINT ( 'NONE',  ( 799.9999999999993179, 205.0000000000000568, 339.9999999999999432 ) ) ;
#3635=DIRECTION ( 'NONE',  ( -0.000000000000000000, 1.000000000000000000, -0.000000000000000000 ) ) ;
#3637=CARTESIAN_POINT ( 'NONE',  ( 805.6418435158337843, -149.4636090269711417, 363.8556311672236916 ) ) ;
#3639=CARTESIAN_POINT ( 'NONE',  ( 747.2067596250078623, -75.18005720387485269, 352.2312462859687230 ) ) ;
#3643=CARTESIAN_POINT ( 'NONE',  ( 758.0580252608178853, -174.4527844766018063, 328.0187753319985404 ) ) ;
#3644=CARTESIAN_POINT ( 'NONE',  ( 814.8207195650702488, -458.1908817542429802, 336.2433038121456548 ) ) ;
#3649=CARTESIAN_POINT ( 'NONE',  ( 810.1134526219336749, 15.46713098285775878, 357.8822607201570349 ) ) ;
#3653=CARTESIAN_POINT ( 'NONE',  ( 814.8230680027162407, -317.8055962898684470, 333.7305795820267917 ) ) ;
#3654=CARTESIAN_POINT ( 'NONE',  ( 803.4237431249931660, -111.1800572038747532, 331.2633955100225194 ) ) ;
#3656=CARTESIAN_POINT ( 'NONE',  ( 756.5762568750052424, -315.1800572038740711, 348.7366044899774238 ) ) ;
#3658=CARTESIAN_POINT ( 'NONE',  ( 814.2001403089898304, -89.36187538569299704, 347.4397851343538264 ) ) ;
#3664=CARTESIAN_POINT ( 'NONE',  ( 791.9812246680005501, -20.63460265842048003, 361.9419747391813189 ) ) ;
#3666=CARTESIAN_POINT ( 'NONE',  ( 747.2067596250078623, -363.1800572038739006, 352.2312462859687230 ) ) ;
#3667=CARTESIAN_POINT ( 'NONE',  ( 776.2433038121456548, -300.8965053807775689, 374.8207195650711014 ) ) ;
#3668=CARTESIAN_POINT ( 'NONE',  ( 807.5423716828161105, -57.07832356259658013, 362.2119215644372048 ) ) ;
#3673=CARTESIAN_POINT ( 'NONE',  ( 804.6798772138708955, -255.7255117493287742, 334.6312213355107019 ) ) ;
#3674=CARTESIAN_POINT ( 'NONE',  ( 767.7687537140311633, -383.9073299311466485, 372.7932403749916830 ) ) ;
#3680=CARTESIAN_POINT ( 'NONE',  ( 760.7433823573367135, -252.0090635724254184, 355.9930595647440441 ) ) ;
#3681=CARTESIAN_POINT ( 'NONE',  ( 800.2193346964447755, -114.9982390220565236, 355.1360043628815788 ) ) ;
#3685=CARTESIAN_POINT ( 'NONE',  ( 766.7756240680305382, -278.5328690171412518, 361.5560724626415663 ) ) ;
#3687=CARTESIAN_POINT ( 'NONE',  ( 745.1792804349281596, -38.19088175424422360, 343.7566961878542884 ) ) ;
#3689=CARTESIAN_POINT ( 'NONE',  ( 814.2001403089898304, -161.3618753856927697, 347.4397851343538264 ) ) ;
#3690=CARTESIAN_POINT ( 'NONE',  ( 805.1927285166397041, -64.81642084023852135, 341.8018195045277707 ) ) ;
#3693=CARTESIAN_POINT ( 'NONE',  ( 761.4292242960306112, 6.536390973028352924, 323.2154366446414429 ) ) ;
#3696=CARTESIAN_POINT ( 'NONE',  ( 758.6633372737375112, -356.5328690171410813, 326.9102291470432533 ) ) ;
#3697=CARTESIAN_POINT ( 'NONE',  ( 745.4481719005789273, -51.72551174932947049, 347.5162901302853697 ) ) ;
#3699=CARTESIAN_POINT ( 'NONE',  ( 789.9200121543843807, -49.98741447168749374, 317.0176451133914384 ) ) ;
#3702=CARTESIAN_POINT ( 'NONE',  ( 773.7943932421234194, -191.8055962898689017, 305.5313806188329409 ) ) ;
#3703=CARTESIAN_POINT ( 'NONE',  ( 762.3223304703356007, -31.54369356751135456, 322.3223304703362828 ) ) ;
#3704=CARTESIAN_POINT ( 'NONE',  ( 787.6308680596127942, -371.2601417444136587, 364.1105419155492768 ) ) ;
#3707=CARTESIAN_POINT ( 'NONE',  ( 804.4286716492782716, -209.3618753856926276, 345.3141322388244703 ) ) ;
#3709=CARTESIAN_POINT ( 'NONE',  ( 792.1044303154646968, -324.4527844766013231, 317.8323909638837677 ) ) ;
#3712=CARTESIAN_POINT ( 'NONE',  ( 756.7813123517142913, -43.98741447168752217, 329.9779781133712504 ) ) ;
#3714=CARTESIAN_POINT ( 'NONE',  ( 777.5031285880264704, -262.8164208402379245, 374.9108240113588408 ) ) ;
#3715=CARTESIAN_POINT ( 'NONE',  ( 752.4576283171824116, 2.921676437403253779, 317.7880784355627952 ) ) ;
#3720=CARTESIAN_POINT ( 'NONE',  ( 805.0032342141412300, -277.5436935675105019, 314.9967657858571783 ) ) ;
#3722=CARTESIAN_POINT ( 'NONE',  ( 799.4546378042377910, -345.0783235625956991, 356.1575198192848006 ) ) ;
#3724=CARTESIAN_POINT ( 'NONE',  ( 761.4292242960306112, -161.4636090269711133, 323.2154366446414429 ) ) ;
#3725=CARTESIAN_POINT ( 'NONE',  ( 803.4237431249931660, -15.18005720387504631, 331.2633955100225194 ) ) ;
#3729=CARTESIAN_POINT ( 'NONE',  ( 813.5763878283155464, -219.8272453906073167, 351.1614460488615350 ) ) ;
#3730=CARTESIAN_POINT ( 'NONE',  ( 775.9200461376533440, -191.8055962898689017, 315.3028492785443291 ) ) ;
#3732=CARTESIAN_POINT ( 'NONE',  ( 791.9460785601769430, -462.7578698805381237, 362.0383033825738721 ) ) ;
#3735=CARTESIAN_POINT ( 'NONE',  ( 763.0537975583475827, -0.4527844766023628176, 371.0346526505627480 ) ) ;
#3736=CARTESIAN_POINT ( 'NONE',  ( 759.0252816721024374, -72.99823902205667991, 368.0189434323527280 ) ) ;
#3740=CARTESIAN_POINT ( 'NONE',  ( 813.5763878283155464, -339.8272453906069472, 351.1614460488615350 ) ) ;
#3742=CARTESIAN_POINT ( 'NONE',  ( 813.1304606946830518, -329.9073299311467053, 352.3570229623690580 ) ) ;
#3744=ADVANCED_FACE ( 'NONE', ( #37655, #9262 ), #2308, .F. ) ;
#3746=CARTESIAN_POINT ( 'NONE',  ( 799.9999999999993179, -512.9681489794448908, 339.9999999999999432 ) ) ;
#3747=CARTESIAN_POINT ( 'NONE',  ( 795.1360043628807261, -428.0891481129644944, 360.2193346964456282 ) ) ;
#3748=CARTESIAN_POINT ( 'NONE',  ( 763.0428371773158460, -203.4636090269709996, 358.7617431975195359 ) ) ;
#3751=CARTESIAN_POINT ( 'NONE',  ( 752.4576283171824116, -117.0783235625963528, 317.7880784355627952 ) ) ;
#3752=CARTESIAN_POINT ( 'NONE',  ( 792.1044303154646968, -396.4527844766010958, 317.8323909638837677 ) ) ;
#3757=CARTESIAN_POINT ( 'NONE',  ( 791.9812246680005501, -236.6346026584198228, 361.9419747391813189 ) ) ;
#3758=CARTESIAN_POINT ( 'NONE',  ( 805.1927285166399315, -208.8164208402380666, 341.8018195045277707 ) ) ;
#3762=CARTESIAN_POINT ( 'NONE',  ( 803.4237431249931660, -423.1800572038737300, 331.2633955100225194 ) ) ;
#3766=CARTESIAN_POINT ( 'NONE',  ( 796.7737145352015204, -164.6346026584200217, 370.7187646348536987 ) ) ;
#3767=CARTESIAN_POINT ( 'NONE',  ( 769.0155153010367712, -274.3726999360617356, 362.7791456095907279 ) ) ;
#3773=CARTESIAN_POINT ( 'NONE',  ( 802.7791456095903868, -220.7146871989596661, 329.0155153010375102 ) ) ;
#3782=CARTESIAN_POINT ( 'NONE',  ( 783.7953271457878373, -152.1908817542438612, 375.1787889125761239 ) ) ;
#3786=( BOUNDED_CURVE ( )  B_SPLINE_CURVE ( 2, ( #44669, #39067, #37967, #22, #482, #14343, #21489, #23851, #23626, #7414, #2626, #16725, #13029 ),
 .UNSPECIFIED., .F., .T. ) 
 B_SPLINE_CURVE_WITH_KNOTS ( ( 3, 2, 2, 2, 2, 2, 3 ),
 ( 0.000000000000000000, 0.0008527428137030668154, 0.003125470086430381933, 0.005398197359157586028, 0.007670924631884902013, 0.009943651904612216264, 0.01049328897333767253 ),
 .UNSPECIFIED. ) 
 CURVE ( )  GEOMETRIC_REPRESENTATION_ITEM ( )  RATIONAL_B_SPLINE_CURVE ( ( 0.4976140944542620792, 0.4980906878130254567, 0.5000002209606652093, 0.4949109396520706139, 0.5000002209606652093, 0.4949109396520706139, 0.5000002209606652093, 0.4949109396520706139, 0.5000002209606652093, 0.4949109396520706139, 0.5000002209606652093, 0.4987694275901001228, 0.4981339451206906466 ) ) 
 REPRESENTATION_ITEM ( '' )  );
#3790=CARTESIAN_POINT ( 'NONE',  ( 760.0363995740630116, -370.9181544815159555, 368.7758568127991907 ) ) ;
#3794=CARTESIAN_POINT ( 'NONE',  ( 791.9812246680005501, -20.63460265842048003, 361.9419747391813189 ) ) ;
#3795=CARTESIAN_POINT ( 'NONE',  ( 815.3608509340175488, -266.7363362996981095, 341.2497674668889545 ) ) ;
#3797=CARTESIAN_POINT ( 'NONE',  ( 808.0189434323515343, -230.0891481129652618, 319.0252816721025511 ) ) ;
#3801=CARTESIAN_POINT ( 'NONE',  ( 803.6646147819161570, -329.9073299311467053, 348.8264449731210561 ) ) ;
#3802=CARTESIAN_POINT ( 'NONE',  ( 805.2837595273609850, -98.73633629969859271, 340.5290396650784714 ) ) ;
#3803=CARTESIAN_POINT ( 'NONE',  ( 763.8424801807145741, -66.00906357242595845, 320.5453621957614700 ) ) ;
#3807=CARTESIAN_POINT ( 'NONE',  ( 756.1348686366196716, -113.2601417444145682, 347.5531968255698416 ) ) ;
#3808=CARTESIAN_POINT ( 'NONE',  ( 785.3141322388236176, -357.7255117493285184, 364.4286716492789537 ) ) ;
#3811=CARTESIAN_POINT ( 'NONE',  ( 785.3687786644884454, -107.3618753856928976, 315.3201227861279676 ) ) ;
#3814=CARTESIAN_POINT ( 'NONE',  ( 746.0683387631852383, -427.4419599262317888, 331.3260364891676204 ) ) ;
#3817=CARTESIAN_POINT ( 'NONE',  ( 756.3353852180819104, -317.9073299311468190, 331.1735550268788302 ) ) ;
#3822=CARTESIAN_POINT ( 'NONE',  ( 802.1676090361156639, -398.6346026584193396, 327.8955696845344505 ) ) ;
#3829=CARTESIAN_POINT ( 'NONE',  ( 801.9419747391806368, -114.4527844766020053, 351.9812246680014027 ) ) ;
#3830=CARTESIAN_POINT ( 'NONE',  ( 755.5913626894240451, -445.6454272087883055, 346.6156483768012890 ) ) ;
#3831=CARTESIAN_POINT ( 'NONE',  ( 780.5290396650775619, -132.3510508353235764, 365.2837595273619513 ) ) ;
#3834=CARTESIAN_POINT ( 'NONE',  ( 783.7566961878529810, -408.8965053807772847, 305.1792804349288417 ) ) ;
#3839=CARTESIAN_POINT ( 'NONE',  ( 791.0478386215596629, -45.82724539060783542, 306.7653713866226326 ) ) ;
#3848=CARTESIAN_POINT ( 'NONE',  ( 755.5913626894240451, -349.6454272087887603, 346.6156483768012890 ) ) ;
#3849=EDGE_CURVE ( 'NONE', #20161, #21828, #36164, .T. ) ;
#3850=CARTESIAN_POINT ( 'NONE',  ( 747.6481478633932056, -349.0999726633342561, 353.4146539503763620 ) ) ;
#3854=CARTESIAN_POINT ( 'NONE',  ( 744.6391490659812007, -134.7363362996984790, 338.7502325331110455 ) ) ;
#3856=CARTESIAN_POINT ( 'NONE',  ( 746.8695393053150156, -125.9073299311474159, 327.6429770376306010 ) ) ;
#3861=CARTESIAN_POINT ( 'NONE',  ( 800.2193346964447755, -186.9982390220563104, 355.1360043628815788 ) ) ;
#3863=CARTESIAN_POINT ( 'NONE',  ( 763.8424801807145741, 5.990936427573807954, 320.5453621957614700 ) ) ;
#3867=CARTESIAN_POINT ( 'NONE',  ( 791.1614460488616487, -11.26014174441488258, 373.5763878283158874 ) ) ;
#3868=ORIENTED_EDGE ( 'NONE', *, *, #1507, .F. ) ;
#3871=CARTESIAN_POINT ( 'NONE',  ( 803.8556311672234642, -321.6237781080502600, 365.6418435158340117 ) ) ;
#3872=CARTESIAN_POINT ( 'NONE',  ( 804.4286716492782716, -137.3618753856928265, 345.3141322388244703 ) ) ;
#3874=CARTESIAN_POINT ( 'NONE',  ( 762.3223304703356007, -319.5436935675104451, 322.3223304703362828 ) ) ;
#3877=CARTESIAN_POINT ( 'NONE',  ( 748.9653473494365699, -74.63460265842030594, 356.9462024416520762 ) ) ;
#3878=ORIENTED_EDGE ( 'NONE', *, *, #26405, .T. ) ;
#3880=ORIENTED_EDGE ( 'NONE', *, *, #12353, .F. ) ;
#3882=CARTESIAN_POINT ( 'NONE',  ( 788.7366044899766848, -35.90732993114770011, 316.5762568750059813 ) ) ;
#3884=CARTESIAN_POINT ( 'NONE',  ( 767.6429770376291799, -393.1800572038737869, 306.8695393053162093 ) ) ;
#3885=CARTESIAN_POINT ( 'NONE',  ( 795.6651683502461765, -274.7146871989594388, 371.3240766477733814 ) ) ;
#3886=CARTESIAN_POINT ( 'NONE',  ( 811.6461892240364477, -76.71468719896012090, 324.1737431748509835 ) ) ;
#3893=CARTESIAN_POINT ( 'NONE',  ( 787.4397851343537695, -405.7255117493283478, 374.2001403089903988 ) ) ;
#3895=CARTESIAN_POINT ( 'NONE',  ( 799.9999999999993179, 205.0000000000000568, 350.0000000000000000 ) ) ;
#3897=CARTESIAN_POINT ( 'NONE',  ( 799.9999999999993179, -512.9681489794448908, 339.9999999999999432 ) ) ;
#3899=CARTESIAN_POINT ( 'NONE',  ( 766.0291762391763086, -250.9181544815163534, 360.7704444035551319 ) ) ;
#3900=CARTESIAN_POINT ( 'NONE',  ( 781.8018195045266339, -166.2709662947835909, 365.1927285166406705 ) ) ;
#3904=CARTESIAN_POINT ( 'NONE',  ( 759.2295555964440155, -328.1692326535048210, 353.9708237608231229 ) ) ;
#3906=CARTESIAN_POINT ( 'NONE',  ( 754.3581564841646241, -41.46360902697149697, 316.1443688327762516 ) ) ;
#3908=CARTESIAN_POINT ( 'NONE',  ( 787.4397851343537695, -213.7255117493289731, 374.2001403089903988 ) ) ;
#3909=CARTESIAN_POINT ( 'NONE',  ( 791.9812246680005501, -68.63460265842033436, 361.9419747391813189 ) ) ;
#3914=CARTESIAN_POINT ( 'NONE',  ( 812.3518521366052028, -457.0999726633339151, 326.5853460496235243 ) ) ;
#3916=CARTESIAN_POINT ( 'NONE',  ( 786.6156483768007774, -361.4419599262319593, 315.5913626894246136 ) ) ;
#3917=CARTESIAN_POINT ( 'NONE',  ( 782.4968714119720516, -58.81642084023854267, 305.0891759886411023 ) ) ;
#3919=CARTESIAN_POINT ( 'NONE',  ( 763.2154366446407039, -69.62377810805107003, 321.4292242960311228 ) ) ;
#3922=CARTESIAN_POINT ( 'NONE',  ( 801.9858362298568863, -219.0783235625960401, 312.7379699480935642 ) ) ;
#3923=CARTESIAN_POINT ( 'NONE',  ( 771.1735550268780344, -33.18005720387498769, 316.3353852180828198 ) ) ;
#3926=CARTESIAN_POINT ( 'NONE',  ( 774.6312213355099630, -215.3618753856925423, 364.6798772138717482 ) ) ;
#3928=CARTESIAN_POINT ( 'NONE',  ( 771.2633955100217236, -335.9073299311468190, 363.4237431249939618 ) ) ;
#3930=CARTESIAN_POINT ( 'NONE',  ( 758.7867965644026071, 16.45630643248849267, 318.7867965644036303 ) ) ;
#3932=CARTESIAN_POINT ( 'NONE',  ( 787.6308680596127942, -59.26014174441473870, 364.1105419155492768 ) ) ;
#3934=CARTESIAN_POINT ( 'NONE',  ( 782.4968714119720516, -298.8164208402377540, 305.0891759886411023 ) ) ;
#3935=CARTESIAN_POINT ( 'NONE',  ( 751.2241431872005251, 7.830767346494148740, 359.9636004259367610 ) ) ;
#3942=CARTESIAN_POINT ( 'NONE',  ( 751.9810565676468741, -290.0891481129650629, 360.9747183278973921 ) ) ;
#3944=CARTESIAN_POINT ( 'NONE',  ( 794.1144889064781864, -346.1692326535047641, 360.9840315886528401 ) ) ;
#3946=CARTESIAN_POINT ( 'NONE',  ( 779.4763451958990572, -152.7363362996983938, 365.0264073115438919 ) ) ;
#3947=CARTESIAN_POINT ( 'NONE',  ( 754.8072714833581358, -28.81642084023863148, 338.1981804954720587 ) ) ;
#3953=CARTESIAN_POINT ( 'NONE',  ( 771.3260364891663130, -283.6454272087889308, 306.0683387631859773 ) ) ;
#3954=CARTESIAN_POINT ( 'NONE',  ( 776.9566956441375396, -204.8965053807779100, 364.8461984189686405 ) ) ;
#3956=CARTESIAN_POINT ( 'NONE',  ( 762.3223304703356007, 16.45630643248849267, 322.3223304703362828 ) ) ;
#3959=CARTESIAN_POINT ( 'NONE',  ( 772.4837098697144029, 0.6381246143067236254, 374.5518280994205611 ) ) ;
#3960=CARTESIAN_POINT ( 'NONE',  ( 814.5518280994195948, -87.72551174932937101, 332.4837098697145734 ) ) ;
#3961=DIRECTION ( 'NONE',  ( 1.000000000000000000, -0.000000000000000000, -0.000000000000000000 ) ) ;
#3963=LINE ( 'NONE', #21507, #30562 ) ;
#3964=CARTESIAN_POINT ( 'NONE',  ( 757.7880784355613741, -354.0090635724250774, 312.4576283171834916 ) ) ;
#3966=CARTESIAN_POINT ( 'NONE',  ( 745.0891759886404770, -316.2709662947832499, 342.4968714119734159 ) ) ;
#3970=CARTESIAN_POINT ( 'NONE',  ( 756.3353852180819104, -437.9073299311463074, 331.1735550268788302 ) ) ;
#3972=CARTESIAN_POINT ( 'NONE',  ( 786.5483106153019435, -199.6454272087891582, 364.1601925771022366 ) ) ;
#3975=CARTESIAN_POINT ( 'NONE',  ( 813.9316612368132837, -103.4419599262327836, 348.6739635108323228 ) ) ;
#3976=CARTESIAN_POINT ( 'NONE',  ( 794.9819416627830151, -420.9982390220555999, 319.9864689768909898 ) ) ;
#3981=CARTESIAN_POINT ( 'NONE',  ( 755.5713283507202505, -245.3618753856925139, 334.6858677611754729 ) ) ;
#3982=CARTESIAN_POINT ( 'NONE',  ( 765.0180583372156207, -240.9982390220561683, 360.0135310231089534 ) ) ;
#3986=CARTESIAN_POINT ( 'NONE',  ( 794.9819416627830151, -420.9982390220555999, 319.9864689768909898 ) ) ;
#3990=CARTESIAN_POINT ( 'NONE',  ( 755.2512626584698410, -151.5436935675109851, 315.2512626584710915 ) ) ;
#3991=CARTESIAN_POINT ( 'NONE',  ( 760.7433823573367135, -252.0090635724254184, 355.9930595647440441 ) ) ;
#3998=CARTESIAN_POINT ( 'NONE',  ( 754.9735926884551418, -234.3510508353232638, 340.5236548041000333 ) ) ;
#4010=CARTESIAN_POINT ( 'NONE',  ( 745.1792804349281596, -182.1908817542437760, 343.7566961878542884 ) ) ;
#4015=CARTESIAN_POINT ( 'NONE',  ( 776.2046728542105711, -380.1908817542431507, 304.8212110874238761 ) ) ;
#4020=CARTESIAN_POINT ( 'NONE',  ( 804.6798772138708955, -15.72551174932958951, 334.6312213355107019 ) ) ;
#4021=CARTESIAN_POINT ( 'NONE',  ( 744.6391490659812007, -254.7363362996981095, 338.7502325331110455 ) ) ;
#4023=CARTESIAN_POINT ( 'NONE',  ( 801.1904061080336987, -236.0891481129651766, 368.3070685750235498 ) ) ;
#4028=CARTESIAN_POINT ( 'NONE',  ( 762.1405469898971887, -313.5436935675102745, 357.8594530101015607 ) ) ;
#4030=CARTESIAN_POINT ( 'NONE',  ( 783.0745993439762742, -104.1908817542440175, 365.1016975059196739 ) ) ;
#4031=CARTESIAN_POINT ( 'NONE',  ( 784.1219089521767955, -69.28179084515321051, 315.0488828828318333 ) ) ;
#4035=CARTESIAN_POINT ( 'NONE',  ( 765.8855110935204493, -166.1692326535053041, 319.0159684113471599 ) ) ;
#4036=CARTESIAN_POINT ( 'NONE',  ( 788.8264449731200330, -357.1800572038739006, 363.6646147819171233 ) ) ;
#4040=CARTESIAN_POINT ( 'NONE',  ( 800.2193346964447755, -114.9982390220565236, 355.1360043628815788 ) ) ;
#4044=CARTESIAN_POINT ( 'NONE',  ( 773.7943932421234194, -407.8055962898681628, 305.5313806188329409 ) ) ;
#4045=ORIENTED_EDGE ( 'NONE', *, *, #41678, .F. ) ;
#4046=CARTESIAN_POINT ( 'NONE',  ( 788.8264449731200330, -309.1800572038740711, 363.6646147819171233 ) ) ;
#4051=CARTESIAN_POINT ( 'NONE',  ( 758.0580252608178853, -438.4527844766009821, 328.0187753319985404 ) ) ;
#4056=ORIENTED_EDGE ( 'NONE', *, *, #11433, .F. ) ;
#4059=CARTESIAN_POINT ( 'NONE',  ( 805.1927285166397041, 7.183579159761247723, 341.8018195045277707 ) ) ;
#4060=CARTESIAN_POINT ( 'NONE',  ( 761.2382568024794409, -111.6237781080509279, 356.9571628226838129 ) ) ;
#4063=CARTESIAN_POINT ( 'NONE',  ( 781.2497674668890113, -396.3510508353228374, 375.3608509340180603 ) ) ;
#4065=AXIS2_PLACEMENT_3D ( 'NONE', #36577, #1457, #36799 ) ;
#4071=CARTESIAN_POINT ( 'NONE',  ( 778.7629533639073998, -32.73633629969879877, 375.0009284576466371 ) ) ;
#4077=CARTESIAN_POINT ( 'NONE',  ( 791.7608162188021197, 205.0000000000000568, 319.9999999999999432 ) ) ;
#4079=CARTESIAN_POINT ( 'NONE',  ( 784.1219089521767955, -357.2817908451523294, 315.0488828828318333 ) ) ;
#4081=CARTESIAN_POINT ( 'NONE',  ( 813.5763878283155464, -339.8272453906069472, 351.1614460488615350 ) ) ;
#4088=CARTESIAN_POINT ( 'NONE',  ( 802.2119215644370342, -150.0090635724257027, 367.5423716828165084 ) ) ;
#4091=CARTESIAN_POINT ( 'NONE',  ( 763.2262854647970016, -104.6346026584202207, 309.2812353651462445 ) ) ;
#4095=CARTESIAN_POINT ( 'NONE',  ( 762.1405469898971887, -217.5436935675107293, 357.8594530101015607 ) ) ;
#4097=CARTESIAN_POINT ( 'NONE',  ( 811.3240766477731540, -460.3726999360611103, 355.6651683502462902 ) ) ;
#4102=CARTESIAN_POINT ( 'NONE',  ( 749.8865473780648472, 3.467130982857797417, 322.1177392798429082 ) ) ;
#4105=CARTESIAN_POINT ( 'NONE',  ( 805.1927285166397041, -16.81642084023866701, 341.8018195045277707 ) ) ;
#4108=CARTESIAN_POINT ( 'NONE',  ( 811.6461892240364477, -316.7146871989593819, 324.1737431748509835 ) ) ;
#4109=CARTESIAN_POINT ( 'NONE',  ( 795.1360043628808398, -164.0891481129654892, 360.2193346964456282 ) ) ;
#4113=CARTESIAN_POINT ( 'NONE',  ( 802.1676090361156639, -302.6346026584196238, 327.8955696845344505 ) ) ;
#4116=CARTESIAN_POINT ( 'NONE',  ( 808.0189434323515343, -86.08914811296573077, 319.0252816721025511 ) ) ;
#4122=CARTESIAN_POINT ( 'NONE',  ( 771.2633955100217236, -71.90732993114760063, 363.4237431249939618 ) ) ;
#4123=CARTESIAN_POINT ( 'NONE',  ( 780.5236548040995785, -332.7363362996979390, 314.9735926884559944 ) ) ;
#4126=CARTESIAN_POINT ( 'NONE',  ( 758.8095938919644823, -392.0891481129647786, 311.6929314249762797 ) ) ;
#4127=CARTESIAN_POINT ( 'NONE',  ( 815.1787889125755555, -270.8965053807777394, 343.7953271457877804 ) ) ;
#4129=CARTESIAN_POINT ( 'NONE',  ( 759.8311093483677041, -70.16923265350563099, 310.9282345327691814 ) ) ;
#4135=CARTESIAN_POINT ( 'NONE',  ( 814.5518280994195948, -399.7255117493283478, 332.4837098697145734 ) ) ;
#4137=CARTESIAN_POINT ( 'NONE',  ( 779.9999999999990905, 18.49609980828599376, 309.9999999999999432 ) ) ;
#4141=DIRECTION ( 'NONE',  ( -1.000000000000000000, -0.000000000000000000, 0.000000000000000000 ) ) ;
#4142=CARTESIAN_POINT ( 'NONE',  ( 755.8894580844503253, -255.8272453906072315, 332.3691319403863531 ) ) ;
#4143=CARTESIAN_POINT ( 'NONE',  ( 765.0180583372156207, -144.9982390220564525, 360.0135310231089534 ) ) ;
#4147=CARTESIAN_POINT ( 'NONE',  ( 794.1144889064781864, -322.1692326535048210, 360.9840315886528401 ) ) ;
#4149=CARTESIAN_POINT ( 'NONE',  ( 797.8822607201568644, -54.55451811788054783, 370.1134526219340160 ) ) ;
#4152=CARTESIAN_POINT ( 'NONE',  ( 805.0032342141412300, -205.5436935675108430, 314.9967657858571783 ) ) ;
#4153=CARTESIAN_POINT ( 'NONE',  ( 788.8264449731200330, -117.1800572038746964, 363.6646147819171233 ) ) ;
#4157=CARTESIAN_POINT ( 'NONE',  ( 795.8262568251477660, -454.3726999360611103, 308.3538107759623585 ) ) ;
#4160=CARTESIAN_POINT ( 'NONE',  ( 802.7791456095903868, -364.7146871989592114, 329.0155153010375102 ) ) ;
#4162=CARTESIAN_POINT ( 'NONE',  ( 812.7932403749906598, -39.18005720387496638, 327.7687537140311633 ) ) ;
#4164=CARTESIAN_POINT ( 'NONE',  ( 766.7756240680305382, -38.53286901714206891, 361.5560724626415663 ) ) ;
#4166=CARTESIAN_POINT ( 'NONE',  ( 759.8311093483677041, -190.1692326535052189, 310.9282345327691814 ) ) ;
#4167=CARTESIAN_POINT ( 'NONE',  ( 797.6776695296629214, -43.54369356751131903, 357.6776695296636603 ) ) ;
#4172=CARTESIAN_POINT ( 'NONE',  ( 774.6312213355099630, -191.3618753856925991, 364.6798772138717482 ) ) ;
#4175=CARTESIAN_POINT ( 'NONE',  ( 800.0135310231082713, -326.0891481129649492, 325.0180583372163028 ) ) ;
#4179=CARTESIAN_POINT ( 'NONE',  ( 761.2382568024794409, -63.62377810805107714, 356.9571628226838129 ) ) ;
#4181=CARTESIAN_POINT ( 'NONE',  ( 814.9108240113580450, -280.2709662947833067, 337.5031285880265273 ) ) ;
#4182=CARTESIAN_POINT ( 'NONE',  ( 801.9858362298568863, -3.078323562596726681, 312.7379699480935642 ) ) ;
#4188=CARTESIAN_POINT ( 'NONE',  ( 811.0346526505616112, -302.6346026584196238, 323.0537975583477532 ) ) ;
#4190=CARTESIAN_POINT ( 'NONE',  ( 787.5531968255692163, -213.8272453906073167, 316.1348686366205811 ) ) ;
#4193=CARTESIAN_POINT ( 'NONE',  ( 796.9571628226829034, -167.4636090269711133, 321.2382568024804641 ) ) ;
#4194=CARTESIAN_POINT ( 'NONE',  ( 774.6858677611749044, -33.72551174932952733, 315.5713283507209894 ) ) ;
#4199=CARTESIAN_POINT ( 'NONE',  ( 745.5313806188320314, -255.2817908451526705, 333.7943932421247268 ) ) ;
#4200=CARTESIAN_POINT ( 'NONE',  ( 757.2208543904082489, -208.7146871989596946, 350.9844846989624330 ) ) ;
#4203=CARTESIAN_POINT ( 'NONE',  ( 778.1981804954714335, 13.72903370521577138, 314.8072714833589885 ) ) ;
#4206=CARTESIAN_POINT ( 'NONE',  ( 747.2067596250078623, -3.180057203875080063, 352.2312462859687230 ) ) ;
#4207=CARTESIAN_POINT ( 'NONE',  ( 758.8095938919642549, -104.0891481129656881, 311.6929314249763365 ) ) ;
#4210=DIRECTION ( 'NONE',  ( 0.000000000000000000, 1.000000000000000000, 0.000000000000000000 ) ) ;
#4211=CARTESIAN_POINT ( 'NONE',  ( 799.9636004259356241, -382.9181544815159555, 311.2241431872006956 ) ) ;
#4213=CARTESIAN_POINT ( 'NONE',  ( 745.7998596910086917, -317.3618753856922581, 332.5602148656461168 ) ) ;
#4217=CARTESIAN_POINT ( 'NONE',  ( 788.7366044899766848, -443.9073299311464780, 316.5762568750059813 ) ) ;
#4218=CARTESIAN_POINT ( 'NONE',  ( 755.8894580844503253, -183.8272453906074020, 332.3691319403863531 ) ) ;
#4221=CARTESIAN_POINT ( 'NONE',  ( 771.2368401574024119, -109.4419599262327836, 374.2805881961240857 ) ) ;
#4222=CARTESIAN_POINT ( 'NONE',  ( 755.5713283507202505, -413.3618753856920307, 334.6858677611754729 ) ) ;
#4230=CARTESIAN_POINT ( 'NONE',  ( 804.6798772138708955, -231.7255117493288310, 334.6312213355107019 ) ) ;
#4231=CARTESIAN_POINT ( 'NONE',  ( 803.4237431249931660, -231.1800572038743553, 331.2633955100225194 ) ) ;
#4235=CARTESIAN_POINT ( 'NONE',  ( 754.8072714833581358, -412.8164208402372992, 338.1981804954720587 ) ) ;
#4238=VECTOR ( 'NONE', #23176, 1000.000000000000000 ) ;
#4239=CARTESIAN_POINT ( 'NONE',  ( 763.0537975583476964, -192.4527844766017211, 371.0346526505628617 ) ) ;
#4240=CARTESIAN_POINT ( 'NONE',  ( 769.9779781133707957, -259.0999726633343698, 316.7813123517150871 ) ) ;
#4243=CARTESIAN_POINT ( 'NONE',  ( 808.7758568127978833, -220.1692326535051052, 320.0363995740631822 ) ) ;
#4248=CARTESIAN_POINT ( 'NONE',  ( 801.3366627262608972, -248.5328690171414223, 353.0897708529566899 ) ) ;
#4256=CARTESIAN_POINT ( 'NONE',  ( 771.3260364891663130, -187.6454272087892434, 306.0683387631859773 ) ) ;
#4264=CARTESIAN_POINT ( 'NONE',  ( 797.8594530101008786, -13.54369356751140785, 322.1405469898980982 ) ) ;
#4265=AXIS2_PLACEMENT_3D ( 'NONE', #26627, #44191, #15789 ) ;
#4266=CARTESIAN_POINT ( 'NONE',  ( 815.3608509340175488, -242.7363362996980811, 341.2497674668889545 ) ) ;
#4268=CARTESIAN_POINT ( 'NONE',  ( 810.7187646348534145, -210.4527844766016926, 356.7737145352016341 ) ) ;
#4272=CARTESIAN_POINT ( 'NONE',  ( 755.5713283507202505, -317.3618753856922581, 334.6858677611754729 ) ) ;
#4273=CARTESIAN_POINT ( 'NONE',  ( 755.8894580844503253, -87.82724539060770041, 332.3691319403863531 ) ) ;
#4277=CARTESIAN_POINT ( 'NONE',  ( 765.8855110935204493, -142.1692326535054178, 319.0159684113471599 ) ) ;
#4278=CARTESIAN_POINT ( 'NONE',  ( 778.1981804954714335, -346.2709662947830793, 314.8072714833589885 ) ) ;
#4284=CARTESIAN_POINT ( 'NONE',  ( 813.2346286133761168, -437.2601417444135450, 328.9521613784389160 ) ) ;
#4286=CARTESIAN_POINT ( 'NONE',  ( 804.4286716492782716, -329.3618753856922581, 345.3141322388244703 ) ) ;
#4293=AXIS2_PLACEMENT_3D ( 'NONE', #11828, #43461, #29389 ) ;
#4295=CARTESIAN_POINT ( 'NONE',  ( 800.9840315886518738, -460.9181544815156713, 354.1144889064786412 ) ) ;
#4296=CARTESIAN_POINT ( 'NONE',  ( 765.8855110935204493, -142.1692326535054178, 319.0159684113471599 ) ) ;
#4299=CARTESIAN_POINT ( 'NONE',  ( 761.9338519418445230, -398.5328690171409107, 370.4231160770881957 ) ) ;
#4304=CARTESIAN_POINT ( 'NONE',  ( 788.6739635108323228, -79.64542720878957027, 373.9316612368139090 ) ) ;
#4311=CARTESIAN_POINT ( 'NONE',  ( 787.5531968255692163, -405.8272453906067199, 316.1348686366205811 ) ) ;
#4312=CARTESIAN_POINT ( 'NONE',  ( 764.1737431748507561, -346.3726999360614514, 371.6461892240376415 ) ) ;
#4316=CARTESIAN_POINT ( 'NONE',  ( 783.7953271457878373, -128.1908817542439465, 375.1787889125761239 ) ) ;
#4318=CARTESIAN_POINT ( 'NONE',  ( 747.2067596250078623, -123.1800572038747106, 352.2312462859687230 ) ) ;
#4323=CARTESIAN_POINT ( 'NONE',  ( 759.9864689768902508, -218.0891481129653187, 354.9819416627836404 ) ) ;
#4324=CARTESIAN_POINT ( 'NONE',  ( 754.3581564841646241, -449.4636090269702322, 316.1443688327762516 ) ) ;
#4329=CARTESIAN_POINT ( 'NONE',  ( 768.8385539511368734, -47.26014174441477422, 306.4236121716840557 ) ) ;
#4333=CARTESIAN_POINT ( 'NONE',  ( 804.6798772138708955, -15.72551174932958951, 334.6312213355107019 ) ) ;
#4336=CARTESIAN_POINT ( 'NONE',  ( 748.3538107759620743, -328.7146871989592682, 355.8262568251490165 ) ) ;
#4337=CARTESIAN_POINT ( 'NONE',  ( 762.1405469898973024, -145.5436935675109851, 357.8594530101016176 ) ) ;
#4339=CARTESIAN_POINT ( 'NONE',  ( 785.3141322388236176, -333.7255117493286320, 364.4286716492789537 ) ) ;
#4346=CARTESIAN_POINT ( 'NONE',  ( 755.5713283507202505, -53.36187538569310362, 334.6858677611754729 ) ) ;
#4347=CARTESIAN_POINT ( 'NONE',  ( 798.5707757039680246, -365.4636090269705164, 356.7845633553585003 ) ) ;
#4349=CARTESIAN_POINT ( 'NONE',  ( 792.3570229623691148, -381.1800572038739006, 373.1304606946836770 ) ) ;
#4350=CARTESIAN_POINT ( 'NONE',  ( 744.8212110874229666, -282.8965053807776258, 336.2046728542121627 ) ) ;
#4351=CARTESIAN_POINT ( 'NONE',  ( 747.3154664389472828, -67.98741447168742980, 326.4474001241230781 ) ) ;
#4360=CARTESIAN_POINT ( 'NONE',  ( 777.5031285880264704, -430.8164208402374129, 374.9108240113588408 ) ) ;
#4365=CARTESIAN_POINT ( 'NONE',  ( 801.5560724626406000, -264.5545181178798657, 326.7756240680316182 ) ) ;
#4366=CARTESIAN_POINT ( 'NONE',  ( 804.9363028652555840, -136.2709662947837330, 338.2165204200192079 ) ) ;
#4367=ORIENTED_EDGE ( 'NONE', *, *, #29445, .F. ) ;
#4369=CARTESIAN_POINT ( 'NONE',  ( 803.2186876482843445, -319.9874144716866340, 350.0220218866286928 ) ) ;
#4372=CARTESIAN_POINT ( 'NONE',  ( 788.6739635108323228, -55.64542720878963422, 373.9316612368139090 ) ) ;
#4375=CARTESIAN_POINT ( 'NONE',  ( 759.7806653035534055, -126.9982390220565094, 324.8639956371180801 ) ) ;
#4378=CARTESIAN_POINT ( 'NONE',  ( 776.2046728542105711, -452.1908817542428665, 304.8212110874238761 ) ) ;
#4381=CARTESIAN_POINT ( 'NONE',  ( 802.7791456095903868, -388.7146871989592114, 329.0155153010375102 ) ) ;
#4386=CARTESIAN_POINT ( 'NONE',  ( 770.0799878456142551, -61.98741447168745822, 362.9823548866085616 ) ) ;
#4389=CARTESIAN_POINT ( 'NONE',  ( 752.4576283171824116, -189.0783235625961822, 317.7880784355627952 ) ) ;
#4390=CARTESIAN_POINT ( 'NONE',  ( 801.9419747391806368, -42.45278447660223264, 351.9812246680014027 ) ) ;
#4394=CARTESIAN_POINT ( 'NONE',  ( 758.0580252608178853, -246.4527844766016074, 328.0187753319985404 ) ) ;
#4396=CARTESIAN_POINT ( 'NONE',  ( 792.1044303154646968, -348.4527844766012095, 317.8323909638837677 ) ) ;
#4402=CARTESIAN_POINT ( 'NONE',  ( 796.9462024416508257, -276.4527844766014368, 308.9653473494370246 ) ) ;
#4403=CARTESIAN_POINT ( 'NONE',  ( 808.7758568127978833, -4.169232653505813069, 320.0363995740631822 ) ) ;
#4409=CARTESIAN_POINT ( 'NONE',  ( 808.3070685750230950, -282.9982390220558841, 361.1904061080339261 ) ) ;
#4411=CARTESIAN_POINT ( 'NONE',  ( 769.9779781133707957, -211.0999726633346540, 316.7813123517150871 ) ) ;
#4413=CARTESIAN_POINT ( 'NONE',  ( 755.3028492785439312, -159.2817908451529547, 335.9200461376539693 ) ) ;
#4414=CARTESIAN_POINT ( 'NONE',  ( 762.1405469898971887, -49.54369356751129061, 357.8594530101015607 ) ) ;
#4419=CARTESIAN_POINT ( 'NONE',  ( 786.2694204179717872, -261.2817908451526705, 305.1769319972829067 ) ) ;
#4421=CARTESIAN_POINT ( 'NONE',  ( 793.2243759319678702, -218.5328690171414792, 318.4439275373583200 ) ) ;
#4425=CARTESIAN_POINT ( 'NONE',  ( 804.1105419155481968, -459.8272453906066062, 347.6308680596136469 ) ) ;
#4429=CARTESIAN_POINT ( 'NONE',  ( 815.2698199232961542, -40.81642084023859951, 342.5225473063383106 ) ) ;
#4430=CARTESIAN_POINT ( 'NONE',  ( 792.3570229623688874, -117.1800572038746964, 373.1304606946836202 ) ) ;
#4433=CARTESIAN_POINT ( 'NONE',  ( 744.6391490659812007, -398.7363362996976548, 338.7502325331110455 ) ) ;
#4435=CARTESIAN_POINT ( 'NONE',  ( 763.2262854647970016, -344.6346026584195101, 309.2812353651462445 ) ) ;
#4436=ADVANCED_FACE ( 'NONE', ( #45133 ), #13034, .T. ) ;
#4440=CARTESIAN_POINT ( 'NONE',  ( 785.3687786644884454, -419.3618753856918033, 315.3201227861279676 ) ) ;
#4441=CARTESIAN_POINT ( 'NONE',  ( 796.1575198192839480, -198.0090635724255606, 359.4546378042384163 ) ) ;
#4444=CARTESIAN_POINT ( 'NONE',  ( 783.7566961878529810, -96.89650538077825104, 305.1792804349288417 ) ) ;
#4445=CARTESIAN_POINT ( 'NONE',  ( 801.9419747391806368, -450.4527844766009821, 351.9812246680014027 ) ) ;
#4451=CARTESIAN_POINT ( 'NONE',  ( 764.8639956371174549, -248.0891481129651481, 319.7806653035542013 ) ) ;
#4452=CARTESIAN_POINT ( 'NONE',  ( 792.1044303154646968, -276.4527844766014368, 317.8323909638837677 ) ) ;
#4455=CARTESIAN_POINT ( 'NONE',  ( 805.1927285166397041, -424.8164208402372992, 341.8018195045277707 ) ) ;
#4457=CARTESIAN_POINT ( 'NONE',  ( 749.2812353651451076, -198.4527844766017495, 323.2262854647983090 ) ) ;
#4458=CARTESIAN_POINT ( 'NONE',  ( 799.2566176426618085, -264.0090635724253616, 324.0069404352559559 ) ) ;
#4461=CARTESIAN_POINT ( 'NONE',  ( 795.6651683502461765, -202.7146871989597514, 371.3240766477733814 ) ) ;
#4466=CARTESIAN_POINT ( 'NONE',  ( 799.4546378042377910, -273.0783235625958696, 356.1575198192848006 ) ) ;
#4473=CARTESIAN_POINT ( 'NONE',  ( 752.7379699480933368, -156.0090635724256742, 361.9858362298580232 ) ) ;
#4478=CARTESIAN_POINT ( 'NONE',  ( 745.4481719005789273, -27.72551174932954510, 347.5162901302853129 ) ) ;
#4483=CARTESIAN_POINT ( 'NONE',  ( 804.4286716492782716, -17.36187538569322086, 345.3141322388244703 ) ) ;
#4484=CARTESIAN_POINT ( 'NONE',  ( 788.6739635108323228, -271.6454272087889876, 373.9316612368139090 ) ) ;
#4486=CARTESIAN_POINT ( 'NONE',  ( 745.7998596910086917, -221.3618753856925707, 332.5602148656461168 ) ) ;
#4489=EDGE_LOOP ( 'NONE', ( #21907, #19475, #16357, #6946 ) ) ;
#4490=CARTESIAN_POINT ( 'NONE',  ( 756.3353852180819104, -317.9073299311468190, 331.1735550268788302 ) ) ;
#4491=CARTESIAN_POINT ( 'NONE',  ( 802.9823548866075953, -97.09997266333496668, 330.0799878456151077 ) ) ;
#4495=CARTESIAN_POINT ( 'NONE',  ( 760.5453621957607311, -165.0783235625962391, 323.8424801807151425 ) ) ;
#4496=CARTESIAN_POINT ( 'NONE',  ( 804.4286716492782716, -377.3618753856920875, 345.3141322388244703 ) ) ;
#4499=CARTESIAN_POINT ( 'NONE',  ( 762.3223304703356007, -175.5436935675108998, 322.3223304703362828 ) ) ;
#4502=CARTESIAN_POINT ( 'NONE',  ( 787.5162901302840055, 12.63812461430668321, 305.4481719005792684 ) ) ;
#4504=CARTESIAN_POINT ( 'NONE',  ( 756.5762568750052424, -315.1800572038740711, 348.7366044899774238 ) ) ;
#4512=CARTESIAN_POINT ( 'NONE',  ( 764.8639956371174549, 15.91085188703394238, 319.7806653035542013 ) ) ;
#4513=CARTESIAN_POINT ( 'NONE',  ( 804.7487373415286811, -235.5436935675107293, 364.7487373415288516 ) ) ;
#4514=CARTESIAN_POINT ( 'NONE',  ( 803.2186876482843445, -175.9874144716871172, 350.0220218866286928 ) ) ;
#4517=CARTESIAN_POINT ( 'NONE',  ( 805.9055244015594326, -411.6237781080499758, 315.8990559732753240 ) ) ;
#4522=CARTESIAN_POINT ( 'NONE',  ( 752.7379699480933368, -60.00906357242598688, 361.9858362298580232 ) ) ;
#4530=CARTESIAN_POINT ( 'NONE',  ( 804.6971507214547046, -411.2817908451521589, 344.0799538623459739 ) ) ;
#4534=CARTESIAN_POINT ( 'NONE',  ( 814.2805881961230625, -169.6454272087892718, 331.2368401574024119 ) ) ;
#4536=CARTESIAN_POINT ( 'NONE',  ( 745.4481719005789273, -123.7255117493292147, 347.5162901302853129 ) ) ;
#4540=CARTESIAN_POINT ( 'NONE',  ( 758.0580252608178853, -222.4527844766016642, 328.0187753319985404 ) ) ;
#4541=CARTESIAN_POINT ( 'NONE',  ( 760.0363995740630116, -442.9181544815157849, 368.7758568127991907 ) ) ;
#4545=CARTESIAN_POINT ( 'NONE',  ( 758.0141637701419768, -15.07832356259669560, 367.2620300519063790 ) ) ;
#4548=CARTESIAN_POINT ( 'NONE',  ( 788.8264449731200330, -21.18005720387502677, 363.6646147819171233 ) ) ;
#4552=CARTESIAN_POINT ( 'NONE',  ( 808.7758568127978833, -340.1692326535047641, 320.0363995740631822 ) ) ;
#4553=CARTESIAN_POINT ( 'NONE',  ( 804.9363028652555840, -160.2709662947836762, 338.2165204200192079 ) ) ;
#4556=CARTESIAN_POINT ( 'NONE',  ( 746.7653713866222915, -425.2601417444136018, 351.0478386215610271 ) ) ;
#4558=CARTESIAN_POINT ( 'NONE',  ( 788.7366044899766848, -323.9073299311468190, 316.5762568750059813 ) ) ;
#4564=CARTESIAN_POINT ( 'NONE',  ( 804.6798772138708955, -63.72551174932939233, 334.6312213355107019 ) ) ;
#4565=CARTESIAN_POINT ( 'NONE',  ( 758.4439275373578084, -372.5545181178796383, 353.2243759319684386 ) ) ;
#4567=CARTESIAN_POINT ( 'NONE',  ( 796.7737145352015204, -380.6346026584192828, 370.7187646348536987 ) ) ;
#4568=CARTESIAN_POINT ( 'NONE',  ( 748.3538107759620743, -280.7146871989594956, 355.8262568251490165 ) ) ;
#4575=CARTESIAN_POINT ( 'NONE',  ( 763.0537975583475827, -408.4527844766009252, 371.0346526505627480 ) ) ;
#4582=CARTESIAN_POINT ( 'NONE',  ( 800.9840315886518738, -292.9181544815162397, 354.1144889064786412 ) ) ;
#4583=CARTESIAN_POINT ( 'NONE',  ( 774.6312213355099630, -143.3618753856927697, 364.6798772138717482 ) ) ;
#4586=CARTESIAN_POINT ( 'NONE',  ( 765.8855110935204493, -310.1692326535048778, 319.0159684113471599 ) ) ;
#4588=CARTESIAN_POINT ( 'NONE',  ( 802.2119215644370342, -78.00906357242591582, 367.5423716828165084 ) ) ;
#4590=CARTESIAN_POINT ( 'NONE',  ( 778.2165204200184689, -118.8164208402383508, 364.9363028652563230 ) ) ;
#4592=CARTESIAN_POINT ( 'NONE',  ( 793.0897708529556667, -6.554518117880697048, 361.3366627262616362 ) ) ;
#4595=CARTESIAN_POINT ( 'NONE',  ( 795.9930595647434757, -387.0783235625955285, 320.7433823573372820 ) ) ;
#4601=CARTESIAN_POINT ( 'NONE',  ( 810.1134526219336749, -248.5328690171414223, 357.8822607201570349 ) ) ;
#4602=CARTESIAN_POINT ( 'NONE',  ( 791.9812246680005501, -44.63460265842040542, 361.9419747391813189 ) ) ;
#4604=CARTESIAN_POINT ( 'NONE',  ( 794.9819416627830151, -228.9982390220561683, 319.9864689768909898 ) ) ;
#4609=CARTESIAN_POINT ( 'NONE',  ( 767.6429770376291799, -297.1800572038741279, 306.8695393053162093 ) ) ;
#4611=CARTESIAN_POINT ( 'NONE',  ( 786.2056067578752163, -35.80559628986934229, 374.4686193811670023 ) ) ;
#4618=CARTESIAN_POINT ( 'NONE',  ( 804.7487373415286811, -307.5436935675104451, 364.7487373415288516 ) ) ;
#4620=CARTESIAN_POINT ( 'NONE',  ( 804.1105419155481968, -219.8272453906073167, 347.6308680596136469 ) ) ;
#4621=CARTESIAN_POINT ( 'NONE',  ( 804.1601925771018387, -367.4419599262319025, 346.5483106153029098 ) ) ;
#4625=CARTESIAN_POINT ( 'NONE',  ( 805.2837595273609850, -194.7363362996982517, 340.5290396650784714 ) ) ;
#4626=CARTESIAN_POINT ( 'NONE',  ( 781.7834795799800531, -58.81642084023854267, 315.0636971347436202 ) ) ;
#4631=CARTESIAN_POINT ( 'NONE',  ( 814.2805881961230625, -265.6454272087889876, 331.2368401574024119 ) ) ;
#4632=CARTESIAN_POINT ( 'NONE',  ( 754.8983024940795303, -210.8965053807778816, 336.9254006560228163 ) ) ;
#4635=CARTESIAN_POINT ( 'NONE',  ( 803.4237431249931660, 8.819942796124882634, 331.2633955100225194 ) ) ;
#4638=CARTESIAN_POINT ( 'NONE',  ( 758.8095938919642549, -56.08914811296580893, 311.6929314249763365 ) ) ;
#4639=CARTESIAN_POINT ( 'NONE',  ( 747.2067596250078623, -123.1800572038747106, 352.2312462859687230 ) ) ;
#4640=FACE_OUTER_BOUND ( 'NONE', #16546, .T. ) ;
#4641=CARTESIAN_POINT ( 'NONE',  ( 799.9999999999993179, 205.0000000000000568, 360.0000000000000000 ) ) ;
#4643=CARTESIAN_POINT ( 'NONE',  ( 746.4236121716829757, -399.8272453906067767, 328.8385539511384650 ) ) ;
#4644=CARTESIAN_POINT ( 'NONE',  ( 745.7194118038753459, -397.6454272087885329, 348.7631598425976449 ) ) ;
#4647=CARTESIAN_POINT ( 'NONE',  ( 814.2001403089898304, -377.3618753856920875, 347.4397851343538264 ) ) ;
#4649=CARTESIAN_POINT ( 'NONE',  ( 754.8072714833581358, -412.8164208402372992, 338.1981804954720587 ) ) ;
#4650=CARTESIAN_POINT ( 'NONE',  ( 790.0220218866281812, -175.0999726633346825, 363.2186876482849129 ) ) ;
#4653=CARTESIAN_POINT ( 'NONE',  ( 801.9858362298568863, -147.0783235625962959, 312.7379699480935642 ) ) ;
#4654=CARTESIAN_POINT ( 'NONE',  ( 788.7366044899766848, -443.9073299311464780, 316.5762568750059813 ) ) ;
#4659=CARTESIAN_POINT ( 'NONE',  ( 785.3141322388236176, -261.7255117493288026, 364.4286716492789537 ) ) ;
#4660=CARTESIAN_POINT ( 'NONE',  ( 797.8594530101009923, -253.5436935675105588, 322.1405469898982119 ) ) ;
#4664=CARTESIAN_POINT ( 'NONE',  ( 798.7617431975189675, 20.37622189194865285, 323.0428371773161871 ) ) ;
#4669=CARTESIAN_POINT ( 'NONE',  ( 814.2001403089898304, -185.3618753856926844, 347.4397851343538264 ) ) ;
#4671=CARTESIAN_POINT ( 'NONE',  ( 757.0176451133909268, -277.0999726633344267, 349.9200121543848354 ) ) ;
#4672=ORIENTED_EDGE ( 'NONE', *, *, #59, .T. ) ;
#4674=CARTESIAN_POINT ( 'NONE',  ( 788.7631598425961101, -217.4419599262324141, 305.7194118038759143 ) ) ;
#4680=CARTESIAN_POINT ( 'NONE',  ( 790.8726784830453198, -250.7146871989595809, 362.5472867521010585 ) ) ;
#4688=CARTESIAN_POINT ( 'NONE',  ( 814.4686193811664907, -171.2817908451529263, 346.2056067578752732 ) ) ;
#4691=DIRECTION ( 'NONE',  ( -0.000000000000000000, 1.000000000000000000, -0.000000000000000000 ) ) ;
#4696=CARTESIAN_POINT ( 'NONE',  ( 804.9363028652555840, -40.27096629478405987, 338.2165204200192079 ) ) ;
#4698=CARTESIAN_POINT ( 'NONE',  ( 815.3608509340175488, -290.7363362996980527, 341.2497674668889545 ) ) ;
#4700=CARTESIAN_POINT ( 'NONE',  ( 777.4774526936600978, -274.2709662947833067, 304.7301800767027657 ) ) ;
#4704=CARTESIAN_POINT ( 'NONE',  ( 774.6312213355099630, -335.3618753856920307, 364.6798772138717482 ) ) ;
#4705=CARTESIAN_POINT ( 'NONE',  ( 805.2837595273609850, -74.73633629969866377, 340.5290396650784714 ) ) ;
#4710=CARTESIAN_POINT ( 'NONE',  ( 769.1273215169530886, -142.7146871989599219, 317.4527132478988847 ) ) ;
#4711=CARTESIAN_POINT ( 'NONE',  ( 795.1360043628807261, -380.0891481129646650, 360.2193346964456282 ) ) ;
#4715=CARTESIAN_POINT ( 'NONE',  ( 805.1927285166397041, -160.8164208402382371, 341.8018195045277707 ) ) ;
#4718=CARTESIAN_POINT ( 'NONE',  ( 805.9055244015594326, -435.6237781080499190, 315.8990559732753240 ) ) ;
#4720=CARTESIAN_POINT ( 'NONE',  ( 781.8018195045266339, -358.2709662947829088, 365.1927285166406705 ) ) ;
#4725=CARTESIAN_POINT ( 'NONE',  ( 757.8323909638827445, -434.6346026584190554, 352.1044303154654358 ) ) ;
#4727=EDGE_LOOP ( 'NONE', ( #41516, #15746, #36210, #41308 ) ) ;
#4733=CARTESIAN_POINT ( 'NONE',  ( 759.7806653035534055, -6.998239022056885972, 324.8639956371180801 ) ) ;
#4734=CARTESIAN_POINT ( 'NONE',  ( 779.4709603349208464, -144.3510508353235764, 314.7162404726379918 ) ) ;
#4742=CARTESIAN_POINT ( 'NONE',  ( 807.2620300519052989, -72.00906357242594424, 318.0141637701419768 ) ) ;
#4750=CARTESIAN_POINT ( 'NONE',  ( 801.5560724626406000, -408.5545181178794110, 326.7756240680316182 ) ) ;
#4753=CARTESIAN_POINT ( 'NONE',  ( 763.8424801807145741, -234.0090635724255037, 320.5453621957614700 ) ) ;
#4756=CARTESIAN_POINT ( 'NONE',  ( 812.3518521366052028, -169.0999726633347393, 326.5853460496235243 ) ) ;
#4758=CARTESIAN_POINT ( 'NONE',  ( 787.4397851343537695, -117.7255117493292715, 374.2001403089903988 ) ) ;
#4762=CARTESIAN_POINT ( 'NONE',  ( 797.6776695296629214, -235.5436935675107293, 357.6776695296636603 ) ) ;
#4764=CARTESIAN_POINT ( 'NONE',  ( 760.7433823573367135, -36.00906357242605793, 355.9930595647440441 ) ) ;
#4768=CARTESIAN_POINT ( 'NONE',  ( 756.1443688327750579, -21.62377810805121570, 314.3581564841659315 ) ) ;
#4771=CARTESIAN_POINT ( 'NONE',  ( 792.1044303154645831, -36.45278447660223975, 317.8323909638837677 ) ) ;
#4774=CARTESIAN_POINT ( 'NONE',  ( 768.8385539511368734, -359.2601417444137724, 306.4236121716840557 ) ) ;
#4778=CARTESIAN_POINT ( 'NONE',  ( 749.8865473780648472, -428.5328690171409107, 322.1177392798429082 ) ) ;
#4779=CARTESIAN_POINT ( 'NONE',  ( 800.0135310231082713, -350.0891481129648923, 325.0180583372163028 ) ) ;
#4787=CARTESIAN_POINT ( 'NONE',  ( 759.9864689768902508, -50.08914811296584446, 354.9819416627836404 ) ) ;
#4788=CARTESIAN_POINT ( 'NONE',  ( 766.0291762391763086, -370.9181544815159555, 360.7704444035551319 ) ) ;
#4790=CARTESIAN_POINT ( 'NONE',  ( 812.7932403749906598, -399.1800572038738437, 327.7687537140311633 ) ) ;
#4791=CARTESIAN_POINT ( 'NONE',  ( 744.8212110874229666, -306.8965053807775689, 336.2046728542121627 ) ) ;
#4792=CARTESIAN_POINT ( 'NONE',  ( 783.7566961878529810, -96.89650538077825104, 305.1792804349288417 ) ) ;
#4799=CARTESIAN_POINT ( 'NONE',  ( 763.2262854647970016, -416.6346026584192259, 309.2812353651462445 ) ) ;
#4800=CARTESIAN_POINT ( 'NONE',  ( 787.4999999999992042, -462.9681489794448339, 370.0000000000000568 ) ) ;
#4801=DIRECTION ( 'NONE',  ( 0.000000000000000000, 1.000000000000000000, 0.000000000000000000 ) ) ;
#4805=CARTESIAN_POINT ( 'NONE',  ( 796.1575198192839480, -294.0090635724253048, 359.4546378042384163 ) ) ;
#4806=CARTESIAN_POINT ( 'NONE',  ( 795.1360043628807261, -140.0891481129654892, 360.2193346964456282 ) ) ;
#4810=CARTESIAN_POINT ( 'NONE',  ( 804.9511171171677688, -317.8055962898684470, 335.8780910478229202 ) ) ;
#4813=CARTESIAN_POINT ( 'NONE',  ( 747.6481478633932056, -61.09997266333506616, 353.4146539503763620 ) ) ;
#4817=CARTESIAN_POINT ( 'NONE',  ( 804.7487373415286811, -211.5436935675107861, 364.7487373415288516 ) ) ;
#4818=CARTESIAN_POINT ( 'NONE',  ( 771.1735550268778070, -129.1800572038746111, 316.3353852180827630 ) ) ;
#4819=ORIENTED_EDGE ( 'NONE', *, *, #30930, .T. ) ;
#4821=CARTESIAN_POINT ( 'NONE',  ( 760.7433823573367135, -12.00906357242613609, 355.9930595647440441 ) ) ;
#4824=CARTESIAN_POINT ( 'NONE',  ( 801.3366627262608972, -392.5328690171409107, 353.0897708529566899 ) ) ;
#4830=CARTESIAN_POINT ( 'NONE',  ( 748.3538107759620743, -232.7146871989596377, 355.8262568251490165 ) ) ;
#4831=CARTESIAN_POINT ( 'NONE',  ( 771.1735550268780344, -57.18005720387490243, 316.3353852180828198 ) ) ;
#4833=CARTESIAN_POINT ( 'NONE',  ( 768.0187753319979720, -248.6346026584197659, 318.0580252608186242 ) ) ;
#4834=CIRCLE ( 'NONE', #6313, 30.00000000000008171 ) ;
#4837=ORIENTED_EDGE ( 'NONE', *, *, #10015, .F. ) ;
#4839=CARTESIAN_POINT ( 'NONE',  ( 763.2154366446407039, -69.62377810805107003, 321.4292242960311228 ) ) ;
#4843=CARTESIAN_POINT ( 'NONE',  ( 814.2001403089898304, -305.3618753856922581, 347.4397851343538264 ) ) ;
#4844=CARTESIAN_POINT ( 'NONE',  ( 801.9858362298568863, -27.07832356259665474, 312.7379699480935642 ) ) ;
#4852=CARTESIAN_POINT ( 'NONE',  ( 745.7998596910086917, -317.3618753856922581, 332.5602148656461168 ) ) ;
#4855=CARTESIAN_POINT ( 'NONE',  ( 775.8780910478218402, -201.2817908451528126, 364.9511171171680530 ) ) ;
#4856=CARTESIAN_POINT ( 'NONE',  ( 792.1044303154645831, -36.45278447660223975, 317.8323909638837677 ) ) ;
#4860=CARTESIAN_POINT ( 'NONE',  ( 756.1348686366196716, -233.2601417444141987, 347.5531968255698416 ) ) ;
#4864=CARTESIAN_POINT ( 'NONE',  ( 796.7737145352015204, -428.6346026584192259, 370.7187646348536987 ) ) ;
#4868=CARTESIAN_POINT ( 'NONE',  ( 810.7187646348534145, -66.45278447660216159, 356.7737145352016341 ) ) ;
#4869=CARTESIAN_POINT ( 'NONE',  ( 801.1904061080336987, -116.0891481129656029, 368.3070685750235498 ) ) ;
#4873=CARTESIAN_POINT ( 'NONE',  ( 802.2119215644370342, -390.0090635724249069, 367.5423716828165084 ) ) ;
#4875=CARTESIAN_POINT ( 'NONE',  ( 751.6929314249748586, -366.9982390220556567, 318.8095938919659034 ) ) ;
#4878=CARTESIAN_POINT ( 'NONE',  ( 800.2193346964447755, -450.9982390220554294, 355.1360043628815788 ) ) ;
#4881=CARTESIAN_POINT ( 'NONE',  ( 759.8311093483677041, -142.1692326535054178, 310.9282345327691814 ) ) ;
#4882=CARTESIAN_POINT ( 'NONE',  ( 795.1360043628808398, -452.0891481129646081, 360.2193346964456282 ) ) ;
#4886=CARTESIAN_POINT ( 'NONE',  ( 767.8955696845333705, -120.4527844766019484, 362.1676090361162323 ) ) ;
#4889=CARTESIAN_POINT ( 'NONE',  ( 800.0135310231082713, -254.0891481129652334, 325.0180583372163028 ) ) ;
#4890=CARTESIAN_POINT ( 'NONE',  ( 765.0180583372156207, -264.9982390220561115, 360.0135310231089534 ) ) ;
#4894=CARTESIAN_POINT ( 'NONE',  ( 783.0433043558608688, 23.10349461922137237, 315.1538015810313027 ) ) ;
#4898=CARTESIAN_POINT ( 'NONE',  ( 763.2262854647970016, -200.6346026584199365, 309.2812353651462445 ) ) ;
#4899=CARTESIAN_POINT ( 'NONE',  ( 763.8424801807145741, -306.0090635724252479, 320.5453621957614700 ) ) ;
#4900=CARTESIAN_POINT ( 'NONE',  ( 803.2186876482843445, -415.9874144716862361, 350.0220218866286928 ) ) ;
#4908=CARTESIAN_POINT ( 'NONE',  ( 789.9200121543843807, -265.9874144716867477, 317.0176451133914384 ) ) ;
#4916=CARTESIAN_POINT ( 'NONE',  ( 793.5525998758768083, -175.0999726633346825, 372.6845335610516941 ) ) ;
#4921=CARTESIAN_POINT ( 'NONE',  ( 796.7737145352015204, -20.63460265842048003, 370.7187646348536987 ) ) ;
#4926=CARTESIAN_POINT ( 'NONE',  ( 785.3141322388236176, -45.72551174932949181, 364.4286716492789537 ) ) ;
#4928=CARTESIAN_POINT ( 'NONE',  ( 783.7953271457878373, -272.1908817542434917, 375.1787889125761239 ) ) ;
#4930=CARTESIAN_POINT ( 'NONE',  ( 804.7487373415286811, -259.5436935675106156, 364.7487373415288516 ) ) ;
#4934=ADVANCED_FACE ( 'NONE', ( #40265, #32871 ), #18781, .F. ) ;
#4936=CARTESIAN_POINT ( 'NONE',  ( 768.0187753319979720, -344.6346026584195101, 318.0580252608186242 ) ) ;
#4937=CARTESIAN_POINT ( 'NONE',  ( 796.9571628226829034, -71.46360902697141171, 321.2382568024804641 ) ) ;
#4940=CARTESIAN_POINT ( 'NONE',  ( 772.4999999999993179, -512.9681489794448908, 329.9999999999999432 ) ) ;
#4942=CARTESIAN_POINT ( 'NONE',  ( 797.8594530101008786, -397.5436935675100472, 322.1405469898980982 ) ) ;
#4949=CARTESIAN_POINT ( 'NONE',  ( 781.8018195045266339, -166.2709662947835909, 365.1927285166406705 ) ) ;
#4953=CARTESIAN_POINT ( 'NONE',  ( 778.2165204200184689, -358.8164208402375834, 364.9363028652563230 ) ) ;
#4956=CARTESIAN_POINT ( 'NONE',  ( 803.4237431249931660, -447.1800572038736732, 331.2633955100225194 ) ) ;
#4958=CARTESIAN_POINT ( 'NONE',  ( 763.0537975583476964, -96.45278447660204790, 371.0346526505628617 ) ) ;
#4959=ORIENTED_EDGE ( 'NONE', *, *, #14494, .F. ) ;
#4965=CARTESIAN_POINT ( 'NONE',  ( 755.3201227861273992, -3.725511749329622813, 345.3687786644892981 ) ) ;
#4966=CARTESIAN_POINT ( 'NONE',  ( 745.0891759886404770, -220.2709662947834772, 342.4968714119734159 ) ) ;
#4967=CARTESIAN_POINT ( 'NONE',  ( 760.5453621957607311, -165.0783235625962391, 323.8424801807151425 ) ) ;
#4969=ORIENTED_EDGE ( 'NONE', *, *, #2102, .F. ) ;
#4973=CARTESIAN_POINT ( 'NONE',  ( 752.7379699480933368, -84.00906357242590161, 361.9858362298580232 ) ) ;
#4983=CARTESIAN_POINT ( 'NONE',  ( 775.8780910478218402, -393.2817908451522726, 364.9511171171680530 ) ) ;
#4985=CARTESIAN_POINT ( 'NONE',  ( 784.1219089521767955, -237.2817908451526421, 315.0488828828318333 ) ) ;
#4989=CARTESIAN_POINT ( 'NONE',  ( 783.7953271457878373, -176.1908817542438328, 375.1787889125761239 ) ) ;
#4991=CARTESIAN_POINT ( 'NONE',  ( 782.5225473063381969, -166.2709662947835909, 375.2698199232970637 ) ) ;
#4996=CARTESIAN_POINT ( 'NONE',  ( 781.7834795799800531, -226.8164208402380098, 315.0636971347436202 ) ) ;
#4997=CARTESIAN_POINT ( 'NONE',  ( 761.4292242960306112, -17.46360902697157513, 323.2154366446414429 ) ) ;
#5002=CARTESIAN_POINT ( 'NONE',  ( 747.3154664389472828, -19.98741447168758256, 326.4474001241230781 ) ) ;
#5003=CARTESIAN_POINT ( 'NONE',  ( 804.6798772138708955, -303.7255117493287457, 334.6312213355107019 ) ) ;
#5007=CARTESIAN_POINT ( 'NONE',  ( 803.4237431249931660, -39.18005720387496638, 331.2633955100225194 ) ) ;
#5010=CARTESIAN_POINT ( 'NONE',  ( 786.2056067578752163, -347.8055962898683333, 374.4686193811670023 ) ) ;
#5013=CARTESIAN_POINT ( 'NONE',  ( 810.1134526219336749, -416.5328690171409107, 357.8822607201570349 ) ) ;
#5015=CARTESIAN_POINT ( 'NONE',  ( 803.6646147819161570, -329.9073299311467053, 348.8264449731210561 ) ) ;
#5023=CARTESIAN_POINT ( 'NONE',  ( 797.6776695296629214, -67.54369356751125508, 357.6776695296636603 ) ) ;
#5024=CARTESIAN_POINT ( 'NONE',  ( 804.8461984189677878, -386.1908817542432075, 336.9566956441385628 ) ) ;
#5025=CARTESIAN_POINT ( 'NONE',  ( 792.2312462859673587, -419.9073299311465348, 307.2067596250082602 ) ) ;
#5027=CARTESIAN_POINT ( 'NONE',  ( 814.8230680027162407, -317.8055962898684470, 333.7305795820267917 ) ) ;
#5028=CARTESIAN_POINT ( 'NONE',  ( 803.8556311672234642, -105.6237781080509421, 365.6418435158340117 ) ) ;
#5032=CARTESIAN_POINT ( 'NONE',  ( 796.9462024416508257, -420.4527844766009252, 308.9653473494370246 ) ) ;
#5033=CARTESIAN_POINT ( 'NONE',  ( 793.2534793918160858, 16.75597696963228955, 312.9842977579731382 ) ) ;
#5038=CARTESIAN_POINT ( 'NONE',  ( 769.0155153010367712, -298.3726999360616787, 362.7791456095907279 ) ) ;
#5039=ORIENTED_EDGE ( 'NONE', *, *, #37944, .F. ) ;
#5043=CARTESIAN_POINT ( 'NONE',  ( 744.6391490659812007, -86.73633629969862113, 338.7502325331110455 ) ) ;
#5046=CARTESIAN_POINT ( 'NONE',  ( 762.3223304703356007, -103.5436935675111272, 322.3223304703362828 ) ) ;
#5050=CARTESIAN_POINT ( 'NONE',  ( 804.6971507214547046, -27.28179084515336328, 344.0799538623459739 ) ) ;
#5053=CARTESIAN_POINT ( 'NONE',  ( 779.4709603349208464, -408.3510508353227806, 314.7162404726379918 ) ) ;
#5057=CARTESIAN_POINT ( 'NONE',  ( 758.0141637701419768, -255.0783235625958980, 367.2620300519063790 ) ) ;
#5058=CARTESIAN_POINT ( 'NONE',  ( 804.6798772138710092, -39.72551174932951312, 334.6312213355106451 ) ) ;
#5061=CARTESIAN_POINT ( 'NONE',  ( 767.8955696845333705, -240.4527844766015221, 362.1676090361162323 ) ) ;
#5070=CARTESIAN_POINT ( 'NONE',  ( 796.7737145352015204, -308.6346026584195670, 370.7187646348536987 ) ) ;
#5071=CARTESIAN_POINT ( 'NONE',  ( 814.8230680027162407, -29.80559628986937781, 333.7305795820267917 ) ) ;
#5076=CARTESIAN_POINT ( 'NONE',  ( 778.1981804954714335, -226.2709662947834204, 314.8072714833589885 ) ) ;
#5078=CARTESIAN_POINT ( 'NONE',  ( 751.9810565676468741, -314.0891481129650629, 360.9747183278973921 ) ) ;
#5080=CARTESIAN_POINT ( 'NONE',  ( 783.0433043558608688, -360.8965053807773984, 315.1538015810313027 ) ) ;
#5083=CARTESIAN_POINT ( 'NONE',  ( 755.8894580844503253, -207.8272453906073451, 332.3691319403863531 ) ) ;
#5084=CARTESIAN_POINT ( 'NONE',  ( 771.1735550268778070, -33.18005720387498769, 316.3353852180827630 ) ) ;
#5088=CARTESIAN_POINT ( 'NONE',  ( 764.0069404352550464, -231.0783235625960401, 359.2566176426627180 ) ) ;
#5091=CARTESIAN_POINT ( 'NONE',  ( 744.7301800767019131, -436.8164208402372992, 337.4774526936615757 ) ) ;
#5095=CARTESIAN_POINT ( 'NONE',  ( 782.5225473063381969, -46.27096629478404566, 375.2698199232970637 ) ) ;
#5096=CARTESIAN_POINT ( 'NONE',  ( 748.9653473494363425, -122.6346026584201354, 356.9462024416521331 ) ) ;
#5097=CARTESIAN_POINT ( 'NONE',  ( 799.9999999999993179, -512.9681489794448908, 329.9999999999999432 ) ) ;
#5102=CARTESIAN_POINT ( 'NONE',  ( 777.4774526936600978, -370.2709662947831362, 304.7301800767027657 ) ) ;
#5104=CARTESIAN_POINT ( 'NONE',  ( 773.3843516231979720, 10.55804007376686826, 364.4086373105754433 ) ) ;
#5107=CARTESIAN_POINT ( 'NONE',  ( 813.2346286133761168, -125.2601417444145255, 328.9521613784389160 ) ) ;
#5108=CARTESIAN_POINT ( 'NONE',  ( 803.6646147819162707, -425.9073299311463643, 348.8264449731211130 ) ) ;
#5111=CARTESIAN_POINT ( 'NONE',  ( 765.0180583372156207, -120.9982390220565378, 360.0135310231089534 ) ) ;
#5114=CARTESIAN_POINT ( 'NONE',  ( 804.9363028652555840, -256.2709662947834204, 338.2165204200192079 ) ) ;
#5115=CARTESIAN_POINT ( 'NONE',  ( 762.3223304703356007, -247.5436935675106724, 322.3223304703362828 ) ) ;
#5116=CYLINDRICAL_SURFACE ( 'NONE', #44096, 30.00000000000008171 ) ;
#5118=CARTESIAN_POINT ( 'NONE',  ( 791.9812246680005501, -452.6346026584191691, 361.9419747391813189 ) ) ;
#5122=CARTESIAN_POINT ( 'NONE',  ( 759.0252816721024374, -192.9982390220562820, 368.0189434323527280 ) ) ;
#5123=CARTESIAN_POINT ( 'NONE',  ( 755.8894580844503253, -303.8272453906071178, 332.3691319403863531 ) ) ;
#5124=CARTESIAN_POINT ( 'NONE',  ( 798.7617431975189675, -387.6237781080499758, 323.0428371773161871 ) ) ;
#5132=CARTESIAN_POINT ( 'NONE',  ( 790.8726784830453198, -274.7146871989594388, 362.5472867521010585 ) ) ;
#5136=CARTESIAN_POINT ( 'NONE',  ( 772.4999999999993179, -462.9681489794447202, 270.0000000000000568 ) ) ;
#5140=CARTESIAN_POINT ( 'NONE',  ( 766.4474001241216001, -211.0999726633346540, 307.3154664389482491 ) ) ;
#5141=LINE ( 'NONE', #19227, #14310 ) ;
#5146=CARTESIAN_POINT ( 'NONE',  ( 787.5162901302840055, -11.36187538569323863, 305.4481719005792684 ) ) ;
#5151=CARTESIAN_POINT ( 'NONE',  ( 755.0636971347428243, -52.27096629478401724, 341.7834795799807353 ) ) ;
#5152=CARTESIAN_POINT ( 'NONE',  ( 745.5313806188320314, -279.2817908451526137, 333.7943932421247268 ) ) ;
#5153=CARTESIAN_POINT ( 'NONE',  ( 787.5162901302840055, -275.3618753856923149, 305.4481719005792684 ) ) ;
#5157=CARTESIAN_POINT ( 'NONE',  ( 778.1981804954714335, -370.2709662947831362, 314.8072714833589885 ) ) ;
#5158=CARTESIAN_POINT ( 'NONE',  ( 755.8894580844503253, -111.8272453906076151, 332.3691319403863531 ) ) ;
#5162=CARTESIAN_POINT ( 'NONE',  ( 778.1981804954714335, -394.2709662947827951, 314.8072714833589885 ) ) ;
#5165=CARTESIAN_POINT ( 'NONE',  ( 774.6312213355099630, -167.3618753856927412, 364.6798772138717482 ) ) ;
#5170=CARTESIAN_POINT ( 'NONE',  ( 788.8264449731200330, -357.1800572038739006, 363.6646147819171233 ) ) ;
#5173=CARTESIAN_POINT ( 'NONE',  ( 747.2067596250078623, -75.18005720387485269, 352.2312462859687230 ) ) ;
#5178=CARTESIAN_POINT ( 'NONE',  ( 810.7187646348534145, -258.4527844766016074, 356.7737145352016341 ) ) ;
#5179=CARTESIAN_POINT ( 'NONE',  ( 758.6633372737375112, -164.5328690171416781, 326.9102291470432533 ) ) ;
#5183=EDGE_LOOP ( 'NONE', ( #43149, #44103, #43067, #16129, #38130, #1310 ) ) ;
#5187=CARTESIAN_POINT ( 'NONE',  ( 746.4236121716829757, -63.82724539060779279, 328.8385539511384650 ) ) ;
#5198=CARTESIAN_POINT ( 'NONE',  ( 759.0159684113467620, -400.9181544815159555, 325.8855110935213020 ) ) ;
#5203=CARTESIAN_POINT ( 'NONE',  ( 766.4474001241216001, -163.0999726633347677, 307.3154664389482491 ) ) ;
#5205=CARTESIAN_POINT ( 'NONE',  ( 792.3570229623688874, -141.1800572038746395, 373.1304606946836202 ) ) ;
#5208=CARTESIAN_POINT ( 'NONE',  ( 762.1405469898971887, -241.5436935675106156, 357.8594530101015607 ) ) ;
#5209=CARTESIAN_POINT ( 'NONE',  ( 805.2837595273609850, -26.73633629969882008, 340.5290396650784714 ) ) ;
#5216=CARTESIAN_POINT ( 'NONE',  ( 803.2186876482843445, -103.9874144716873161, 350.0220218866286928 ) ) ;
#5217=ORIENTED_EDGE ( 'NONE', *, *, #39667, .T. ) ;
#5219=CARTESIAN_POINT ( 'NONE',  ( 805.1927285166397041, -64.81642084023852135, 341.8018195045277707 ) ) ;
#5222=CARTESIAN_POINT ( 'NONE',  ( 781.2497674668890113, -348.3510508353228943, 375.3608509340180603 ) ) ;
#5224=CARTESIAN_POINT ( 'NONE',  ( 766.5853460496234675, -421.9874144716863498, 372.3518521366060554 ) ) ;
#5226=CARTESIAN_POINT ( 'NONE',  ( 785.3687786644884454, -323.3618753856923149, 315.3201227861279676 ) ) ;
#5234=CARTESIAN_POINT ( 'NONE',  ( 764.8639956371174549, -104.0891481129656881, 319.7806653035542013 ) ) ;
#5235=CARTESIAN_POINT ( 'NONE',  ( 755.5913626894240451, -373.6454272087887034, 346.6156483768012890 ) ) ;
#5236=CARTESIAN_POINT ( 'NONE',  ( 772.4837098697145166, -431.3618753856918602, 374.5518280994205611 ) ) ;
#5238=CARTESIAN_POINT ( 'NONE',  ( 807.5423716828161105, -321.0783235625956991, 362.2119215644372048 ) ) ;
#5240=CARTESIAN_POINT ( 'NONE',  ( 781.2497674668890113, -108.3510508353236759, 375.3608509340180603 ) ) ;
#5244=CARTESIAN_POINT ( 'NONE',  ( 744.7301800767019131, -436.8164208402372992, 337.4774526936615757 ) ) ;
#5245=PLANE ( 'NONE',  #13062 ) ;
#5251=CARTESIAN_POINT ( 'NONE',  ( 804.4086373105744769, -313.6454272087888171, 333.3843516231986541 ) ) ;
#5254=CARTESIAN_POINT ( 'NONE',  ( 799.9999999999993179, -512.9681489794448908, 339.9999999999999432 ) ) ;
#5255=CARTESIAN_POINT ( 'NONE',  ( 776.2046728542105711, -68.19088175424413123, 304.8212110874238761 ) ) ;
#5258=CARTESIAN_POINT ( 'NONE',  ( 801.9419747391806368, -138.4527844766019200, 351.9812246680014027 ) ) ;
#5262=CARTESIAN_POINT ( 'NONE',  ( 755.3028492785439312, -15.28179084515340058, 335.9200461376539693 ) ) ;
#5265=CARTESIAN_POINT ( 'NONE',  ( 795.9930595647434757, -411.0783235625954717, 320.7433823573372820 ) ) ;
#5267=CARTESIAN_POINT ( 'NONE',  ( 798.7617431975189675, -75.62377810805104161, 323.0428371773161871 ) ) ;
#5271=CARTESIAN_POINT ( 'NONE',  ( 745.1769319972822814, -257.8055962898686744, 346.2694204179732083 ) ) ;
#5272=CARTESIAN_POINT ( 'NONE',  ( 767.8955696845334842, -72.45278447660213317, 362.1676090361161755 ) ) ;
#5276=CARTESIAN_POINT ( 'NONE',  ( 762.3223304703356007, -247.5436935675106724, 322.3223304703362828 ) ) ;
#5279=CYLINDRICAL_SURFACE ( 'NONE', #25408, 20.00000000000001776 ) ;
#5284=CARTESIAN_POINT ( 'NONE',  ( 744.7301800767020268, -340.8164208402376403, 337.4774526936615189 ) ) ;
#5285=CARTESIAN_POINT ( 'NONE',  ( 749.8865473780648472, -44.53286901714205470, 322.1177392798429082 ) ) ;
#5290=CARTESIAN_POINT ( 'NONE',  ( 785.3687786644884454, -203.3618753856925991, 315.3201227861279676 ) ) ;
#5292=CARTESIAN_POINT ( 'NONE',  ( 754.9967657858570647, -313.5436935675102745, 365.0032342141425374 ) ) ;
#5295=DIRECTION ( 'NONE',  ( -1.000000000000000000, -0.000000000000000000, -0.000000000000000000 ) ) ;
#5296=CARTESIAN_POINT ( 'NONE',  ( 759.0159684113467620, -184.9181544815165239, 325.8855110935213020 ) ) ;
#5297=CARTESIAN_POINT ( 'NONE',  ( 802.1676090361156639, -86.63460265842023489, 327.8955696845344505 ) ) ;
#5301=CARTESIAN_POINT ( 'NONE',  ( 769.1273215169530886, -262.7146871989594956, 317.4527132478988847 ) ) ;
#5304=CARTESIAN_POINT ( 'NONE',  ( 749.2812353651451076, -438.4527844766009821, 323.2262854647983090 ) ) ;
#5305=CARTESIAN_POINT ( 'NONE',  ( 779.9999999999992042, -462.9681489794448339, 309.9999999999998863 ) ) ;
#5308=CARTESIAN_POINT ( 'NONE',  ( 746.8695393053150156, -53.90732993114765037, 327.6429770376306010 ) ) ;
#5309=CARTESIAN_POINT ( 'NONE',  ( 815.2698199232961542, -136.8164208402382371, 342.5225473063383106 ) ) ;
#5313=CARTESIAN_POINT ( 'NONE',  ( 763.0537975583475827, -360.4527844766010958, 371.0346526505627480 ) ) ;
#5315=CARTESIAN_POINT ( 'NONE',  ( 765.8855110935204493, 1.830767346494167391, 319.0159684113471599 ) ) ;
#5319=CARTESIAN_POINT ( 'NONE',  ( 788.7631598425961101, -145.4419599262326699, 305.7194118038759143 ) ) ;
#5320=CARTESIAN_POINT ( 'NONE',  ( 804.4286716492782716, -449.3618753856918602, 345.3141322388244703 ) ) ;
#5321=CARTESIAN_POINT ( 'NONE',  ( 778.7502325331095108, -168.3510508353234911, 304.6391490659818828 ) ) ;
#5324=CARTESIAN_POINT ( 'NONE',  ( 774.6858677611749044, -129.7255117493292289, 315.5713283507209894 ) ) ;
#5326=CARTESIAN_POINT ( 'NONE',  ( 794.9819416627830151, -276.9982390220559978, 319.9864689768909898 ) ) ;
#5327=CARTESIAN_POINT ( 'NONE',  ( 759.7806653035535192, -270.9982390220561115, 324.8639956371181370 ) ) ;
#5330=CARTESIAN_POINT ( 'NONE',  ( 802.1676090361156639, -446.6346026584189985, 327.8955696845344505 ) ) ;
#5334=CARTESIAN_POINT ( 'NONE',  ( 814.2001403089898304, -209.3618753856926276, 347.4397851343538264 ) ) ;
#5335=CARTESIAN_POINT ( 'NONE',  ( 757.0176451133909268, -301.0999726633342561, 349.9200121543848354 ) ) ;
#5336=CARTESIAN_POINT ( 'NONE',  ( 755.8398074228967971, -403.4419599262317888, 333.4516893846970333 ) ) ;
#5344=CARTESIAN_POINT ( 'NONE',  ( 786.6156483768007774, -289.4419599262321299, 315.5913626894246136 ) ) ;
#5351=CARTESIAN_POINT ( 'NONE',  ( 746.4236121716829757, -207.8272453906073451, 328.8385539511384650 ) ) ;
#5356=CARTESIAN_POINT ( 'NONE',  ( 792.2312462859673587, -35.90732993114770011, 307.2067596250082602 ) ) ;
#5359=DIRECTION ( 'NONE',  ( -1.000000000000000000, -0.000000000000000000, 0.000000000000000000 ) ) ;
#5360=CARTESIAN_POINT ( 'NONE',  ( 765.0180583372156207, -48.99823902205675807, 360.0135310231089534 ) ) ;
#5361=CARTESIAN_POINT ( 'NONE',  ( 745.5313806188320314, -327.2817908451525000, 333.7943932421247268 ) ) ;
#5362=CARTESIAN_POINT ( 'NONE',  ( 755.2512626584698410, -247.5436935675106724, 315.2512626584710915 ) ) ;
#5366=CARTESIAN_POINT ( 'NONE',  ( 805.1927285166397041, -352.8164208402374129, 341.8018195045277707 ) ) ;
#5368=CARTESIAN_POINT ( 'NONE',  ( 766.0291762391763086, -106.9181544815167371, 360.7704444035551319 ) ) ;
#5373=CARTESIAN_POINT ( 'NONE',  ( 791.1614460488616487, -131.2601417444144829, 373.5763878283158874 ) ) ;
#5374=CARTESIAN_POINT ( 'NONE',  ( 774.6312213355099630, -407.3618753856920307, 364.6798772138717482 ) ) ;
#5377=CARTESIAN_POINT ( 'NONE',  ( 795.1360043628807261, -164.0891481129655176, 360.2193346964456282 ) ) ;
#5378=CARTESIAN_POINT ( 'NONE',  ( 792.1044303154646968, -156.4527844766018916, 317.8323909638837677 ) ) ;
#5382=CARTESIAN_POINT ( 'NONE',  ( 771.2633955100217236, -359.9073299311467053, 363.4237431249939618 ) ) ;
#5386=CARTESIAN_POINT ( 'NONE',  ( 755.2512626584698410, -103.5436935675111272, 315.2512626584710915 ) ) ;
#5391=CARTESIAN_POINT ( 'NONE',  ( 745.0891759886404770, -268.2709662947833067, 342.4968714119734159 ) ) ;
#5392=CARTESIAN_POINT ( 'NONE',  ( 755.0488828828309806, -161.8055962898689870, 344.1219089521771934 ) ) ;
#5393=CARTESIAN_POINT ( 'NONE',  ( 759.9999999999992042, 166.4563064324884465, 360.0000000000000000 ) ) ;
#5400=CARTESIAN_POINT ( 'NONE',  ( 749.5768839229115201, -108.5545181178803915, 358.0661480581553064 ) ) ;
#5409=CARTESIAN_POINT ( 'NONE',  ( 766.0291762391763086, -418.9181544815157849, 360.7704444035551319 ) ) ;
#5411=CARTESIAN_POINT ( 'NONE',  ( 786.2694204179717872, -357.2817908451523294, 305.1769319972829067 ) ) ;
#5413=CARTESIAN_POINT ( 'NONE',  ( 798.5707757039680246, -245.4636090269709143, 356.7845633553585003 ) ) ;
#5418=CARTESIAN_POINT ( 'NONE',  ( 813.5763878283155464, -171.8272453906074304, 351.1614460488615350 ) ) ;
#5420=CARTESIAN_POINT ( 'NONE',  ( 746.8695393053150156, -149.9073299311473875, 327.6429770376306010 ) ) ;
#5423=CARTESIAN_POINT ( 'NONE',  ( 785.3687786644884454, -251.3618753856923149, 315.3201227861279676 ) ) ;
#5424=CARTESIAN_POINT ( 'NONE',  ( 804.4086373105744769, -25.64542720878973014, 333.3843516231986541 ) ) ;
#5429=CARTESIAN_POINT ( 'NONE',  ( 758.6633372737375112, -92.53286901714190549, 326.9102291470432533 ) ) ;
#5434=CARTESIAN_POINT ( 'NONE',  ( 804.4286716492782716, -65.36187538569306810, 345.3141322388244703 ) ) ;
#5438=CARTESIAN_POINT ( 'NONE',  ( 805.9055244015594326, -363.6237781080502032, 315.8990559732753240 ) ) ;
#5440=CARTESIAN_POINT ( 'NONE',  ( 759.8311093483677041, -430.1692326535043094, 310.9282345327691814 ) ) ;
#5442=CARTESIAN_POINT ( 'NONE',  ( 788.7366044899766848, -371.9073299311465917, 316.5762568750059813 ) ) ;
#5451=CARTESIAN_POINT ( 'NONE',  ( 767.8955696845333705, -96.45278447660203369, 362.1676090361162323 ) ) ;
#5452=CARTESIAN_POINT ( 'NONE',  ( 783.0745993439762742, -392.1908817542432075, 365.1016975059196739 ) ) ;
#5453=CARTESIAN_POINT ( 'NONE',  ( 812.7932403749906598, -423.1800572038737300, 327.7687537140311633 ) ) ;
#5455=CARTESIAN_POINT ( 'NONE',  ( 778.7502325331095108, -336.3510508353228943, 304.6391490659818828 ) ) ;
#5456=CARTESIAN_POINT ( 'NONE',  ( 747.3154664389472828, -91.98741447168737295, 326.4474001241230781 ) ) ;
#5460=EDGE_CURVE ( 'NONE', #25515, #38059, #44855, .T. ) ;
#5461=CARTESIAN_POINT ( 'NONE',  ( 796.7737145352015204, -452.6346026584191691, 370.7187646348536987 ) ) ;
#5465=ADVANCED_FACE ( 'NONE', ( #41388 ), #25890, .F. ) ;
#5467=CARTESIAN_POINT ( 'NONE',  ( 790.0183182880230106, -452.9681489794449476, 362.9048749981275250 ) ) ;
#5468=CARTESIAN_POINT ( 'NONE',  ( 799.9999999999993179, -462.9681489794448339, 309.9999999999998863 ) ) ;
#5469=CARTESIAN_POINT ( 'NONE',  ( 763.8424801807145741, -282.0090635724253048, 320.5453621957614700 ) ) ;
#5470=CARTESIAN_POINT ( 'NONE',  ( 754.8072714833581358, -172.8164208402381234, 338.1981804954720587 ) ) ;
#5472=CARTESIAN_POINT ( 'NONE',  ( 757.7880784355613741, -282.0090635724253048, 312.4576283171834916 ) ) ;
#5474=DIRECTION ( 'NONE',  ( 0.000000000000000000, 1.110223024625155554E-15, -1.000000000000000000 ) ) ;
#5475=CARTESIAN_POINT ( 'NONE',  ( 755.8990559732751535, -59.46360902697142592, 365.9055244015606831 ) ) ;
#5478=CARTESIAN_POINT ( 'NONE',  ( 756.3353852180819104, -149.9073299311473875, 331.1735550268788302 ) ) ;
#5483=CARTESIAN_POINT ( 'NONE',  ( 775.8780910478218402, -33.28179084515333130, 364.9511171171680530 ) ) ;
#5486=CARTESIAN_POINT ( 'NONE',  ( 801.3366627262608972, -416.5328690171409107, 353.0897708529566899 ) ) ;
#5487=ORIENTED_EDGE ( 'NONE', *, *, #18705, .F. ) ;
#5488=CARTESIAN_POINT ( 'NONE',  ( 775.9200461376533440, -71.80559628986922860, 315.3028492785443291 ) ) ;
#5493=CARTESIAN_POINT ( 'NONE',  ( 761.9338519418445230, -230.5328690171415076, 370.4231160770881957 ) ) ;
#5494=CARTESIAN_POINT ( 'NONE',  ( 771.1735550268780344, -81.18005720387482427, 316.3353852180828198 ) ) ;
#5498=CARTESIAN_POINT ( 'NONE',  ( 804.9363028652555840, -256.2709662947834204, 338.2165204200192079 ) ) ;
#5507=CARTESIAN_POINT ( 'NONE',  ( 772.4837098697145166, -311.3618753856923149, 374.5518280994205611 ) ) ;
#5508=CARTESIAN_POINT ( 'NONE',  ( 800.1688906516307043, -226.1692326535051052, 369.0717654672308186 ) ) ;
#5509=CARTESIAN_POINT ( 'NONE',  ( 793.4146539503750546, -49.98741447168749374, 307.6481478633938877 ) ) ;
#5514=CARTESIAN_POINT ( 'NONE',  ( 797.8594530101008786, -205.5436935675108430, 322.1405469898980982 ) ) ;
#5517=CARTESIAN_POINT ( 'NONE',  ( 767.7687537140311633, -311.9073299311468759, 372.7932403749916830 ) ) ;
#5519=DIRECTION ( 'NONE',  ( 0.000000000000000000, 0.000000000000000000, 1.000000000000000000 ) ) ;
#5521=CARTESIAN_POINT ( 'NONE',  ( 761.4292242960306112, -185.4636090269710280, 323.2154366446414429 ) ) ;
#5523=CARTESIAN_POINT ( 'NONE',  ( 800.2193346964447755, -66.99823902205672255, 355.1360043628815788 ) ) ;
#5527=CARTESIAN_POINT ( 'NONE',  ( 804.1601925771018387, -247.4419599262323004, 346.5483106153029098 ) ) ;
#5530=CARTESIAN_POINT ( 'NONE',  ( 810.7187646348534145, -426.4527844766010389, 356.7737145352016341 ) ) ;
#5531=DIRECTION ( 'NONE',  ( 0.000000000000000000, 0.000000000000000000, 1.000000000000000000 ) ) ;
#5535=CARTESIAN_POINT ( 'NONE',  ( 815.2698199232961542, -88.81642084023842187, 342.5225473063383106 ) ) ;
#5536=CARTESIAN_POINT ( 'NONE',  ( 751.9810565676468741, -146.0891481129655176, 360.9747183278973921 ) ) ;
#5537=DIRECTION ( 'NONE',  ( -1.000000000000000000, -0.000000000000000000, 0.000000000000000000 ) ) ;
#5544=CARTESIAN_POINT ( 'NONE',  ( 747.2067596250078623, -363.1800572038739006, 352.2312462859687230 ) ) ;
#5545=CARTESIAN_POINT ( 'NONE',  ( 748.9653473494365699, -2.634602658420536425, 356.9462024416520762 ) ) ;
#5548=CARTESIAN_POINT ( 'NONE',  ( 805.1016975059191054, 17.10349461922139369, 343.0745993439771837 ) ) ;
#5552=CARTESIAN_POINT ( 'NONE',  ( 771.2368401574024119, -133.4419599262326699, 374.2805881961240857 ) ) ;
#5553=CARTESIAN_POINT ( 'NONE',  ( 774.6858677611749044, 14.27448825067031812, 315.5713283507209894 ) ) ;
#5555=CARTESIAN_POINT ( 'NONE',  ( 773.7943932421234194, -167.8055962898689586, 305.5313806188329409 ) ) ;
#5559=CARTESIAN_POINT ( 'NONE',  ( 765.0180583372156207, -144.9982390220564525, 360.0135310231089534 ) ) ;
#5562=CARTESIAN_POINT ( 'NONE',  ( 804.4286716492782716, -281.3618753856923718, 345.3141322388244703 ) ) ;
#5565=CARTESIAN_POINT ( 'NONE',  ( 770.0799878456142551, 10.01258552831232329, 362.9823548866085616 ) ) ;
#5569=CARTESIAN_POINT ( 'NONE',  ( 749.2812353651451076, -222.4527844766016642, 323.2262854647983090 ) ) ;
#5570=CARTESIAN_POINT ( 'NONE',  ( 784.1219089521767955, -285.2817908451526137, 315.0488828828318333 ) ) ;
#5571=CARTESIAN_POINT ( 'NONE',  ( 769.1273215169530886, -406.7146871989590409, 317.4527132478988847 ) ) ;
#5576=AXIS2_PLACEMENT_3D ( 'NONE', #5136, #22228, #25707 ) ;
#5581=CARTESIAN_POINT ( 'NONE',  ( 759.2295555964440155, -304.1692326535048210, 353.9708237608231229 ) ) ;
#5587=CARTESIAN_POINT ( 'NONE',  ( 793.5525998758768083, -199.0999726633346825, 372.6845335610516941 ) ) ;
#5594=CARTESIAN_POINT ( 'NONE',  ( 814.2001403089898304, -41.36187538569314626, 347.4397851343538264 ) ) ;
#5598=CARTESIAN_POINT ( 'NONE',  ( 768.0187753319979720, -56.63460265842036279, 318.0580252608186242 ) ) ;
#5599=CARTESIAN_POINT ( 'NONE',  ( 752.7379699480933368, -324.0090635724251911, 361.9858362298580232 ) ) ;
#5600=CARTESIAN_POINT ( 'NONE',  ( 748.9653473494363425, -266.6346026584197375, 356.9462024416521331 ) ) ;
#5603=CARTESIAN_POINT ( 'NONE',  ( 759.9999999999992042, -462.9681489794448339, 309.9999999999998863 ) ) ;
#5604=CARTESIAN_POINT ( 'NONE',  ( 771.2633955100217236, -359.9073299311467053, 363.4237431249939618 ) ) ;
#5605=CARTESIAN_POINT ( 'NONE',  ( 769.0155153010367712, -106.3726999360621903, 362.7791456095907279 ) ) ;
#5607=CARTESIAN_POINT ( 'NONE',  ( 762.1405469898973024, -385.5436935675102745, 357.8594530101016176 ) ) ;
#5611=CARTESIAN_POINT ( 'NONE',  ( 771.1735550268778070, -393.1800572038737300, 316.3353852180827630 ) ) ;
#5612=VERTEX_POINT ( 'NONE', #39249 ) ;
#5615=CARTESIAN_POINT ( 'NONE',  ( 778.1981804954714335, -202.2709662947834772, 314.8072714833589885 ) ) ;
#5616=CARTESIAN_POINT ( 'NONE',  ( 765.0180583372156207, -144.9982390220564525, 360.0135310231089534 ) ) ;
#5620=CARTESIAN_POINT ( 'NONE',  ( 803.4237431249931660, -351.1800572038740142, 331.2633955100225194 ) ) ;
#5625=CARTESIAN_POINT ( 'NONE',  ( 812.7932403749906598, -111.1800572038747532, 327.7687537140311633 ) ) ;
#5631=CARTESIAN_POINT ( 'NONE',  ( 745.4481719005789273, -267.7255117493286320, 347.5162901302853129 ) ) ;
#5632=CARTESIAN_POINT ( 'NONE',  ( 765.8855110935204493, -190.1692326535052189, 319.0159684113471599 ) ) ;
#5636=ORIENTED_EDGE ( 'NONE', *, *, #28615, .F. ) ;
#5642=CARTESIAN_POINT ( 'NONE',  ( 810.4231160770870019, -120.5545181178803205, 321.9338519418446936 ) ) ;
#5653=CARTESIAN_POINT ( 'NONE',  ( 766.0291762391763086, -442.9181544815157849, 360.7704444035551319 ) ) ;
#5661=CARTESIAN_POINT ( 'NONE',  ( 768.9521613784389729, -201.8272453906073451, 373.2346286133773106 ) ) ;
#5663=CARTESIAN_POINT ( 'NONE',  ( 772.4837098697144029, -167.3618753856927412, 374.5518280994205611 ) ) ;
#5667=CARTESIAN_POINT ( 'NONE',  ( 803.6646147819161570, -257.9073299311469896, 348.8264449731210561 ) ) ;
#5668=CARTESIAN_POINT ( 'NONE',  ( 766.0291762391763086, -10.91815448151704793, 360.7704444035551319 ) ) ;
#5673=CARTESIAN_POINT ( 'NONE',  ( 796.7845633553578182, -105.6237781080509421, 358.5707757039688204 ) ) ;
#5677=CARTESIAN_POINT ( 'NONE',  ( 774.6312213355099630, -71.36187538569302546, 364.6798772138717482 ) ) ;
#5680=CARTESIAN_POINT ( 'NONE',  ( 745.1769319972822814, -377.8055962898682765, 346.2694204179732083 ) ) ;
#5683=CARTESIAN_POINT ( 'NONE',  ( 782.4968714119720516, 13.18357915976123174, 305.0891759886411023 ) ) ;
#5686=CARTESIAN_POINT ( 'NONE',  ( 771.1735550268778070, -369.1800572038739574, 316.3353852180827630 ) ) ;
#5687=VECTOR ( 'NONE', #28837, 1000.000000000000000 ) ;
#5696=CARTESIAN_POINT ( 'NONE',  ( 764.8639956371174549, -80.08914811296574499, 319.7806653035542013 ) ) ;
#5697=CARTESIAN_POINT ( 'NONE',  ( 784.1219089521767955, -405.2817908451522158, 315.0488828828318333 ) ) ;
#5698=CARTESIAN_POINT ( 'NONE',  ( 756.1348686366196716, -89.26014174441463922, 347.5531968255698416 ) ) ;
#5699=CARTESIAN_POINT ( 'NONE',  ( 755.2512626584698410, -415.5436935675102177, 315.2512626584710915 ) ) ;
#5701=CARTESIAN_POINT ( 'NONE',  ( 803.8556311672234642, -321.6237781080502600, 365.6418435158340117 ) ) ;
#5702=CARTESIAN_POINT ( 'NONE',  ( 801.9858362298568863, -123.0783235625963385, 312.7379699480935642 ) ) ;
#5706=CARTESIAN_POINT ( 'NONE',  ( 776.2046728542105711, 3.809118245755632959, 304.8212110874238761 ) ) ;
#5712=CARTESIAN_POINT ( 'NONE',  ( 761.4292242960306112, -329.4636090269706870, 323.2154366446414429 ) ) ;
#5713=CARTESIAN_POINT ( 'NONE',  ( 795.1360043628807261, -188.0891481129653187, 360.2193346964456282 ) ) ;
#5715=CARTESIAN_POINT ( 'NONE',  ( 788.6739635108323228, -319.6454272087888739, 373.9316612368139090 ) ) ;
#5718=CARTESIAN_POINT ( 'NONE',  ( 752.7379699480933368, -108.0090635724258448, 361.9858362298580232 ) ) ;
#5722=CARTESIAN_POINT ( 'NONE',  ( 801.9419747391806368, -162.4527844766018632, 351.9812246680014027 ) ) ;
#5724=CARTESIAN_POINT ( 'NONE',  ( 776.2046728542105711, -404.1908817542431507, 304.8212110874238761 ) ) ;
#5728=CARTESIAN_POINT ( 'NONE',  ( 780.5236548040995785, -44.73633629969875614, 314.9735926884559944 ) ) ;
#5731=CARTESIAN_POINT ( 'NONE',  ( 804.9511171171677688, -437.8055962898679923, 335.8780910478229202 ) ) ;
#5732=ORIENTED_EDGE ( 'NONE', *, *, #34778, .F. ) ;
#5734=DIRECTION ( 'NONE',  ( 0.000000000000000000, 0.000000000000000000, -1.000000000000000000 ) ) ;
#5735=CARTESIAN_POINT ( 'NONE',  ( 766.5853460496234675, -277.9874144716867477, 372.3518521366060554 ) ) ;
#5736=CARTESIAN_POINT ( 'NONE',  ( 764.8639956371174549, -80.08914811296574499, 319.7806653035542581 ) ) ;
#5737=EDGE_LOOP ( 'NONE', ( #38692, #13151, #1478, #22065, #14540, #26370, #12442, #27865, #33086, #25061, #17683 ) ) ;
#5739=CARTESIAN_POINT ( 'NONE',  ( 771.2633955100217236, -263.9073299311469327, 363.4237431249939618 ) ) ;
#5743=ORIENTED_EDGE ( 'NONE', *, *, #7837, .F. ) ;
#5745=CARTESIAN_POINT ( 'NONE',  ( 788.7366044899766848, -299.9073299311468759, 316.5762568750059813 ) ) ;
#5746=CARTESIAN_POINT ( 'NONE',  ( 745.4481719005789273, -315.7255117493286320, 347.5162901302853697 ) ) ;
#5747=CARTESIAN_POINT ( 'NONE',  ( 748.3538107759620743, -232.7146871989596377, 355.8262568251490165 ) ) ;
#5752=CARTESIAN_POINT ( 'NONE',  ( 762.1405469898971887, -217.5436935675107293, 357.8594530101015607 ) ) ;
#5756=CARTESIAN_POINT ( 'NONE',  ( 763.2262854647970016, -368.6346026584193964, 309.2812353651462445 ) ) ;
#5759=CARTESIAN_POINT ( 'NONE',  ( 793.9408588713487234, 16.45630643248830438, 314.6714885282663090 ) ) ;
#5762=CARTESIAN_POINT ( 'NONE',  ( 775.8780910478218402, -225.2817908451527273, 364.9511171171680530 ) ) ;
#5763=CARTESIAN_POINT ( 'NONE',  ( 805.1927285166397041, -88.81642084023842187, 341.8018195045277707 ) ) ;
#5767=CARTESIAN_POINT ( 'NONE',  ( 801.3366627262608972, -272.5328690171413086, 353.0897708529566899 ) ) ;
#5770=CARTESIAN_POINT ( 'NONE',  ( 801.1904061080336987, -428.0891481129644944, 368.3070685750235498 ) ) ;
#5775=EDGE_CURVE ( 'NONE', #31386, #13608, #14989, .T. ) ;
#5776=CARTESIAN_POINT ( 'NONE',  ( 759.0252816721024374, -96.99823902205660886, 368.0189434323527280 ) ) ;
#5777=CARTESIAN_POINT ( 'NONE',  ( 796.9462024416508257, -156.4527844766018916, 308.9653473494370246 ) ) ;
#5781=CARTESIAN_POINT ( 'NONE',  ( 815.3608509340175488, -410.7363362996976548, 341.2497674668889545 ) ) ;
#5783=CARTESIAN_POINT ( 'NONE',  ( 782.5225473063381969, -406.2709662947829088, 375.2698199232970637 ) ) ;
#5784=CARTESIAN_POINT ( 'NONE',  ( 777.5031285880264704, -22.81642084023865280, 374.9108240113588408 ) ) ;
#5786=CARTESIAN_POINT ( 'NONE',  ( 772.3691319403857278, 0.7398582555850804487, 315.8894580844506663 ) ) ;
#5790=CARTESIAN_POINT ( 'NONE',  ( 746.0683387631852383, -163.4419599262325846, 331.3260364891676204 ) ) ;
#5791=CARTESIAN_POINT ( 'NONE',  ( 764.8639956371174549, 15.91085188703394593, 319.7806653035542581 ) ) ;
#5794=CARTESIAN_POINT ( 'NONE',  ( 814.8230680027162407, -173.8055962898689302, 333.7305795820267917 ) ) ;
#5797=CARTESIAN_POINT ( 'NONE',  ( 762.3223304703356007, -175.5436935675108998, 322.3223304703362828 ) ) ;
#5799=CARTESIAN_POINT ( 'NONE',  ( 803.6646147819161570, -281.9073299311468759, 348.8264449731210561 ) ) ;
#5800=CARTESIAN_POINT ( 'NONE',  ( 781.8018195045267476, -286.2709662947833067, 365.1927285166407273 ) ) ;
#5801=DIRECTION ( 'NONE',  ( 0.000000000000000000, 0.000000000000000000, 1.000000000000000000 ) ) ;
#5803=CARTESIAN_POINT ( 'NONE',  ( 755.0488828828309806, -17.80559628986940979, 344.1219089521771934 ) ) ;
#5807=CARTESIAN_POINT ( 'NONE',  ( 814.5518280994195948, -231.7255117493288594, 332.4837098697145166 ) ) ;
#5808=CARTESIAN_POINT ( 'NONE',  ( 757.4527132478984868, -304.3726999360615082, 329.1273215169538844 ) ) ;
#5809=CARTESIAN_POINT ( 'NONE',  ( 772.3691319403857278, -383.2601417444137155, 315.8894580844506663 ) ) ;
#5818=CARTESIAN_POINT ( 'NONE',  ( 793.2243759319678702, -290.5328690171412518, 318.4439275373583200 ) ) ;
#5822=CARTESIAN_POINT ( 'NONE',  ( 759.9999999999992042, 205.0000000000000568, 319.9999999999999432 ) ) ;
#5825=CARTESIAN_POINT ( 'NONE',  ( 745.7194118038753459, -205.6454272087891297, 348.7631598425976449 ) ) ;
#5830=CARTESIAN_POINT ( 'NONE',  ( 767.6429770376289525, -57.18005720387489532, 306.8695393053162093 ) ) ;
#5834=CARTESIAN_POINT ( 'NONE',  ( 778.1981804954714335, -82.27096629478388934, 314.8072714833589885 ) ) ;
#5835=CARTESIAN_POINT ( 'NONE',  ( 760.0363995740630116, -322.9181544815161260, 368.7758568127991907 ) ) ;
#5837=CARTESIAN_POINT ( 'NONE',  ( 767.6429770376289525, -297.1800572038740711, 306.8695393053162093 ) ) ;
#5840=CARTESIAN_POINT ( 'NONE',  ( 787.4999999999992042, -512.9681489794448908, 339.9999999999999432 ) ) ;
#5841=CARTESIAN_POINT ( 'NONE',  ( 804.6798772138708955, -375.7255117493283478, 334.6312213355107019 ) ) ;
#5842=CARTESIAN_POINT ( 'NONE',  ( 799.2566176426618085, -120.0090635724258021, 324.0069404352559559 ) ) ;
#5844=CARTESIAN_POINT ( 'NONE',  ( 744.9990715423526808, -42.35105083532388193, 341.2370466360926002 ) ) ;
#5845=CARTESIAN_POINT ( 'NONE',  ( 800.2193346964446619, -354.9982390220557136, 355.1360043628816925 ) ) ;
#5847=CARTESIAN_POINT ( 'NONE',  ( 791.9812246680005501, -428.6346026584192259, 361.9419747391813189 ) ) ;
#5850=CARTESIAN_POINT ( 'NONE',  ( 805.1927285166397041, -184.8164208402380950, 341.8018195045277707 ) ) ;
#5851=CARTESIAN_POINT ( 'NONE',  ( 759.7806653035535192, -198.9982390220562536, 324.8639956371181370 ) ) ;
#5855=CARTESIAN_POINT ( 'NONE',  ( 757.8323909638827445, -386.6346026584191691, 352.1044303154654358 ) ) ;
#5859=CARTESIAN_POINT ( 'NONE',  ( 805.0032342141413437, -133.5436935675110419, 314.9967657858572352 ) ) ;
#5860=ORIENTED_EDGE ( 'NONE', *, *, #31546, .F. ) ;
#5865=CARTESIAN_POINT ( 'NONE',  ( 777.5031285880264704, -238.8164208402379813, 374.9108240113588408 ) ) ;
#5866=CARTESIAN_POINT ( 'NONE',  ( 769.1273215169530886, -190.7146871989597798, 317.4527132478988847 ) ) ;
#5876=CARTESIAN_POINT ( 'NONE',  ( 748.6759233522253680, -112.3726999360621761, 324.3348316497537098 ) ) ;
#5884=CARTESIAN_POINT ( 'NONE',  ( 804.4086373105744769, -433.6454272087884760, 333.3843516231986541 ) ) ;
#5891=CARTESIAN_POINT ( 'NONE',  ( 757.7880784355613741, -210.0090635724255321, 312.4576283171834916 ) ) ;
#5893=CARTESIAN_POINT ( 'NONE',  ( 748.9653473494363425, -170.6346026584199649, 356.9462024416521331 ) ) ;
#5896=CARTESIAN_POINT ( 'NONE',  ( 755.0636971347428243, -268.2709662947833067, 341.7834795799807353 ) ) ;
#5897=CARTESIAN_POINT ( 'NONE',  ( 769.0155153010367712, -58.37269993606236085, 362.7791456095907279 ) ) ;
#5901=CARTESIAN_POINT ( 'NONE',  ( 796.7845633553578182, -81.62377810805104161, 358.5707757039688204 ) ) ;
#5904=CARTESIAN_POINT ( 'NONE',  ( 778.2165204200184689, -46.81642084023858530, 364.9363028652563230 ) ) ;
#5907=CARTESIAN_POINT ( 'NONE',  ( 791.1614460488616487, -371.2601417444136587, 373.5763878283158874 ) ) ;
#5910=CARTESIAN_POINT ( 'NONE',  ( 756.3353852180819104, -365.9073299311465917, 331.1735550268788302 ) ) ;
#5917=CARTESIAN_POINT ( 'NONE',  ( 797.8594530101008786, -85.54369356751118403, 322.1405469898980982 ) ) ;
#5918=CARTESIAN_POINT ( 'NONE',  ( 754.7162404726377645, -398.7363362996976548, 339.4709603349214717 ) ) ;
#5919=CARTESIAN_POINT ( 'NONE',  ( 812.7932403749906598, -447.1800572038736732, 327.7687537140311633 ) ) ;
#5921=CARTESIAN_POINT ( 'NONE',  ( 788.7631598425961101, -361.4419599262319593, 305.7194118038759143 ) ) ;
#5925=CARTESIAN_POINT ( 'NONE',  ( 815.3608509340175488, -2.736336299698892027, 341.2497674668889545 ) ) ;
#5929=DIRECTION ( 'NONE',  ( 0.000000000000000000, 1.000000000000000000, 0.000000000000000000 ) ) ;
#5931=CARTESIAN_POINT ( 'NONE',  ( 769.9779781133707957, -331.0999726633342561, 316.7813123517150871 ) ) ;
#5932=CARTESIAN_POINT ( 'NONE',  ( 804.4286716492782716, -185.3618753856926844, 345.3141322388244703 ) ) ;
#5934=CARTESIAN_POINT ( 'NONE',  ( 744.6391490659812007, -302.7363362996979959, 338.7502325331110455 ) ) ;
#5937=CARTESIAN_POINT ( 'NONE',  ( 745.5313806188320314, -111.2817908451530968, 333.7943932421247268 ) ) ;
#5940=CARTESIAN_POINT ( 'NONE',  ( 755.3201227861273992, -147.7255117493291152, 345.3687786644892981 ) ) ;
#5942=CARTESIAN_POINT ( 'NONE',  ( 744.6391490659812007, -422.7363362996975980, 338.7502325331110455 ) ) ;
#5945=CARTESIAN_POINT ( 'NONE',  ( 769.9779781133707957, -43.09997266333511590, 316.7813123517150871 ) ) ;
#5948=CARTESIAN_POINT ( 'NONE',  ( 768.8385539511368734, 24.73985825558500551, 306.4236121716840557 ) ) ;
#5950=CARTESIAN_POINT ( 'NONE',  ( 790.8726784830453198, -82.71468719896012090, 362.5472867521010585 ) ) ;
#5953=CARTESIAN_POINT ( 'NONE',  ( 812.6845335610512393, -271.9874144716868045, 353.5525998758768651 ) ) ;
#5954=CARTESIAN_POINT ( 'NONE',  ( 771.2633955100217236, -71.90732993114760063, 363.4237431249939618 ) ) ;
#5957=CARTESIAN_POINT ( 'NONE',  ( 792.1044303154645831, -252.4527844766015789, 317.8323909638837677 ) ) ;
#5964=CARTESIAN_POINT ( 'NONE',  ( 767.7687537140311633, -311.9073299311468759, 372.7932403749916830 ) ) ;
#5965=CARTESIAN_POINT ( 'NONE',  ( 800.1688906516307043, -250.1692326535050199, 369.0717654672308186 ) ) ;
#5969=CARTESIAN_POINT ( 'NONE',  ( 781.7834795799800531, -202.8164208402380950, 315.0636971347436202 ) ) ;
#5972=CARTESIAN_POINT ( 'NONE',  ( 787.5162901302840055, -347.3618753856922012, 305.4481719005792684 ) ) ;
#5974=CARTESIAN_POINT ( 'NONE',  ( 778.5401871010416244, 16.45630643248848912, 314.2029270906900251 ) ) ;
#5976=CARTESIAN_POINT ( 'NONE',  ( 773.4516893846965786, -235.6454272087890729, 315.8398074228977066 ) ) ;
#5977=CARTESIAN_POINT ( 'NONE',  ( 757.8323909638827445, -98.63460265842024910, 352.1044303154654358 ) ) ;
#5981=CARTESIAN_POINT ( 'NONE',  ( 795.9930595647434757, -267.0783235625958696, 320.7433823573372820 ) ) ;
#5984=CARTESIAN_POINT ( 'NONE',  ( 746.4236121716829757, -15.82724539060794200, 328.8385539511384650 ) ) ;
#5988=CARTESIAN_POINT ( 'NONE',  ( 763.0537975583475827, -72.45278447660213317, 371.0346526505627480 ) ) ;
#5990=CARTESIAN_POINT ( 'NONE',  ( 812.7932403749906598, -159.1800572038746111, 327.7687537140311633 ) ) ;
#5993=CARTESIAN_POINT ( 'NONE',  ( 804.1009440267234822, -407.4636090269703459, 314.0944755984392600 ) ) ;
#5995=CARTESIAN_POINT ( 'NONE',  ( 779.9999999999992042, -462.9681489794448339, 339.9999999999999432 ) ) ;
#5996=CARTESIAN_POINT ( 'NONE',  ( 751.9810565676468741, -386.0891481129647786, 360.9747183278973921 ) ) ;
#5997=CARTESIAN_POINT ( 'NONE',  ( 777.4774526936600978, -10.27096629478415046, 304.7301800767028226 ) ) ;
#5999=CARTESIAN_POINT ( 'NONE',  ( 780.5290396650775619, -12.35105083532396897, 365.2837595273619513 ) ) ;
#6002=CARTESIAN_POINT ( 'NONE',  ( 778.7502325331095108, -168.3510508353234911, 304.6391490659818828 ) ) ;
#6004=CARTESIAN_POINT ( 'NONE',  ( 803.8556311672234642, -177.6237781080507148, 365.6418435158340117 ) ) ;
#6008=CARTESIAN_POINT ( 'NONE',  ( 800.0135310231082713, -158.0891481129655176, 325.0180583372163028 ) ) ;
#6011=CARTESIAN_POINT ( 'NONE',  ( 804.4286716492782716, -281.3618753856923718, 345.3141322388244703 ) ) ;
#6012=CARTESIAN_POINT ( 'NONE',  ( 762.3223304703356007, -295.5436935675105588, 322.3223304703362828 ) ) ;
#6016=CARTESIAN_POINT ( 'NONE',  ( 754.8983024940795303, -18.89650538077849617, 336.9254006560228163 ) ) ;
#6021=CARTESIAN_POINT ( 'NONE',  ( 767.7687537140311633, -215.9073299311471317, 372.7932403749916830 ) ) ;
#6022=CARTESIAN_POINT ( 'NONE',  ( 798.5707757039680246, -341.4636090269705733, 356.7845633553585003 ) ) ;
#6023=CARTESIAN_POINT ( 'NONE',  ( 799.4546378042377910, -417.0783235625954148, 356.1575198192848006 ) ) ;
#6030=CARTESIAN_POINT ( 'NONE',  ( 784.0799538623451781, -299.8055962898685038, 364.6971507214555572 ) ) ;
#6031=CARTESIAN_POINT ( 'NONE',  ( 793.4322487044281615, -453.3695810002254234, 372.3199466871218419 ) ) ;
#6033=CARTESIAN_POINT ( 'NONE',  ( 793.0897708529556667, -126.5545181178803205, 361.3366627262616362 ) ) ;
#6034=CARTESIAN_POINT ( 'NONE',  ( 764.8639956371174549, 15.91085188703394238, 319.7806653035542013 ) ) ;
#6038=CARTESIAN_POINT ( 'NONE',  ( 795.8262568251477660, -214.3726999360618493, 308.3538107759623585 ) ) ;
#6040=EDGE_CURVE ( 'NONE', #40029, #29782, #8281, .T. ) ;
#6044=CARTESIAN_POINT ( 'NONE',  ( 796.7737145352015204, -44.63460265842040542, 370.7187646348536987 ) ) ;
#6045=CARTESIAN_POINT ( 'NONE',  ( 791.3800697268461590, -452.9681489794449476, 362.3092612109132915 ) ) ;
#6048=CARTESIAN_POINT ( 'NONE',  ( 810.4231160770870019, -312.5545181178797520, 321.9338519418446936 ) ) ;
#6049=CARTESIAN_POINT ( 'NONE',  ( 759.2380499001254748, 21.41625977839825978, 318.3449445151863415 ) ) ;
#6050=CARTESIAN_POINT ( 'NONE',  ( 777.4774526936600978, -298.2709662947830793, 304.7301800767027657 ) ) ;
#6054=CARTESIAN_POINT ( 'NONE',  ( 768.0187753319979720, -392.6346026584193396, 318.0580252608186242 ) ) ;
#6055=CARTESIAN_POINT ( 'NONE',  ( 787.5531968255692163, -141.8272453906075157, 316.1348686366205811 ) ) ;
#6057=CARTESIAN_POINT ( 'NONE',  ( 764.3348316497523456, -70.71468719896014932, 308.6759233522265617 ) ) ;
#6058=CARTESIAN_POINT ( 'NONE',  ( 788.8264449731201466, -357.1800572038739574, 363.6646147819170665 ) ) ;
#6062=CARTESIAN_POINT ( 'NONE',  ( 804.4286716492782716, -425.3618753856919170, 345.3141322388244703 ) ) ;
#6067=CARTESIAN_POINT ( 'NONE',  ( 794.9819416627830151, -180.9982390220563389, 319.9864689768909898 ) ) ;
#6068=CARTESIAN_POINT ( 'NONE',  ( 794.9819416627830151, -204.9982390220562820, 319.9864689768909898 ) ) ;
#6073=CARTESIAN_POINT ( 'NONE',  ( 803.6646147819161570, -401.9073299311463643, 348.8264449731210561 ) ) ;
#6075=DIRECTION ( 'NONE',  ( 1.000000000000000000, 0.000000000000000000, 0.000000000000000000 ) ) ;
#6076=EDGE_CURVE ( 'NONE', #35766, #21705, #6448, .T. ) ;
#6078=CARTESIAN_POINT ( 'NONE',  ( 754.9967657858570647, -121.5436935675110561, 365.0032342141425943 ) ) ;
#6085=CARTESIAN_POINT ( 'NONE',  ( 763.0537975583475827, -240.4527844766015221, 371.0346526505627480 ) ) ;
#6086=CARTESIAN_POINT ( 'NONE',  ( 802.7791456095903868, -196.7146871989598083, 329.0155153010375102 ) ) ;
#6088=CARTESIAN_POINT ( 'NONE',  ( 779.9999999999992042, -462.9681489794448339, 339.9999999999999432 ) ) ;
#6095=CARTESIAN_POINT ( 'NONE',  ( 776.2046728542105711, -92.19088175424406018, 304.8212110874238761 ) ) ;
#6103=CARTESIAN_POINT ( 'NONE',  ( 754.7162404726377645, -446.7363362996975980, 339.4709603349214717 ) ) ;
#6104=CARTESIAN_POINT ( 'NONE',  ( 813.5763878283155464, -363.8272453906068336, 351.1614460488615350 ) ) ;
#6111=CARTESIAN_POINT ( 'NONE',  ( 814.2805881961230625, -217.6454272087891582, 331.2368401574024119 ) ) ;
#6113=CARTESIAN_POINT ( 'NONE',  ( 758.8095938919642549, -176.0891481129653755, 311.6929314249763365 ) ) ;
#6116=CARTESIAN_POINT ( 'NONE',  ( 781.8018195045266339, -286.2709662947833635, 365.1927285166406705 ) ) ;
#6117=CARTESIAN_POINT ( 'NONE',  ( 787.5531968255692163, -69.82724539060775726, 316.1348686366205811 ) ) ;
#6122=CARTESIAN_POINT ( 'NONE',  ( 802.7791456095903868, -100.7146871989600356, 329.0155153010375102 ) ) ;
#6123=CARTESIAN_POINT ( 'NONE',  ( 755.5713283507202505, -317.3618753856922581, 334.6858677611754729 ) ) ;
#6126=CARTESIAN_POINT ( 'NONE',  ( 797.6776695296629214, -43.54369356751131903, 357.6776695296636603 ) ) ;
#6129=CARTESIAN_POINT ( 'NONE',  ( 756.1443688327750579, -381.6237781080500326, 314.3581564841659315 ) ) ;
#6131=CARTESIAN_POINT ( 'NONE',  ( 792.1044303154645831, -276.4527844766013800, 317.8323909638837677 ) ) ;
#6132=CARTESIAN_POINT ( 'NONE',  ( 815.2698199232961542, 7.183579159761247723, 342.5225473063383106 ) ) ;
#6134=CARTESIAN_POINT ( 'NONE',  ( 788.8264449731200330, -381.1800572038737869, 363.6646147819171233 ) ) ;
#6136=AXIS2_PLACEMENT_3D ( 'NONE', #41745, #16807, #27880 ) ;
#6142=CARTESIAN_POINT ( 'NONE',  ( 781.7834795799800531, -106.8164208402383935, 315.0636971347436202 ) ) ;
#6143=CARTESIAN_POINT ( 'NONE',  ( 755.1538015810308480, -398.1908817542431507, 343.0433043558613804 ) ) ;
#6144=CARTESIAN_POINT ( 'NONE',  ( 815.2698199232962679, -448.8164208402372424, 342.5225473063383674 ) ) ;
#6146=CARTESIAN_POINT ( 'NONE',  ( 764.3348316497523456, -358.7146871989592114, 308.6759233522265617 ) ) ;
#6147=CARTESIAN_POINT ( 'NONE',  ( 756.1443688327750579, -117.6237781080509279, 314.3581564841659315 ) ) ;
#6151=CARTESIAN_POINT ( 'NONE',  ( 773.7305795820266212, -9.281790845153418346, 374.8230680027170365 ) ) ;
#6157=LINE ( 'NONE', #1765, #15302 ) ;
#6159=CARTESIAN_POINT ( 'NONE',  ( 755.5913626894240451, -325.6454272087888739, 346.6156483768012890 ) ) ;
#6161=CARTESIAN_POINT ( 'NONE',  ( 795.8262568251477660, -310.3726999360616219, 308.3538107759623585 ) ) ;
#6163=DIRECTION ( 'NONE',  ( -1.000000000000000000, -0.000000000000000000, -0.000000000000000000 ) ) ;
#6164=CARTESIAN_POINT ( 'NONE',  ( 815.3608509340175488, -122.7363362996985074, 341.2497674668889545 ) ) ;
#6168=CARTESIAN_POINT ( 'NONE',  ( 771.2633955100217236, -143.9073299311473590, 363.4237431249939618 ) ) ;
#6171=CARTESIAN_POINT ( 'NONE',  ( 797.8822607201568644, -414.5545181178795247, 370.1134526219340160 ) ) ;
#6175=CARTESIAN_POINT ( 'NONE',  ( 790.0220218866281812, -55.09997266333508747, 363.2186876482849129 ) ) ;
#6178=CARTESIAN_POINT ( 'NONE',  ( 798.0661480581538854, 21.46713098285774279, 309.5768839229118043 ) ) ;
#6179=EDGE_LOOP ( 'NONE', ( #8966, #14743, #44375, #33457 ) ) ;
#6182=CARTESIAN_POINT ( 'NONE',  ( 778.7502325331095108, -288.3510508353231216, 304.6391490659818828 ) ) ;
#6183=CARTESIAN_POINT ( 'NONE',  ( 767.8955696845334842, -96.45278447660204790, 362.1676090361161755 ) ) ;
#6186=CARTESIAN_POINT ( 'NONE',  ( 804.4286716492782716, -281.3618753856923718, 345.3141322388244703 ) ) ;
#6192=CARTESIAN_POINT ( 'NONE',  ( 782.5225473063383106, -358.2709662947830225, 375.2698199232970637 ) ) ;
#6193=CARTESIAN_POINT ( 'NONE',  ( 768.8385539511368734, -263.2601417444141134, 306.4236121716840557 ) ) ;
#6198=CARTESIAN_POINT ( 'NONE',  ( 756.5762568750052424, -243.1800572038743269, 348.7366044899774238 ) ) ;
#6200=CARTESIAN_POINT ( 'NONE',  ( 758.8095938919642549, -368.0891481129647786, 311.6929314249763365 ) ) ;
#6203=CARTESIAN_POINT ( 'NONE',  ( 788.0874520139973356, 16.45630643248838609, 314.0623709945898554 ) ) ;
#6205=CARTESIAN_POINT ( 'NONE',  ( 757.4527132478984868, -232.3726999360617924, 329.1273215169538844 ) ) ;
#6206=CARTESIAN_POINT ( 'NONE',  ( 764.8639956371174549, -128.0891481129655176, 319.7806653035542013 ) ) ;
#6210=CARTESIAN_POINT ( 'NONE',  ( 802.7791456095903868, -244.7146871989596093, 329.0155153010375102 ) ) ;
#6214=CARTESIAN_POINT ( 'NONE',  ( 793.3938497862117174, -453.0432664090020012, 372.3358127763067955 ) ) ;
#6218=CARTESIAN_POINT ( 'NONE',  ( 745.7998596910086917, -101.3618753856929544, 332.5602148656461168 ) ) ;
#6219=CARTESIAN_POINT ( 'NONE',  ( 815.2698199232961542, -184.8164208402380950, 342.5225473063383106 ) ) ;
#6223=CARTESIAN_POINT ( 'NONE',  ( 773.7305795820266212, -417.2817908451522158, 374.8230680027170365 ) ) ;
#6226=CARTESIAN_POINT ( 'NONE',  ( 744.7301800767019131, -388.8164208402374129, 337.4774526936615757 ) ) ;
#6227=CARTESIAN_POINT ( 'NONE',  ( 772.4837098697145166, 0.6381246143067237364, 374.5518280994205611 ) ) ;
#6230=CARTESIAN_POINT ( 'NONE',  ( 764.0069404352550464, -15.07832356259669560, 359.2566176426627180 ) ) ;
#6231=AXIS2_PLACEMENT_3D ( 'NONE', #9528, #43942, #16447 ) ;
#6234=CARTESIAN_POINT ( 'NONE',  ( 761.9338519418445230, -182.5328690171416497, 370.4231160770881957 ) ) ;
#6237=CARTESIAN_POINT ( 'NONE',  ( 771.2368401574024119, -181.4419599262325278, 374.2805881961240857 ) ) ;
#6242=CARTESIAN_POINT ( 'NONE',  ( 781.8018195045266339, -166.2709662947835909, 365.1927285166406705 ) ) ;
#6244=CARTESIAN_POINT ( 'NONE',  ( 755.5713283507202505, -293.3618753856923718, 334.6858677611754729 ) ) ;
#6245=CARTESIAN_POINT ( 'NONE',  ( 785.3141322388236176, -285.7255117493286889, 364.4286716492789537 ) ) ;
#6248=CARTESIAN_POINT ( 'NONE',  ( 783.0433043558608688, -24.89650538077847486, 315.1538015810313027 ) ) ;
#6250=AXIS2_PLACEMENT_3D ( 'NONE', #27206, #16590, #30672 ) ;
#6253=CARTESIAN_POINT ( 'NONE',  ( 745.0891759886404770, -220.2709662947834772, 342.4968714119734159 ) ) ;
#6254=CARTESIAN_POINT ( 'NONE',  ( 786.5483106153019435, -343.6454272087887603, 364.1601925771022366 ) ) ;
#6256=CARTESIAN_POINT ( 'NONE',  ( 804.1601925771018387, -439.4419599262316751, 346.5483106153029098 ) ) ;
#6262=CARTESIAN_POINT ( 'NONE',  ( 763.2154366446407039, -285.6237781080502600, 321.4292242960311228 ) ) ;
#6265=AXIS2_PLACEMENT_3D ( 'NONE', #5840, #30781, #19926 ) ;
#6266=CARTESIAN_POINT ( 'NONE',  ( 786.5483106153019435, -127.6454272087894140, 364.1601925771022366 ) ) ;
#6268=ORIENTED_EDGE ( 'NONE', *, *, #138, .T. ) ;
#6271=CARTESIAN_POINT ( 'NONE',  ( 781.2370466360911223, -236.7363362996981380, 304.9990715423533629 ) ) ;
#6277=CARTESIAN_POINT ( 'NONE',  ( 812.7932403749906598, -63.18005720387488822, 327.7687537140311633 ) ) ;
#6278=CARTESIAN_POINT ( 'NONE',  ( 807.0960494954803153, -452.9681489794450613, 341.9322302743943851 ) ) ;
#6283=CARTESIAN_POINT ( 'NONE',  ( 788.6739635108323228, -319.6454272087888739, 373.9316612368139090 ) ) ;
#6284=CARTESIAN_POINT ( 'NONE',  ( 804.7487373415286811, -283.5436935675105019, 364.7487373415288516 ) ) ;
#6290=CARTESIAN_POINT ( 'NONE',  ( 767.8955696845333705, -384.4527844766011526, 362.1676090361162323 ) ) ;
#6291=CARTESIAN_POINT ( 'NONE',  ( 757.4527132478984868, -160.3726999360620482, 329.1273215169538844 ) ) ;
#6293=CARTESIAN_POINT ( 'NONE',  ( 810.1134526219336749, -56.53286901714201917, 357.8822607201570349 ) ) ;
#6294=CARTESIAN_POINT ( 'NONE',  ( 757.8323909638828582, -362.6346026584193964, 352.1044303154654358 ) ) ;
#6296=DIRECTION ( 'NONE',  ( -0.000000000000000000, 1.000000000000000000, -0.000000000000000000 ) ) ;
#6297=CARTESIAN_POINT ( 'NONE',  ( 746.0683387631852383, -139.4419599262326699, 331.3260364891676204 ) ) ;
#6298=CARTESIAN_POINT ( 'NONE',  ( 803.4237431249931660, -447.1800572038736732, 331.2633955100225194 ) ) ;
#6302=CARTESIAN_POINT ( 'NONE',  ( 804.6798772138708955, -207.7255117493289447, 334.6312213355107019 ) ) ;
#6303=CARTESIAN_POINT ( 'NONE',  ( 756.3353852180820240, -173.9073299311472454, 331.1735550268787733 ) ) ;
#6308=CARTESIAN_POINT ( 'NONE',  ( 756.5762568750052424, -387.1800572038738437, 348.7366044899774238 ) ) ;
#6310=EDGE_CURVE ( 'NONE', #6, #26042, #34965, .T. ) ;
#6311=EDGE_LOOP ( 'NONE', ( #29313, #22494, #1938, #24019 ) ) ;
#6313=AXIS2_PLACEMENT_3D ( 'NONE', #11902, #1049, #25075 ) ;
#6315=CARTESIAN_POINT ( 'NONE',  ( 767.6429770376291799, -129.1800572038746679, 306.8695393053162093 ) ) ;
#6320=MECHANICAL_DESIGN_GEOMETRIC_PRESENTATION_REPRESENTATION('',(#1887),#7831);
#6321=CARTESIAN_POINT ( 'NONE',  ( 764.0069404352550464, -183.0783235625961538, 359.2566176426627180 ) ) ;
#6332=CARTESIAN_POINT ( 'NONE',  ( 746.4236121716829757, -87.82724539060770041, 328.8385539511384650 ) ) ;
#6341=CARTESIAN_POINT ( 'NONE',  ( 763.8424801807145741, -450.0090635724248500, 320.5453621957614700 ) ) ;
#6346=DIRECTION ( 'NONE',  ( 0.000000000000000000, 1.000000000000000000, 1.056348263647623421E-15 ) ) ;
#6350=CARTESIAN_POINT ( 'NONE',  ( 788.6739635108323228, -199.6454272087891582, 373.9316612368139090 ) ) ;
#6352=CARTESIAN_POINT ( 'NONE',  ( 749.2812353651451076, -174.4527844766018063, 323.2262854647983090 ) ) ;
#6358=CARTESIAN_POINT ( 'NONE',  ( 792.1044303154645831, -300.4527844766012663, 317.8323909638837677 ) ) ;
#6359=CARTESIAN_POINT ( 'NONE',  ( 780.5236548040995785, -44.73633629969875614, 314.9735926884559944 ) ) ;
#6362=CARTESIAN_POINT ( 'NONE',  ( 799.9999999999993179, 205.0000000000000568, 329.9999999999999432 ) ) ;
#6364=CARTESIAN_POINT ( 'NONE',  ( 798.7617431975189675, -123.6237781080508569, 323.0428371773161871 ) ) ;
#6365=CARTESIAN_POINT ( 'NONE',  ( 758.0580252608178853, -318.4527844766014368, 328.0187753319985404 ) ) ;
#6370=CARTESIAN_POINT ( 'NONE',  ( 788.8264449731200330, -93.18005720387481006, 363.6646147819171233 ) ) ;
#6373=CARTESIAN_POINT ( 'NONE',  ( 781.2497674668890113, -396.3510508353228374, 375.3608509340180603 ) ) ;
#6376=CARTESIAN_POINT ( 'NONE',  ( 764.8639956371174549, -272.0891481129651197, 319.7806653035542013 ) ) ;
#6380=CARTESIAN_POINT ( 'NONE',  ( 759.9864689768902508, -362.0891481129648923, 354.9819416627836404 ) ) ;
#6387=CARTESIAN_POINT ( 'NONE',  ( 804.4286716492782716, -137.3618753856928265, 345.3141322388244703 ) ) ;
#6388=CARTESIAN_POINT ( 'NONE',  ( 758.4439275373578084, -396.5545181178794678, 353.2243759319684386 ) ) ;
#6390=CARTESIAN_POINT ( 'NONE',  ( 810.7187646348534145, -450.4527844766009821, 356.7737145352016341 ) ) ;
#6392=CARTESIAN_POINT ( 'NONE',  ( 759.8311093483677041, -358.1692326535047641, 310.9282345327691814 ) ) ;
#6397=CARTESIAN_POINT ( 'NONE',  ( 797.8822607201568644, -6.554518117880697048, 370.1134526219340160 ) ) ;
#6405=CARTESIAN_POINT ( 'NONE',  ( 754.7162404726377645, -326.7363362996979390, 339.4709603349214717 ) ) ;
#6407=CARTESIAN_POINT ( 'NONE',  ( 755.8990559732751535, -299.4636090269707438, 365.9055244015606831 ) ) ;
#6410=CARTESIAN_POINT ( 'NONE',  ( 814.2805881961230625, -121.6454272087894282, 331.2368401574024119 ) ) ;
#6414=CARTESIAN_POINT ( 'NONE',  ( 792.1044303154645831, -180.4527844766017211, 317.8323909638837677 ) ) ;
#6416=CARTESIAN_POINT ( 'NONE',  ( 786.2694204179717872, -429.2817908451521021, 305.1769319972829067 ) ) ;
#6418=VECTOR ( 'NONE', #44154, 1000.000000000000000 ) ;
#6420=CARTESIAN_POINT ( 'NONE',  ( 796.1575198192839480, -54.00906357242601530, 359.4546378042384163 ) ) ;
#6423=CARTESIAN_POINT ( 'NONE',  ( 803.2186876482843445, -415.9874144716862361, 350.0220218866286928 ) ) ;
#6425=CARTESIAN_POINT ( 'NONE',  ( 762.1405469898971887, -265.5436935675106156, 357.8594530101015607 ) ) ;
#6429=CARTESIAN_POINT ( 'NONE',  ( 813.9316612368132837, -271.4419599262321867, 348.6739635108323228 ) ) ;
#6430=CARTESIAN_POINT ( 'NONE',  ( 788.7366044899766848, -107.9073299311474727, 316.5762568750059813 ) ) ;
#6434=CARTESIAN_POINT ( 'NONE',  ( 795.1360043628807261, -284.0891481129650629, 360.2193346964456282 ) ) ;
#6441=CARTESIAN_POINT ( 'NONE',  ( 814.5518280994195948, -351.7255117493284615, 332.4837098697145166 ) ) ;
#6442=CARTESIAN_POINT ( 'NONE',  ( 814.8230680027162407, -269.8055962898686175, 333.7305795820267917 ) ) ;
#6447=CARTESIAN_POINT ( 'NONE',  ( 755.3201227861273992, -243.7255117493287742, 345.3687786644892981 ) ) ;
#6448=CIRCLE ( 'NONE', #33008, 10.00000000000000888 ) ;
#6449=CARTESIAN_POINT ( 'NONE',  ( 787.4397851343537695, -357.7255117493285184, 374.2001403089903988 ) ) ;
#6454=CARTESIAN_POINT ( 'NONE',  ( 780.5236548040995785, -236.7363362996981380, 314.9735926884559944 ) ) ;
#6455=CARTESIAN_POINT ( 'NONE',  ( 797.8594530101008786, -133.5436935675110135, 322.1405469898980982 ) ) ;
#6456=EDGE_LOOP ( 'NONE', ( #37914, #41071, #7295, #41535 ) ) ;
#6459=CARTESIAN_POINT ( 'NONE',  ( 755.0488828828309806, -281.8055962898686175, 344.1219089521771934 ) ) ;
#6463=CARTESIAN_POINT ( 'NONE',  ( 795.1271208383656131, -452.8379544210779954, 371.6178728169206238 ) ) ;
#6465=CARTESIAN_POINT ( 'NONE',  ( 800.9747183278959710, -84.99823902205663728, 311.9810565676471583 ) ) ;
#6466=CARTESIAN_POINT ( 'NONE',  ( 787.4397851343537695, -165.7255117493291152, 374.2001403089903988 ) ) ;
#6470=CARTESIAN_POINT ( 'NONE',  ( 802.2119215644370342, -414.0090635724249637, 367.5423716828165084 ) ) ;
#6473=CARTESIAN_POINT ( 'NONE',  ( 745.4481719005789273, -387.7255117493283478, 347.5162901302853129 ) ) ;
#6474=CARTESIAN_POINT ( 'NONE',  ( 751.9810565676468741, -26.08914811296592262, 360.9747183278973921 ) ) ;
#6476=CARTESIAN_POINT ( 'NONE',  ( 769.1273215169530886, -22.71468719896029853, 317.4527132478988847 ) ) ;
#6479=CARTESIAN_POINT ( 'NONE',  ( 751.2241431872005251, -160.1692326535053326, 359.9636004259367610 ) ) ;
#6480=DIRECTION ( 'NONE',  ( 0.000000000000000000, -1.000000000000000000, 0.000000000000000000 ) ) ;
#6484=CARTESIAN_POINT ( 'NONE',  ( 759.7806653035534055, -150.9982390220563957, 324.8639956371180801 ) ) ;
#6486=CARTESIAN_POINT ( 'NONE',  ( 792.1044303154646968, -300.4527844766013231, 317.8323909638837677 ) ) ;
#6489=CARTESIAN_POINT ( 'NONE',  ( 764.0069404352550464, -15.07832356259669560, 359.2566176426627180 ) ) ;
#6492=CARTESIAN_POINT ( 'NONE',  ( 777.5031285880264704, -238.8164208402379813, 374.9108240113588408 ) ) ;
#6493=CARTESIAN_POINT ( 'NONE',  ( 757.0176451133909268, -325.0999726633342561, 349.9200121543848354 ) ) ;
#6494=CARTESIAN_POINT ( 'NONE',  ( 761.2382568024794409, -423.6237781080499190, 356.9571628226838129 ) ) ;
#6499=CARTESIAN_POINT ( 'NONE',  ( 755.8398074228967971, -331.4419599262320162, 333.4516893846970333 ) ) ;
#6501=CARTESIAN_POINT ( 'NONE',  ( 805.2837595273609850, -122.7363362996985074, 340.5290396650784714 ) ) ;
#6502=CARTESIAN_POINT ( 'NONE',  ( 758.0580252608178853, -6.452784476602343666, 328.0187753319985404 ) ) ;
#6507=CARTESIAN_POINT ( 'NONE',  ( 786.5483106153019435, -223.6454272087891013, 364.1601925771022366 ) ) ;
#6508=CARTESIAN_POINT ( 'NONE',  ( 813.5763878283155464, -243.8272453906072030, 351.1614460488615350 ) ) ;
#6509=CARTESIAN_POINT ( 'NONE',  ( 803.2186876482843445, -175.9874144716871172, 350.0220218866286928 ) ) ;
#6516=CARTESIAN_POINT ( 'NONE',  ( 804.1009440267234822, -359.4636090269705164, 314.0944755984392600 ) ) ;
#6518=CARTESIAN_POINT ( 'NONE',  ( 746.8695393053150156, -293.9073299311468759, 327.6429770376306010 ) ) ;
#6522=CARTESIAN_POINT ( 'NONE',  ( 803.4237431249931660, -399.1800572038738437, 331.2633955100225194 ) ) ;
#6523=CARTESIAN_POINT ( 'NONE',  ( 769.0155153010367712, -154.3726999360620198, 362.7791456095907279 ) ) ;
#6525=CARTESIAN_POINT ( 'NONE',  ( 808.7758568127978833, -76.16923265350557415, 320.0363995740631822 ) ) ;
#6526=CARTESIAN_POINT ( 'NONE',  ( 788.8264449731201466, -381.1800572038739006, 363.6646147819170665 ) ) ;
#6528=CARTESIAN_POINT ( 'NONE',  ( 762.3223304703356007, -415.5436935675102177, 322.3223304703362828 ) ) ;
#6532=CARTESIAN_POINT ( 'NONE',  ( 759.9864689768902508, -194.0891481129654039, 354.9819416627836404 ) ) ;
#6533=CARTESIAN_POINT ( 'NONE',  ( 778.1981804954715471, -178.2709662947835909, 314.8072714833591021 ) ) ;
#6535=DIRECTION ( 'NONE',  ( 0.000000000000000000, 0.000000000000000000, 1.000000000000000000 ) ) ;
#6537=CARTESIAN_POINT ( 'NONE',  ( 785.3141322388236176, -405.7255117493283478, 364.4286716492789537 ) ) ;
#6541=CARTESIAN_POINT ( 'NONE',  ( 815.2698199232962679, -136.8164208402382656, 342.5225473063383674 ) ) ;
#6549=CARTESIAN_POINT ( 'NONE',  ( 793.2243759319678702, -194.5328690171415644, 318.4439275373583200 ) ) ;
#6550=DIRECTION ( 'NONE',  ( 0.000000000000000000, 0.000000000000000000, 1.000000000000000000 ) ) ;
#6559=CARTESIAN_POINT ( 'NONE',  ( 814.8207195650702488, -122.1908817542439749, 336.2433038121456548 ) ) ;
#6566=CARTESIAN_POINT ( 'NONE',  ( 814.4686193811664907, -387.2817908451522726, 346.2056067578752732 ) ) ;
#6572=CARTESIAN_POINT ( 'NONE',  ( 773.7305795820266212, -201.2817908451528126, 374.8230680027170365 ) ) ;
#6574=CARTESIAN_POINT ( 'NONE',  ( 808.0189434323515343, -182.0891481129654323, 319.0252816721025511 ) ) ;
#6578=CARTESIAN_POINT ( 'NONE',  ( 800.2193346964447755, -282.9982390220558841, 355.1360043628815788 ) ) ;
#6579=CARTESIAN_POINT ( 'NONE',  ( 757.4527132478984868, -64.37269993606231822, 329.1273215169538844 ) ) ;
#6584=CARTESIAN_POINT ( 'NONE',  ( 780.5290396650775619, -132.3510508353235764, 365.2837595273619513 ) ) ;
#6585=CARTESIAN_POINT ( 'NONE',  ( 788.8264449731200330, -333.1800572038740142, 363.6646147819171233 ) ) ;
#6586=EDGE_LOOP ( 'NONE', ( #9517, #24298, #13776, #21381 ) ) ;
#6588=CARTESIAN_POINT ( 'NONE',  ( 758.0580252608178853, -102.4527844766020337, 328.0187753319985404 ) ) ;
#6591=CARTESIAN_POINT ( 'NONE',  ( 747.3154664389472828, -403.9874144716863498, 326.4474001241230781 ) ) ;
#6593=CARTESIAN_POINT ( 'NONE',  ( 774.6858677611749044, -297.7255117493286889, 315.5713283507209894 ) ) ;
#6597=CARTESIAN_POINT ( 'NONE',  ( 792.1044303154645831, -420.4527844766009252, 317.8323909638837677 ) ) ;
#6598=ADVANCED_FACE ( 'NONE', ( #16746, #9803 ), #20867, .F. ) ;
#6604=CARTESIAN_POINT ( 'NONE',  ( 768.0187753319979720, -128.6346026584201354, 318.0580252608186242 ) ) ;
#6605=CARTESIAN_POINT ( 'NONE',  ( 793.9708237608222134, -454.9181544815156713, 319.2295555964448681 ) ) ;
#6606=CARTESIAN_POINT ( 'NONE',  ( 796.7845633553578182, -105.6237781080509421, 358.5707757039688204 ) ) ;
#6609=DIRECTION ( 'NONE',  ( -0.000000000000000000, -1.000000000000000000, 0.000000000000000000 ) ) ;
#6610=CARTESIAN_POINT ( 'NONE',  ( 766.5853460496234675, -373.9874144716864066, 372.3518521366060554 ) ) ;
#6617=CARTESIAN_POINT ( 'NONE',  ( 814.4686193811664907, -27.28179084515336328, 346.2056067578752732 ) ) ;
#6624=CARTESIAN_POINT ( 'NONE',  ( 758.4439275373578084, -348.5545181178796383, 353.2243759319684386 ) ) ;
#6625=CARTESIAN_POINT ( 'NONE',  ( 752.7379699480933368, -300.0090635724252479, 361.9858362298580232 ) ) ;
#6629=CARTESIAN_POINT ( 'NONE',  ( 804.1009440267234822, -95.46360902697132644, 314.0944755984392600 ) ) ;
#6632=DIRECTION ( 'NONE',  ( -1.000000000000000000, -0.000000000000000000, 0.000000000000000000 ) ) ;
#6634=CARTESIAN_POINT ( 'NONE',  ( 755.3201227861273992, -171.7255117493291152, 345.3687786644892981 ) ) ;
#6636=CARTESIAN_POINT ( 'NONE',  ( 783.7953271457878373, -416.1908817542430938, 375.1787889125761239 ) ) ;
#6639=CARTESIAN_POINT ( 'NONE',  ( 761.4292242960306112, -65.46360902697142592, 323.2154366446414429 ) ) ;
#6642=CARTESIAN_POINT ( 'NONE',  ( 768.8385539511368734, 0.7398582555850804487, 306.4236121716840557 ) ) ;
#6646=CARTESIAN_POINT ( 'NONE',  ( 759.8311093483677041, -262.1692326535049347, 310.9282345327691814 ) ) ;
#6647=CARTESIAN_POINT ( 'NONE',  ( 764.8639956371174549, -104.0891481129656739, 319.7806653035542581 ) ) ;
#6650=CARTESIAN_POINT ( 'NONE',  ( 755.5713283507202505, -293.3618753856923718, 334.6858677611754729 ) ) ;
#6653=FACE_OUTER_BOUND ( 'NONE', #30548, .T. ) ;
#6656=CARTESIAN_POINT ( 'NONE',  ( 800.2193346964447755, -18.99823902205683979, 355.1360043628815788 ) ) ;
#6659=CARTESIAN_POINT ( 'NONE',  ( 746.8695393053151292, -365.9073299311466485, 327.6429770376306578 ) ) ;
#6660=CARTESIAN_POINT ( 'NONE',  ( 803.8556311672234642, -249.6237781080505158, 365.6418435158340117 ) ) ;
#6666=CARTESIAN_POINT ( 'NONE',  ( 802.1676090361156639, -230.6346026584197659, 327.8955696845344505 ) ) ;
#6667=CARTESIAN_POINT ( 'NONE',  ( 763.0537975583475827, -360.4527844766010958, 371.0346526505627480 ) ) ;
#6672=CARTESIAN_POINT ( 'NONE',  ( 760.7433823573367135, -228.0090635724254753, 355.9930595647440441 ) ) ;
#6673=CARTESIAN_POINT ( 'NONE',  ( 788.7366044899766848, -131.9073299311473875, 316.5762568750059813 ) ) ;
#6677=CARTESIAN_POINT ( 'NONE',  ( 784.0799538623451781, -275.8055962898685038, 364.6971507214555572 ) ) ;
#6680=CARTESIAN_POINT ( 'NONE',  ( 749.5768839229115201, -12.55451811788067751, 358.0661480581553064 ) ) ;
#6682=CARTESIAN_POINT ( 'NONE',  ( 800.9747183278959710, -180.9982390220563389, 311.9810565676471583 ) ) ;
#6683=CARTESIAN_POINT ( 'NONE',  ( 795.1360043628807261, -92.08914811296568814, 360.2193346964456282 ) ) ;
#6687=CARTESIAN_POINT ( 'NONE',  ( 814.8207195650702488, -434.1908817542430370, 336.2433038121456548 ) ) ;
#6690=CARTESIAN_POINT ( 'NONE',  ( 751.6929314249748586, -390.9982390220557136, 318.8095938919659034 ) ) ;
#6691=CARTESIAN_POINT ( 'NONE',  ( 813.1304606946831655, -41.90732993114767879, 352.3570229623691716 ) ) ;
#6693=CARTESIAN_POINT ( 'NONE',  ( 754.9735926884551418, -18.35105083532395298, 340.5236548041000333 ) ) ;
#6696=CARTESIAN_POINT ( 'NONE',  ( 801.9858362298568863, -171.0783235625962106, 312.7379699480935642 ) ) ;
#6697=CARTESIAN_POINT ( 'NONE',  ( 764.8639956371174549, -8.089148112965974136, 319.7806653035542581 ) ) ;
#6703=CARTESIAN_POINT ( 'NONE',  ( 756.5762568750052424, -171.1800572038745543, 348.7366044899774238 ) ) ;
#6705=CARTESIAN_POINT ( 'NONE',  ( 774.6858677611749044, -345.7255117493285184, 315.5713283507209894 ) ) ;
#6707=ORIENTED_EDGE ( 'NONE', *, *, #37624, .T. ) ;
#6708=CARTESIAN_POINT ( 'NONE',  ( 786.6156483768007774, -1.441959926233096656, 315.5913626894246136 ) ) ;
#6710=CARTESIAN_POINT ( 'NONE',  ( 787.5162901302840055, -251.3618753856923718, 305.4481719005793252 ) ) ;
#6711=CARTESIAN_POINT ( 'NONE',  ( 769.0155153010367712, -346.3726999360614514, 362.7791456095907279 ) ) ;
#6712=CARTESIAN_POINT ( 'NONE',  ( 764.0069404352550464, -423.0783235625953580, 359.2566176426627180 ) ) ;
#6717=ORIENTED_EDGE ( 'NONE', *, *, #30074, .T. ) ;
#6719=CARTESIAN_POINT ( 'NONE',  ( 756.7813123517142913, -331.9874144716865203, 329.9779781133712504 ) ) ;
#6721=CARTESIAN_POINT ( 'NONE',  ( 755.3028492785439312, -111.2817908451530968, 335.9200461376539693 ) ) ;
#6722=CARTESIAN_POINT ( 'NONE',  ( 754.8072714833581358, -4.816420840238714085, 338.1981804954720587 ) ) ;
#6726=CARTESIAN_POINT ( 'NONE',  ( 769.0155153010367712, -226.3726999360617924, 362.7791456095907279 ) ) ;
#6727=CARTESIAN_POINT ( 'NONE',  ( 797.8822607201568644, -222.5545181178800362, 370.1134526219340160 ) ) ;
#6728=CARTESIAN_POINT ( 'NONE',  ( 773.3843516231979720, -181.4419599262325278, 364.4086373105754433 ) ) ;
#6732=CARTESIAN_POINT ( 'NONE',  ( 782.5225473063381969, -22.27096629478410250, 375.2698199232970637 ) ) ;
#6733=CARTESIAN_POINT ( 'NONE',  ( 772.4837098697144029, -71.36187538569302546, 374.5518280994205611 ) ) ;
#6734=CARTESIAN_POINT ( 'NONE',  ( 792.6815175455323015, -452.9681489794447202, 361.6124358662449367 ) ) ;
#6737=CARTESIAN_POINT ( 'NONE',  ( 778.7629533639073998, -368.7363362996977685, 375.0009284576466371 ) ) ;
#6739=CARTESIAN_POINT ( 'NONE',  ( 810.7187646348534145, -282.4527844766014937, 356.7737145352016341 ) ) ;
#6743=CARTESIAN_POINT ( 'NONE',  ( 759.9864689768902508, -386.0891481129647786, 354.9819416627836404 ) ) ;
#6745=CARTESIAN_POINT ( 'NONE',  ( 786.5483106153019435, -151.6454272087892718, 364.1601925771022366 ) ) ;
#6748=CARTESIAN_POINT ( 'NONE',  ( 746.0683387631852383, -67.44195992623289726, 331.3260364891676204 ) ) ;
#6749=CARTESIAN_POINT ( 'NONE',  ( 778.1981804954715471, -394.2709662947829088, 314.8072714833591021 ) ) ;
#6750=CARTESIAN_POINT ( 'NONE',  ( 796.9462024416508257, 11.54721552339759860, 308.9653473494370246 ) ) ;
#6752=CARTESIAN_POINT ( 'NONE',  ( 759.8311093483677041, -142.1692326535054178, 310.9282345327691814 ) ) ;
#6753=CARTESIAN_POINT ( 'NONE',  ( 759.7806653035534055, -414.9982390220555430, 324.8639956371180801 ) ) ;
#6758=CARTESIAN_POINT ( 'NONE',  ( 781.7834795799800531, -226.8164208402380098, 315.0636971347436202 ) ) ;
#6759=CARTESIAN_POINT ( 'NONE',  ( 794.9819416627830151, -180.9982390220563389, 319.9864689768909898 ) ) ;
#6763=VERTEX_POINT ( 'NONE', #28960 ) ;
#6764=CARTESIAN_POINT ( 'NONE',  ( 767.8955696845333705, -408.4527844766009252, 362.1676090361162323 ) ) ;
#6767=CARTESIAN_POINT ( 'NONE',  ( 805.0032342141413437, -157.5436935675109282, 314.9967657858572352 ) ) ;
#6773=CARTESIAN_POINT ( 'NONE',  ( 801.3366627262608972, -224.5328690171415076, 353.0897708529566899 ) ) ;
#6779=CARTESIAN_POINT ( 'NONE',  ( 759.9999999999992042, -512.9681489794448908, 339.9999999999999432 ) ) ;
#6782=CARTESIAN_POINT ( 'NONE',  ( 807.2620300519052989, -144.0090635724257027, 318.0141637701419768 ) ) ;
#6789=CARTESIAN_POINT ( 'NONE',  ( 747.6481478633932056, -373.0999726633340856, 353.4146539503763620 ) ) ;
#6794=CARTESIAN_POINT ( 'NONE',  ( 762.3223304703356007, 16.45630643248849267, 322.3223304703362828 ) ) ;
#6796=CARTESIAN_POINT ( 'NONE',  ( 814.8207195650702488, -242.1908817542435770, 336.2433038121456548 ) ) ;
#6798=CARTESIAN_POINT ( 'NONE',  ( 772.5602148656447525, -177.7255117493290868, 305.7998596910095443 ) ) ;
#6801=CARTESIAN_POINT ( 'NONE',  ( 801.9419747391806368, -282.4527844766014937, 351.9812246680014027 ) ) ;
#6802=CARTESIAN_POINT ( 'NONE',  ( 754.7162404726377645, -86.73633629969862113, 339.4709603349214717 ) ) ;
#6805=CARTESIAN_POINT ( 'NONE',  ( 787.4999999999992042, -462.9681489794448339, 370.0000000000000568 ) ) ;
#6806=CARTESIAN_POINT ( 'NONE',  ( 763.2154366446407039, -117.6237781080509279, 321.4292242960311228 ) ) ;
#6807=CARTESIAN_POINT ( 'NONE',  ( 781.8018195045266339, -334.2709662947829656, 365.1927285166406705 ) ) ;
#6810=CARTESIAN_POINT ( 'NONE',  ( 759.7806653035534055, -102.9982390220565520, 324.8639956371180801 ) ) ;
#6814=CARTESIAN_POINT ( 'NONE',  ( 752.4576283171824116, -405.0783235625954148, 317.7880784355627952 ) ) ;
#6816=CARTESIAN_POINT ( 'NONE',  ( 774.6858677611749044, -273.7255117493288026, 315.5713283507209894 ) ) ;
#6820=CARTESIAN_POINT ( 'NONE',  ( 774.6858677611749044, -417.7255117493283478, 315.5713283507209894 ) ) ;
#6825=CARTESIAN_POINT ( 'NONE',  ( 778.2165204200184689, -118.8164208402383508, 364.9363028652563230 ) ) ;
#6826=CARTESIAN_POINT ( 'NONE',  ( 799.2566176426618085, -432.0090635724247932, 324.0069404352559559 ) ) ;
#6827=CARTESIAN_POINT ( 'NONE',  ( 763.2154366446407039, -117.6237781080509279, 321.4292242960311228 ) ) ;
#6830=CARTESIAN_POINT ( 'NONE',  ( 803.8556311672234642, -345.6237781080501463, 365.6418435158340117 ) ) ;
#6836=CARTESIAN_POINT ( 'NONE',  ( 807.2620300519052989, -24.00906357242609346, 318.0141637701419768 ) ) ;
#6844=CARTESIAN_POINT ( 'NONE',  ( 769.9779781133707957, -379.0999726633341993, 316.7813123517150871 ) ) ;
#6845=CARTESIAN_POINT ( 'NONE',  ( 791.0478386215596629, -333.8272453906070041, 306.7653713866226326 ) ) ;
#6848=CARTESIAN_POINT ( 'NONE',  ( 745.5313806188320314, -159.2817908451529547, 333.7943932421247268 ) ) ;
#6853=CARTESIAN_POINT ( 'NONE',  ( 788.7366044899766848, -179.9073299311472454, 316.5762568750059813 ) ) ;
#6855=CARTESIAN_POINT ( 'NONE',  ( 807.2620300519052989, -408.0090635724249069, 318.0141637701419768 ) ) ;
#6860=CARTESIAN_POINT ( 'NONE',  ( 807.5423716828161105, -9.078323562596708030, 362.2119215644372048 ) ) ;
#6863=CIRCLE ( 'NONE', #34887, 30.00000000000008171 ) ;
#6866=CARTESIAN_POINT ( 'NONE',  ( 800.1688906516307043, -298.1692326535049347, 369.0717654672308186 ) ) ;
#6867=CARTESIAN_POINT ( 'NONE',  ( 804.9363028652555840, -112.2709662947838325, 338.2165204200192079 ) ) ;
#6868=CARTESIAN_POINT ( 'NONE',  ( 814.2001403089898304, -41.36187538569314626, 347.4397851343538264 ) ) ;
#6870=CARTESIAN_POINT ( 'NONE',  ( 801.9419747391806368, -306.4527844766013800, 351.9812246680014027 ) ) ;
#6880=CARTESIAN_POINT ( 'NONE',  ( 803.4237431249931660, -15.18005720387504631, 331.2633955100225194 ) ) ;
#6882=CARTESIAN_POINT ( 'NONE',  ( 796.7737145352015204, -356.6346026584193964, 370.7187646348536987 ) ) ;
#6883=CARTESIAN_POINT ( 'NONE',  ( 801.9858362298568863, -243.0783235625959833, 312.7379699480935642 ) ) ;
#6884=CARTESIAN_POINT ( 'NONE',  ( 815.0009284576459549, -78.35105083532376113, 338.7629533639073429 ) ) ;
#6889=CARTESIAN_POINT ( 'NONE',  ( 795.1360043628807261, -236.0891481129651766, 360.2193346964456282 ) ) ;
#6891=CARTESIAN_POINT ( 'NONE',  ( 749.2812353651451076, -390.4527844766011526, 323.2262854647983090 ) ) ;
#6896=CARTESIAN_POINT ( 'NONE',  ( 763.8424801807145741, -258.0090635724253616, 320.5453621957614700 ) ) ;
#6897=CARTESIAN_POINT ( 'NONE',  ( 781.8018195045266339, -118.2709662947837899, 365.1927285166406705 ) ) ;
#6903=CARTESIAN_POINT ( 'NONE',  ( 765.8855110935204493, -286.1692326535048778, 319.0159684113471599 ) ) ;
#6904=DIRECTION ( 'NONE',  ( 0.000000000000000000, -1.000000000000000000, 0.000000000000000000 ) ) ;
#6906=CARTESIAN_POINT ( 'NONE',  ( 802.2119215644370342, -6.009063572426154742, 367.5423716828165084 ) ) ;
#6909=CARTESIAN_POINT ( 'NONE',  ( 772.4837098697144029, -191.3618753856925991, 374.5518280994205611 ) ) ;
#6910=CARTESIAN_POINT ( 'NONE',  ( 774.6858677611749044, -81.72551174932937101, 315.5713283507209894 ) ) ;
#6914=CARTESIAN_POINT ( 'NONE',  ( 769.9779781133707957, 4.900027336664720679, 316.7813123517150871 ) ) ;
#6917=CARTESIAN_POINT ( 'NONE',  ( 799.4546378042377910, -369.0783235625956422, 356.1575198192848006 ) ) ;
#6918=CARTESIAN_POINT ( 'NONE',  ( 772.4837098697145166, -47.36187538569312494, 374.5518280994205611 ) ) ;
#6922=CARTESIAN_POINT ( 'NONE',  ( 764.0069404352550464, -63.07832356259653750, 359.2566176426627180 ) ) ;
#6925=CARTESIAN_POINT ( 'NONE',  ( 786.2056067578752163, -203.8055962898688449, 374.4686193811670023 ) ) ;
#6926=CARTESIAN_POINT ( 'NONE',  ( 754.8072714833583632, -4.816420840238714085, 338.1981804954721156 ) ) ;
#6927=CARTESIAN_POINT ( 'NONE',  ( 776.9566956441375396, -372.8965053807773415, 364.8461984189686405 ) ) ;
#6930=CARTESIAN_POINT ( 'NONE',  ( 765.0180583372156207, -192.9982390220562820, 360.0135310231089534 ) ) ;
#6932=CARTESIAN_POINT ( 'NONE',  ( 756.3353852180820240, -341.9073299311466485, 331.1735550268787733 ) ) ;
#6937=CARTESIAN_POINT ( 'NONE',  ( 761.2382568024794409, -39.62377810805116951, 356.9571628226838129 ) ) ;
#6940=CARTESIAN_POINT ( 'NONE',  ( 814.9108240113580450, -256.2709662947834204, 337.5031285880265273 ) ) ;
#6941=CARTESIAN_POINT ( 'NONE',  ( 766.9102291470427417, -330.5545181178796952, 318.6633372737382501 ) ) ;
#6942=CARTESIAN_POINT ( 'NONE',  ( 773.3843516231979720, -421.4419599262317888, 364.4086373105754433 ) ) ;
#6946=ORIENTED_EDGE ( 'NONE', *, *, #26405, .F. ) ;
#6947=CARTESIAN_POINT ( 'NONE',  ( 814.9108240113580450, -304.2709662947832499, 337.5031285880265273 ) ) ;
#6949=CARTESIAN_POINT ( 'NONE',  ( 754.9735926884551418, -330.3510508353229511, 340.5236548041000333 ) ) ;
#6952=CARTESIAN_POINT ( 'NONE',  ( 759.0159684113467620, -112.9181544815167229, 325.8855110935213020 ) ) ;
#6953=CARTESIAN_POINT ( 'NONE',  ( 785.3141322388236176, -21.72551174932956641, 364.4286716492789537 ) ) ;
#6956=LINE ( 'NONE', #35127, #38755 ) ;
#6957=CARTESIAN_POINT ( 'NONE',  ( 757.0176451133909268, -229.0999726633345404, 349.9200121543848354 ) ) ;
#6958=CARTESIAN_POINT ( 'NONE',  ( 773.7305795820266212, -249.2817908451526421, 374.8230680027170365 ) ) ;
#6959=CARTESIAN_POINT ( 'NONE',  ( 798.7617431975189675, -195.6237781080506863, 323.0428371773161871 ) ) ;
#6966=CARTESIAN_POINT ( 'NONE',  ( 749.2812353651451076, -30.45278447660226817, 323.2262854647983090 ) ) ;
#6967=CARTESIAN_POINT ( 'NONE',  ( 758.8095938919642549, -80.08914811296574499, 311.6929314249763365 ) ) ;
#6968=CARTESIAN_POINT ( 'NONE',  ( 804.5667330414263461, -452.9681489794450044, 348.7981942340067576 ) ) ;
#6972=CARTESIAN_POINT ( 'NONE',  ( 788.6739635108323228, -343.6454272087887603, 373.9316612368139090 ) ) ;
#6974=CARTESIAN_POINT ( 'NONE',  ( 751.6929314249748586, -318.9982390220557704, 318.8095938919659034 ) ) ;
#6979=CARTESIAN_POINT ( 'NONE',  ( 803.6646147819161570, -377.9073299311466485, 348.8264449731210561 ) ) ;
#6980=CARTESIAN_POINT ( 'NONE',  ( 787.5531968255692163, -165.8272453906074873, 316.1348686366205811 ) ) ;
#6983=CARTESIAN_POINT ( 'NONE',  ( 771.2368401574024119, -61.44195992623291147, 374.2805881961240857 ) ) ;
#6984=CARTESIAN_POINT ( 'NONE',  ( 800.0135310231082713, -398.0891481129647218, 325.0180583372163028 ) ) ;
#6985=CARTESIAN_POINT ( 'NONE',  ( 810.7187646348534145, 5.547215523397618142, 356.7737145352016341 ) ) ;
#6994=CARTESIAN_POINT ( 'NONE',  ( 803.6646147819161570, -233.9073299311470180, 348.8264449731210561 ) ) ;
#6995=CARTESIAN_POINT ( 'NONE',  ( 756.3353852180820240, -221.9073299311471033, 331.1735550268787733 ) ) ;
#6997=CARTESIAN_POINT ( 'NONE',  ( 767.6429770376289525, 14.81994279612486309, 306.8695393053162093 ) ) ;
#7000=CARTESIAN_POINT ( 'NONE',  ( 781.7834795799800531, -442.8164208402372992, 315.0636971347436202 ) ) ;
#7003=CARTESIAN_POINT ( 'NONE',  ( 796.9462024416508257, -156.4527844766018916, 308.9653473494370246 ) ) ;
#7010=CARTESIAN_POINT ( 'NONE',  ( 755.0488828828309806, -233.8055962898687028, 344.1219089521771934 ) ) ;
#7016=EDGE_LOOP ( 'NONE', ( #4819, #3878 ) ) ;
#7019=CARTESIAN_POINT ( 'NONE',  ( 776.2046728542105711, -140.1908817542438896, 304.8212110874238761 ) ) ;
#7029=CARTESIAN_POINT ( 'NONE',  ( 764.1737431748507561, -394.3726999360613377, 371.6461892240376415 ) ) ;
#7036=CARTESIAN_POINT ( 'NONE',  ( 813.5763878283155464, -243.8272453906072030, 351.1614460488615350 ) ) ;
#7038=CARTESIAN_POINT ( 'NONE',  ( 749.2812353651451076, -222.4527844766016642, 323.2262854647983090 ) ) ;
#7040=DIRECTION ( 'NONE',  ( -1.000000000000000000, -0.000000000000000000, -0.000000000000000000 ) ) ;
#7042=CARTESIAN_POINT ( 'NONE',  ( 803.6646147819161570, -305.9073299311467622, 348.8264449731210561 ) ) ;
#7044=CARTESIAN_POINT ( 'NONE',  ( 755.3028492785439312, -87.28179084515316788, 335.9200461376539693 ) ) ;
#7049=CARTESIAN_POINT ( 'NONE',  ( 803.2186876482843445, -127.9874144716872308, 350.0220218866286928 ) ) ;
#7050=CARTESIAN_POINT ( 'NONE',  ( 803.6646147819161570, -329.9073299311467053, 348.8264449731210561 ) ) ;
#7054=CARTESIAN_POINT ( 'NONE',  ( 762.3223304703356007, -103.5436935675111272, 322.3223304703362828 ) ) ;
#7057=CARTESIAN_POINT ( 'NONE',  ( 801.9858362298568863, -411.0783235625954717, 312.7379699480935642 ) ) ;
#7059=CARTESIAN_POINT ( 'NONE',  ( 804.6798772138708955, -303.7255117493287457, 334.6312213355107019 ) ) ;
#7064=CARTESIAN_POINT ( 'NONE',  ( 754.8072714833581358, -412.8164208402372992, 338.1981804954720587 ) ) ;
#7071=CARTESIAN_POINT ( 'NONE',  ( 771.2633955100217236, -119.9073299311474443, 363.4237431249939618 ) ) ;
#7072=CARTESIAN_POINT ( 'NONE',  ( 757.4527132478984868, -448.3726999360611103, 329.1273215169538844 ) ) ;
#7073=CARTESIAN_POINT ( 'NONE',  ( 776.9566956441375396, -132.8965053807781374, 364.8461984189686405 ) ) ;
#7075=CARTESIAN_POINT ( 'NONE',  ( 799.9999999999993179, -512.9681489794448908, 339.9999999999999432 ) ) ;
#7076=CARTESIAN_POINT ( 'NONE',  ( 778.7502325331095108, -408.3510508353227806, 304.6391490659818828 ) ) ;
#7082=CARTESIAN_POINT ( 'NONE',  ( 814.8207195650702488, -50.19088175424420939, 336.2433038121456548 ) ) ;
#7092=CARTESIAN_POINT ( 'NONE',  ( 757.4527132478984868, -376.3726999360614514, 329.1273215169538844 ) ) ;
#7093=CARTESIAN_POINT ( 'NONE',  ( 795.8262568251477660, -334.3726999360615082, 308.3538107759623585 ) ) ;
#7097=VECTOR ( 'NONE', #33793, 1000.000000000000000 ) ;
#7098=CARTESIAN_POINT ( 'NONE',  ( 814.4686193811664907, -147.2817908451529547, 346.2056067578752732 ) ) ;
#7104=CARTESIAN_POINT ( 'NONE',  ( 768.0187753319979720, -176.6346026584199933, 318.0580252608186242 ) ) ;
#7106=CARTESIAN_POINT ( 'NONE',  ( 757.7880784355613741, -450.0090635724248500, 312.4576283171834916 ) ) ;
#7111=CARTESIAN_POINT ( 'NONE',  ( 783.7566961878529810, -0.8965053807785533513, 305.1792804349288417 ) ) ;
#7115=CARTESIAN_POINT ( 'NONE',  ( 758.0141637701419768, -303.0783235625957559, 367.2620300519063790 ) ) ;
#7116=CARTESIAN_POINT ( 'NONE',  ( 768.0187753319979720, -104.6346026584202207, 318.0580252608186242 ) ) ;
#7118=CARTESIAN_POINT ( 'NONE',  ( 758.0580252608178853, -318.4527844766014368, 328.0187753319985404 ) ) ;
#7121=CARTESIAN_POINT ( 'NONE',  ( 814.5518280994195948, -87.72551174932935680, 332.4837098697145166 ) ) ;
#7126=CARTESIAN_POINT ( 'NONE',  ( 755.3201227861273992, -27.72551174932954510, 345.3687786644892981 ) ) ;
#7128=CIRCLE ( 'NONE', #1216, 10.00000000000000888 ) ;
#7129=CARTESIAN_POINT ( 'NONE',  ( 751.9810565676468741, -362.0891481129648923, 360.9747183278973921 ) ) ;
#7130=CARTESIAN_POINT ( 'NONE',  ( 766.5853460496234675, -277.9874144716867477, 372.3518521366060554 ) ) ;
#7131=CARTESIAN_POINT ( 'NONE',  ( 793.4146539503750546, -73.98741447168741558, 307.6481478633938877 ) ) ;
#7136=CARTESIAN_POINT ( 'NONE',  ( 762.3223304703356007, -247.5436935675106724, 322.3223304703362828 ) ) ;
#7137=CARTESIAN_POINT ( 'NONE',  ( 814.9108240113580450, -376.2709662947829656, 337.5031285880265273 ) ) ;
#7144=CARTESIAN_POINT ( 'NONE',  ( 786.5483106153019435, -271.6454272087889876, 364.1601925771022366 ) ) ;
#7145=CARTESIAN_POINT ( 'NONE',  ( 800.0135310231082713, -110.0891481129656597, 325.0180583372163028 ) ) ;
#7150=CARTESIAN_POINT ( 'NONE',  ( 763.2154366446407039, -285.6237781080502600, 321.4292242960311228 ) ) ;
#7152=CARTESIAN_POINT ( 'NONE',  ( 814.4686193811664907, -27.28179084515336328, 346.2056067578752732 ) ) ;
#7156=CARTESIAN_POINT ( 'NONE',  ( 767.6429770376289525, -177.1800572038744690, 306.8695393053162093 ) ) ;
#7157=CARTESIAN_POINT ( 'NONE',  ( 765.0180583372156207, -96.99823902205660886, 360.0135310231089534 ) ) ;
#7161=CARTESIAN_POINT ( 'NONE',  ( 773.7305795820266212, -441.2817908451521021, 374.8230680027170365 ) ) ;
#7164=CARTESIAN_POINT ( 'NONE',  ( 805.1016975059191054, -366.8965053807773984, 343.0745993439771837 ) ) ;
#7165=CARTESIAN_POINT ( 'NONE',  ( 792.2312462859673587, -35.90732993114770011, 307.2067596250082602 ) ) ;
#7168=CARTESIAN_POINT ( 'NONE',  ( 765.8855110935204493, -46.16923265350568784, 319.0159684113471599 ) ) ;
#7170=CARTESIAN_POINT ( 'NONE',  ( 749.8865473780648472, -188.5328690171416497, 322.1177392798429082 ) ) ;
#7171=CARTESIAN_POINT ( 'NONE',  ( 754.8072714833583632, -28.81642084023863504, 338.1981804954721156 ) ) ;
#7172=CARTESIAN_POINT ( 'NONE',  ( 773.3843516231979720, -373.4419599262319593, 364.4086373105754433 ) ) ;
#7176=CARTESIAN_POINT ( 'NONE',  ( 762.1405469898971887, -193.5436935675108714, 357.8594530101015607 ) ) ;
#7178=CARTESIAN_POINT ( 'NONE',  ( 778.2165204200184689, -334.8164208402376403, 364.9363028652563230 ) ) ;
#7180=CARTESIAN_POINT ( 'NONE',  ( 772.3691319403857278, -47.26014174441477422, 315.8894580844506663 ) ) ;
#7184=CARTESIAN_POINT ( 'NONE',  ( 747.2067596250078623, -243.1800572038743269, 352.2312462859687230 ) ) ;
#7186=CARTESIAN_POINT ( 'NONE',  ( 813.2346286133761168, -5.260141744414903897, 328.9521613784389160 ) ) ;
#7192=CARTESIAN_POINT ( 'NONE',  ( 777.4774526936600978, -298.2709662947830793, 304.7301800767027657 ) ) ;
#7194=CARTESIAN_POINT ( 'NONE',  ( 795.9930595647434757, -339.0783235625956422, 320.7433823573372820 ) ) ;
#7198=CARTESIAN_POINT ( 'NONE',  ( 780.5236548040995785, -140.7363362996984506, 314.9735926884559944 ) ) ;
#7199=CARTESIAN_POINT ( 'NONE',  ( 804.6798772138708955, -15.72551174932958951, 334.6312213355107019 ) ) ;
#7203=CARTESIAN_POINT ( 'NONE',  ( 805.6418435158337843, -221.4636090269709428, 363.8556311672236916 ) ) ;
#7204=CARTESIAN_POINT ( 'NONE',  ( 805.1016975059191054, -198.8965053807779384, 343.0745993439771837 ) ) ;
#7206=CARTESIAN_POINT ( 'NONE',  ( 804.6971507214547046, -459.2817908451519884, 344.0799538623459739 ) ) ;
#7209=CARTESIAN_POINT ( 'NONE',  ( 812.7932403749906598, -15.18005720387504631, 327.7687537140311633 ) ) ;
#7210=CARTESIAN_POINT ( 'NONE',  ( 748.9653473494363425, -74.63460265842032015, 356.9462024416521331 ) ) ;
#7215=CARTESIAN_POINT ( 'NONE',  ( 771.3260364891663130, -355.6454272087887603, 306.0683387631859773 ) ) ;
#7218=CARTESIAN_POINT ( 'NONE',  ( 755.2512626584698410, -319.5436935675104451, 315.2512626584710915 ) ) ;
#7223=CARTESIAN_POINT ( 'NONE',  ( 788.7366044899766848, -419.9073299311465348, 316.5762568750059813 ) ) ;
#7224=CARTESIAN_POINT ( 'NONE',  ( 759.0159684113467620, -184.9181544815165239, 325.8855110935213020 ) ) ;
#7227=CARTESIAN_POINT ( 'NONE',  ( 744.8212110874229666, -114.8965053807782226, 336.2046728542121627 ) ) ;
#7228=CARTESIAN_POINT ( 'NONE',  ( 755.0636971347428243, -412.2709662947829088, 341.7834795799807353 ) ) ;
#7231=CARTESIAN_POINT ( 'NONE',  ( 754.0944755984390895, -159.6237781080508285, 364.1009440267246760 ) ) ;
#7232=CARTESIAN_POINT ( 'NONE',  ( 790.8050863131179540, -452.8379544210779954, 362.5841948692291226 ) ) ;
#7236=CARTESIAN_POINT ( 'NONE',  ( 804.9363028652555840, -232.2709662947834488, 338.2165204200192079 ) ) ;
#7237=CARTESIAN_POINT ( 'NONE',  ( 755.0636971347428243, -220.2709662947834772, 341.7834795799807353 ) ) ;
#7239=CARTESIAN_POINT ( 'NONE',  ( 751.9810565676468741, -2.089148112965993231, 360.9747183278973921 ) ) ;
#7242=CARTESIAN_POINT ( 'NONE',  ( 756.5762568750052424, -411.1800572038738437, 348.7366044899774238 ) ) ;
#7246=CARTESIAN_POINT ( 'NONE',  ( 808.3070685750232087, -162.9982390220563673, 361.1904061080339829 ) ) ;
#7249=CARTESIAN_POINT ( 'NONE',  ( 778.7502325331095108, -192.3510508353233774, 304.6391490659818828 ) ) ;
#7254=CARTESIAN_POINT ( 'NONE',  ( 775.9200461376533440, -239.8055962898687028, 315.3028492785443291 ) ) ;
#7255=DIRECTION ( 'NONE',  ( 0.7071067811865753283, 0.000000000000000000, 0.7071067811865198172 ) ) ;
#7263=CARTESIAN_POINT ( 'NONE',  ( 778.7629533639073998, -152.7363362996983938, 375.0009284576466371 ) ) ;
#7270=CARTESIAN_POINT ( 'NONE',  ( 762.1177392798416577, -378.5545181178795247, 309.8865473780659272 ) ) ;
#7275=CARTESIAN_POINT ( 'NONE',  ( 800.2193346964447755, -18.99823902205683979, 355.1360043628815788 ) ) ;
#7277=CARTESIAN_POINT ( 'NONE',  ( 788.6739635108323228, -247.6454272087890160, 373.9316612368139090 ) ) ;
#7279=CARTESIAN_POINT ( 'NONE',  ( 814.9108240113580450, -208.2709662947835341, 337.5031285880265273 ) ) ;
#7282=CARTESIAN_POINT ( 'NONE',  ( 754.8072714833581358, -340.8164208402376971, 338.1981804954720587 ) ) ;
#7283=CARTESIAN_POINT ( 'NONE',  ( 800.9840315886518738, -76.91815448151683654, 354.1144889064786412 ) ) ;
#7287=CARTESIAN_POINT ( 'NONE',  ( 770.0799878456142551, -109.9874144716873019, 362.9823548866085616 ) ) ;
#7288=CARTESIAN_POINT ( 'NONE',  ( 800.0135310231082713, -350.0891481129648923, 325.0180583372163028 ) ) ;
#7291=CARTESIAN_POINT ( 'NONE',  ( 774.6858677611749044, -105.7255117493293000, 315.5713283507209894 ) ) ;
#7294=CARTESIAN_POINT ( 'NONE',  ( 810.1134526219336749, -416.5328690171409107, 357.8822607201570349 ) ) ;
#7295=ORIENTED_EDGE ( 'NONE', *, *, #7452, .T. ) ;
#7296=CARTESIAN_POINT ( 'NONE',  ( 771.2633955100217236, -311.9073299311468759, 363.4237431249939618 ) ) ;
#7300=CARTESIAN_POINT ( 'NONE',  ( 756.5762568750052424, -411.1800572038738437, 348.7366044899774238 ) ) ;
#7304=ORIENTED_EDGE ( 'NONE', *, *, #38557, .T. ) ;
#7306=CARTESIAN_POINT ( 'NONE',  ( 804.9363028652555840, -136.2709662947837330, 338.2165204200192079 ) ) ;
#7307=CARTESIAN_POINT ( 'NONE',  ( 769.0155153010367712, -442.3726999360611103, 362.7791456095907279 ) ) ;
#7308=CARTESIAN_POINT ( 'NONE',  ( 799.4546378042377910, -129.0783235625963243, 356.1575198192848006 ) ) ;
#7311=CARTESIAN_POINT ( 'NONE',  ( 815.1787889125755555, -390.8965053807772279, 343.7953271457877804 ) ) ;
#7316=CARTESIAN_POINT ( 'NONE',  ( 747.6481478633932056, -37.09997266333514432, 353.4146539503763620 ) ) ;
#7324=CARTESIAN_POINT ( 'NONE',  ( 763.0428371773158460, -371.4636090269705164, 358.7617431975195359 ) ) ;
#7325=CARTESIAN_POINT ( 'NONE',  ( 773.7305795820266212, -321.2817908451525000, 374.8230680027170365 ) ) ;
#7329=CARTESIAN_POINT ( 'NONE',  ( 757.7880784355613741, -162.0090635724256742, 312.4576283171834916 ) ) ;
#7331=CARTESIAN_POINT ( 'NONE',  ( 755.2512626584698410, -103.5436935675111272, 315.2512626584710915 ) ) ;
#7335=CARTESIAN_POINT ( 'NONE',  ( 762.3223304703356007, -175.5436935675108998, 322.3223304703362828 ) ) ;
#7336=CARTESIAN_POINT ( 'NONE',  ( 804.8461984189677878, -2.190881754244347945, 336.9566956441385628 ) ) ;
#7340=CARTESIAN_POINT ( 'NONE',  ( 814.8230680027162407, -5.805596289869448867, 333.7305795820267917 ) ) ;
#7341=ORIENTED_EDGE ( 'NONE', *, *, #24465, .F. ) ;
#7344=CARTESIAN_POINT ( 'NONE',  ( 766.5853460496234675, -325.9874144716865771, 372.3518521366060554 ) ) ;
#7345=CARTESIAN_POINT ( 'NONE',  ( 805.1927285166399315, -112.8164208402383650, 341.8018195045277707 ) ) ;
#7347=CARTESIAN_POINT ( 'NONE',  ( 759.7806653035534055, -318.9982390220557704, 324.8639956371180801 ) ) ;
#7349=CARTESIAN_POINT ( 'NONE',  ( 748.9653473494365699, -98.63460265842023489, 356.9462024416520762 ) ) ;
#7355=CARTESIAN_POINT ( 'NONE',  ( 764.8639956371174549, -32.08914811296588709, 319.7806653035542013 ) ) ;
#7357=CARTESIAN_POINT ( 'NONE',  ( 744.7301800767020268, -412.8164208402373561, 337.4774526936615189 ) ) ;
#7358=CARTESIAN_POINT ( 'NONE',  ( 766.5853460496234675, -301.9874144716867477, 372.3518521366060554 ) ) ;
#7359=CARTESIAN_POINT ( 'NONE',  ( 761.9338519418445230, -86.53286901714194812, 370.4231160770881957 ) ) ;
#7365=CARTESIAN_POINT ( 'NONE',  ( 813.1304606946830518, -401.9073299311463643, 352.3570229623690580 ) ) ;
#7371=CARTESIAN_POINT ( 'NONE',  ( 776.9254006560222479, -260.1908817542435486, 314.8983024940802125 ) ) ;
#7372=CARTESIAN_POINT ( 'NONE',  ( 788.8264449731200330, -165.1800572038745258, 363.6646147819171233 ) ) ;
#7376=CARTESIAN_POINT ( 'NONE',  ( 758.6633372737375112, -308.5328690171412518, 326.9102291470432533 ) ) ;
#7378=CARTESIAN_POINT ( 'NONE',  ( 778.7629533639073998, -32.73633629969879877, 375.0009284576466371 ) ) ;
#7380=CARTESIAN_POINT ( 'NONE',  ( 796.7737145352015204, -212.6346026584198796, 370.7187646348536987 ) ) ;
#7381=CARTESIAN_POINT ( 'NONE',  ( 765.0180583372156207, -72.99823902205667991, 360.0135310231089534 ) ) ;
#7384=CARTESIAN_POINT ( 'NONE',  ( 783.7953271457878373, -440.1908817542430370, 375.1787889125761239 ) ) ;
#7387=CARTESIAN_POINT ( 'NONE',  ( 766.7756240680305382, -374.5328690171410813, 361.5560724626415663 ) ) ;
#7388=CARTESIAN_POINT ( 'NONE',  ( 755.2512626584698410, -31.54369356751135456, 315.2512626584710915 ) ) ;
#7390=CARTESIAN_POINT ( 'NONE',  ( 761.2382568024794409, -63.62377810805107714, 356.9571628226838129 ) ) ;
#7394=CARTESIAN_POINT ( 'NONE',  ( 813.2346286133761168, -221.2601417444142271, 328.9521613784389160 ) ) ;
#7395=CARTESIAN_POINT ( 'NONE',  ( 795.1360043628808398, -20.08914811296593328, 360.2193346964456282 ) ) ;
#7398=CARTESIAN_POINT ( 'NONE',  ( 778.1981804954714335, -202.2709662947834772, 314.8072714833589885 ) ) ;
#7401=CARTESIAN_POINT ( 'NONE',  ( 758.0580252608178853, -318.4527844766014368, 328.0187753319985404 ) ) ;
#7405=CARTESIAN_POINT ( 'NONE',  ( 780.5290396650775619, -60.35105083532383219, 365.2837595273619513 ) ) ;
#7407=CARTESIAN_POINT ( 'NONE',  ( 758.8095938919644823, -248.0891481129651766, 311.6929314249762797 ) ) ;
#7408=CARTESIAN_POINT ( 'NONE',  ( 811.6461892240364477, -4.714687198960358039, 324.1737431748509835 ) ) ;
#7413=CARTESIAN_POINT ( 'NONE',  ( 810.7187646348534145, -282.4527844766014937, 356.7737145352016341 ) ) ;
#7414=CARTESIAN_POINT ( 'NONE',  ( 810.2700907235021077, -453.7763741861470521, 341.5253149289871999 ) ) ;
#7415=CARTESIAN_POINT ( 'NONE',  ( 773.4516893846965786, -211.6454272087891582, 315.8398074228977066 ) ) ;
#7416=CARTESIAN_POINT ( 'NONE',  ( 780.5290396650775619, -324.3510508353229511, 365.2837595273619513 ) ) ;
#7418=CARTESIAN_POINT ( 'NONE',  ( 804.4086373105744769, -169.6454272087892718, 333.3843516231986541 ) ) ;
#7419=CARTESIAN_POINT ( 'NONE',  ( 755.0636971347428243, -28.27096629478409540, 341.7834795799807353 ) ) ;
#7424=CARTESIAN_POINT ( 'NONE',  ( 795.8262568251477660, -262.3726999360617924, 308.3538107759623585 ) ) ;
#7425=CARTESIAN_POINT ( 'NONE',  ( 780.5290396650775619, -204.3510508353233774, 365.2837595273619513 ) ) ;
#7427=CARTESIAN_POINT ( 'NONE',  ( 804.4086373105744769, -457.6454272087884760, 333.3843516231986541 ) ) ;
#7430=CARTESIAN_POINT ( 'NONE',  ( 792.3570229623688874, -21.18005720387502677, 373.1304606946836202 ) ) ;
#7431=CARTESIAN_POINT ( 'NONE',  ( 751.9810565676468741, -74.08914811296577341, 360.9747183278973921 ) ) ;
#7435=CARTESIAN_POINT ( 'NONE',  ( 783.7953271457878373, -368.1908817542433212, 375.1787889125761239 ) ) ;
#7437=CARTESIAN_POINT ( 'NONE',  ( 792.2312462859673587, -323.9073299311468190, 307.2067596250082602 ) ) ;
#7442=CARTESIAN_POINT ( 'NONE',  ( 791.9812246680005501, -428.6346026584192259, 361.9419747391813189 ) ) ;
#7443=CARTESIAN_POINT ( 'NONE',  ( 783.0745993439762742, -176.1908817542438328, 365.1016975059196739 ) ) ;
#7446=CARTESIAN_POINT ( 'NONE',  ( 815.1787889125755555, -102.8965053807782368, 343.7953271457877804 ) ) ;
#7447=CARTESIAN_POINT ( 'NONE',  ( 794.9819416627830151, -396.9982390220556567, 319.9864689768909898 ) ) ;
#7448=CARTESIAN_POINT ( 'NONE',  ( 813.9316612368132837, -151.4419599262326415, 348.6739635108323228 ) ) ;
#7452=EDGE_CURVE ( 'NONE', #22109, #23565, #13906, .T. ) ;
#7454=CARTESIAN_POINT ( 'NONE',  ( 797.6776695296629214, -235.5436935675107293, 357.6776695296636603 ) ) ;
#7455=CARTESIAN_POINT ( 'NONE',  ( 800.2193346964446619, -210.9982390220562252, 355.1360043628816925 ) ) ;
#7460=CARTESIAN_POINT ( 'NONE',  ( 781.7834795799800531, -418.8164208402374129, 315.0636971347436202 ) ) ;
#7463=CARTESIAN_POINT ( 'NONE',  ( 759.0252816721024374, -144.9982390220564525, 368.0189434323527280 ) ) ;
#7464=CARTESIAN_POINT ( 'NONE',  ( 790.9844846989617508, -262.3726999360617924, 317.2208543904092721 ) ) ;
#7465=CARTESIAN_POINT ( 'NONE',  ( 756.7813123517142913, -379.9874144716865203, 329.9779781133712504 ) ) ;
#7470=EDGE_CURVE ( 'NONE', #38419, #21828, #42689, .T. ) ;
#7474=CARTESIAN_POINT ( 'NONE',  ( 804.9511171171677688, -221.8055962898687881, 335.8780910478229202 ) ) ;
#7484=CARTESIAN_POINT ( 'NONE',  ( 754.3581564841646241, -137.4636090269711985, 316.1443688327762516 ) ) ;
#7493=CARTESIAN_POINT ( 'NONE',  ( 785.3141322388236176, 2.274488250670355871, 364.4286716492789537 ) ) ;
#7495=CARTESIAN_POINT ( 'NONE',  ( 747.6481478633932056, -253.0999726633345119, 353.4146539503763620 ) ) ;
#7497=CARTESIAN_POINT ( 'NONE',  ( 813.1304606946830518, -233.9073299311470180, 352.3570229623690580 ) ) ;
#7501=CARTESIAN_POINT ( 'NONE',  ( 759.9864689768902508, -314.0891481129650629, 354.9819416627836404 ) ) ;
#7502=CARTESIAN_POINT ( 'NONE',  ( 798.5707757039680246, -101.4636090269713264, 356.7845633553585003 ) ) ;
#7503=CARTESIAN_POINT ( 'NONE',  ( 790.0220218866281812, -103.0999726633349525, 363.2186876482849129 ) ) ;
#7506=LINE ( 'NONE', #21578, #15912 ) ;
#7507=CARTESIAN_POINT ( 'NONE',  ( 784.0799538623451781, -155.8055962898689586, 364.6971507214555572 ) ) ;
#7508=CARTESIAN_POINT ( 'NONE',  ( 762.3223304703356007, -343.5436935675103314, 322.3223304703362828 ) ) ;
#7512=CARTESIAN_POINT ( 'NONE',  ( 785.3141322388236176, -117.7255117493292715, 364.4286716492789537 ) ) ;
#7515=CARTESIAN_POINT ( 'NONE',  ( 768.8385539511368734, -431.2601417444136018, 306.4236121716840557 ) ) ;
#7517=CARTESIAN_POINT ( 'NONE',  ( 755.3201227861273992, -315.7255117493286320, 345.3687786644892981 ) ) ;
#7521=CARTESIAN_POINT ( 'NONE',  ( 756.3353852180819104, -413.9073299311465348, 331.1735550268788302 ) ) ;
#7528=CARTESIAN_POINT ( 'NONE',  ( 757.0176451133909268, -445.0999726633338582, 349.9200121543848354 ) ) ;
#7529=CARTESIAN_POINT ( 'NONE',  ( 763.2154366446407039, -141.6237781080508569, 321.4292242960311228 ) ) ;
#7532=CARTESIAN_POINT ( 'NONE',  ( 805.9055244015594326, -387.6237781080499758, 315.8990559732753240 ) ) ;
#7537=CARTESIAN_POINT ( 'NONE',  ( 813.5763878283155464, -27.82724539060790292, 351.1614460488615350 ) ) ;
#7545=CARTESIAN_POINT ( 'NONE',  ( 772.4468031744293057, -369.8272453906068904, 363.8651313633793620 ) ) ;
#7546=CARTESIAN_POINT ( 'NONE',  ( 744.6391490659812007, -326.7363362996979390, 338.7502325331110455 ) ) ;
#7551=CARTESIAN_POINT ( 'NONE',  ( 744.6391490659812007, -158.7363362996984222, 338.7502325331110455 ) ) ;
#7553=CARTESIAN_POINT ( 'NONE',  ( 808.3070685750230950, -114.9982390220565236, 361.1904061080339261 ) ) ;
#7557=CARTESIAN_POINT ( 'NONE',  ( 788.7366044899766848, -203.9073299311471885, 316.5762568750059813 ) ) ;
#7559=CARTESIAN_POINT ( 'NONE',  ( 802.5472867521000353, -4.372699936062523385, 350.8726784830461156 ) ) ;
#7563=CARTESIAN_POINT ( 'NONE',  ( 803.8556311672234642, 14.37622189194867417, 365.6418435158340117 ) ) ;
#7565=CARTESIAN_POINT ( 'NONE',  ( 791.9812246680005501, -20.63460265842048003, 361.9419747391813189 ) ) ;
#7568=CARTESIAN_POINT ( 'NONE',  ( 791.1614460488616487, -299.2601417444139997, 373.5763878283158874 ) ) ;
#7569=CARTESIAN_POINT ( 'NONE',  ( 756.3353852180820240, -149.9073299311473875, 331.1735550268787733 ) ) ;
#7571=CARTESIAN_POINT ( 'NONE',  ( 754.8072714833581358, -292.8164208402376971, 338.1981804954720587 ) ) ;
#7574=CARTESIAN_POINT ( 'NONE',  ( 777.5031285880264704, -70.81642084023850714, 374.9108240113588408 ) ) ;
#7579=CARTESIAN_POINT ( 'NONE',  ( 794.9819416627830151, -36.99823902205679360, 319.9864689768909898 ) ) ;
#7581=CARTESIAN_POINT ( 'NONE',  ( 792.3570229623691148, -405.1800572038737869, 373.1304606946836770 ) ) ;
#7582=CARTESIAN_POINT ( 'NONE',  ( 781.2497674668890113, -276.3510508353231785, 375.3608509340180603 ) ) ;
#7583=CARTESIAN_POINT ( 'NONE',  ( 768.8385539511368734, -71.26014174441469606, 306.4236121716840557 ) ) ;
#7589=CARTESIAN_POINT ( 'NONE',  ( 746.8695393053150156, -389.9073299311465348, 327.6429770376306010 ) ) ;
#7591=LINE ( 'NONE', #1105, #27781 ) ;
#7594=FACE_OUTER_BOUND ( 'NONE', #11213, .T. ) ;
#7595=CARTESIAN_POINT ( 'NONE',  ( 769.0155153010367712, -250.3726999360618208, 362.7791456095907279 ) ) ;
#7596=CARTESIAN_POINT ( 'NONE',  ( 756.5762568750052424, -147.1800572038746395, 348.7366044899774238 ) ) ;
#7600=CARTESIAN_POINT ( 'NONE',  ( 798.7617431975189675, -339.6237781080502600, 323.0428371773161871 ) ) ;
#7602=CARTESIAN_POINT ( 'NONE',  ( 773.7305795820266212, -33.28179084515333130, 374.8230680027170365 ) ) ;
#7604=CARTESIAN_POINT ( 'NONE',  ( 748.9653473494363425, -194.6346026584198796, 356.9462024416521331 ) ) ;
#7605=CARTESIAN_POINT ( 'NONE',  ( 805.1927285166397041, -112.8164208402383508, 341.8018195045277707 ) ) ;
#7609=CARTESIAN_POINT ( 'NONE',  ( 814.8207195650702488, -458.1908817542429802, 336.2433038121456548 ) ) ;
#7612=CARTESIAN_POINT ( 'NONE',  ( 755.0488828828309806, -377.8055962898682765, 344.1219089521771934 ) ) ;
#7613=CARTESIAN_POINT ( 'NONE',  ( 812.7932403749906598, -63.18005720387488822, 327.7687537140311633 ) ) ;
#7615=CARTESIAN_POINT ( 'NONE',  ( 803.8651313633788504, -53.26014174441475291, 332.4468031744301015 ) ) ;
#7618=CARTESIAN_POINT ( 'NONE',  ( 783.7566961878529810, -216.8965053807778816, 305.1792804349288417 ) ) ;
#7619=CARTESIAN_POINT ( 'NONE',  ( 778.1981804954715471, -10.27096629478415046, 314.8072714833591021 ) ) ;
#7622=CARTESIAN_POINT ( 'NONE',  ( 764.8639956371174549, -200.0891481129653187, 319.7806653035542013 ) ) ;
#7624=CARTESIAN_POINT ( 'NONE',  ( 804.6798772138710092, -327.7255117493285752, 334.6312213355106451 ) ) ;
#7628=CARTESIAN_POINT ( 'NONE',  ( 783.0433043558608688, -48.89650538077840025, 315.1538015810313027 ) ) ;
#7630=CARTESIAN_POINT ( 'NONE',  ( 763.2262854647970016, -296.6346026584195670, 309.2812353651462445 ) ) ;
#7631=CARTESIAN_POINT ( 'NONE',  ( 813.9316612368132837, -7.441959926233078448, 348.6739635108323228 ) ) ;
#7637=CIRCLE ( 'NONE', #23100, 30.00000000000002842 ) ;
#7639=CARTESIAN_POINT ( 'NONE',  ( 763.2262854647970016, -296.6346026584195670, 309.2812353651462445 ) ) ;
#7642=CARTESIAN_POINT ( 'NONE',  ( 804.4086373105744769, -145.6454272087893287, 333.3843516231986541 ) ) ;
#7643=CARTESIAN_POINT ( 'NONE',  ( 803.6646147819161570, -65.90732993114758642, 348.8264449731210561 ) ) ;
#7647=CARTESIAN_POINT ( 'NONE',  ( 762.1177392798416577, -258.5545181178799226, 309.8865473780659272 ) ) ;
#7648=CARTESIAN_POINT ( 'NONE',  ( 759.2295555964440155, -232.1692326535051620, 353.9708237608231229 ) ) ;
#7651=CARTESIAN_POINT ( 'NONE',  ( 801.9419747391806368, 5.547215523397618142, 351.9812246680014027 ) ) ;
#7654=CARTESIAN_POINT ( 'NONE',  ( 755.2512626584698410, -7.543693567511430942, 315.2512626584710915 ) ) ;
#7655=CARTESIAN_POINT ( 'NONE',  ( 808.0189434323515343, -110.0891481129656597, 319.0252816721025511 ) ) ;
#7657=DIRECTION ( 'NONE',  ( 0.000000000000000000, -1.000000000000000000, 0.000000000000000000 ) ) ;
#7660=CARTESIAN_POINT ( 'NONE',  ( 814.8207195650702488, -386.1908817542432075, 336.2433038121456548 ) ) ;
#7662=CARTESIAN_POINT ( 'NONE',  ( 745.4481719005789273, -315.7255117493286320, 347.5162901302853129 ) ) ;
#7666=CARTESIAN_POINT ( 'NONE',  ( 774.6858677611749044, -441.7255117493282910, 315.5713283507209894 ) ) ;
#7668=CARTESIAN_POINT ( 'NONE',  ( 755.1538015810308480, -182.1908817542437760, 343.0433043558613804 ) ) ;
#7671=CARTESIAN_POINT ( 'NONE',  ( 781.2497674668890113, -84.35105083532374692, 375.3608509340180603 ) ) ;
#7672=CARTESIAN_POINT ( 'NONE',  ( 804.4286716492782716, -401.3618753856920307, 345.3141322388244703 ) ) ;
#7675=VERTEX_POINT ( 'NONE', #45091 ) ;
#7679=CARTESIAN_POINT ( 'NONE',  ( 800.2193346964447755, -234.9982390220561683, 355.1360043628815788 ) ) ;
#7680=CARTESIAN_POINT ( 'NONE',  ( 804.4286716492782716, -209.3618753856926276, 345.3141322388244703 ) ) ;
#7683=ORIENTED_EDGE ( 'NONE', *, *, #8040, .F. ) ;
#7684=CARTESIAN_POINT ( 'NONE',  ( 774.6312213355099630, -431.3618753856918033, 364.6798772138717482 ) ) ;
#7688=CARTESIAN_POINT ( 'NONE',  ( 813.1304606946831655, -185.9073299311472169, 352.3570229623691716 ) ) ;
#7689=CARTESIAN_POINT ( 'NONE',  ( 766.9102291470427417, -258.5545181178799226, 318.6633372737382501 ) ) ;
#7696=CARTESIAN_POINT ( 'NONE',  ( 803.8651313633788504, -245.2601417444141987, 332.4468031744301015 ) ) ;
#7700=ORIENTED_EDGE ( 'NONE', *, *, #28642, .T. ) ;
#7707=CARTESIAN_POINT ( 'NONE',  ( 754.3581564841646241, -185.4636090269710280, 316.1443688327762516 ) ) ;
#7716=CARTESIAN_POINT ( 'NONE',  ( 759.7806653035534055, -6.998239022056885972, 324.8639956371180801 ) ) ;
#7718=CARTESIAN_POINT ( 'NONE',  ( 757.7880784355613741, -234.0090635724255037, 312.4576283171834916 ) ) ;
#7720=CARTESIAN_POINT ( 'NONE',  ( 747.2067596250078623, -219.1800572038744122, 352.2312462859687230 ) ) ;
#7724=CARTESIAN_POINT ( 'NONE',  ( 762.3223304703356007, -319.5436935675104451, 322.3223304703362828 ) ) ;
#7725=CARTESIAN_POINT ( 'NONE',  ( 757.0176451133909268, -85.09997266333499510, 349.9200121543848354 ) ) ;
#7726=CARTESIAN_POINT ( 'NONE',  ( 757.4527132478984868, -88.37269993606226137, 329.1273215169538844 ) ) ;
#7731=CARTESIAN_POINT ( 'NONE',  ( 772.3691319403857278, -167.2601417444143976, 315.8894580844506663 ) ) ;
#7732=CARTESIAN_POINT ( 'NONE',  ( 755.5713283507202505, -365.3618753856920875, 334.6858677611754729 ) ) ;
#7736=CARTESIAN_POINT ( 'NONE',  ( 758.0580252608178853, -126.4527844766019626, 328.0187753319985404 ) ) ;
#7737=CIRCLE ( 'NONE', #36509, 10.00000000000000888 ) ;
#7740=CARTESIAN_POINT ( 'NONE',  ( 800.1688906516307043, -442.1692326535044231, 369.0717654672308186 ) ) ;
#7742=CARTESIAN_POINT ( 'NONE',  ( 762.1405469898971887, -337.5436935675102177, 357.8594530101015607 ) ) ;
#7745=CARTESIAN_POINT ( 'NONE',  ( 804.6798772138708955, -447.7255117493280636, 334.6312213355107019 ) ) ;
#7751=ADVANCED_FACE ( 'NONE', ( #1177, #4640 ), #18300, .F. ) ;
#7752=CARTESIAN_POINT ( 'NONE',  ( 796.1575198192839480, -462.0090635724247932, 359.4546378042384163 ) ) ;
#7753=CARTESIAN_POINT ( 'NONE',  ( 770.0799878456142551, -133.9874144716872024, 362.9823548866085616 ) ) ;
#7756=CARTESIAN_POINT ( 'NONE',  ( 771.2368401574024119, -397.4419599262317320, 374.2805881961240857 ) ) ;
#7758=ADVANCED_FACE ( 'NONE', ( #28903 ), #18519, .F. ) ;
#7764=CARTESIAN_POINT ( 'NONE',  ( 811.3240766477731540, -76.37269993606228979, 355.6651683502462902 ) ) ;
#7772=EDGE_CURVE ( 'NONE', #23907, #22842, #11472, .T. ) ;
#7774=CARTESIAN_POINT ( 'NONE',  ( 758.4439275373578084, -372.5545181178796383, 353.2243759319684386 ) ) ;
#7776=CARTESIAN_POINT ( 'NONE',  ( 814.8207195650702488, -338.1908817542433212, 336.2433038121456548 ) ) ;
#7782=CARTESIAN_POINT ( 'NONE',  ( 778.7629533639073998, -128.7363362996984790, 375.0009284576466371 ) ) ;
#7784=CARTESIAN_POINT ( 'NONE',  ( 751.6929314249748586, -102.9982390220565520, 318.8095938919659034 ) ) ;
#7788=CARTESIAN_POINT ( 'NONE',  ( 797.8594530101008786, -205.5436935675108430, 322.1405469898980982 ) ) ;
#7790=CARTESIAN_POINT ( 'NONE',  ( 766.9102291470427417, 5.445481882119263872, 318.6633372737382501 ) ) ;
#7797=CARTESIAN_POINT ( 'NONE',  ( 786.2056067578752163, -35.80559628986934229, 374.4686193811670023 ) ) ;
#7801=CARTESIAN_POINT ( 'NONE',  ( 802.1676090361156639, -14.63460265842049424, 327.8955696845344505 ) ) ;
#7804=CARTESIAN_POINT ( 'NONE',  ( 778.7502325331095108, -312.3510508353230080, 304.6391490659818828 ) ) ;
#7805=CARTESIAN_POINT ( 'NONE',  ( 755.0636971347428243, -148.2709662947837330, 341.7834795799807353 ) ) ;
#7807=CARTESIAN_POINT ( 'NONE',  ( 774.6858677611749044, -321.7255117493286320, 315.5713283507209894 ) ) ;
#7817=CARTESIAN_POINT ( 'NONE',  ( 762.1405469898971887, -49.54369356751129061, 357.8594530101015607 ) ) ;
#7818=CARTESIAN_POINT ( 'NONE',  ( 804.4086373105744769, -385.6454272087888171, 333.3843516231986541 ) ) ;
#7820=CARTESIAN_POINT ( 'NONE',  ( 811.0346526505617248, -398.6346026584193396, 323.0537975583478101 ) ) ;
#7821=CARTESIAN_POINT ( 'NONE',  ( 754.0944755984390895, -279.6237781080503737, 364.1009440267246760 ) ) ;
#7823=CARTESIAN_POINT ( 'NONE',  ( 781.2497674668890113, -60.35105083532383219, 375.3608509340180603 ) ) ;
#7830=CARTESIAN_POINT ( 'NONE',  ( 805.0032342141412300, -397.5436935675100472, 314.9967657858571783 ) ) ;
#7831=( GEOMETRIC_REPRESENTATION_CONTEXT ( 3 ) GLOBAL_UNCERTAINTY_ASSIGNED_CONTEXT ( ( #43509 ) ) GLOBAL_UNIT_ASSIGNED_CONTEXT ( ( #24063, #41636, #34227 ) ) REPRESENTATION_CONTEXT ( 'NONE', 'WORKASPACE' ) );
#7837=EDGE_CURVE ( 'NONE', #20106, #6, #39508, .T. ) ;
#7839=CARTESIAN_POINT ( 'NONE',  ( 793.9708237608222134, -262.9181544815162965, 319.2295555964448681 ) ) ;
#7840=CARTESIAN_POINT ( 'NONE',  ( 801.9419747391806368, -138.4527844766019200, 351.9812246680014027 ) ) ;
#7843=CARTESIAN_POINT ( 'NONE',  ( 783.0433043558608688, -336.8965053807774552, 315.1538015810313027 ) ) ;
#7845=CARTESIAN_POINT ( 'NONE',  ( 748.6759233522253680, -40.37269993606240348, 324.3348316497537098 ) ) ;
#7847=CARTESIAN_POINT ( 'NONE',  ( 814.5518280994195948, -207.7255117493289447, 332.4837098697145734 ) ) ;
#7848=CARTESIAN_POINT ( 'NONE',  ( 762.1405469898971887, -121.5436935675110419, 357.8594530101015607 ) ) ;
#7852=CARTESIAN_POINT ( 'NONE',  ( 813.5763878283155464, -435.8272453906066062, 351.1614460488615350 ) ) ;
#7855=CARTESIAN_POINT ( 'NONE',  ( 803.2186876482843445, -391.9874144716864066, 350.0220218866286928 ) ) ;
#7859=CARTESIAN_POINT ( 'NONE',  ( 758.6633372737375112, -44.53286901714205470, 326.9102291470432533 ) ) ;
#7862=CARTESIAN_POINT ( 'NONE',  ( 756.1443688327750579, -213.6237781080506011, 314.3581564841659315 ) ) ;
#7863=CARTESIAN_POINT ( 'NONE',  ( 794.9819416627830151, -36.99823902205679360, 319.9864689768909898 ) ) ;
#7867=CARTESIAN_POINT ( 'NONE',  ( 802.1676090361156639, -206.6346026584198512, 327.8955696845344505 ) ) ;
#7870=CARTESIAN_POINT ( 'NONE',  ( 794.9819416627830151, -348.9982390220558273, 319.9864689768909898 ) ) ;
#7871=CARTESIAN_POINT ( 'NONE',  ( 787.4999999999992042, -512.9681489794448908, 370.0000000000000000 ) ) ;
#7874=CARTESIAN_POINT ( 'NONE',  ( 784.0799538623451781, -59.80559628986927834, 364.6971507214555572 ) ) ;
#7877=CARTESIAN_POINT ( 'NONE',  ( 782.4968714119720516, -274.8164208402378108, 305.0891759886411023 ) ) ;
#7878=CARTESIAN_POINT ( 'NONE',  ( 747.3154664389472828, 4.012585528312341054, 326.4474001241230781 ) ) ;
#7885=CARTESIAN_POINT ( 'NONE',  ( 782.4968714119720516, -274.8164208402378108, 305.0891759886411023 ) ) ;
#7887=CARTESIAN_POINT ( 'NONE',  ( 796.9571628226829034, -215.4636090269709712, 321.2382568024804641 ) ) ;
#7890=CARTESIAN_POINT ( 'NONE',  ( 786.5483106153019435, -151.6454272087892718, 364.1601925771022366 ) ) ;
#7891=CARTESIAN_POINT ( 'NONE',  ( 774.6312213355099630, -47.36187538569312494, 364.6798772138717482 ) ) ;
#7896=CARTESIAN_POINT ( 'NONE',  ( 754.3581564841646241, -257.4636090269708575, 316.1443688327762516 ) ) ;
#7897=CARTESIAN_POINT ( 'NONE',  ( 765.8855110935204493, -214.1692326535052189, 319.0159684113471599 ) ) ;
#7901=CARTESIAN_POINT ( 'NONE',  ( 771.2633955100217236, 0.09267006885218045942, 363.4237431249939618 ) ) ;
#7905=CARTESIAN_POINT ( 'NONE',  ( 800.9747183278959710, -60.99823902205671544, 311.9810565676471583 ) ) ;
#7906=CARTESIAN_POINT ( 'NONE',  ( 749.2812353651451076, -102.4527844766020337, 323.2262854647983090 ) ) ;
#7907=CARTESIAN_POINT ( 'NONE',  ( 772.4999999999993179, -512.9681489794448908, 339.9999999999999432 ) ) ;
#7909=CARTESIAN_POINT ( 'NONE',  ( 786.2694204179717872, -381.2817908451523294, 305.1769319972829067 ) ) ;
#7911=CARTESIAN_POINT ( 'NONE',  ( 815.2698199232961542, -328.8164208402375834, 342.5225473063383106 ) ) ;
#7914=CARTESIAN_POINT ( 'NONE',  ( 797.8594530101008786, -445.5436935675098766, 322.1405469898980982 ) ) ;
#7915=CARTESIAN_POINT ( 'NONE',  ( 798.5707757039680246, -197.4636090269709996, 356.7845633553585003 ) ) ;
#7918=CARTESIAN_POINT ( 'NONE',  ( 758.0141637701419768, -111.0783235625964096, 367.2620300519063790 ) ) ;
#7919=CARTESIAN_POINT ( 'NONE',  ( 794.9819416627830151, -444.9982390220554862, 319.9864689768909898 ) ) ;
#7922=ORIENTED_EDGE ( 'NONE', *, *, #27251, .T. ) ;
#7926=CARTESIAN_POINT ( 'NONE',  ( 804.6798772138708955, -279.7255117493288026, 334.6312213355107019 ) ) ;
#7927=CARTESIAN_POINT ( 'NONE',  ( 771.2633955100217236, -215.9073299311471317, 363.4237431249939618 ) ) ;
#7930=CARTESIAN_POINT ( 'NONE',  ( 778.1981804954714335, -418.2709662947827383, 314.8072714833589885 ) ) ;
#7932=ORIENTED_EDGE ( 'NONE', *, *, #2999, .T. ) ;
#7935=CARTESIAN_POINT ( 'NONE',  ( 811.0346526505617248, -182.6346026584199649, 323.0537975583478101 ) ) ;
#7936=CARTESIAN_POINT ( 'NONE',  ( 766.0291762391763086, -250.9181544815163534, 360.7704444035551319 ) ) ;
#7939=CARTESIAN_POINT ( 'NONE',  ( 807.5423716828161105, -225.0783235625959833, 362.2119215644372048 ) ) ;
#7944=CARTESIAN_POINT ( 'NONE',  ( 754.9735926884551418, -258.3510508353231785, 340.5236548041000333 ) ) ;
#7945=DIRECTION ( 'NONE',  ( -0.7014439490181308967, 0.1263042864341425708, 0.7014439490181749726 ) ) ;
#7951=CARTESIAN_POINT ( 'NONE',  ( 810.4231160770870019, -168.5545181178802352, 321.9338519418446936 ) ) ;
#7956=CARTESIAN_POINT ( 'NONE',  ( 777.5031285880264704, -22.81642084023865280, 374.9108240113588408 ) ) ;
#7961=CARTESIAN_POINT ( 'NONE',  ( 764.8639956371174549, -8.089148112965974136, 319.7806653035542013 ) ) ;
#7963=CARTESIAN_POINT ( 'NONE',  ( 799.9636004259356241, -286.9181544815161828, 311.2241431872006956 ) ) ;
#7965=CARTESIAN_POINT ( 'NONE',  ( 763.0537975583475827, -240.4527844766015221, 371.0346526505627480 ) ) ;
#7969=CARTESIAN_POINT ( 'NONE',  ( 788.8264449731200330, -333.1800572038740142, 363.6646147819171233 ) ) ;
#7970=CARTESIAN_POINT ( 'NONE',  ( 804.4086373105744769, -97.64542720878949922, 333.3843516231986541 ) ) ;
#7974=CARTESIAN_POINT ( 'NONE',  ( 803.8651313633788504, -149.2601417444144261, 332.4468031744301015 ) ) ;
#7975=CARTESIAN_POINT ( 'NONE',  ( 759.7806653035534055, -366.9982390220556567, 324.8639956371180801 ) ) ;
#7978=CARTESIAN_POINT ( 'NONE',  ( 762.1405469898971887, -145.5436935675109851, 357.8594530101015607 ) ) ;
#7982=CARTESIAN_POINT ( 'NONE',  ( 815.1787889125755555, -438.8965053807771710, 343.7953271457877804 ) ) ;
#7985=CARTESIAN_POINT ( 'NONE',  ( 778.2165204200184689, -310.8164208402377540, 364.9363028652563230 ) ) ;
#7987=CARTESIAN_POINT ( 'NONE',  ( 778.1981804954714335, -442.2709662947826814, 314.8072714833589885 ) ) ;
#7994=CARTESIAN_POINT ( 'NONE',  ( 762.3223304703356007, 16.45630643248849267, 322.3223304703362828 ) ) ;
#7995=CARTESIAN_POINT ( 'NONE',  ( 808.3070685750230950, -234.9982390220561683, 361.1904061080339261 ) ) ;
#7996=CARTESIAN_POINT ( 'NONE',  ( 799.4546378042377910, -177.0783235625961538, 356.1575198192848006 ) ) ;
#7999=CARTESIAN_POINT ( 'NONE',  ( 803.8556311672234642, -393.6237781080500326, 365.6418435158340117 ) ) ;
#8004=CARTESIAN_POINT ( 'NONE',  ( 764.1737431748507561, -82.37269993606227558, 371.6461892240376415 ) ) ;
#8015=CARTESIAN_POINT ( 'NONE',  ( 802.2119215644370342, -174.0090635724256742, 367.5423716828165084 ) ) ;
#8017=CARTESIAN_POINT ( 'NONE',  ( 745.7998596910086917, -125.3618753856928834, 332.5602148656461168 ) ) ;
#8021=CARTESIAN_POINT ( 'NONE',  ( 804.4286716492782716, -209.3618753856926276, 345.3141322388244703 ) ) ;
#8022=CARTESIAN_POINT ( 'NONE',  ( 813.5763878283155464, -459.8272453906066062, 351.1614460488615350 ) ) ;
#8027=CARTESIAN_POINT ( 'NONE',  ( 748.3538107759620743, -16.71468719896031985, 355.8262568251490165 ) ) ;
#8031=CARTESIAN_POINT ( 'NONE',  ( 797.8594530101008786, -13.54369356751140785, 322.1405469898980982 ) ) ;
#8034=CARTESIAN_POINT ( 'NONE',  ( 752.4576283171824116, -333.0783235625956991, 317.7880784355627952 ) ) ;
#8035=CARTESIAN_POINT ( 'NONE',  ( 764.8639956371174549, -152.0891481129655460, 319.7806653035542581 ) ) ;
#8036=ORIENTED_EDGE ( 'NONE', *, *, #9964, .F. ) ;
#8037=CARTESIAN_POINT ( 'NONE',  ( 776.2433038121456548, -420.8965053807772279, 374.8207195650711014 ) ) ;
#8039=CARTESIAN_POINT ( 'NONE',  ( 778.1981804954714335, -346.2709662947830793, 314.8072714833589885 ) ) ;
#8040=EDGE_CURVE ( 'NONE', #22842, #5612, #22403, .T. ) ;
#8047=CARTESIAN_POINT ( 'NONE',  ( 791.9812246680005501, -44.63460265842040542, 361.9419747391813189 ) ) ;
#8048=CARTESIAN_POINT ( 'NONE',  ( 761.4292242960306112, -353.4636090269705733, 323.2154366446414429 ) ) ;
#8050=CARTESIAN_POINT ( 'NONE',  ( 772.4837098697145166, -407.3618753856920307, 374.5518280994205611 ) ) ;
#8051=CARTESIAN_POINT ( 'NONE',  ( 761.9338519418445230, -278.5328690171412518, 370.4231160770881957 ) ) ;
#8060=CARTESIAN_POINT ( 'NONE',  ( 782.4968714119720516, -418.8164208402374129, 305.0891759886411023 ) ) ;
#8067=CARTESIAN_POINT ( 'NONE',  ( 776.9254006560222479, -284.1908817542434917, 314.8983024940802125 ) ) ;
#8068=CARTESIAN_POINT ( 'NONE',  ( 767.8955696845333705, -144.4527844766018632, 362.1676090361162323 ) ) ;
#8071=CARTESIAN_POINT ( 'NONE',  ( 756.7813123517142913, -331.9874144716865203, 329.9779781133712504 ) ) ;
#8073=CARTESIAN_POINT ( 'NONE',  ( 795.8262568251477660, -46.37269993606239638, 308.3538107759623585 ) ) ;
#8075=CARTESIAN_POINT ( 'NONE',  ( 787.5162901302840055, -203.3618753856925991, 305.4481719005792684 ) ) ;
#8076=CARTESIAN_POINT ( 'NONE',  ( 762.3223304703356007, -127.5436935675110561, 322.3223304703362828 ) ) ;
#8080=CARTESIAN_POINT ( 'NONE',  ( 784.1219089521767955, -21.28179084515337749, 315.0488828828318333 ) ) ;
#8083=CARTESIAN_POINT ( 'NONE',  ( 789.9200121543843807, -385.9874144716864066, 317.0176451133914384 ) ) ;
#8090=CARTESIAN_POINT ( 'NONE',  ( 783.7566961878529810, -240.8965053807777963, 305.1792804349288417 ) ) ;
#8091=CARTESIAN_POINT ( 'NONE',  ( 788.7366044899766848, -59.90732993114762905, 316.5762568750059813 ) ) ;
#8095=CARTESIAN_POINT ( 'NONE',  ( 785.3687786644884454, -227.3618753856925707, 315.3201227861279676 ) ) ;
#8101=CARTESIAN_POINT ( 'NONE',  ( 777.5031285880264704, -286.8164208402378677, 374.9108240113588408 ) ) ;
#8102=CARTESIAN_POINT ( 'NONE',  ( 800.1688906516307043, 13.83076734649413098, 369.0717654672308186 ) ) ;
#8109=CARTESIAN_POINT ( 'NONE',  ( 767.7687537140311633, -335.9073299311468190, 372.7932403749916830 ) ) ;
#8111=CARTESIAN_POINT ( 'NONE',  ( 761.4292242960306112, -209.4636090269709996, 323.2154366446414429 ) ) ;
#8112=CARTESIAN_POINT ( 'NONE',  ( 789.9200121543843807, -361.9874144716864635, 317.0176451133914384 ) ) ;
#8114=CARTESIAN_POINT ( 'NONE',  ( 769.9779781133707957, -163.0999726633347677, 316.7813123517150871 ) ) ;
#8115=CARTESIAN_POINT ( 'NONE',  ( 785.3687786644884454, -59.36187538569306810, 315.3201227861279676 ) ) ;
#8119=CARTESIAN_POINT ( 'NONE',  ( 766.4474001241216001, -259.0999726633343698, 307.3154664389482491 ) ) ;
#8120=CARTESIAN_POINT ( 'NONE',  ( 760.5453621957607311, -237.0783235625960117, 323.8424801807151425 ) ) ;
#8123=CARTESIAN_POINT ( 'NONE',  ( 758.0580252608178853, -6.452784476602343666, 328.0187753319985404 ) ) ;
#8126=CARTESIAN_POINT ( 'NONE',  ( 804.7487373415286811, -43.54369356751131903, 364.7487373415288516 ) ) ;
#8127=CARTESIAN_POINT ( 'NONE',  ( 754.9967657858570647, -97.54369356751112718, 365.0032342141425374 ) ) ;
#8130=CARTESIAN_POINT ( 'NONE',  ( 745.5313806188320314, -399.2817908451522726, 333.7943932421247268 ) ) ;
#8133=CARTESIAN_POINT ( 'NONE',  ( 805.0032342141412300, -349.5436935675102745, 314.9967657858571783 ) ) ;
#8135=CARTESIAN_POINT ( 'NONE',  ( 778.2165204200184689, -430.8164208402374129, 364.9363028652563230 ) ) ;
#8136=CARTESIAN_POINT ( 'NONE',  ( 783.0745993439762742, -200.1908817542436907, 365.1016975059196739 ) ) ;
#8139=CARTESIAN_POINT ( 'NONE',  ( 778.7502325331095108, -96.35105083532370429, 304.6391490659818828 ) ) ;
#8140=CARTESIAN_POINT ( 'NONE',  ( 781.7834795799800531, -442.8164208402372992, 315.0636971347436202 ) ) ;
#8141=CARTESIAN_POINT ( 'NONE',  ( 808.7758568127978833, -172.1692326535052757, 320.0363995740631822 ) ) ;
#8146=CARTESIAN_POINT ( 'NONE',  ( 756.3353852180819104, -269.9073299311468190, 331.1735550268788302 ) ) ;
#8147=CARTESIAN_POINT ( 'NONE',  ( 774.6312213355098493, -263.3618753856924286, 364.6798772138717482 ) ) ;
#8150=CARTESIAN_POINT ( 'NONE',  ( 796.7845633553578182, 14.37622189194867417, 358.5707757039688204 ) ) ;
#8152=CARTESIAN_POINT ( 'NONE',  ( 763.2262854647970016, -176.6346026584199933, 309.2812353651462445 ) ) ;
#8153=CARTESIAN_POINT ( 'NONE',  ( 772.4468031744293057, -273.8272453906071746, 363.8651313633793620 ) ) ;
#8156=CARTESIAN_POINT ( 'NONE',  ( 813.9316612368132837, -223.4419599262323857, 348.6739635108323228 ) ) ;
#8161=CARTESIAN_POINT ( 'NONE',  ( 770.0799878456142551, -253.9874144716868329, 362.9823548866085616 ) ) ;
#8168=CARTESIAN_POINT ( 'NONE',  ( 814.8207195650702488, -170.1908817542438328, 336.2433038121456548 ) ) ;
#8176=CARTESIAN_POINT ( 'NONE',  ( 771.2633955100217236, 0.09267006885218045942, 363.4237431249939618 ) ) ;
#8177=CARTESIAN_POINT ( 'NONE',  ( 768.9521613784389729, -273.8272453906071746, 373.2346286133773106 ) ) ;
#8179=CARTESIAN_POINT ( 'NONE',  ( 751.6929314249748586, -246.9982390220560546, 318.8095938919659034 ) ) ;
#8183=CARTESIAN_POINT ( 'NONE',  ( 759.9864689768902508, -338.0891481129649492, 354.9819416627836404 ) ) ;
#8184=CARTESIAN_POINT ( 'NONE',  ( 787.5531968255692163, -69.82724539060775726, 316.1348686366205811 ) ) ;
#8187=DIRECTION ( 'NONE',  ( 0.000000000000000000, 1.000000000000000000, 0.000000000000000000 ) ) ;
#8188=CARTESIAN_POINT ( 'NONE',  ( 779.4709603349208464, -168.3510508353234911, 314.7162404726379918 ) ) ;
#8189=CARTESIAN_POINT ( 'NONE',  ( 797.6776695296629214, -355.5436935675103882, 357.6776695296636603 ) ) ;
#8192=CARTESIAN_POINT ( 'NONE',  ( 759.9864689768902508, -146.0891481129655176, 354.9819416627836404 ) ) ;
#8195=CARTESIAN_POINT ( 'NONE',  ( 805.0032342141412300, 10.45630643248850866, 314.9967657858571783 ) ) ;
#8197=CARTESIAN_POINT ( 'NONE',  ( 759.9864689768902508, -314.0891481129650629, 354.9819416627836404 ) ) ;
#8200=CARTESIAN_POINT ( 'NONE',  ( 781.8018195045266339, -430.2709662947827383, 365.1927285166406705 ) ) ;
#8206=CARTESIAN_POINT ( 'NONE',  ( 755.5713283507202505, -5.361875385693257279, 334.6858677611754729 ) ) ;
#8207=CARTESIAN_POINT ( 'NONE',  ( 787.5162901302840055, -227.3618753856925707, 305.4481719005792684 ) ) ;
#8208=CARTESIAN_POINT ( 'NONE',  ( 754.8983024940795303, -162.8965053807780521, 336.9254006560228163 ) ) ;
#8209=DIRECTION ( 'NONE',  ( 0.000000000000000000, -1.000000000000000000, 0.000000000000000000 ) ) ;
#8215=CARTESIAN_POINT ( 'NONE',  ( 748.6759233522253680, -64.37269993606231822, 324.3348316497537098 ) ) ;
#8223=CARTESIAN_POINT ( 'NONE',  ( 760.7433823573367135, -396.0090635724249637, 355.9930595647440441 ) ) ;
#8225=CARTESIAN_POINT ( 'NONE',  ( 793.9708237608222134, -238.9181544815163534, 319.2295555964448681 ) ) ;
#8228=CARTESIAN_POINT ( 'NONE',  ( 786.2694204179717872, -189.2817908451528979, 305.1769319972829067 ) ) ;
#8230=CARTESIAN_POINT ( 'NONE',  ( 767.6429770376289525, -129.1800572038746111, 306.8695393053162093 ) ) ;
#8233=FACE_BOUND ( 'NONE', #23348, .T. ) ;
#8234=CARTESIAN_POINT ( 'NONE',  ( 801.9419747391806368, -234.4527844766016358, 351.9812246680014027 ) ) ;
#8235=CARTESIAN_POINT ( 'NONE',  ( 786.5483106153019435, -31.64542720878970883, 364.1601925771022366 ) ) ;
#8239=CARTESIAN_POINT ( 'NONE',  ( 813.2346286133761168, -29.26014174441482751, 328.9521613784389160 ) ) ;
#8242=CARTESIAN_POINT ( 'NONE',  ( 778.1981804954714335, -34.27096629478407408, 314.8072714833589885 ) ) ;
#8246=CARTESIAN_POINT ( 'NONE',  ( 748.3538107759620743, -352.7146871989593251, 355.8262568251490165 ) ) ;
#8248=CARTESIAN_POINT ( 'NONE',  ( 800.1688906516307043, -418.1692326535044799, 369.0717654672308186 ) ) ;
#8250=CARTESIAN_POINT ( 'NONE',  ( 788.8264449731200330, -333.1800572038740142, 363.6646147819171233 ) ) ;
#8257=CARTESIAN_POINT ( 'NONE',  ( 795.1360043628807261, -44.08914811296584446, 360.2193346964456282 ) ) ;
#8258=CARTESIAN_POINT ( 'NONE',  ( 790.9844846989617508, -358.3726999360613945, 317.2208543904092721 ) ) ;
#8260=CARTESIAN_POINT ( 'NONE',  ( 777.5031285880264704, -382.8164208402374697, 374.9108240113588408 ) ) ;
#8261=CARTESIAN_POINT ( 'NONE',  ( 751.2241431872005251, -328.1692326535048210, 359.9636004259367610 ) ) ;
#8262=CARTESIAN_POINT ( 'NONE',  ( 808.7758568127978833, -100.1692326535055315, 320.0363995740631822 ) ) ;
#8268=CARTESIAN_POINT ( 'NONE',  ( 751.6929314249748586, -414.9982390220555430, 318.8095938919659034 ) ) ;
#8275=CARTESIAN_POINT ( 'NONE',  ( 787.5531968255692163, -309.8272453906070041, 316.1348686366205811 ) ) ;
#8276=CARTESIAN_POINT ( 'NONE',  ( 762.1405469898971887, -145.5436935675109851, 357.8594530101015607 ) ) ;
#8277=ORIENTED_EDGE ( 'NONE', *, *, #10242, .T. ) ;
#8280=CARTESIAN_POINT ( 'NONE',  ( 754.9735926884551418, -330.3510508353229511, 340.5236548041000333 ) ) ;
#8281=LINE ( 'NONE', #39936, #34463 ) ;
#8282=CARTESIAN_POINT ( 'NONE',  ( 752.7379699480933368, -60.00906357242598688, 361.9858362298580232 ) ) ;
#8283=CARTESIAN_POINT ( 'NONE',  ( 757.8323909638827445, -194.6346026584198796, 352.1044303154654358 ) ) ;
#8286=CARTESIAN_POINT ( 'NONE',  ( 813.1304606946830518, -209.9073299311470748, 352.3570229623690580 ) ) ;
#8287=CARTESIAN_POINT ( 'NONE',  ( 803.6646147819161570, -113.9073299311474301, 348.8264449731210561 ) ) ;
#8290=CARTESIAN_POINT ( 'NONE',  ( 779.4763451958990572, -8.736336299698871599, 365.0264073115438919 ) ) ;
#8293=CARTESIAN_POINT ( 'NONE',  ( 783.0433043558608688, -384.8965053807772847, 315.1538015810313027 ) ) ;
#8299=CARTESIAN_POINT ( 'NONE',  ( 803.8556311672234642, -249.6237781080505158, 365.6418435158340117 ) ) ;
#8300=CARTESIAN_POINT ( 'NONE',  ( 804.6798772138710092, -63.72551174932941365, 334.6312213355106451 ) ) ;
#8303=CARTESIAN_POINT ( 'NONE',  ( 756.5762568750052424, -243.1800572038743269, 348.7366044899774238 ) ) ;
#8310=CARTESIAN_POINT ( 'NONE',  ( 792.2312462859673587, -299.9073299311468759, 307.2067596250082602 ) ) ;
#8311=CARTESIAN_POINT ( 'NONE',  ( 751.2241431872005251, -40.16923265350570915, 359.9636004259367610 ) ) ;
#8318=CARTESIAN_POINT ( 'NONE',  ( 759.0252816721024374, -312.9982390220559409, 368.0189434323527280 ) ) ;
#8321=CARTESIAN_POINT ( 'NONE',  ( 772.3691319403857278, -359.2601417444137724, 315.8894580844506663 ) ) ;
#8324=CARTESIAN_POINT ( 'NONE',  ( 755.3028492785439312, -183.2817908451528695, 335.9200461376539693 ) ) ;
#8325=CARTESIAN_POINT ( 'NONE',  ( 762.3223304703356007, -31.54369356751135456, 322.3223304703362828 ) ) ;
#8326=VERTEX_POINT ( 'NONE', #27468 ) ;
#8330=CARTESIAN_POINT ( 'NONE',  ( 775.9200461376533440, -215.8055962898687881, 315.3028492785443291 ) ) ;
#8333=CARTESIAN_POINT ( 'NONE',  ( 754.9967657858570647, -433.5436935675099903, 365.0032342141425374 ) ) ;
#8338=CARTESIAN_POINT ( 'NONE',  ( 815.2698199232961542, -64.81642084023852135, 342.5225473063383106 ) ) ;
#8339=CARTESIAN_POINT ( 'NONE',  ( 751.6929314249748586, -102.9982390220565520, 318.8095938919659034 ) ) ;
#8341=CARTESIAN_POINT ( 'NONE',  ( 757.7880784355613741, -402.0090635724250205, 312.4576283171834916 ) ) ;
#8342=CARTESIAN_POINT ( 'NONE',  ( 744.6391490659812007, -398.7363362996976548, 338.7502325331110455 ) ) ;
#8344=CARTESIAN_POINT ( 'NONE',  ( 787.4397851343537695, -357.7255117493285184, 374.2001403089903988 ) ) ;
#8346=CARTESIAN_POINT ( 'NONE',  ( 800.7704444035546203, 19.83076734649410966, 326.0291762391768771 ) ) ;
#8349=CARTESIAN_POINT ( 'NONE',  ( 745.1769319972822814, -137.8055962898690154, 346.2694204179732083 ) ) ;
#8350=CARTESIAN_POINT ( 'NONE',  ( 756.5762568750052424, -435.1800572038737869, 348.7366044899774238 ) ) ;
#8352=CARTESIAN_POINT ( 'NONE',  ( 744.9990715423526808, -162.3510508353235196, 341.2370466360926002 ) ) ;
#8357=CARTESIAN_POINT ( 'NONE',  ( 758.0580252608178853, -270.4527844766014937, 328.0187753319985404 ) ) ;
#8358=CARTESIAN_POINT ( 'NONE',  ( 771.2633955100217236, -263.9073299311469327, 363.4237431249939618 ) ) ;
#8362=CARTESIAN_POINT ( 'NONE',  ( 790.8050863131179540, -452.8379544210779954, 362.5841948692291226 ) ) ;
#8363=CARTESIAN_POINT ( 'NONE',  ( 784.0799538623451781, -371.8055962898682765, 364.6971507214555572 ) ) ;
#8365=CARTESIAN_POINT ( 'NONE',  ( 808.3070685750232087, -186.9982390220563104, 361.1904061080339829 ) ) ;
#8366=CARTESIAN_POINT ( 'NONE',  ( 755.8894580844503253, -279.8272453906071746, 332.3691319403863531 ) ) ;
#8367=CARTESIAN_POINT ( 'NONE',  ( 804.1601925771018387, -415.4419599262318457, 346.5483106153029098 ) ) ;
#8370=CARTESIAN_POINT ( 'NONE',  ( 803.8556311672234642, -201.6237781080506863, 365.6418435158340117 ) ) ;
#8377=CARTESIAN_POINT ( 'NONE',  ( 795.9930595647434757, -267.0783235625958696, 320.7433823573372820 ) ) ;
#8380=EDGE_CURVE ( 'NONE', #11197, #20161, #34853, .T. ) ;
#8385=CARTESIAN_POINT ( 'NONE',  ( 747.6481478633932056, -181.0999726633347109, 353.4146539503763620 ) ) ;
#8390=CARTESIAN_POINT ( 'NONE',  ( 801.1904061080336987, -20.08914811296592973, 368.3070685750235498 ) ) ;
#8391=AXIS2_PLACEMENT_3D ( 'NONE', #19288, #44456, #16059 ) ;
#8395=CARTESIAN_POINT ( 'NONE',  ( 794.9819416627830151, -36.99823902205679360, 319.9864689768909898 ) ) ;
#8397=CARTESIAN_POINT ( 'NONE',  ( 750.9282345327678740, -280.9181544815162965, 319.8311093483690115 ) ) ;
#8399=CARTESIAN_POINT ( 'NONE',  ( 814.2001403089898304, -257.3618753856924286, 347.4397851343538264 ) ) ;
#8403=CARTESIAN_POINT ( 'NONE',  ( 765.0180583372156207, -360.9982390220557704, 360.0135310231089534 ) ) ;
#8404=CARTESIAN_POINT ( 'NONE',  ( 760.7433823573367135, -84.00906357242590161, 355.9930595647440441 ) ) ;
#8409=CARTESIAN_POINT ( 'NONE',  ( 815.0009284576459549, -126.3510508353236048, 338.7629533639073429 ) ) ;
#8410=CARTESIAN_POINT ( 'NONE',  ( 805.1927285166397041, -400.8164208402373561, 341.8018195045277707 ) ) ;
#8414=CARTESIAN_POINT ( 'NONE',  ( 767.8955696845333705, -144.4527844766018632, 362.1676090361162323 ) ) ;
#8417=CARTESIAN_POINT ( 'NONE',  ( 813.9316612368132837, -439.4419599262316751, 348.6739635108323228 ) ) ;
#8419=CARTESIAN_POINT ( 'NONE',  ( 804.4286716492782716, -353.3618753856922012, 345.3141322388244703 ) ) ;
#8422=CARTESIAN_POINT ( 'NONE',  ( 788.8264449731200330, -429.1800572038737869, 363.6646147819171233 ) ) ;
#8430=CARTESIAN_POINT ( 'NONE',  ( 804.4086373105744769, -457.6454272087884760, 333.3843516231986541 ) ) ;
#8431=CARTESIAN_POINT ( 'NONE',  ( 792.2312462859673587, -227.9073299311471033, 307.2067596250082602 ) ) ;
#8432=CARTESIAN_POINT ( 'NONE',  ( 799.4546378042377910, -153.0783235625962675, 356.1575198192848006 ) ) ;
#8434=LINE ( 'NONE', #13487, #21842 ) ;
#8439=CARTESIAN_POINT ( 'NONE',  ( 783.7953271457878373, -80.19088175424411702, 375.1787889125761239 ) ) ;
#8443=DIRECTION ( 'NONE',  ( -1.000000000000000000, -0.000000000000000000, -0.000000000000000000 ) ) ;
#8448=CARTESIAN_POINT ( 'NONE',  ( 800.9840315886518738, -388.9181544815158986, 354.1144889064786412 ) ) ;
#8453=CARTESIAN_POINT ( 'NONE',  ( 748.6759233522253680, -184.3726999360619629, 324.3348316497537098 ) ) ;
#8455=CARTESIAN_POINT ( 'NONE',  ( 796.7737145352015204, -140.6346026584201070, 370.7187646348536987 ) ) ;
#8460=CARTESIAN_POINT ( 'NONE',  ( 792.1044303154645831, -228.4527844766015789, 317.8323909638837677 ) ) ;
#8461=CIRCLE ( 'NONE', #1771, 10.00000000000000888 ) ;
#8462=CARTESIAN_POINT ( 'NONE',  ( 755.1538015810308480, -14.19088175424431242, 343.0433043558613804 ) ) ;
#8467=CARTESIAN_POINT ( 'NONE',  ( 803.8556311672234642, -33.62377810805116951, 365.6418435158340117 ) ) ;
#8468=CARTESIAN_POINT ( 'NONE',  ( 803.4237431249931660, -303.1800572038740711, 331.2633955100225194 ) ) ;
#8469=ORIENTED_EDGE ( 'NONE', *, *, #42688, .F. ) ;
#8471=CARTESIAN_POINT ( 'NONE',  ( 778.1981804954714335, -10.27096629478414691, 314.8072714833589885 ) ) ;
#8474=CARTESIAN_POINT ( 'NONE',  ( 783.7566961878529810, -360.8965053807773984, 305.1792804349288417 ) ) ;
#8478=CARTESIAN_POINT ( 'NONE',  ( 793.4146539503750546, -433.9874144716862361, 307.6481478633938877 ) ) ;
#8479=CARTESIAN_POINT ( 'NONE',  ( 792.1044303154645831, -348.4527844766012663, 317.8323909638837677 ) ) ;
#8487=CARTESIAN_POINT ( 'NONE',  ( 785.3687786644884454, -59.36187538569306810, 315.3201227861279676 ) ) ;
#8488=CARTESIAN_POINT ( 'NONE',  ( 763.8424801807145741, -378.0090635724250774, 320.5453621957614700 ) ) ;
#8490=CARTESIAN_POINT ( 'NONE',  ( 763.2262854647970016, -440.6346026584191122, 309.2812353651462445 ) ) ;
#8492=CARTESIAN_POINT ( 'NONE',  ( 749.8865473780648472, -332.5328690171411381, 322.1177392798429082 ) ) ;
#8500=CARTESIAN_POINT ( 'NONE',  ( 763.0537975583475827, -432.4527844766008684, 371.0346526505627480 ) ) ;
#8507=CARTESIAN_POINT ( 'NONE',  ( 757.4527132478984868, -280.3726999360616787, 329.1273215169538844 ) ) ;
#8508=CARTESIAN_POINT ( 'NONE',  ( 756.3353852180819104, -173.9073299311472169, 331.1735550268788302 ) ) ;
#8512=CARTESIAN_POINT ( 'NONE',  ( 760.5453621957607311, -333.0783235625956991, 323.8424801807151425 ) ) ;
#8514=CARTESIAN_POINT ( 'NONE',  ( 747.6481478633932056, -85.09997266333499510, 353.4146539503763620 ) ) ;
#8518=CARTESIAN_POINT ( 'NONE',  ( 767.8955696845333705, -120.4527844766019484, 362.1676090361162323 ) ) ;
#8522=CARTESIAN_POINT ( 'NONE',  ( 787.5531968255692163, -21.82724539060792424, 316.1348686366205811 ) ) ;
#8525=CARTESIAN_POINT ( 'NONE',  ( 772.3691319403857278, -407.2601417444137155, 315.8894580844506663 ) ) ;
#8526=VERTEX_POINT ( 'NONE', #34086 ) ;
#8532=CARTESIAN_POINT ( 'NONE',  ( 744.8212110874229666, -234.8965053807777963, 336.2046728542121627 ) ) ;
#8533=CARTESIAN_POINT ( 'NONE',  ( 788.7366044899766848, -35.90732993114770011, 316.5762568750059813 ) ) ;
#8535=CARTESIAN_POINT ( 'NONE',  ( 764.8639956371174549, -224.0891481129653187, 319.7806653035542013 ) ) ;
#8546=CARTESIAN_POINT ( 'NONE',  ( 767.7687537140311633, -335.9073299311468190, 372.7932403749916830 ) ) ;
#8547=CARTESIAN_POINT ( 'NONE',  ( 754.0944755984390895, -39.62377810805116951, 364.1009440267246760 ) ) ;
#8553=CARTESIAN_POINT ( 'NONE',  ( 771.1735550268778070, -225.1800572038743269, 316.3353852180827630 ) ) ;
#8556=CARTESIAN_POINT ( 'NONE',  ( 792.3570229623688874, -333.1800572038740142, 373.1304606946836202 ) ) ;
#8560=CARTESIAN_POINT ( 'NONE',  ( 772.4468031744293057, -201.8272453906073451, 363.8651313633793620 ) ) ;
#8561=CARTESIAN_POINT ( 'NONE',  ( 785.3141322388236176, -45.72551174932949181, 364.4286716492789537 ) ) ;
#8565=CARTESIAN_POINT ( 'NONE',  ( 775.9200461376533440, -239.8055962898687028, 315.3028492785443291 ) ) ;
#8566=VECTOR ( 'NONE', #27340, 1000.000000000000000 ) ;
#8569=CARTESIAN_POINT ( 'NONE',  ( 767.6429770376289525, -417.1800572038736163, 306.8695393053162093 ) ) ;
#8575=CARTESIAN_POINT ( 'NONE',  ( 751.6929314249748586, -54.99823902205672255, 318.8095938919659034 ) ) ;
#8576=CARTESIAN_POINT ( 'NONE',  ( 810.7187646348534145, -114.4527844766020053, 356.7737145352016341 ) ) ;
#8581=CARTESIAN_POINT ( 'NONE',  ( 745.7998596910086917, -365.3618753856920875, 332.5602148656461168 ) ) ;
#8584=CARTESIAN_POINT ( 'NONE',  ( 786.6156483768007774, 22.55804007376682918, 315.5913626894246136 ) ) ;
#8587=CARTESIAN_POINT ( 'NONE',  ( 744.9990715423526808, -138.3510508353236048, 341.2370466360926002 ) ) ;
#8588=CARTESIAN_POINT ( 'NONE',  ( 771.2633955100217236, -431.9073299311464211, 363.4237431249939618 ) ) ;
#8592=CARTESIAN_POINT ( 'NONE',  ( 801.9419747391806368, -114.4527844766020053, 351.9812246680014027 ) ) ;
#8595=CARTESIAN_POINT ( 'NONE',  ( 778.1981804954714335, -250.2709662947832783, 314.8072714833589885 ) ) ;
#8596=CARTESIAN_POINT ( 'NONE',  ( 778.2165204200184689, -262.8164208402379245, 364.9363028652563230 ) ) ;
#8599=CARTESIAN_POINT ( 'NONE',  ( 764.0069404352550464, 8.921676437403235127, 359.2566176426627180 ) ) ;
#8605=CARTESIAN_POINT ( 'NONE',  ( 782.4968714119720516, -202.8164208402380950, 305.0891759886411023 ) ) ;
#8606=CARTESIAN_POINT ( 'NONE',  ( 786.5483106153019435, -295.6454272087888739, 364.1601925771022366 ) ) ;
#8607=CARTESIAN_POINT ( 'NONE',  ( 765.8855110935204493, -406.1692326535045368, 319.0159684113471599 ) ) ;
#8614=CARTESIAN_POINT ( 'NONE',  ( 761.2382568024794409, -255.6237781080504874, 356.9571628226838129 ) ) ;
#8623=CARTESIAN_POINT ( 'NONE',  ( 752.7379699480933368, -180.0090635724255890, 361.9858362298580232 ) ) ;
#8629=CARTESIAN_POINT ( 'NONE',  ( 751.6929314249748586, -6.998239022056885972, 318.8095938919659034 ) ) ;
#8632=CYLINDRICAL_SURFACE ( 'NONE', #6231, 10.00000000000000888 ) ;
#8633=CARTESIAN_POINT ( 'NONE',  ( 803.6646147819161570, -41.90732993114767169, 348.8264449731210561 ) ) ;
#8634=CARTESIAN_POINT ( 'NONE',  ( 783.7953271457878373, -296.1908817542434917, 375.1787889125761239 ) ) ;
#8635=CARTESIAN_POINT ( 'NONE',  ( 767.6429770376289525, -273.1800572038742985, 306.8695393053162093 ) ) ;
#8640=CARTESIAN_POINT ( 'NONE',  ( 764.8639956371174549, -344.0891481129647786, 319.7806653035542013 ) ) ;
#8642=CARTESIAN_POINT ( 'NONE',  ( 755.1538015810308480, -110.1908817542440033, 343.0433043558613804 ) ) ;
#8648=CARTESIAN_POINT ( 'NONE',  ( 755.0636971347428243, -388.2709662947829656, 341.7834795799807353 ) ) ;
#8650=ADVANCED_FACE ( 'NONE', ( #37563 ), #19548, .F. ) ;
#8652=CARTESIAN_POINT ( 'NONE',  ( 797.8594530101008786, -157.5436935675108998, 322.1405469898980982 ) ) ;
#8655=ORIENTED_EDGE ( 'NONE', *, *, #8659, .T. ) ;
#8656=CARTESIAN_POINT ( 'NONE',  ( 785.3141322388236176, -357.7255117493285184, 364.4286716492789537 ) ) ;
#8658=CARTESIAN_POINT ( 'NONE',  ( 771.1735550268778070, -441.1800572038735027, 316.3353852180827630 ) ) ;
#8659=EDGE_CURVE ( 'NONE', #7675, #10891, #20010, .T. ) ;
#8662=CARTESIAN_POINT ( 'NONE',  ( 787.5162901302840055, -83.36187538569299704, 305.4481719005793252 ) ) ;
#8668=CARTESIAN_POINT ( 'NONE',  ( 785.3141322388236176, 2.274488250670355871, 364.4286716492789537 ) ) ;
#8669=CARTESIAN_POINT ( 'NONE',  ( 801.1904061080336987, -260.0891481129650060, 368.3070685750235498 ) ) ;
#8670=CARTESIAN_POINT ( 'NONE',  ( 794.1144889064781864, -154.1692326535053894, 360.9840315886528401 ) ) ;
#8677=CARTESIAN_POINT ( 'NONE',  ( 768.9521613784389729, -57.82724539060780700, 373.2346286133773106 ) ) ;
#8687=CARTESIAN_POINT ( 'NONE',  ( 804.1105419155481968, -387.8272453906067767, 347.6308680596136469 ) ) ;
#8689=CARTESIAN_POINT ( 'NONE',  ( 796.9571628226829034, -239.4636090269709143, 321.2382568024804641 ) ) ;
#8692=CARTESIAN_POINT ( 'NONE',  ( 791.0478386215596629, -189.8272453906073736, 306.7653713866226326 ) ) ;
#8694=CARTESIAN_POINT ( 'NONE',  ( 772.5602148656447525, -153.7255117493291721, 305.7998596910095443 ) ) ;
#8698=CARTESIAN_POINT ( 'NONE',  ( 804.6798772138708955, -255.7255117493287742, 334.6312213355107019 ) ) ;
#8699=CARTESIAN_POINT ( 'NONE',  ( 780.5236548040995785, -20.73633629969883430, 314.9735926884559944 ) ) ;
#8704=CARTESIAN_POINT ( 'NONE',  ( 799.4546378042377910, -81.07832356259649487, 356.1575198192848006 ) ) ;
#8707=CARTESIAN_POINT ( 'NONE',  ( 804.6798772138708955, -63.72551174932939233, 334.6312213355107019 ) ) ;
#8710=CARTESIAN_POINT ( 'NONE',  ( 746.0683387631852383, -355.4419599262319593, 331.3260364891676204 ) ) ;
#8713=CARTESIAN_POINT ( 'NONE',  ( 745.1769319972822814, -425.8055962898680491, 346.2694204179732083 ) ) ;
#8715=CARTESIAN_POINT ( 'NONE',  ( 802.1676090361156639, -326.6346026584193396, 327.8955696845344505 ) ) ;
#8723=CARTESIAN_POINT ( 'NONE',  ( 762.3223304703356007, -79.54369356751119824, 322.3223304703362828 ) ) ;
#8724=CARTESIAN_POINT ( 'NONE',  ( 759.0159684113467620, -376.9181544815159555, 325.8855110935213020 ) ) ;
#8725=CARTESIAN_POINT ( 'NONE',  ( 787.5162901302840055, -419.3618753856918602, 305.4481719005793252 ) ) ;
#8727=CARTESIAN_POINT ( 'NONE',  ( 800.1688906516307043, -322.1692326535048210, 369.0717654672308186 ) ) ;
#8728=CARTESIAN_POINT ( 'NONE',  ( 778.7502325331095108, -96.35105083532370429, 304.6391490659818828 ) ) ;
#8732=CARTESIAN_POINT ( 'NONE',  ( 759.0252816721024374, -432.9982390220555999, 368.0189434323527280 ) ) ;
#8736=LINE ( 'NONE', #14764, #5687 ) ;
#8737=CARTESIAN_POINT ( 'NONE',  ( 759.9999999999992042, -512.9681489794448908, 339.9999999999999432 ) ) ;
#8738=CARTESIAN_POINT ( 'NONE',  ( 804.6971507214547046, -291.2817908451525000, 344.0799538623459739 ) ) ;
#8739=CARTESIAN_POINT ( 'NONE',  ( 804.6798772138708955, -183.7255117493290015, 334.6312213355107019 ) ) ;
#8743=CARTESIAN_POINT ( 'NONE',  ( 755.8990559732751535, -83.46360902697136908, 365.9055244015606831 ) ) ;
#8746=CARTESIAN_POINT ( 'NONE',  ( 785.3141322388236176, -141.7255117493291721, 364.4286716492789537 ) ) ;
#8750=CARTESIAN_POINT ( 'NONE',  ( 796.1575198192839480, -6.009063572426154742, 359.4546378042384163 ) ) ;
#8752=PLANE ( 'NONE',  #29858 ) ;
#8753=CARTESIAN_POINT ( 'NONE',  ( 763.2154366446407039, -381.6237781080500326, 321.4292242960311228 ) ) ;
#8757=CARTESIAN_POINT ( 'NONE',  ( 813.2346286133761168, -245.2601417444141987, 328.9521613784389160 ) ) ;
#8758=CARTESIAN_POINT ( 'NONE',  ( 802.1676090361155502, -38.63460265842041963, 327.8955696845344505 ) ) ;
#8761=CARTESIAN_POINT ( 'NONE',  ( 768.0187753319979720, -224.6346026584198228, 318.0580252608186242 ) ) ;
#8764=DIRECTION ( 'NONE',  ( 0.000000000000000000, 0.000000000000000000, -1.000000000000000000 ) ) ;
#8769=CARTESIAN_POINT ( 'NONE',  ( 759.0252816721024374, -336.9982390220558273, 368.0189434323527280 ) ) ;
#8770=CARTESIAN_POINT ( 'NONE',  ( 746.0683387631852383, -43.44195992623296831, 331.3260364891676204 ) ) ;
#8775=CARTESIAN_POINT ( 'NONE',  ( 800.2193346964447755, -210.9982390220561967, 355.1360043628815788 ) ) ;
#8778=CARTESIAN_POINT ( 'NONE',  ( 751.6929314249748586, -318.9982390220557704, 318.8095938919659034 ) ) ;
#8782=CARTESIAN_POINT ( 'NONE',  ( 775.8780910478218402, -177.2817908451528695, 364.9511171171680530 ) ) ;
#8783=CARTESIAN_POINT ( 'NONE',  ( 754.8072714833581358, -100.8164208402383792, 338.1981804954720587 ) ) ;
#8787=CARTESIAN_POINT ( 'NONE',  ( 780.5290396650775619, -252.3510508353232353, 365.2837595273619513 ) ) ;
#8790=CARTESIAN_POINT ( 'NONE',  ( 745.0891759886404770, -436.2709662947827951, 342.4968714119734159 ) ) ;
#8794=CARTESIAN_POINT ( 'NONE',  ( 808.0189434323515343, -62.08914811296580183, 319.0252816721025511 ) ) ;
#8795=CARTESIAN_POINT ( 'NONE',  ( 814.9108240113580450, -136.2709662947837330, 337.5031285880265273 ) ) ;
#8800=CARTESIAN_POINT ( 'NONE',  ( 787.5162901302840055, -347.3618753856922012, 305.4481719005792684 ) ) ;
#8803=CARTESIAN_POINT ( 'NONE',  ( 756.1348686366196716, 6.739858255585061464, 347.5531968255698416 ) ) ;
#8806=CARTESIAN_POINT ( 'NONE',  ( 768.8385539511368734, -143.2601417444144829, 306.4236121716840557 ) ) ;
#8811=CARTESIAN_POINT ( 'NONE',  ( 791.9812246680005501, -140.6346026584201070, 361.9419747391813189 ) ) ;
#8813=CARTESIAN_POINT ( 'NONE',  ( 788.7366044899766848, -275.9073299311469896, 316.5762568750059813 ) ) ;
#8814=CARTESIAN_POINT ( 'NONE',  ( 778.1981804954715471, -250.2709662947833351, 314.8072714833591021 ) ) ;
#8817=CARTESIAN_POINT ( 'NONE',  ( 756.7813123517142913, 4.012585528312341054, 329.9779781133712504 ) ) ;
#8821=CARTESIAN_POINT ( 'NONE',  ( 812.7932403749906598, -207.1800572038744406, 327.7687537140311633 ) ) ;
#8822=CARTESIAN_POINT ( 'NONE',  ( 780.5236548040995785, -308.7363362996979390, 314.9735926884559944 ) ) ;
#8823=CARTESIAN_POINT ( 'NONE',  ( 780.5290396650775619, -396.3510508353228374, 365.2837595273619513 ) ) ;
#8827=VERTEX_POINT ( 'NONE', #15637 ) ;
#8831=CARTESIAN_POINT ( 'NONE',  ( 759.2295555964440155, -280.1692326535049347, 353.9708237608231229 ) ) ;
#8834=CARTESIAN_POINT ( 'NONE',  ( 792.1044303154645831, 11.54721552339760038, 317.8323909638837677 ) ) ;
#8837=CARTESIAN_POINT ( 'NONE',  ( 791.0478386215596629, -213.8272453906073167, 306.7653713866226326 ) ) ;
#8843=CARTESIAN_POINT ( 'NONE',  ( 748.9653473494363425, -50.63460265842036989, 356.9462024416521331 ) ) ;
#8846=DIRECTION ( 'NONE',  ( -0.000000000000000000, 1.000000000000000000, -0.000000000000000000 ) ) ;
#8847=CARTESIAN_POINT ( 'NONE',  ( 800.0135310231082713, -38.08914811296587999, 325.0180583372163028 ) ) ;
#8848=CARTESIAN_POINT ( 'NONE',  ( 747.6481478633932056, -277.0999726633344267, 353.4146539503763620 ) ) ;
#8849=CARTESIAN_POINT ( 'NONE',  ( 751.9810565676468741, -266.0891481129651197, 360.9747183278973921 ) ) ;
#8854=CARTESIAN_POINT ( 'NONE',  ( 797.8594530101008786, -349.5436935675102745, 322.1405469898980982 ) ) ;
#8855=CARTESIAN_POINT ( 'NONE',  ( 804.1105419155481968, -123.8272453906076009, 347.6308680596136469 ) ) ;
#8859=CARTESIAN_POINT ( 'NONE',  ( 795.1360043628807261, -404.0891481129646081, 360.2193346964456282 ) ) ;
#8862=CARTESIAN_POINT ( 'NONE',  ( 767.8955696845333705, -168.4527844766018347, 362.1676090361162323 ) ) ;
#8863=CARTESIAN_POINT ( 'NONE',  ( 755.3201227861273992, -171.7255117493290868, 345.3687786644892981 ) ) ;
#8864=PRODUCT_DEFINITION_CONTEXT ( 'detailed design', #17542, 'design' ) ;
#8869=CARTESIAN_POINT ( 'NONE',  ( 755.0636971347428243, -364.2709662947830793, 341.7834795799807353 ) ) ;
#8873=CARTESIAN_POINT ( 'NONE',  ( 767.7687537140311633, -119.9073299311474443, 372.7932403749916830 ) ) ;
#8878=CARTESIAN_POINT ( 'NONE',  ( 814.9108240113580450, -256.2709662947834204, 337.5031285880265273 ) ) ;
#8879=CARTESIAN_POINT ( 'NONE',  ( 805.0264073115434940, -174.3510508353234627, 339.4763451958999099 ) ) ;
#8886=CARTESIAN_POINT ( 'NONE',  ( 746.4236121716829757, -111.8272453906076151, 328.8385539511384650 ) ) ;
#8896=CARTESIAN_POINT ( 'NONE',  ( 766.0291762391763086, -394.9181544815158418, 360.7704444035551319 ) ) ;
#8897=ADVANCED_FACE ( 'NONE', ( #44963 ), #41490, .F. ) ;
#8902=CARTESIAN_POINT ( 'NONE',  ( 809.0717654672305343, -196.9181544815164386, 360.1688906516309885 ) ) ;
#8904=CARTESIAN_POINT ( 'NONE',  ( 814.2001403089898304, -137.3618753856928265, 347.4397851343538264 ) ) ;
#8906=EDGE_CURVE ( 'NONE', #34191, #16721, #13320, .T. ) ;
#8908=CARTESIAN_POINT ( 'NONE',  ( 767.8955696845333705, -240.4527844766015221, 362.1676090361162323 ) ) ;
#8909=CARTESIAN_POINT ( 'NONE',  ( 763.0428371773158460, -35.46360902697151829, 358.7617431975195359 ) ) ;
#8914=CARTESIAN_POINT ( 'NONE',  ( 754.8983024940795303, -90.89650538077827946, 336.9254006560228163 ) ) ;
#8917=CARTESIAN_POINT ( 'NONE',  ( 756.5762568750052424, -75.18005720387485269, 348.7366044899774238 ) ) ;
#8919=CARTESIAN_POINT ( 'NONE',  ( 754.0944755984390895, -351.6237781080502032, 364.1009440267246760 ) ) ;
#8921=CARTESIAN_POINT ( 'NONE',  ( 814.8230680027162407, -437.8055962898679923, 333.7305795820267917 ) ) ;
#8923=CARTESIAN_POINT ( 'NONE',  ( 764.8639956371174549, -368.0891481129647786, 319.7806653035542013 ) ) ;
#8928=ORIENTED_EDGE ( 'NONE', *, *, #17368, .T. ) ;
#8930=CARTESIAN_POINT ( 'NONE',  ( 756.5762568750052424, -99.18005720387478164, 348.7366044899774238 ) ) ;
#8931=CARTESIAN_POINT ( 'NONE',  ( 758.4439275373578084, -420.5545181178793541, 353.2243759319684386 ) ) ;
#8932=CARTESIAN_POINT ( 'NONE',  ( 749.2812353651451076, -414.4527844766010389, 323.2262854647983090 ) ) ;
#8934=CARTESIAN_POINT ( 'NONE',  ( 756.1443688327750579, -333.6237781080502600, 314.3581564841659315 ) ) ;
#8935=CARTESIAN_POINT ( 'NONE',  ( 754.0944755984390895, -111.6237781080509279, 364.1009440267246760 ) ) ;
#8940=CARTESIAN_POINT ( 'NONE',  ( 758.8095938919642549, -440.0891481129644944, 311.6929314249763365 ) ) ;
#8948=CARTESIAN_POINT ( 'NONE',  ( 783.0745993439762742, -296.1908817542434917, 365.1016975059196739 ) ) ;
#8949=EDGE_CURVE ( 'NONE', #44204, #45600, #28075, .T. ) ;
#8950=CARTESIAN_POINT ( 'NONE',  ( 800.0135310231082713, -182.0891481129654323, 325.0180583372163028 ) ) ;
#8952=CARTESIAN_POINT ( 'NONE',  ( 814.4686193811664907, -267.2817908451526137, 346.2056067578752732 ) ) ;
#8955=CARTESIAN_POINT ( 'NONE',  ( 776.2046728542105711, -92.19088175424406018, 304.8212110874238761 ) ) ;
#8958=CARTESIAN_POINT ( 'NONE',  ( 797.6776695296629214, -163.5436935675109567, 357.6776695296636603 ) ) ;
#8962=CARTESIAN_POINT ( 'NONE',  ( 790.0220218866281812, -31.09997266333516919, 363.2186876482849129 ) ) ;
#8965=CARTESIAN_POINT ( 'NONE',  ( 789.9200121543843807, -433.9874144716862361, 317.0176451133914384 ) ) ;
#8966=ORIENTED_EDGE ( 'NONE', *, *, #29262, .F. ) ;
#8970=CARTESIAN_POINT ( 'NONE',  ( 791.1614460488616487, -227.2601417444141987, 373.5763878283158874 ) ) ;
#8971=CARTESIAN_POINT ( 'NONE',  ( 805.1927285166399315, -88.81642084023843609, 341.8018195045277707 ) ) ;
#8974=CARTESIAN_POINT ( 'NONE',  ( 754.8072714833581358, -268.8164208402378108, 338.1981804954720587 ) ) ;
#8976=DIRECTION ( 'NONE',  ( -1.000000000000000000, -0.000000000000000000, 0.000000000000000000 ) ) ;
#8981=CARTESIAN_POINT ( 'NONE',  ( 800.9747183278959710, -324.9982390220559409, 311.9810565676471583 ) ) ;
#8982=CARTESIAN_POINT ( 'NONE',  ( 764.3348316497523456, -22.71468719896029853, 308.6759233522265617 ) ) ;
#8987=EDGE_LOOP ( 'NONE', ( #2012, #36325, #4837, #24253, #26408, #12665, #37665, #4056 ) ) ;
#8988=CARTESIAN_POINT ( 'NONE',  ( 792.1044303154645831, -204.4527844766016926, 317.8323909638837677 ) ) ;
#8991=CARTESIAN_POINT ( 'NONE',  ( 745.4481719005789273, -315.7255117493286320, 347.5162901302853129 ) ) ;
#8992=DIRECTION ( 'NONE',  ( -0.000000000000000000, 1.000000000000000000, -0.000000000000000000 ) ) ;
#8993=DIRECTION ( 'NONE',  ( -0.000000000000000000, 1.000000000000000000, -0.000000000000000000 ) ) ;
#8995=CARTESIAN_POINT ( 'NONE',  ( 804.6971507214547046, -195.2817908451528410, 344.0799538623459739 ) ) ;
#8996=CARTESIAN_POINT ( 'NONE',  ( 794.9819416627830151, -84.99823902205663728, 319.9864689768909898 ) ) ;
#9000=CARTESIAN_POINT ( 'NONE',  ( 773.3843516231979720, -253.4419599262323572, 364.4086373105754433 ) ) ;
#9003=CARTESIAN_POINT ( 'NONE',  ( 805.0032342141412300, -421.5436935675101040, 314.9967657858571783 ) ) ;
#9007=CARTESIAN_POINT ( 'NONE',  ( 812.7932403749906598, -87.18005720387481006, 327.7687537140311633 ) ) ;
#9008=CARTESIAN_POINT ( 'NONE',  ( 811.0346526505616112, -134.6346026584201070, 323.0537975583477532 ) ) ;
#9012=CARTESIAN_POINT ( 'NONE',  ( 800.9747183278959710, -348.9982390220558273, 311.9810565676471583 ) ) ;
#9014=CARTESIAN_POINT ( 'NONE',  ( 803.8651313633788504, 18.73985825558501972, 332.4468031744301015 ) ) ;
#9018=CARTESIAN_POINT ( 'NONE',  ( 756.1443688327750579, -141.6237781080508569, 314.3581564841659315 ) ) ;
#9019=CARTESIAN_POINT ( 'NONE',  ( 801.9419747391806368, 5.547215523397618142, 351.9812246680014027 ) ) ;
#9023=CARTESIAN_POINT ( 'NONE',  ( 774.6312213355099630, -119.3618753856928691, 364.6798772138717482 ) ) ;
#9025=CARTESIAN_POINT ( 'NONE',  ( 788.8264449731200330, -285.1800572038740711, 363.6646147819171233 ) ) ;
#9026=CARTESIAN_POINT ( 'NONE',  ( 785.3687786644885591, -275.3618753856924286, 315.3201227861280813 ) ) ;
#9028=ORIENTED_EDGE ( 'NONE', *, *, #19257, .T. ) ;
#9029=CARTESIAN_POINT ( 'NONE',  ( 804.1601925771018387, 16.55804007376685050, 346.5483106153029098 ) ) ;
#9033=CARTESIAN_POINT ( 'NONE',  ( 815.2698199232962679, -208.8164208402380666, 342.5225473063383674 ) ) ;
#9034=CARTESIAN_POINT ( 'NONE',  ( 804.6971507214547046, -315.2817908451525000, 344.0799538623459739 ) ) ;
#9035=CARTESIAN_POINT ( 'NONE',  ( 773.3843516231979720, -397.4419599262317320, 364.4086373105754433 ) ) ;
#9044=CARTESIAN_POINT ( 'NONE',  ( 760.5453621957607311, -285.0783235625958127, 323.8424801807151425 ) ) ;
#9046=DIRECTION ( 'NONE',  ( 0.000000000000000000, 0.000000000000000000, -1.000000000000000000 ) ) ;
#9047=CARTESIAN_POINT ( 'NONE',  ( 794.9819416627830151, 11.00176097794305541, 319.9864689768909898 ) ) ;
#9051=ADVANCED_FACE ( 'NONE', ( #31556 ), #27619, .F. ) ;
#9052=CARTESIAN_POINT ( 'NONE',  ( 814.2805881961230625, -193.6454272087891582, 331.2368401574024119 ) ) ;
#9057=CARTESIAN_POINT ( 'NONE',  ( 808.0189434323515343, -38.08914811296587999, 319.0252816721025511 ) ) ;
#9061=CARTESIAN_POINT ( 'NONE',  ( 788.8264449731200330, -45.18005720387493085, 363.6646147819171233 ) ) ;
#9062=CARTESIAN_POINT ( 'NONE',  ( 797.8822607201568644, -318.5545181178796952, 370.1134526219340160 ) ) ;
#9063=CARTESIAN_POINT ( 'NONE',  ( 744.7301800767019131, -244.8164208402378961, 337.4774526936615757 ) ) ;
#9068=CARTESIAN_POINT ( 'NONE',  ( 788.7366044899766848, -347.9073299311467053, 316.5762568750059813 ) ) ;
#9070=CARTESIAN_POINT ( 'NONE',  ( 754.7162404726377645, -134.7363362996984790, 339.4709603349214717 ) ) ;
#9072=CARTESIAN_POINT ( 'NONE',  ( 791.9812246680005501, -356.6346026584193964, 361.9419747391813189 ) ) ;
#9076=CARTESIAN_POINT ( 'NONE',  ( 778.2165204200184689, -406.8164208402375266, 364.9363028652563230 ) ) ;
#9079=CARTESIAN_POINT ( 'NONE',  ( 785.3687786644884454, -179.3618753856927128, 315.3201227861279676 ) ) ;
#9080=CARTESIAN_POINT ( 'NONE',  ( 791.9812246680005501, -140.6346026584201070, 361.9419747391813189 ) ) ;
#9084=CARTESIAN_POINT ( 'NONE',  ( 755.3201227861273992, -363.7255117493284047, 345.3687786644892981 ) ) ;
#9088=CARTESIAN_POINT ( 'NONE',  ( 808.0189434323515343, -110.0891481129656597, 319.0252816721025511 ) ) ;
#9093=CARTESIAN_POINT ( 'NONE',  ( 787.4397851343537695, -261.7255117493288026, 374.2001403089903988 ) ) ;
#9094=CARTESIAN_POINT ( 'NONE',  ( 758.6633372737375112, -212.5328690171415076, 326.9102291470432533 ) ) ;
#9106=CARTESIAN_POINT ( 'NONE',  ( 750.9282345327678740, -112.9181544815167229, 319.8311093483690115 ) ) ;
#9115=CARTESIAN_POINT ( 'NONE',  ( 776.9254006560222479, -452.1908817542428665, 314.8983024940802125 ) ) ;
#9116=CARTESIAN_POINT ( 'NONE',  ( 807.2620300519052989, -360.0090635724250774, 318.0141637701419768 ) ) ;
#9124=CARTESIAN_POINT ( 'NONE',  ( 745.5313806188320314, -207.2817908451527842, 333.7943932421247268 ) ) ;
#9126=CARTESIAN_POINT ( 'NONE',  ( 777.5031285880264704, -166.8164208402382087, 374.9108240113588408 ) ) ;
#9129=CARTESIAN_POINT ( 'NONE',  ( 759.7806653035534055, -246.9982390220560546, 324.8639956371180801 ) ) ;
#9130=CARTESIAN_POINT ( 'NONE',  ( 776.9254006560222479, -20.19088175424429110, 314.8983024940802125 ) ) ;
#9135=CARTESIAN_POINT ( 'NONE',  ( 801.3366627262608972, -104.5328690171418913, 353.0897708529566899 ) ) ;
#9138=VECTOR ( 'NONE', #19978, 1000.000000000000000 ) ;
#9139=CARTESIAN_POINT ( 'NONE',  ( 756.3353852180819104, -53.90732993114765037, 331.1735550268788302 ) ) ;
#9140=AXIS2_PLACEMENT_3D ( 'NONE', #31515, #31049, #38922 ) ;
#9143=CARTESIAN_POINT ( 'NONE',  ( 812.6845335610512393, -391.9874144716864066, 353.5525998758768651 ) ) ;
#9145=CARTESIAN_POINT ( 'NONE',  ( 746.8695393053150156, -5.907329931147798696, 327.6429770376306010 ) ) ;
#9148=CARTESIAN_POINT ( 'NONE',  ( 771.2633955100217236, -359.9073299311467053, 363.4237431249939618 ) ) ;
#9156=CARTESIAN_POINT ( 'NONE',  ( 795.1360043628807261, -92.08914811296568814, 360.2193346964456282 ) ) ;
#9157=CARTESIAN_POINT ( 'NONE',  ( 763.8424801807145741, -402.0090635724250205, 320.5453621957614700 ) ) ;
#9158=CARTESIAN_POINT ( 'NONE',  ( 763.2262854647970016, -416.6346026584192259, 309.2812353651462445 ) ) ;
#9160=CARTESIAN_POINT ( 'NONE',  ( 805.9055244015594326, -315.6237781080503169, 315.8990559732753240 ) ) ;
#9161=ADVANCED_FACE ( 'NONE', ( #41267 ), #3382, .F. ) ;
#9165=CARTESIAN_POINT ( 'NONE',  ( 814.5518280994195948, -447.7255117493280636, 332.4837098697145734 ) ) ;
#9171=CARTESIAN_POINT ( 'NONE',  ( 790.9844846989617508, -334.3726999360615082, 317.2208543904092721 ) ) ;
#9173=CARTESIAN_POINT ( 'NONE',  ( 805.1927285166397041, -184.8164208402380950, 341.8018195045277707 ) ) ;
#9174=ORIENTED_EDGE ( 'NONE', *, *, #40721, .F. ) ;
#9176=CARTESIAN_POINT ( 'NONE',  ( 813.5763878283155464, -315.8272453906070609, 351.1614460488615350 ) ) ;
#9177=AXIS2_PLACEMENT_3D ( 'NONE', #19234, #41859, #16916 ) ;
#9181=CARTESIAN_POINT ( 'NONE',  ( 762.1177392798416577, -66.55451811788050520, 309.8865473780659272 ) ) ;
#9185=CARTESIAN_POINT ( 'NONE',  ( 754.8072714833581358, -148.8164208402382656, 338.1981804954720587 ) ) ;
#9186=ORIENTED_EDGE ( 'NONE', *, *, #19085, .T. ) ;
#9187=CARTESIAN_POINT ( 'NONE',  ( 754.3581564841646241, -401.4636090269704027, 316.1443688327762516 ) ) ;
#9191=CARTESIAN_POINT ( 'NONE',  ( 773.4516893846965786, -67.64542720878958448, 315.8398074228977066 ) ) ;
#9194=CARTESIAN_POINT ( 'NONE',  ( 795.9930595647434757, -435.0783235625953580, 320.7433823573372820 ) ) ;
#9200=CARTESIAN_POINT ( 'NONE',  ( 801.9858362298568863, -267.0783235625958696, 312.7379699480935642 ) ) ;
#9201=CARTESIAN_POINT ( 'NONE',  ( 791.9812246680005501, -92.63460265842026331, 361.9419747391813189 ) ) ;
#9205=CARTESIAN_POINT ( 'NONE',  ( 778.2165204200184689, -262.8164208402379245, 364.9363028652563230 ) ) ;
#9212=CARTESIAN_POINT ( 'NONE',  ( 797.8594530101008786, -301.5436935675105588, 322.1405469898980982 ) ) ;
#9215=CARTESIAN_POINT ( 'NONE',  ( 745.7998596910086917, -341.3618753856922012, 332.5602148656461168 ) ) ;
#9216=CARTESIAN_POINT ( 'NONE',  ( 745.1769319972822814, -209.8055962898687881, 346.2694204179732083 ) ) ;
#9217=CARTESIAN_POINT ( 'NONE',  ( 815.1787889125755555, -30.89650538077846065, 343.7953271457877804 ) ) ;
#9222=CARTESIAN_POINT ( 'NONE',  ( 756.5762568750052424, -219.1800572038744122, 348.7366044899774238 ) ) ;
#9225=CARTESIAN_POINT ( 'NONE',  ( 796.9462024416508257, -372.4527844766010958, 308.9653473494370246 ) ) ;
#9228=CARTESIAN_POINT ( 'NONE',  ( 768.1267186599862953, 16.45630643248851044, 317.8138973628999224 ) ) ;
#9231=CARTESIAN_POINT ( 'NONE',  ( 793.9708237608222134, -238.9181544815163534, 319.2295555964448681 ) ) ;
#9233=CARTESIAN_POINT ( 'NONE',  ( 768.0187753319979720, -80.63460265842029173, 318.0580252608186242 ) ) ;
#9237=CARTESIAN_POINT ( 'NONE',  ( 789.9200121543843807, -241.9874144716869182, 317.0176451133914384 ) ) ;
#9240=CARTESIAN_POINT ( 'NONE',  ( 751.6929314249748586, -438.9982390220553157, 318.8095938919659034 ) ) ;
#9245=CARTESIAN_POINT ( 'NONE',  ( 772.4837098697144029, -95.36187538569294020, 374.5518280994205611 ) ) ;
#9246=CARTESIAN_POINT ( 'NONE',  ( 792.2312462859673587, -155.9073299311473306, 307.2067596250082602 ) ) ;
#9249=DIRECTION ( 'NONE',  ( 0.000000000000000000, 1.000000000000000000, 0.000000000000000000 ) ) ;
#9252=CARTESIAN_POINT ( 'NONE',  ( 747.6481478633932056, -397.0999726633340288, 353.4146539503763620 ) ) ;
#9254=CARTESIAN_POINT ( 'NONE',  ( 812.7932403749906598, -399.1800572038738437, 327.7687537140311633 ) ) ;
#9255=CARTESIAN_POINT ( 'NONE',  ( 745.0891759886404770, -28.27096629478409540, 342.4968714119734159 ) ) ;
#9257=CARTESIAN_POINT ( 'NONE',  ( 798.7617431975189675, 20.37622189194865285, 323.0428371773161871 ) ) ;
#9261=CARTESIAN_POINT ( 'NONE',  ( 808.7758568127978833, -172.1692326535052757, 320.0363995740631822 ) ) ;
#9262=FACE_OUTER_BOUND ( 'NONE', #30378, .T. ) ;
#9265=CARTESIAN_POINT ( 'NONE',  ( 794.9819416627830151, -156.9982390220564241, 319.9864689768909898 ) ) ;
#9267=PRODUCT ( 'MirrorTreadle Extension Return Springs', 'MirrorTreadle Extension Return Springs', '', ( #24889 ) ) ;
#9269=CARTESIAN_POINT ( 'NONE',  ( 804.9363028652555840, -280.2709662947833067, 338.2165204200192079 ) ) ;
#9273=CARTESIAN_POINT ( 'NONE',  ( 763.2154366446407039, -21.62377810805121570, 321.4292242960311228 ) ) ;
#9275=ORIENTED_EDGE ( 'NONE', *, *, #14012, .F. ) ;
#9276=CARTESIAN_POINT ( 'NONE',  ( 745.4481719005789273, -219.7255117493289447, 347.5162901302853697 ) ) ;
#9277=CARTESIAN_POINT ( 'NONE',  ( 769.0155153010367712, -298.3726999360616787, 362.7791456095907279 ) ) ;
#9278=CARTESIAN_POINT ( 'NONE',  ( 802.7791456095903868, -412.7146871989590409, 329.0155153010375102 ) ) ;
#9285=VECTOR ( 'NONE', #6609, 1000.000000000000000 ) ;
#9286=CARTESIAN_POINT ( 'NONE',  ( 776.9566956441375396, -300.8965053807775689, 364.8461984189686405 ) ) ;
#9292=CARTESIAN_POINT ( 'NONE',  ( 776.2046728542105711, -188.1908817542437760, 304.8212110874238761 ) ) ;
#9295=CARTESIAN_POINT ( 'NONE',  ( 799.9999999999993179, -462.9681489794448339, 309.9999999999998863 ) ) ;
#9297=CARTESIAN_POINT ( 'NONE',  ( 746.8695393053150156, -53.90732993114765037, 327.6429770376306010 ) ) ;
#9300=CARTESIAN_POINT ( 'NONE',  ( 799.9999999999993179, -462.9681489794448339, 309.9999999999998863 ) ) ;
#9301=CARTESIAN_POINT ( 'NONE',  ( 755.5713283507202505, -29.36187538569318178, 334.6858677611754729 ) ) ;
#9302=CARTESIAN_POINT ( 'NONE',  ( 786.2694204179717872, -333.2817908451523863, 305.1769319972829067 ) ) ;
#9303=CARTESIAN_POINT ( 'NONE',  ( 805.0032342141412300, -277.5436935675105019, 314.9967657858571783 ) ) ;
#9307=CARTESIAN_POINT ( 'NONE',  ( 802.1676090361156639, -374.6346026584192828, 327.8955696845344505 ) ) ;
#9308=CARTESIAN_POINT ( 'NONE',  ( 763.0428371773158460, -107.4636090269713122, 358.7617431975195359 ) ) ;
#9310=CARTESIAN_POINT ( 'NONE',  ( 745.1769319972822814, -41.80559628986934229, 346.2694204179732083 ) ) ;
#9311=CARTESIAN_POINT ( 'NONE',  ( 802.1676090361155502, -374.6346026584193396, 327.8955696845344505 ) ) ;
#9314=CARTESIAN_POINT ( 'NONE',  ( 762.3223304703356007, -439.5436935675101040, 322.3223304703362828 ) ) ;
#9318=CARTESIAN_POINT ( 'NONE',  ( 794.9819416627830151, -204.9982390220562820, 319.9864689768909898 ) ) ;
#9319=CARTESIAN_POINT ( 'NONE',  ( 778.1981804954715471, -202.2709662947835341, 314.8072714833591021 ) ) ;
#9324=CARTESIAN_POINT ( 'NONE',  ( 762.1405469898971887, -385.5436935675102745, 357.8594530101015607 ) ) ;
#9328=CARTESIAN_POINT ( 'NONE',  ( 796.7737145352015204, -116.6346026584201780, 370.7187646348536987 ) ) ;
#9334=CARTESIAN_POINT ( 'NONE',  ( 777.4774526936600978, -250.2709662947832783, 304.7301800767027657 ) ) ;
#9335=CARTESIAN_POINT ( 'NONE',  ( 795.9930595647434757, -195.0783235625961538, 320.7433823573372820 ) ) ;
#9345=CARTESIAN_POINT ( 'NONE',  ( 805.6418435158337843, -101.4636090269713264, 363.8556311672236916 ) ) ;
#9355=CARTESIAN_POINT ( 'NONE',  ( 757.4527132478984868, -424.3726999360612808, 329.1273215169538844 ) ) ;
#9363=CARTESIAN_POINT ( 'NONE',  ( 755.8990559732751535, -227.4636090269709143, 365.9055244015606831 ) ) ;
#9365=CARTESIAN_POINT ( 'NONE',  ( 810.7187646348534145, -162.4527844766018632, 356.7737145352016341 ) ) ;
#9369=CARTESIAN_POINT ( 'NONE',  ( 755.5713283507202505, -245.3618753856925139, 334.6858677611754729 ) ) ;
#9370=CARTESIAN_POINT ( 'NONE',  ( 761.4292242960306112, -41.46360902697149697, 323.2154366446414429 ) ) ;
#9374=CARTESIAN_POINT ( 'NONE',  ( 800.7704444035546203, -100.1692326535055315, 326.0291762391768771 ) ) ;
#9375=ORIENTED_EDGE ( 'NONE', *, *, #8380, .F. ) ;
#9379=CARTESIAN_POINT ( 'NONE',  ( 803.6646147819161570, -65.90732993114758642, 348.8264449731210561 ) ) ;
#9381=CARTESIAN_POINT ( 'NONE',  ( 810.1134526219336749, -368.5328690171409676, 357.8822607201570349 ) ) ;
#9383=CARTESIAN_POINT ( 'NONE',  ( 814.2001403089898304, 6.638124614306706306, 347.4397851343538264 ) ) ;
#9385=CARTESIAN_POINT ( 'NONE',  ( 802.1676090361156639, -374.6346026584192828, 327.8955696845344505 ) ) ;
#9391=CARTESIAN_POINT ( 'NONE',  ( 804.4286716492782716, -89.36187538569299704, 345.3141322388244703 ) ) ;
#9392=CARTESIAN_POINT ( 'NONE',  ( 793.0897708529556667, -414.5545181178795247, 361.3366627262616362 ) ) ;
#9393=CARTESIAN_POINT ( 'NONE',  ( 802.7791456095903868, -100.7146871989600356, 329.0155153010375102 ) ) ;
#9395=CARTESIAN_POINT ( 'NONE',  ( 763.0537975583476964, -432.4527844766009252, 371.0346526505628617 ) ) ;
#9397=CARTESIAN_POINT ( 'NONE',  ( 813.9316612368132837, -367.4419599262319025, 348.6739635108323228 ) ) ;
#9398=CARTESIAN_POINT ( 'NONE',  ( 768.8385539511368734, -119.2601417444145397, 306.4236121716840557 ) ) ;
#9402=CARTESIAN_POINT ( 'NONE',  ( 771.3260364891663130, 4.354572791210176597, 306.0683387631859773 ) ) ;
#9408=CARTESIAN_POINT ( 'NONE',  ( 759.0159684113467620, -328.9181544815160692, 325.8855110935213020 ) ) ;
#9409=CARTESIAN_POINT ( 'NONE',  ( 800.2193346964447755, -186.9982390220563104, 355.1360043628815788 ) ) ;
#9411=CARTESIAN_POINT ( 'NONE',  ( 814.8207195650702488, -290.1908817542434349, 336.2433038121456548 ) ) ;
#9413=DIRECTION ( 'NONE',  ( 0.000000000000000000, -1.000000000000000000, -1.110223024625155554E-15 ) ) ;
#9414=CARTESIAN_POINT ( 'NONE',  ( 812.3518521366052028, -97.09997266333496668, 326.5853460496235243 ) ) ;
#9418=CARTESIAN_POINT ( 'NONE',  ( 762.3223304703356007, -151.5436935675109851, 322.3223304703362828 ) ) ;
#9420=CARTESIAN_POINT ( 'NONE',  ( 745.5313806188320314, -423.2817908451521589, 333.7943932421247268 ) ) ;
#9424=CARTESIAN_POINT ( 'NONE',  ( 804.4086373105744769, -49.64542720878965554, 333.3843516231986541 ) ) ;
#9427=CARTESIAN_POINT ( 'NONE',  ( 804.1601925771018387, -439.4419599262316751, 346.5483106153029098 ) ) ;
#9429=CARTESIAN_POINT ( 'NONE',  ( 772.3691319403857278, -71.26014174441469606, 315.8894580844506663 ) ) ;
#9434=CARTESIAN_POINT ( 'NONE',  ( 752.4576283171824116, -285.0783235625958127, 317.7880784355627952 ) ) ;
#9435=CARTESIAN_POINT ( 'NONE',  ( 774.6858677611749044, -81.72551174932937101, 315.5713283507209894 ) ) ;
#9437=CARTESIAN_POINT ( 'NONE',  ( 791.9812246680005501, -260.6346026584197375, 361.9419747391813189 ) ) ;
#9446=CARTESIAN_POINT ( 'NONE',  ( 787.4397851343537695, -333.7255117493286320, 374.2001403089903988 ) ) ;
#9447=CARTESIAN_POINT ( 'NONE',  ( 815.1787889125755555, -222.8965053807778531, 343.7953271457877804 ) ) ;
#9452=CARTESIAN_POINT ( 'NONE',  ( 755.0636971347428243, -196.2709662947835909, 341.7834795799807353 ) ) ;
#9456=CARTESIAN_POINT ( 'NONE',  ( 814.9108240113580450, -352.2709662947830225, 337.5031285880265273 ) ) ;
#9458=CARTESIAN_POINT ( 'NONE',  ( 785.1593951492109227, 16.45630643248848912, 313.8313994339321766 ) ) ;
#9459=DIRECTION ( 'NONE',  ( 0.000000000000000000, 0.000000000000000000, 1.000000000000000000 ) ) ;
#9460=CARTESIAN_POINT ( 'NONE',  ( 787.5531968255692163, -213.8272453906073167, 316.1348686366205811 ) ) ;
#9461=CARTESIAN_POINT ( 'NONE',  ( 759.9864689768902508, -98.08914811296568814, 354.9819416627836404 ) ) ;
#9465=CARTESIAN_POINT ( 'NONE',  ( 799.4546378042377910, -249.0783235625959549, 356.1575198192848006 ) ) ;
#9469=CARTESIAN_POINT ( 'NONE',  ( 814.8207195650702488, -2.190881754244347945, 336.2433038121456548 ) ) ;
#9474=CARTESIAN_POINT ( 'NONE',  ( 767.7687537140311633, -95.90732993114751537, 372.7932403749916830 ) ) ;
#9475=CARTESIAN_POINT ( 'NONE',  ( 811.0346526505616112, -158.6346026584199933, 323.0537975583477532 ) ) ;
#9478=CARTESIAN_POINT ( 'NONE',  ( 768.9521613784389729, -417.8272453906067199, 373.2346286133773106 ) ) ;
#9481=CARTESIAN_POINT ( 'NONE',  ( 811.0346526505616112, -398.6346026584193396, 323.0537975583477532 ) ) ;
#9482=CARTESIAN_POINT ( 'NONE',  ( 745.0891759886404770, -4.270966294784170003, 342.4968714119734159 ) ) ;
#9485=CARTESIAN_POINT ( 'NONE',  ( 805.1016975059191054, -6.896505380778533478, 343.0745993439771837 ) ) ;
#9488=CARTESIAN_POINT ( 'NONE',  ( 791.1614460488616487, -155.2601417444144261, 373.5763878283158874 ) ) ;
#9491=ORIENTED_EDGE ( 'NONE', *, *, #35724, .F. ) ;
#9494=CARTESIAN_POINT ( 'NONE',  ( 755.0636971347428243, -148.2709662947837330, 341.7834795799807353 ) ) ;
#9496=CARTESIAN_POINT ( 'NONE',  ( 795.1360043628808398, -284.0891481129651197, 360.2193346964456282 ) ) ;
#9499=CARTESIAN_POINT ( 'NONE',  ( 772.3691319403857278, -23.26014174441484883, 315.8894580844506663 ) ) ;
#9503=CARTESIAN_POINT ( 'NONE',  ( 814.5518280994195948, -207.7255117493289731, 332.4837098697145166 ) ) ;
#9504=CARTESIAN_POINT ( 'NONE',  ( 802.5472867521000353, -340.3726999360615082, 350.8726784830461156 ) ) ;
#9505=CARTESIAN_POINT ( 'NONE',  ( 811.6461892240364477, 19.28531280103956647, 324.1737431748509835 ) ) ;
#9512=CARTESIAN_POINT ( 'NONE',  ( 765.8855110935204493, -310.1692326535048778, 319.0159684113471599 ) ) ;
#9513=CARTESIAN_POINT ( 'NONE',  ( 793.3689467304194523, -456.0926483283658968, 371.2611151693469083 ) ) ;
#9515=CARTESIAN_POINT ( 'NONE',  ( 787.5531968255692163, -117.8272453906076151, 316.1348686366205811 ) ) ;
#9516=CARTESIAN_POINT ( 'NONE',  ( 788.7366044899766848, 12.09267006885214180, 316.5762568750059813 ) ) ;
#9517=ORIENTED_EDGE ( 'NONE', *, *, #45271, .F. ) ;
#9519=CARTESIAN_POINT ( 'NONE',  ( 760.0363995740630116, -202.9181544815164386, 368.7758568127991907 ) ) ;
#9525=CARTESIAN_POINT ( 'NONE',  ( 787.5162901302840055, -35.36187538569316047, 305.4481719005792684 ) ) ;
#9528=CARTESIAN_POINT ( 'NONE',  ( 799.9999999999993179, 205.0000000000000568, 339.9999999999999432 ) ) ;
#9529=CARTESIAN_POINT ( 'NONE',  ( 804.1009440267234822, -335.4636090269705733, 314.0944755984392600 ) ) ;
#9531=CARTESIAN_POINT ( 'NONE',  ( 812.7932403749906598, -303.1800572038740711, 327.7687537140311633 ) ) ;
#9535=CARTESIAN_POINT ( 'NONE',  ( 771.1735550268778070, -393.1800572038737300, 316.3353852180827630 ) ) ;
#9536=CARTESIAN_POINT ( 'NONE',  ( 766.0291762391763086, -130.9181544815166660, 360.7704444035551319 ) ) ;
#9538=CARTESIAN_POINT ( 'NONE',  ( 746.7653713866222915, -65.26014174441471027, 351.0478386215610271 ) ) ;
#9539=CARTESIAN_POINT ( 'NONE',  ( 768.0187753319979720, -368.6346026584193964, 318.0580252608186242 ) ) ;
#9542=CARTESIAN_POINT ( 'NONE',  ( 805.9055244015594326, -147.6237781080508285, 315.8990559732753240 ) ) ;
#9543=CARTESIAN_POINT ( 'NONE',  ( 797.8594530101008786, -445.5436935675098766, 322.1405469898980982 ) ) ;
#9547=CARTESIAN_POINT ( 'NONE',  ( 801.9419747391806368, -186.4527844766017779, 351.9812246680014027 ) ) ;
#9548=CARTESIAN_POINT ( 'NONE',  ( 785.3687786644885591, -203.3618753856926276, 315.3201227861280813 ) ) ;
#9551=B_SPLINE_CURVE_WITH_KNOTS ( 'NONE', 3,
 ( #27068, #430, #40920, #17987, #2568, #9513, #23578, #16433, #2333, #30760, #6031, #34199 ),
 .UNSPECIFIED., .F., .F.,
 ( 4, 2, 2, 2, 2, 4 ),
 ( 0.2497888289850607457, 0.3123416217387972038, 0.3748944144925336897, 0.4374472072462701200, 0.4687236036231350322, 0.5000000000000000000 ),
 .UNSPECIFIED. ) ;
#9553=CARTESIAN_POINT ( 'NONE',  ( 771.2633955100217236, -383.9073299311466485, 363.4237431249939618 ) ) ;
#9558=CARTESIAN_POINT ( 'NONE',  ( 767.6429770376291799, -105.1800572038747390, 306.8695393053162093 ) ) ;
#9564=CARTESIAN_POINT ( 'NONE',  ( 749.2812353651451076, -270.4527844766014937, 323.2262854647983090 ) ) ;
#9565=CARTESIAN_POINT ( 'NONE',  ( 787.6308680596127942, -203.2601417444143124, 364.1105419155492768 ) ) ;
#9571=DIRECTION ( 'NONE',  ( 0.000000000000000000, -1.000000000000000000, 0.000000000000000000 ) ) ;
#9575=CARTESIAN_POINT ( 'NONE',  ( 745.5313806188320314, -111.2817908451530968, 333.7943932421247268 ) ) ;
#9580=FACE_OUTER_BOUND ( 'NONE', #12419, .T. ) ;
#9583=CARTESIAN_POINT ( 'NONE',  ( 758.4439275373578084, -444.5545181178792973, 353.2243759319684386 ) ) ;
#9584=CARTESIAN_POINT ( 'NONE',  ( 810.4231160770870019, -360.5545181178796383, 321.9338519418446936 ) ) ;
#9591=CARTESIAN_POINT ( 'NONE',  ( 754.3581564841646241, -209.4636090269709996, 316.1443688327762516 ) ) ;
#9593=CARTESIAN_POINT ( 'NONE',  ( 755.2512626584698410, -175.5436935675108998, 315.2512626584710915 ) ) ;
#9596=CARTESIAN_POINT ( 'NONE',  ( 755.3201227861273992, -267.7255117493286320, 345.3687786644892981 ) ) ;
#9597=CARTESIAN_POINT ( 'NONE',  ( 755.3028492785439312, -63.28179084515324604, 335.9200461376539693 ) ) ;
#9601=CARTESIAN_POINT ( 'NONE',  ( 805.1016975059191054, -78.89650538077832209, 343.0745993439771837 ) ) ;
#9602=CARTESIAN_POINT ( 'NONE',  ( 785.3687786644884454, -323.3618753856923149, 315.3201227861279676 ) ) ;
#9604=CARTESIAN_POINT ( 'NONE',  ( 781.8018195045266339, -46.27096629478404566, 365.1927285166406705 ) ) ;
#9607=CARTESIAN_POINT ( 'NONE',  ( 798.0661480581538854, -386.5328690171409676, 309.5768839229118043 ) ) ;
#9608=ORIENTED_EDGE ( 'NONE', *, *, #45264, .T. ) ;
#9609=CARTESIAN_POINT ( 'NONE',  ( 774.6312213355099630, -287.3618753856923718, 364.6798772138717482 ) ) ;
#9610=CARTESIAN_POINT ( 'NONE',  ( 811.0346526505616112, 9.365397341579420498, 323.0537975583477532 ) ) ;
#9613=CARTESIAN_POINT ( 'NONE',  ( 762.1405469898971887, -361.5436935675103882, 357.8594530101015607 ) ) ;
#9619=CARTESIAN_POINT ( 'NONE',  ( 768.0187753319979720, -104.6346026584202207, 318.0580252608186242 ) ) ;
#9620=CARTESIAN_POINT ( 'NONE',  ( 773.4516893846965786, -403.6454272087884760, 315.8398074228977066 ) ) ;
#9621=CARTESIAN_POINT ( 'NONE',  ( 757.2208543904082489, -88.71468719896009247, 350.9844846989624330 ) ) ;
#9624=CARTESIAN_POINT ( 'NONE',  ( 766.5853460496234675, -349.9874144716865771, 372.3518521366060554 ) ) ;
#9628=CARTESIAN_POINT ( 'NONE',  ( 783.7953271457878373, -8.190881754244330182, 375.1787889125761239 ) ) ;
#9629=CARTESIAN_POINT ( 'NONE',  ( 795.2725662613897839, 16.45630643248849267, 314.1785221222716586 ) ) ;
#9634=CARTESIAN_POINT ( 'NONE',  ( 775.8780910478218402, -321.2817908451525000, 364.9511171171680530 ) ) ;
#9636=CARTESIAN_POINT ( 'NONE',  ( 757.7880784355613741, -306.0090635724252479, 312.4576283171834916 ) ) ;
#9639=CARTESIAN_POINT ( 'NONE',  ( 746.4236121716829757, -111.8272453906076151, 328.8385539511384650 ) ) ;
#9643=CARTESIAN_POINT ( 'NONE',  ( 767.8955696845333705, -144.4527844766018632, 362.1676090361162323 ) ) ;
#9645=CARTESIAN_POINT ( 'NONE',  ( 814.8207195650702488, -434.1908817542430370, 336.2433038121456548 ) ) ;
#9648=CARTESIAN_POINT ( 'NONE',  ( 784.1219089521767955, -45.28179084515329578, 315.0488828828318333 ) ) ;
#9651=CARTESIAN_POINT ( 'NONE',  ( 799.4546378042377910, -441.0783235625953580, 356.1575198192848006 ) ) ;
#9653=CARTESIAN_POINT ( 'NONE',  ( 759.9864689768902508, -266.0891481129651197, 354.9819416627836404 ) ) ;
#9657=CARTESIAN_POINT ( 'NONE',  ( 756.1443688327750579, -285.6237781080502600, 314.3581564841659315 ) ) ;
#9658=CARTESIAN_POINT ( 'NONE',  ( 755.3201227861273992, -99.72551174932931417, 345.3687786644892981 ) ) ;
#9660=CARTESIAN_POINT ( 'NONE',  ( 792.1044303154645831, -276.4527844766013800, 317.8323909638837677 ) ) ;
#9662=DIRECTION ( 'NONE',  ( 0.000000000000000000, 0.000000000000000000, -1.000000000000000000 ) ) ;
#9667=CARTESIAN_POINT ( 'NONE',  ( 800.9747183278959710, -348.9982390220558273, 311.9810565676471583 ) ) ;
#9668=CARTESIAN_POINT ( 'NONE',  ( 744.8212110874229666, -258.8965053807777963, 336.2046728542121627 ) ) ;
#9673=CARTESIAN_POINT ( 'NONE',  ( 781.8018195045266339, -262.2709662947831930, 365.1927285166406705 ) ) ;
#9675=CARTESIAN_POINT ( 'NONE',  ( 758.8095938919642549, -344.0891481129647786, 311.6929314249763365 ) ) ;
#9676=CARTESIAN_POINT ( 'NONE',  ( 791.7608162188021197, 178.9475563372491251, 360.0000000000000000 ) ) ;
#9677=CARTESIAN_POINT ( 'NONE',  ( 790.2803779376845341, 16.45630643248849623, 314.3272116953297086 ) ) ;
#9680=CARTESIAN_POINT ( 'NONE',  ( 801.5560724626406000, -240.5545181178798941, 326.7756240680316182 ) ) ;
#9681=CARTESIAN_POINT ( 'NONE',  ( 756.3353852180819104, -77.90732993114757221, 331.1735550268788302 ) ) ;
#9685=CARTESIAN_POINT ( 'NONE',  ( 766.7756240680305382, -254.5328690171413655, 361.5560724626415663 ) ) ;
#9688=CARTESIAN_POINT ( 'NONE',  ( 799.9636004259356241, -22.91815448151701062, 311.2241431872006956 ) ) ;
#9692=CARTESIAN_POINT ( 'NONE',  ( 744.7301800767019131, -100.8164208402383792, 337.4774526936615757 ) ) ;
#9693=CARTESIAN_POINT ( 'NONE',  ( 777.4774526936600978, -130.2709662947837899, 304.7301800767027657 ) ) ;
#9697=CARTESIAN_POINT ( 'NONE',  ( 754.3581564841646241, -401.4636090269704027, 316.1443688327762516 ) ) ;
#9701=CARTESIAN_POINT ( 'NONE',  ( 767.7687537140311633, -383.9073299311466485, 372.7932403749916830 ) ) ;
#9702=CARTESIAN_POINT ( 'NONE',  ( 792.3570229623691148, 2.819942796124898621, 373.1304606946836770 ) ) ;
#9704=CARTESIAN_POINT ( 'NONE',  ( 784.0799538623451781, -11.80559628986942577, 364.6971507214555572 ) ) ;
#9708=CARTESIAN_POINT ( 'NONE',  ( 776.2433038121456548, -180.8965053807779952, 374.8207195650711014 ) ) ;
#9709=CARTESIAN_POINT ( 'NONE',  ( 788.8264449731201466, 2.819942796124898621, 363.6646147819170665 ) ) ;
#9713=CARTESIAN_POINT ( 'NONE',  ( 792.1044303154645831, -156.4527844766018916, 317.8323909638837677 ) ) ;
#9715=CARTESIAN_POINT ( 'NONE',  ( 785.3141322388236176, -309.7255117493287457, 364.4286716492789537 ) ) ;
#9716=VECTOR ( 'NONE', #22908, 1000.000000000000000 ) ;
#9719=CARTESIAN_POINT ( 'NONE',  ( 772.3691319403857278, 0.7398582555850804487, 315.8894580844506663 ) ) ;
#9723=CARTESIAN_POINT ( 'NONE',  ( 792.2312462859673587, -227.9073299311471033, 307.2067596250082602 ) ) ;
#9725=CARTESIAN_POINT ( 'NONE',  ( 790.0220218866281812, -319.0999726633342561, 363.2186876482849129 ) ) ;
#9726=CARTESIAN_POINT ( 'NONE',  ( 754.8983024940795303, -426.8965053807771142, 336.9254006560228163 ) ) ;
#9731=CARTESIAN_POINT ( 'NONE',  ( 775.9200461376533440, -287.8055962898685038, 315.3028492785443291 ) ) ;
#9735=CARTESIAN_POINT ( 'NONE',  ( 802.5472867521000353, -124.3726999360621619, 350.8726784830461156 ) ) ;
#9739=CARTESIAN_POINT ( 'NONE',  ( 778.7629533639073998, -200.7363362996982801, 375.0009284576466371 ) ) ;
#9743=CARTESIAN_POINT ( 'NONE',  ( 796.9462024416508257, -60.45278447660215448, 308.9653473494370246 ) ) ;
#9749=CARTESIAN_POINT ( 'NONE',  ( 791.0478386215596629, -309.8272453906070041, 306.7653713866226326 ) ) ;
#9752=CARTESIAN_POINT ( 'NONE',  ( 814.9108240113580450, -304.2709662947832499, 337.5031285880265273 ) ) ;
#9756=CARTESIAN_POINT ( 'NONE',  ( 795.1360043628807261, -404.0891481129646081, 360.2193346964456282 ) ) ;
#9757=CARTESIAN_POINT ( 'NONE',  ( 799.2566176426618085, -144.0090635724257027, 324.0069404352559559 ) ) ;
#9759=CARTESIAN_POINT ( 'NONE',  ( 795.6651683502461765, -58.71468719896019905, 371.3240766477733814 ) ) ;
#9760=CARTESIAN_POINT ( 'NONE',  ( 756.3353852180820240, -365.9073299311466485, 331.1735550268787733 ) ) ;
#9761=CARTESIAN_POINT ( 'NONE',  ( 767.6429770376291799, 14.81994279612486309, 306.8695393053162093 ) ) ;
#9762=CARTESIAN_POINT ( 'NONE',  ( 802.1676090361156639, -446.6346026584189985, 327.8955696845344505 ) ) ;
#9766=CARTESIAN_POINT ( 'NONE',  ( 797.8594530101008786, -205.5436935675108430, 322.1405469898980982 ) ) ;
#9767=CARTESIAN_POINT ( 'NONE',  ( 792.1044303154646968, -180.4527844766017495, 317.8323909638837677 ) ) ;
#9771=VERTEX_POINT ( 'NONE', #30122 ) ;
#9775=CARTESIAN_POINT ( 'NONE',  ( 763.0537975583476964, -120.4527844766019768, 371.0346526505628617 ) ) ;
#9783=CARTESIAN_POINT ( 'NONE',  ( 796.7845633553578182, -201.6237781080506863, 358.5707757039688204 ) ) ;
#9793=CARTESIAN_POINT ( 'NONE',  ( 750.9282345327678740, -88.91815448151682233, 319.8311093483690115 ) ) ;
#9801=CARTESIAN_POINT ( 'NONE',  ( 759.0159684113467620, -448.9181544815156144, 325.8855110935213020 ) ) ;
#9803=FACE_BOUND ( 'NONE', #27502, .T. ) ;
#9810=CARTESIAN_POINT ( 'NONE',  ( 748.6759233522253680, -208.3726999360619061, 324.3348316497537098 ) ) ;
#9812=CARTESIAN_POINT ( 'NONE',  ( 745.0891759886404770, -196.2709662947835909, 342.4968714119734159 ) ) ;
#9815=CARTESIAN_POINT ( 'NONE',  ( 758.0580252608178853, -294.4527844766013800, 328.0187753319985404 ) ) ;
#9816=CARTESIAN_POINT ( 'NONE',  ( 804.8461984189677878, -74.19088175424410281, 336.9566956441385628 ) ) ;
#9820=CARTESIAN_POINT ( 'NONE',  ( 761.2382568024794409, -111.6237781080509279, 356.9571628226838129 ) ) ;
#9821=CARTESIAN_POINT ( 'NONE',  ( 801.9419747391806368, -330.4527844766013231, 351.9812246680014027 ) ) ;
#9825=CARTESIAN_POINT ( 'NONE',  ( 767.8955696845333705, -96.45278447660203369, 362.1676090361162323 ) ) ;
#9828=CARTESIAN_POINT ( 'NONE',  ( 791.1614460488616487, -395.2601417444136587, 373.5763878283158874 ) ) ;
#9830=CARTESIAN_POINT ( 'NONE',  ( 785.3141322388236176, -285.7255117493286889, 364.4286716492789537 ) ) ;
#9834=CARTESIAN_POINT ( 'NONE',  ( 778.1981804954714335, -370.2709662947831362, 314.8072714833589885 ) ) ;
#9840=AXIS2_PLACEMENT_3D ( 'NONE', #20974, #3444, #14537 ) ;
#9842=CARTESIAN_POINT ( 'NONE',  ( 757.4527132478984868, -400.3726999360612808, 329.1273215169538844 ) ) ;
#9843=CARTESIAN_POINT ( 'NONE',  ( 801.1904061080338124, -452.0891481129646081, 368.3070685750236066 ) ) ;
#9844=DIRECTION ( 'NONE',  ( 0.000000000000000000, 0.000000000000000000, 1.000000000000000000 ) ) ;
#9845=CARTESIAN_POINT ( 'NONE',  ( 748.3538107759620743, -352.7146871989593251, 355.8262568251490165 ) ) ;
#9848=CARTESIAN_POINT ( 'NONE',  ( 805.6418435158337843, -5.463609026971610660, 363.8556311672236916 ) ) ;
#9851=DIRECTION ( 'NONE',  ( -1.000000000000000000, -0.000000000000000000, 0.000000000000000000 ) ) ;
#9854=DIRECTION ( 'NONE',  ( -1.000000000000000000, -0.000000000000000000, 0.000000000000000000 ) ) ;
#9855=DIRECTION ( 'NONE',  ( -1.000000000000000000, -0.000000000000000000, 0.000000000000000000 ) ) ;
#9856=CARTESIAN_POINT ( 'NONE',  ( 757.0176451133909268, -325.0999726633342561, 349.9200121543848354 ) ) ;
#9858=CARTESIAN_POINT ( 'NONE',  ( 805.6418435158337843, -317.4636090269706301, 363.8556311672236916 ) ) ;
#9861=CARTESIAN_POINT ( 'NONE',  ( 764.1737431748507561, -106.3726999360621903, 371.6461892240376415 ) ) ;
#9865=CARTESIAN_POINT ( 'NONE',  ( 804.6798772138708955, -183.7255117493290015, 334.6312213355107019 ) ) ;
#9869=CARTESIAN_POINT ( 'NONE',  ( 802.2119215644370342, -438.0090635724247932, 367.5423716828165084 ) ) ;
#9872=CARTESIAN_POINT ( 'NONE',  ( 766.9102291470427417, -42.55451811788057626, 318.6633372737382501 ) ) ;
#9875=CARTESIAN_POINT ( 'NONE',  ( 800.7704444035546203, -436.1692326535044231, 326.0291762391768771 ) ) ;
#9879=CARTESIAN_POINT ( 'NONE',  ( 773.7943932421234194, -263.8055962898686175, 305.5313806188329409 ) ) ;
#9880=CARTESIAN_POINT ( 'NONE',  ( 785.3687786644885591, -131.3618753856928549, 315.3201227861280813 ) ) ;
#9883=CARTESIAN_POINT ( 'NONE',  ( 801.9419747391806368, -258.4527844766016074, 351.9812246680014027 ) ) ;
#9890=CARTESIAN_POINT ( 'NONE',  ( 811.0346526505617248, -350.6346026584193396, 323.0537975583478101 ) ) ;
#9891=CARTESIAN_POINT ( 'NONE',  ( 746.7653713866222915, -257.2601417444141134, 351.0478386215610271 ) ) ;
#9898=CARTESIAN_POINT ( 'NONE',  ( 759.7806653035534055, -246.9982390220560546, 324.8639956371180801 ) ) ;
#9900=CARTESIAN_POINT ( 'NONE',  ( 801.1904061080336987, -356.0891481129647218, 368.3070685750235498 ) ) ;
#9903=CARTESIAN_POINT ( 'NONE',  ( 774.9293440288117836, 16.45630643248849623, 314.9535949064562601 ) ) ;
#9905=CARTESIAN_POINT ( 'NONE',  ( 758.4439275373578084, -228.5545181178799794, 353.2243759319684386 ) ) ;
#9906=CARTESIAN_POINT ( 'NONE',  ( 805.1927285166397041, -112.8164208402383508, 341.8018195045277707 ) ) ;
#9911=CARTESIAN_POINT ( 'NONE',  ( 805.1016975059191054, -294.8965053807775689, 343.0745993439771837 ) ) ;
#9914=AXIS2_PLACEMENT_3D ( 'NONE', #41533, #45224, #9662 ) ;
#9915=CARTESIAN_POINT ( 'NONE',  ( 793.5525998758768083, -7.099972663335241130, 372.6845335610516941 ) ) ;
#9917=CARTESIAN_POINT ( 'NONE',  ( 805.0032342141412300, -85.54369356751118403, 314.9967657858571783 ) ) ;
#9918=CARTESIAN_POINT ( 'NONE',  ( 777.5031285880264704, -166.8164208402382087, 374.9108240113588408 ) ) ;
#9920=CARTESIAN_POINT ( 'NONE',  ( 791.7608162188021197, 205.0000000000000568, 339.9999999999999432 ) ) ;
#9922=CARTESIAN_POINT ( 'NONE',  ( 786.2694204179717872, -405.2817908451522158, 305.1769319972829067 ) ) ;
#9925=CARTESIAN_POINT ( 'NONE',  ( 745.0891759886404770, -412.2709662947829088, 342.4968714119734159 ) ) ;
#9926=CARTESIAN_POINT ( 'NONE',  ( 744.7301800767020268, -4.816420840238714085, 337.4774526936615189 ) ) ;
#9929=CARTESIAN_POINT ( 'NONE',  ( 756.1348686366196716, -17.26014174441486659, 347.5531968255698416 ) ) ;
#9933=CARTESIAN_POINT ( 'NONE',  ( 783.7566961878529810, -168.8965053807780237, 305.1792804349288417 ) ) ;
#9940=CARTESIAN_POINT ( 'NONE',  ( 771.1735550268778070, -153.1800572038746395, 316.3353852180827630 ) ) ;
#9943=CARTESIAN_POINT ( 'NONE',  ( 759.9864689768902508, -290.0891481129650629, 354.9819416627836404 ) ) ;
#9944=CARTESIAN_POINT ( 'NONE',  ( 804.6798772138710092, -279.7255117493288026, 334.6312213355106451 ) ) ;
#9947=CARTESIAN_POINT ( 'NONE',  ( 798.7617431975189675, -3.623778108051270319, 323.0428371773161871 ) ) ;
#9951=CARTESIAN_POINT ( 'NONE',  ( 747.2067596250078623, -267.1800572038742985, 352.2312462859687230 ) ) ;
#9952=CARTESIAN_POINT ( 'NONE',  ( 772.4468031744293057, -321.8272453906070609, 363.8651313633793620 ) ) ;
#9954=CARTESIAN_POINT ( 'NONE',  ( 788.4001350590139054, -443.1233509495419298, 363.5803521658918385 ) ) ;
#9959=CARTESIAN_POINT ( 'NONE',  ( 758.6633372737375112, -284.5328690171412518, 326.9102291470432533 ) ) ;
#9962=CARTESIAN_POINT ( 'NONE',  ( 763.0428371773158460, -131.4636090269711985, 358.7617431975195359 ) ) ;
#9963=CARTESIAN_POINT ( 'NONE',  ( 758.0580252608178853, -30.45278447660226817, 328.0187753319985404 ) ) ;
#9964=EDGE_CURVE ( 'NONE', #17907, #9771, #8434, .T. ) ;
#9968=CARTESIAN_POINT ( 'NONE',  ( 747.6481478633932056, -229.0999726633345404, 353.4146539503763620 ) ) ;
#9969=CARTESIAN_POINT ( 'NONE',  ( 754.9735926884551418, -186.3510508353234343, 340.5236548041000333 ) ) ;
#9974=CARTESIAN_POINT ( 'NONE',  ( 807.9206849184947714, -452.9681489794447202, 338.7201299304387021 ) ) ;
#9978=CARTESIAN_POINT ( 'NONE',  ( 745.5313806188320314, -303.2817908451525000, 333.7943932421247268 ) ) ;
#9979=DIRECTION ( 'NONE',  ( 0.000000000000000000, 0.000000000000000000, -1.000000000000000000 ) ) ;
#9980=CARTESIAN_POINT ( 'NONE',  ( 804.7487373415286811, -307.5436935675104451, 364.7487373415288516 ) ) ;
#9983=AXIS2_PLACEMENT_3D ( 'NONE', #31009, #13464, #3289 ) ;
#9986=CARTESIAN_POINT ( 'NONE',  ( 771.2633955100217236, -407.9073299311465348, 363.4237431249939618 ) ) ;
#9987=CARTESIAN_POINT ( 'NONE',  ( 773.4516893846965786, -139.6454272087893571, 315.8398074228977066 ) ) ;
#9990=CARTESIAN_POINT ( 'NONE',  ( 815.0009284576459549, -54.35105083532383219, 338.7629533639073429 ) ) ;
#9991=CARTESIAN_POINT ( 'NONE',  ( 797.6776695296629214, -379.5436935675102745, 357.6776695296636603 ) ) ;
#9994=CARTESIAN_POINT ( 'NONE',  ( 785.3141322388236176, -429.7255117493282910, 364.4286716492789537 ) ) ;
#9999=CARTESIAN_POINT ( 'NONE',  ( 771.2633955100217236, -191.9073299311471885, 363.4237431249939618 ) ) ;
#10000=CARTESIAN_POINT ( 'NONE',  ( 781.8018195045267476, -190.2709662947835625, 365.1927285166407273 ) ) ;
#10005=ORIENTED_EDGE ( 'NONE', *, *, #37944, .T. ) ;
#10006=CARTESIAN_POINT ( 'NONE',  ( 771.2633955100217236, -407.9073299311465348, 363.4237431249939618 ) ) ;
#10011=CARTESIAN_POINT ( 'NONE',  ( 746.8695393053151292, -149.9073299311473875, 327.6429770376306578 ) ) ;
#10015=EDGE_CURVE ( 'NONE', #31386, #15704, #13721, .T. ) ;
#10020=CARTESIAN_POINT ( 'NONE',  ( 805.0264073115434940, -198.3510508353234059, 339.4763451958999099 ) ) ;
#10031=CARTESIAN_POINT ( 'NONE',  ( 766.4474001241216001, -139.0999726633348530, 307.3154664389482491 ) ) ;
#10038=CARTESIAN_POINT ( 'NONE',  ( 778.7629533639073998, -368.7363362996977685, 375.0009284576466371 ) ) ;
#10042=CARTESIAN_POINT ( 'NONE',  ( 804.6798772138708955, 8.274488250670337663, 334.6312213355107019 ) ) ;
#10044=VECTOR ( 'NONE', #44670, 1000.000000000000000 ) ;
#10046=CARTESIAN_POINT ( 'NONE',  ( 776.2046728542105711, -212.1908817542436623, 304.8212110874238761 ) ) ;
#10048=CARTESIAN_POINT ( 'NONE',  ( 763.2262854647970016, -176.6346026584199933, 309.2812353651462445 ) ) ;
#10052=EDGE_CURVE ( 'NONE', #17907, #7675, #19623, .T. ) ;
#10053=CARTESIAN_POINT ( 'NONE',  ( 774.6858677611749044, -273.7255117493288026, 315.5713283507209894 ) ) ;
#10054=CARTESIAN_POINT ( 'NONE',  ( 796.9571628226829034, -47.46360902697148987, 321.2382568024804641 ) ) ;
#10058=CARTESIAN_POINT ( 'NONE',  ( 794.1144889064781864, -130.1692326535054463, 360.9840315886528401 ) ) ;
#10059=CARTESIAN_POINT ( 'NONE',  ( 805.1927285166397041, -328.8164208402375834, 341.8018195045277707 ) ) ;
#10061=VECTOR ( 'NONE', #25650, 1000.000000000000000 ) ;
#10064=CARTESIAN_POINT ( 'NONE',  ( 797.6776695296629214, -91.54369356751116982, 357.6776695296636603 ) ) ;
#10067=CARTESIAN_POINT ( 'NONE',  ( 798.0661480581538854, -410.5328690171408539, 309.5768839229118043 ) ) ;
#10069=CARTESIAN_POINT ( 'NONE',  ( 771.2633955100217236, -287.9073299311468759, 363.4237431249939618 ) ) ;
#10072=CARTESIAN_POINT ( 'NONE',  ( 804.9363028652555840, -400.2709662947828519, 338.2165204200192079 ) ) ;
#10078=CARTESIAN_POINT ( 'NONE',  ( 755.5713283507202505, -125.3618753856928834, 334.6858677611754729 ) ) ;
#10079=CARTESIAN_POINT ( 'NONE',  ( 780.5236548040995785, -452.7363362996975411, 314.9735926884559944 ) ) ;
#10083=CARTESIAN_POINT ( 'NONE',  ( 781.2497674668890113, -372.3510508353228374, 375.3608509340180603 ) ) ;
#10087=CARTESIAN_POINT ( 'NONE',  ( 766.4474001241216001, -43.09997266333511590, 307.3154664389482491 ) ) ;
#10095=CARTESIAN_POINT ( 'NONE',  ( 804.8461984189677878, -338.1908817542433212, 336.9566956441385628 ) ) ;
#10096=CARTESIAN_POINT ( 'NONE',  ( 811.3240766477731540, -316.3726999360615082, 355.6651683502462902 ) ) ;
#10100=CARTESIAN_POINT ( 'NONE',  ( 750.9282345327678740, -112.9181544815167229, 319.8311093483690115 ) ) ;
#10104=CARTESIAN_POINT ( 'NONE',  ( 755.5713283507202505, -197.3618753856926560, 334.6858677611754729 ) ) ;
#10106=CARTESIAN_POINT ( 'NONE',  ( 778.7629533639073998, -440.7363362996975980, 375.0009284576466371 ) ) ;
#10109=CARTESIAN_POINT ( 'NONE',  ( 802.5472867521000353, -52.37269993606237506, 350.8726784830461156 ) ) ;
#10112=CARTESIAN_POINT ( 'NONE',  ( 744.8212110874229666, 5.103494619221427442, 336.2046728542121627 ) ) ;
#10114=AXIS2_PLACEMENT_3D ( 'NONE', #41791, #31146, #24437 ) ;
#10117=CARTESIAN_POINT ( 'NONE',  ( 764.3348316497523456, -262.7146871989594956, 308.6759233522265617 ) ) ;
#10118=CARTESIAN_POINT ( 'NONE',  ( 756.5762568750052424, -123.1800572038747106, 348.7366044899774238 ) ) ;
#10120=CARTESIAN_POINT ( 'NONE',  ( 778.1981804954714335, -298.2709662947830793, 314.8072714833589885 ) ) ;
#10123=CARTESIAN_POINT ( 'NONE',  ( 792.8617558976345663, -450.5553044913475560, 371.8789995216883995 ) ) ;
#10127=CARTESIAN_POINT ( 'NONE',  ( 778.1981804954714335, -34.27096629478407408, 314.8072714833589885 ) ) ;
#10129=CARTESIAN_POINT ( 'NONE',  ( 758.8095938919644823, -368.0891481129647786, 311.6929314249762797 ) ) ;
#10130=CARTESIAN_POINT ( 'NONE',  ( 815.0009284576459549, -246.3510508353232638, 338.7629533639073429 ) ) ;
#10131=CARTESIAN_POINT ( 'NONE',  ( 814.8230680027162407, -53.80559628986930676, 333.7305795820267917 ) ) ;
#10136=CARTESIAN_POINT ( 'NONE',  ( 794.9819416627830151, -252.9982390220560831, 319.9864689768909898 ) ) ;
#10138=CARTESIAN_POINT ( 'NONE',  ( 772.5602148656447525, -369.7255117493284615, 305.7998596910095443 ) ) ;
#10143=CARTESIAN_POINT ( 'NONE',  ( 772.4468031744293057, -225.8272453906072599, 363.8651313633793620 ) ) ;
#10144=CARTESIAN_POINT ( 'NONE',  ( 803.6646147819161570, -113.9073299311474301, 348.8264449731210561 ) ) ;
#10148=CARTESIAN_POINT ( 'NONE',  ( 786.6156483768007774, -289.4419599262321299, 315.5913626894246136 ) ) ;
#10151=CARTESIAN_POINT ( 'NONE',  ( 791.0478386215596629, 2.172754609392001601, 306.7653713866226326 ) ) ;
#10153=CARTESIAN_POINT ( 'NONE',  ( 802.1676090361156639, -86.63460265842023489, 327.8955696845344505 ) ) ;
#10157=CARTESIAN_POINT ( 'NONE',  ( 814.8207195650702488, -410.1908817542430370, 336.2433038121456548 ) ) ;
#10160=CARTESIAN_POINT ( 'NONE',  ( 782.5225473063381969, -382.2709662947828519, 375.2698199232970637 ) ) ;
#10161=CARTESIAN_POINT ( 'NONE',  ( 758.8095938919644823, -8.089148112965974136, 311.6929314249762797 ) ) ;
#10163=CARTESIAN_POINT ( 'NONE',  ( 770.0799878456142551, -13.98741447168760033, 362.9823548866085616 ) ) ;
#10166=CARTESIAN_POINT ( 'NONE',  ( 812.6845335610512393, -175.9874144716871172, 353.5525998758768651 ) ) ;
#10167=CARTESIAN_POINT ( 'NONE',  ( 794.9819416627830151, -12.99823902205686821, 319.9864689768909898 ) ) ;
#10171=CARTESIAN_POINT ( 'NONE',  ( 774.6858677611749044, -153.7255117493291721, 315.5713283507209894 ) ) ;
#10174=CARTESIAN_POINT ( 'NONE',  ( 805.1927285166399315, -280.8164208402378108, 341.8018195045277707 ) ) ;
#10177=CARTESIAN_POINT ( 'NONE',  ( 805.0264073115434940, -30.35105083532391390, 339.4763451958999099 ) ) ;
#10180=CARTESIAN_POINT ( 'NONE',  ( 754.9967657858570647, -265.5436935675106156, 365.0032342141425943 ) ) ;
#10181=CARTESIAN_POINT ( 'NONE',  ( 779.4763451958990572, -344.7363362996978253, 365.0264073115438919 ) ) ;
#10182=CARTESIAN_POINT ( 'NONE',  ( 758.6633372737375112, -428.5328690171409107, 326.9102291470432533 ) ) ;
#10187=CARTESIAN_POINT ( 'NONE',  ( 775.9200461376533440, -335.8055962898683902, 315.3028492785443291 ) ) ;
#10189=CARTESIAN_POINT ( 'NONE',  ( 755.3028492785439312, -135.2817908451530116, 335.9200461376539693 ) ) ;
#10190=CARTESIAN_POINT ( 'NONE',  ( 781.7834795799800531, -10.81642084023869543, 315.0636971347436202 ) ) ;
#10194=CARTESIAN_POINT ( 'NONE',  ( 779.4763451958990572, -224.7363362996982232, 365.0264073115438919 ) ) ;
#10195=CARTESIAN_POINT ( 'NONE',  ( 773.7305795820266212, -225.2817908451527273, 374.8230680027170365 ) ) ;
#10196=CARTESIAN_POINT ( 'NONE',  ( 799.4546378042377910, -201.0783235625961254, 356.1575198192848006 ) ) ;
#10200=CARTESIAN_POINT ( 'NONE',  ( 747.2067596250078623, -75.18005720387485269, 352.2312462859687230 ) ) ;
#10201=CARTESIAN_POINT ( 'NONE',  ( 803.8904222555790966, -452.9681489794450044, 350.1048529224749473 ) ) ;
#10205=CARTESIAN_POINT ( 'NONE',  ( 814.2805881961230625, -361.6454272087887603, 331.2368401574024119 ) ) ;
#10207=CARTESIAN_POINT ( 'NONE',  ( 792.3570229623688874, -285.1800572038740711, 373.1304606946836202 ) ) ;
#10211=CARTESIAN_POINT ( 'NONE',  ( 757.8323909638827445, -410.6346026584191122, 352.1044303154654358 ) ) ;
#10212=CARTESIAN_POINT ( 'NONE',  ( 779.4763451958990572, -152.7363362996983938, 365.0264073115438919 ) ) ;
#10215=CARTESIAN_POINT ( 'NONE',  ( 812.6845335610512393, -79.98741447168740137, 353.5525998758768651 ) ) ;
#10216=CARTESIAN_POINT ( 'NONE',  ( 756.5762568750052424, -411.1800572038738437, 348.7366044899774238 ) ) ;
#10219=CARTESIAN_POINT ( 'NONE',  ( 804.9363028652555840, -424.2709662947829088, 338.2165204200192079 ) ) ;
#10223=CARTESIAN_POINT ( 'NONE',  ( 774.6312213355099630, -239.3618753856924570, 364.6798772138717482 ) ) ;
#10224=CARTESIAN_POINT ( 'NONE',  ( 781.7834795799800531, -178.8164208402381519, 315.0636971347436202 ) ) ;
#10228=CARTESIAN_POINT ( 'NONE',  ( 800.2193346964447755, -402.9982390220555430, 355.1360043628815788 ) ) ;
#10229=EDGE_LOOP ( 'NONE', ( #34944, #43643 ) ) ;
#10231=CARTESIAN_POINT ( 'NONE',  ( 751.9810565676468741, -146.0891481129655176, 360.9747183278973921 ) ) ;
#10233=CARTESIAN_POINT ( 'NONE',  ( 744.9990715423526808, -186.3510508353234343, 341.2370466360926002 ) ) ;
#10239=CARTESIAN_POINT ( 'NONE',  ( 780.5290396650775619, -228.3510508353232922, 365.2837595273619513 ) ) ;
#10242=EDGE_CURVE ( 'NONE', #45600, #15704, #41002, .T. ) ;
#10247=VERTEX_POINT ( 'NONE', #16726 ) ;
#10249=CARTESIAN_POINT ( 'NONE',  ( 813.5763878283155464, -123.8272453906076009, 351.1614460488615350 ) ) ;
#10257=CARTESIAN_POINT ( 'NONE',  ( 793.5525998758768083, -391.0999726633340288, 372.6845335610516941 ) ) ;
#10262=CARTESIAN_POINT ( 'NONE',  ( 774.6858677611749044, 14.27448825067031812, 315.5713283507209894 ) ) ;
#10264=CARTESIAN_POINT ( 'NONE',  ( 754.3581564841646241, -233.4636090269708575, 316.1443688327762516 ) ) ;
#10266=CARTESIAN_POINT ( 'NONE',  ( 745.7998596910086917, -173.3618753856927128, 332.5602148656461168 ) ) ;
#10269=CARTESIAN_POINT ( 'NONE',  ( 778.1981804954714335, -298.2709662947830793, 314.8072714833589885 ) ) ;
#10270=CARTESIAN_POINT ( 'NONE',  ( 798.5707757039680246, -53.46360902697146855, 356.7845633553585003 ) ) ;
#10277=CARTESIAN_POINT ( 'NONE',  ( 761.2382568024794409, -135.6237781080508853, 356.9571628226838129 ) ) ;
#10278=CARTESIAN_POINT ( 'NONE',  ( 771.2633955100217236, -335.9073299311468190, 363.4237431249939618 ) ) ;
#10281=CARTESIAN_POINT ( 'NONE',  ( 756.3353852180819104, -101.9073299311474727, 331.1735550268788302 ) ) ;
#10284=CARTESIAN_POINT ( 'NONE',  ( 812.6845335610512393, -415.9874144716862361, 353.5525998758768651 ) ) ;
#10286=CARTESIAN_POINT ( 'NONE',  ( 778.2165204200184689, -286.8164208402378677, 364.9363028652563230 ) ) ;
#10289=CARTESIAN_POINT ( 'NONE',  ( 767.8955696845333705, -408.4527844766009252, 362.1676090361162323 ) ) ;
#10295=EDGE_CURVE ( 'NONE', #13889, #16040, #34032, .T. ) ;
#10296=CARTESIAN_POINT ( 'NONE',  ( 774.6858677611749044, -129.7255117493292289, 315.5713283507209894 ) ) ;
#10297=CARTESIAN_POINT ( 'NONE',  ( 800.9840315886518738, -436.9181544815157281, 354.1144889064786412 ) ) ;
#10298=CARTESIAN_POINT ( 'NONE',  ( 758.6633372737375112, -116.5328690171418202, 326.9102291470432533 ) ) ;
#10300=DIRECTION ( 'NONE',  ( -1.000000000000000000, -0.000000000000000000, 0.000000000000000000 ) ) ;
#10301=CARTESIAN_POINT ( 'NONE',  ( 795.6651683502461765, -346.7146871989592682, 371.3240766477733814 ) ) ;
#10308=CARTESIAN_POINT ( 'NONE',  ( 745.5313806188320314, -39.28179084515331709, 333.7943932421247268 ) ) ;
#10309=CARTESIAN_POINT ( 'NONE',  ( 779.9999999999992042, 16.45630643248849267, 339.9999999999999432 ) ) ;
#10317=CARTESIAN_POINT ( 'NONE',  ( 793.9708237608222134, -358.9181544815160123, 319.2295555964448681 ) ) ;
#10318=CARTESIAN_POINT ( 'NONE',  ( 762.1177392798416577, -354.5545181178796383, 309.8865473780659272 ) ) ;
#10321=CARTESIAN_POINT ( 'NONE',  ( 807.2620300519052989, -120.0090635724258021, 318.0141637701419768 ) ) ;
#10325=CARTESIAN_POINT ( 'NONE',  ( 756.5762568750052424, -171.1800572038745543, 348.7366044899774238 ) ) ;
#10327=CARTESIAN_POINT ( 'NONE',  ( 802.2119215644370342, -414.0090635724249637, 367.5423716828165084 ) ) ;
#10333=CARTESIAN_POINT ( 'NONE',  ( 805.9055244015594326, -3.623778108051270319, 315.8990559732753240 ) ) ;
#10337=CARTESIAN_POINT ( 'NONE',  ( 805.9055244015594326, -315.6237781080503169, 315.8990559732753240 ) ) ;
#10338=CARTESIAN_POINT ( 'NONE',  ( 792.1044303154646968, -132.4527844766019200, 317.8323909638837677 ) ) ;
#10340=CARTESIAN_POINT ( 'NONE',  ( 759.9864689768902508, -314.0891481129650629, 354.9819416627836404 ) ) ;
#10347=CARTESIAN_POINT ( 'NONE',  ( 768.0187753319979720, -32.63460265842044095, 318.0580252608186242 ) ) ;
#10349=CARTESIAN_POINT ( 'NONE',  ( 772.5602148656447525, -345.7255117493285184, 305.7998596910095443 ) ) ;
#10350=CARTESIAN_POINT ( 'NONE',  ( 764.3348316497523456, -238.7146871989596661, 308.6759233522265617 ) ) ;
#10356=CARTESIAN_POINT ( 'NONE',  ( 802.1676090361156639, -254.6346026584196238, 327.8955696845344505 ) ) ;
#10358=CARTESIAN_POINT ( 'NONE',  ( 772.4837098697144029, -407.3618753856920307, 374.5518280994205611 ) ) ;
#10364=CARTESIAN_POINT ( 'NONE',  ( 760.7433823573367135, -276.0090635724253048, 355.9930595647440441 ) ) ;
#10365=CARTESIAN_POINT ( 'NONE',  ( 768.0187753319979720, -128.6346026584201354, 318.0580252608186242 ) ) ;
#10369=CARTESIAN_POINT ( 'NONE',  ( 804.9511171171677688, -293.8055962898685607, 335.8780910478229202 ) ) ;
#10371=CARTESIAN_POINT ( 'NONE',  ( 757.7880784355613741, 5.990936427573807954, 312.4576283171834916 ) ) ;
#10373=CARTESIAN_POINT ( 'NONE',  ( 792.3570229623688874, -189.1800572038744122, 373.1304606946836202 ) ) ;
#10374=CARTESIAN_POINT ( 'NONE',  ( 759.7806653035534055, -78.99823902205662307, 324.8639956371180801 ) ) ;
#10377=CARTESIAN_POINT ( 'NONE',  ( 814.2805881961230625, -409.6454272087884760, 331.2368401574024119 ) ) ;
#10380=CARTESIAN_POINT ( 'NONE',  ( 765.8855110935204493, -358.1692326535047641, 319.0159684113471599 ) ) ;
#10381=CARTESIAN_POINT ( 'NONE',  ( 811.0346526505617248, -38.63460265842041963, 323.0537975583478101 ) ) ;
#10384=CARTESIAN_POINT ( 'NONE',  ( 789.9200121543843807, -25.98741447168755769, 317.0176451133914384 ) ) ;
#10388=CARTESIAN_POINT ( 'NONE',  ( 800.1688906516307043, -202.1692326535051905, 369.0717654672308186 ) ) ;
#10389=CARTESIAN_POINT ( 'NONE',  ( 762.3223304703356007, -7.543693567511430942, 322.3223304703362828 ) ) ;
#10393=CARTESIAN_POINT ( 'NONE',  ( 804.6798772138708955, -207.7255117493289447, 334.6312213355107019 ) ) ;
#10394=PRODUCT_DEFINITION_SHAPE ( 'NONE', 'NONE',  #24214 ) ;
#10396=CARTESIAN_POINT ( 'NONE',  ( 797.8594530101009923, -325.5436935675104451, 322.1405469898982119 ) ) ;
#10399=CARTESIAN_POINT ( 'NONE',  ( 754.8983024940795303, -66.89650538077835051, 336.9254006560228163 ) ) ;
#10401=CARTESIAN_POINT ( 'NONE',  ( 755.2512626584698410, -247.5436935675106724, 315.2512626584710915 ) ) ;
#10402=CARTESIAN_POINT ( 'NONE',  ( 755.8894580844503253, -351.8272453906068336, 332.3691319403863531 ) ) ;
#10403=CARTESIAN_POINT ( 'NONE',  ( 756.1348686366196716, -425.2601417444136018, 347.5531968255698416 ) ) ;
#10409=CARTESIAN_POINT ( 'NONE',  ( 796.7737145352015204, -284.6346026584196807, 370.7187646348536987 ) ) ;
#10410=CARTESIAN_POINT ( 'NONE',  ( 805.0264073115434940, -318.3510508353230080, 339.4763451958999099 ) ) ;
#10412=CARTESIAN_POINT ( 'NONE',  ( 790.0220218866281812, -127.0999726633348672, 363.2186876482849129 ) ) ;
#10413=CARTESIAN_POINT ( 'NONE',  ( 768.0187753319979720, -8.634602658420517329, 318.0580252608186242 ) ) ;
#10417=CARTESIAN_POINT ( 'NONE',  ( 798.5707757039680246, -221.4636090269709428, 356.7845633553585003 ) ) ;
#10418=CARTESIAN_POINT ( 'NONE',  ( 793.5525998758768083, -247.0999726633344835, 372.6845335610516941 ) ) ;
#10419=CARTESIAN_POINT ( 'NONE',  ( 764.0069404352550464, -183.0783235625961538, 359.2566176426627180 ) ) ;
#10422=CARTESIAN_POINT ( 'NONE',  ( 748.9653473494363425, -26.63460265842045871, 356.9462024416521331 ) ) ;
#10423=CARTESIAN_POINT ( 'NONE',  ( 814.2001403089898304, -65.36187538569306810, 347.4397851343538264 ) ) ;
#10424=DIRECTION ( 'NONE',  ( -1.000000000000000000, -0.000000000000000000, 0.000000000000000000 ) ) ;
#10427=CARTESIAN_POINT ( 'NONE',  ( 802.2119215644370342, -342.0090635724251342, 367.5423716828165084 ) ) ;
#10429=CARTESIAN_POINT ( 'NONE',  ( 747.2067596250078623, -315.1800572038740711, 352.2312462859687230 ) ) ;
#10434=CARTESIAN_POINT ( 'NONE',  ( 771.2633955100217236, -383.9073299311466485, 363.4237431249939618 ) ) ;
#10436=CARTESIAN_POINT ( 'NONE',  ( 784.1219089521767955, -141.2817908451530400, 315.0488828828318333 ) ) ;
#10439=CARTESIAN_POINT ( 'NONE',  ( 783.7566961878529810, -72.89650538077830788, 305.1792804349288417 ) ) ;
#10440=CARTESIAN_POINT ( 'NONE',  ( 801.9419747391806368, -402.4527844766010389, 351.9812246680014027 ) ) ;
#10448=CARTESIAN_POINT ( 'NONE',  ( 778.2165204200184689, -214.8164208402380666, 364.9363028652563230 ) ) ;
#10449=CARTESIAN_POINT ( 'NONE',  ( 757.8323909638828582, -218.6346026584198228, 352.1044303154654358 ) ) ;
#10453=CARTESIAN_POINT ( 'NONE',  ( 800.0135310231082713, -422.0891481129647218, 325.0180583372163028 ) ) ;
#10456=CARTESIAN_POINT ( 'NONE',  ( 804.7487373415286811, -139.5436935675110135, 364.7487373415288516 ) ) ;
#10463=CARTESIAN_POINT ( 'NONE',  ( 766.7756240680305382, -230.5328690171415076, 361.5560724626415663 ) ) ;
#10473=CARTESIAN_POINT ( 'NONE',  ( 749.5768839229115201, -132.5545181178802920, 358.0661480581553064 ) ) ;
#10480=CARTESIAN_POINT ( 'NONE',  ( 783.7953271457878373, -392.1908817542432075, 375.1787889125761239 ) ) ;
#10487=CARTESIAN_POINT ( 'NONE',  ( 766.4474001241216001, -259.0999726633343698, 307.3154664389482491 ) ) ;
#10489=CARTESIAN_POINT ( 'NONE',  ( 777.5031285880264704, -190.8164208402381234, 374.9108240113588408 ) ) ;
#10492=CARTESIAN_POINT ( 'NONE',  ( 755.0636971347428243, -292.2709662947831930, 341.7834795799807353 ) ) ;
#10493=AXIS2_PLACEMENT_3D ( 'NONE', #31614, #4141, #25128 ) ;
#10494=CARTESIAN_POINT ( 'NONE',  ( 775.8780910478218402, -81.28179084515319630, 364.9511171171680530 ) ) ;
#10498=CARTESIAN_POINT ( 'NONE',  ( 755.8398074228967971, -139.4419599262326699, 333.4516893846970333 ) ) ;
#10499=CARTESIAN_POINT ( 'NONE',  ( 797.6776695296629214, -331.5436935675104451, 357.6776695296636603 ) ) ;
#10502=CARTESIAN_POINT ( 'NONE',  ( 759.9864689768902508, -98.08914811296568814, 354.9819416627836404 ) ) ;
#10505=CARTESIAN_POINT ( 'NONE',  ( 761.9338519418445230, -422.5328690171408539, 370.4231160770881957 ) ) ;
#10507=CARTESIAN_POINT ( 'NONE',  ( 802.1676090361156639, -302.6346026584196238, 327.8955696845344505 ) ) ;
#10511=CARTESIAN_POINT ( 'NONE',  ( 759.9864689768902508, -410.0891481129647218, 354.9819416627836404 ) ) ;
#10517=CARTESIAN_POINT ( 'NONE',  ( 762.1405469898971887, -121.5436935675110419, 357.8594530101015607 ) ) ;
#10518=CARTESIAN_POINT ( 'NONE',  ( 780.5236548040995785, -428.7363362996975980, 314.9735926884559944 ) ) ;
#10519=CARTESIAN_POINT ( 'NONE',  ( 754.8983024940795303, -114.8965053807782226, 336.9254006560228163 ) ) ;
#10522=CARTESIAN_POINT ( 'NONE',  ( 756.1443688327750579, -405.6237781080500326, 314.3581564841659315 ) ) ;
#10528=CARTESIAN_POINT ( 'NONE',  ( 807.2620300519052989, -48.00906357242602951, 318.0141637701419768 ) ) ;
#10536=CARTESIAN_POINT ( 'NONE',  ( 790.0220218866281812, -367.0999726633342561, 363.2186876482849129 ) ) ;
#10537=CARTESIAN_POINT ( 'NONE',  ( 815.3608509340175488, -338.7363362996978822, 341.2497674668889545 ) ) ;
#10541=CARTESIAN_POINT ( 'NONE',  ( 814.2805881961230625, -145.6454272087893287, 331.2368401574024119 ) ) ;
#10546=CARTESIAN_POINT ( 'NONE',  ( 759.9864689768902508, -170.0891481129654608, 354.9819416627836404 ) ) ;
#10548=CARTESIAN_POINT ( 'NONE',  ( 744.6391490659812007, -446.7363362996975980, 338.7502325331110455 ) ) ;
#10554=CARTESIAN_POINT ( 'NONE',  ( 803.8556311672234642, -9.623778108051251223, 365.6418435158340117 ) ) ;
#10560=CARTESIAN_POINT ( 'NONE',  ( 813.2346286133761168, -293.2601417444139429, 328.9521613784389160 ) ) ;
#10561=CARTESIAN_POINT ( 'NONE',  ( 803.6646147819162707, -137.9073299311473875, 348.8264449731211130 ) ) ;
#10565=CARTESIAN_POINT ( 'NONE',  ( 755.0636971347428243, -316.2709662947832499, 341.7834795799807353 ) ) ;
#10566=EDGE_CURVE ( 'NONE', #3123, #20161, #16672, .T. ) ;
#10568=CARTESIAN_POINT ( 'NONE',  ( 789.4635523819913487, -451.6789215907663788, 363.3011154535611809 ) ) ;
#10575=CARTESIAN_POINT ( 'NONE',  ( 757.8323909638827445, -26.63460265842045871, 352.1044303154654358 ) ) ;
#10577=CARTESIAN_POINT ( 'NONE',  ( 755.2512626584698410, -343.5436935675103314, 315.2512626584710915 ) ) ;
#10578=CARTESIAN_POINT ( 'NONE',  ( 783.7566961878529810, -288.8965053807775121, 305.1792804349288417 ) ) ;
#10579=CARTESIAN_POINT ( 'NONE',  ( 814.8230680027162407, -77.80559628986920018, 333.7305795820267917 ) ) ;
#10585=CARTESIAN_POINT ( 'NONE',  ( 785.3687786644884454, -251.3618753856923149, 315.3201227861279676 ) ) ;
#10587=CARTESIAN_POINT ( 'NONE',  ( 755.2512626584698410, -391.5436935675101608, 315.2512626584710915 ) ) ;
#10594=CARTESIAN_POINT ( 'NONE',  ( 755.3028492785439312, -255.2817908451526705, 335.9200461376539693 ) ) ;
#10595=CARTESIAN_POINT ( 'NONE',  ( 774.6858677611749044, -129.7255117493292289, 315.5713283507209894 ) ) ;
#10601=CARTESIAN_POINT ( 'NONE',  ( 773.3843516231979720, -277.4419599262322436, 364.4086373105754433 ) ) ;
#10603=CARTESIAN_POINT ( 'NONE',  ( 802.2119215644370342, -30.00906357242607925, 367.5423716828165084 ) ) ;
#10605=CARTESIAN_POINT ( 'NONE',  ( 771.2633955100217236, -95.90732993114751537, 363.4237431249939618 ) ) ;
#10610=CARTESIAN_POINT ( 'NONE',  ( 754.3581564841646241, -449.4636090269702322, 316.1443688327762516 ) ) ;
#10613=CARTESIAN_POINT ( 'NONE',  ( 790.8726784830453198, -346.7146871989592682, 362.5472867521010585 ) ) ;
#10614=CARTESIAN_POINT ( 'NONE',  ( 751.6929314249750860, -30.99823902205680781, 318.8095938919659034 ) ) ;
#10617=CARTESIAN_POINT ( 'NONE',  ( 760.5453621957607311, -45.07832356259660145, 323.8424801807151425 ) ) ;
#10620=CARTESIAN_POINT ( 'NONE',  ( 749.8865473780648472, -212.5328690171415076, 322.1177392798429082 ) ) ;
#10621=CARTESIAN_POINT ( 'NONE',  ( 781.8018195045267476, -22.27096629478410605, 365.1927285166407273 ) ) ;
#10622=CARTESIAN_POINT ( 'NONE',  ( 780.5290396650775619, -372.3510508353228374, 365.2837595273619513 ) ) ;
#10625=CARTESIAN_POINT ( 'NONE',  ( 804.9363028652555840, -184.2709662947835909, 338.2165204200192079 ) ) ;
#10627=CARTESIAN_POINT ( 'NONE',  ( 788.8264449731201466, -333.1800572038740142, 363.6646147819170665 ) ) ;
#10631=CARTESIAN_POINT ( 'NONE',  ( 754.9735926884551418, -42.35105083532388193, 340.5236548041000333 ) ) ;
#10633=CARTESIAN_POINT ( 'NONE',  ( 801.1904061080338124, -260.0891481129650629, 368.3070685750236066 ) ) ;
#10634=CARTESIAN_POINT ( 'NONE',  ( 761.9338519418445230, -14.53286901714214707, 370.4231160770881957 ) ) ;
#10639=CARTESIAN_POINT ( 'NONE',  ( 792.2312462859673587, -275.9073299311469896, 307.2067596250082602 ) ) ;
#10642=CARTESIAN_POINT ( 'NONE',  ( 786.6156483768007774, -337.4419599262319593, 315.5913626894246136 ) ) ;
#10645=CARTESIAN_POINT ( 'NONE',  ( 783.0745993439762742, -152.1908817542438612, 365.1016975059196739 ) ) ;
#10646=CARTESIAN_POINT ( 'NONE',  ( 755.0636971347428243, -4.270966294784170003, 341.7834795799807353 ) ) ;
#10650=CARTESIAN_POINT ( 'NONE',  ( 812.3518521366052028, -241.0999726633345119, 326.5853460496235243 ) ) ;
#10651=CARTESIAN_POINT ( 'NONE',  ( 796.7845633553578182, -369.6237781080500895, 358.5707757039688204 ) ) ;
#10652=CARTESIAN_POINT ( 'NONE',  ( 766.7756240680305382, -182.5328690171416497, 361.5560724626415663 ) ) ;
#10654=CARTESIAN_POINT ( 'NONE',  ( 790.9844846989617508, -454.3726999360611103, 317.2208543904092721 ) ) ;
#10658=CARTESIAN_POINT ( 'NONE',  ( 805.0032342141412300, -13.54369356751140785, 314.9967657858571783 ) ) ;
#10663=CARTESIAN_POINT ( 'NONE',  ( 745.5313806188320314, -351.2817908451523294, 333.7943932421247268 ) ) ;
#10665=CARTESIAN_POINT ( 'NONE',  ( 754.9967657858570647, -313.5436935675102745, 365.0032342141425374 ) ) ;
#10669=CARTESIAN_POINT ( 'NONE',  ( 768.0187753319979720, -416.6346026584192259, 318.0580252608186242 ) ) ;
#10670=CARTESIAN_POINT ( 'NONE',  ( 801.5560724626406000, -168.5545181178802352, 326.7756240680316182 ) ) ;
#10673=CARTESIAN_POINT ( 'NONE',  ( 746.7653713866222915, -113.2601417444145682, 351.0478386215610271 ) ) ;
#10674=CARTESIAN_POINT ( 'NONE',  ( 767.8955696845334842, -408.4527844766009821, 362.1676090361161755 ) ) ;
#10682=CARTESIAN_POINT ( 'NONE',  ( 755.3201227861273992, -219.7255117493289447, 345.3687786644892981 ) ) ;
#10683=CARTESIAN_POINT ( 'NONE',  ( 759.9864689768902508, -218.0891481129653187, 354.9819416627836404 ) ) ;
#10685=CARTESIAN_POINT ( 'NONE',  ( 763.0537975583475827, -0.4527844766023628176, 371.0346526505627480 ) ) ;
#10688=CARTESIAN_POINT ( 'NONE',  ( 759.7806653035534055, -438.9982390220553157, 324.8639956371180801 ) ) ;
#10691=CARTESIAN_POINT ( 'NONE',  ( 814.9108240113580450, -160.2709662947836762, 337.5031285880265273 ) ) ;
#10693=CARTESIAN_POINT ( 'NONE',  ( 759.2295555964440155, -376.1692326535046504, 353.9708237608231229 ) ) ;
#10697=VERTEX_POINT ( 'NONE', #33099 ) ;
#10701=CARTESIAN_POINT ( 'NONE',  ( 772.3691319403857278, -239.2601417444141987, 315.8894580844506663 ) ) ;
#10709=VECTOR ( 'NONE', #24852, 1000.000000000000000 ) ;
#10710=CARTESIAN_POINT ( 'NONE',  ( 793.5525998758768083, -151.0999726633347677, 372.6845335610516941 ) ) ;
#10719=CARTESIAN_POINT ( 'NONE',  ( 752.7379699480933368, -372.0090635724250205, 361.9858362298580232 ) ) ;
#10724=CARTESIAN_POINT ( 'NONE',  ( 774.6858677611749044, -9.725511749329603717, 315.5713283507209894 ) ) ;
#10726=CARTESIAN_POINT ( 'NONE',  ( 814.8207195650702488, -266.1908817542435486, 336.2433038121456548 ) ) ;
#10728=CARTESIAN_POINT ( 'NONE',  ( 813.1304606946830518, -209.9073299311470748, 352.3570229623690580 ) ) ;
#10731=CARTESIAN_POINT ( 'NONE',  ( 778.2165204200184689, -286.8164208402378677, 364.9363028652563230 ) ) ;
#10733=CARTESIAN_POINT ( 'NONE',  ( 801.5560724626406000, -96.55451811788039151, 326.7756240680316182 ) ) ;
#10738=CARTESIAN_POINT ( 'NONE',  ( 772.3691319403857278, -119.2601417444145397, 315.8894580844506663 ) ) ;
#10739=CARTESIAN_POINT ( 'NONE',  ( 803.4237431249931660, -375.1800572038739574, 331.2633955100225194 ) ) ;
#10742=CARTESIAN_POINT ( 'NONE',  ( 781.7834795799800531, -82.81642084023846451, 315.0636971347436202 ) ) ;
#10743=CARTESIAN_POINT ( 'NONE',  ( 752.7379699480933368, -396.0090635724249637, 361.9858362298580232 ) ) ;
#10746=CARTESIAN_POINT ( 'NONE',  ( 791.1614460488616487, -419.2601417444136587, 373.5763878283158874 ) ) ;
#10748=CARTESIAN_POINT ( 'NONE',  ( 754.8072714833581358, -340.8164208402376971, 338.1981804954720587 ) ) ;
#10749=CIRCLE ( 'NONE', #26991, 10.00000000000000888 ) ;
#10753=CARTESIAN_POINT ( 'NONE',  ( 800.0135310231082713, -398.0891481129647218, 325.0180583372163028 ) ) ;
#10760=CARTESIAN_POINT ( 'NONE',  ( 802.1676090361156639, -134.6346026584201070, 327.8955696845344505 ) ) ;
#10761=CARTESIAN_POINT ( 'NONE',  ( 779.4763451958990572, -440.7363362996975980, 365.0264073115438919 ) ) ;
#10762=CARTESIAN_POINT ( 'NONE',  ( 754.9735926884551418, -114.3510508353236617, 340.5236548041000333 ) ) ;
#10765=CARTESIAN_POINT ( 'NONE',  ( 752.4576283171824116, -381.0783235625954717, 317.7880784355627952 ) ) ;
#10770=CARTESIAN_POINT ( 'NONE',  ( 773.7305795820266212, -33.28179084515333130, 374.8230680027170365 ) ) ;
#10780=CARTESIAN_POINT ( 'NONE',  ( 779.4763451958990572, -368.7363362996977685, 365.0264073115438919 ) ) ;
#10781=CARTESIAN_POINT ( 'NONE',  ( 760.0363995740630116, -346.9181544815160123, 368.7758568127991907 ) ) ;
#10787=CARTESIAN_POINT ( 'NONE',  ( 748.6759233522253680, -160.3726999360620482, 324.3348316497537098 ) ) ;
#10789=CARTESIAN_POINT ( 'NONE',  ( 767.7687537140311633, -119.9073299311474443, 372.7932403749916830 ) ) ;
#10795=CARTESIAN_POINT ( 'NONE',  ( 756.3353852180819104, -173.9073299311472169, 331.1735550268788302 ) ) ;
#10796=CARTESIAN_POINT ( 'NONE',  ( 802.9823548866075953, -1.099972663335260226, 330.0799878456151077 ) ) ;
#10800=CARTESIAN_POINT ( 'NONE',  ( 747.3154664389472828, 4.012585528312341054, 326.4474001241230781 ) ) ;
#10804=CARTESIAN_POINT ( 'NONE',  ( 748.3538107759620743, -304.7146871989594388, 355.8262568251490165 ) ) ;
#10805=CARTESIAN_POINT ( 'NONE',  ( 802.1676090361155502, -134.6346026584201070, 327.8955696845344505 ) ) ;
#10808=CARTESIAN_POINT ( 'NONE',  ( 758.0580252608178853, -294.4527844766013800, 328.0187753319985404 ) ) ;
#10812=CARTESIAN_POINT ( 'NONE',  ( 744.7301800767020268, -76.81642084023847872, 337.4774526936615189 ) ) ;
#10817=CARTESIAN_POINT ( 'NONE',  ( 797.6776695296629214, -19.54369356751139364, 357.6776695296636603 ) ) ;
#10820=CARTESIAN_POINT ( 'NONE',  ( 777.4774526936600978, -394.2709662947829088, 304.7301800767028226 ) ) ;
#10821=CARTESIAN_POINT ( 'NONE',  ( 807.5423716828161105, -297.0783235625957559, 362.2119215644372048 ) ) ;
#10822=CARTESIAN_POINT ( 'NONE',  ( 776.2433038121456548, -84.89650538077830788, 374.8207195650711014 ) ) ;
#10828=CARTESIAN_POINT ( 'NONE',  ( 815.2698199232961542, -400.8164208402373561, 342.5225473063383106 ) ) ;
#10835=CARTESIAN_POINT ( 'NONE',  ( 793.0897708529556667, -270.5545181178798657, 361.3366627262616362 ) ) ;
#10836=CARTESIAN_POINT ( 'NONE',  ( 755.5713283507202505, -125.3618753856928834, 334.6858677611754729 ) ) ;
#10840=CARTESIAN_POINT ( 'NONE',  ( 790.8726784830453198, -298.7146871989593251, 362.5472867521010585 ) ) ;
#10842=CARTESIAN_POINT ( 'NONE',  ( 807.2620300519052989, -24.00906357242609346, 318.0141637701419768 ) ) ;
#10844=AXIS2_PLACEMENT_3D ( 'NONE', #31613, #38784, #39240 ) ;
#10846=CARTESIAN_POINT ( 'NONE',  ( 801.1904061080336987, -188.0891481129653187, 368.3070685750235498 ) ) ;
#10847=CARTESIAN_POINT ( 'NONE',  ( 803.4237431249931660, -87.18005720387481006, 331.2633955100225194 ) ) ;
#10852=CARTESIAN_POINT ( 'NONE',  ( 786.2694204179717872, -453.2817908451519315, 305.1769319972829067 ) ) ;
#10855=CARTESIAN_POINT ( 'NONE',  ( 800.7704444035546203, -364.1692326535046504, 326.0291762391768771 ) ) ;
#10856=CARTESIAN_POINT ( 'NONE',  ( 792.3570229623691148, -45.18005720387493795, 373.1304606946836770 ) ) ;
#10859=CARTESIAN_POINT ( 'NONE',  ( 804.1601925771018387, -55.44195992623293989, 346.5483106153029098 ) ) ;
#10863=CARTESIAN_POINT ( 'NONE',  ( 754.0944755984390895, -207.6237781080506295, 364.1009440267246760 ) ) ;
#10864=CARTESIAN_POINT ( 'NONE',  ( 755.5713283507202505, -29.36187538569318178, 334.6858677611754729 ) ) ;
#10868=CARTESIAN_POINT ( 'NONE',  ( 781.8018195045266339, -214.2709662947834488, 365.1927285166406705 ) ) ;
#10870=CARTESIAN_POINT ( 'NONE',  ( 800.2193346964446619, -330.9982390220558273, 355.1360043628816925 ) ) ;
#10874=CARTESIAN_POINT ( 'NONE',  ( 794.1144889064781864, -58.16923265350564520, 360.9840315886528401 ) ) ;
#10876=CARTESIAN_POINT ( 'NONE',  ( 810.7187646348534145, -258.4527844766016074, 356.7737145352016341 ) ) ;
#10877=CARTESIAN_POINT ( 'NONE',  ( 754.0944755984390895, -15.62377810805123524, 364.1009440267246760 ) ) ;
#10883=CARTESIAN_POINT ( 'NONE',  ( 804.7487373415286811, -283.5436935675105019, 364.7487373415288516 ) ) ;
#10886=CARTESIAN_POINT ( 'NONE',  ( 803.2186876482843445, -343.9874144716865771, 350.0220218866286928 ) ) ;
#10889=CARTESIAN_POINT ( 'NONE',  ( 793.0897708529556667, -150.5545181178802352, 361.3366627262616362 ) ) ;
#10890=CARTESIAN_POINT ( 'NONE',  ( 800.0135310231082713, -14.08914811296595460, 325.0180583372163028 ) ) ;
#10891=VERTEX_POINT ( 'NONE', #1652 ) ;
#10894=CARTESIAN_POINT ( 'NONE',  ( 781.2370466360911223, -284.7363362996979390, 304.9990715423533629 ) ) ;
#10895=CARTESIAN_POINT ( 'NONE',  ( 784.0799538623451781, -203.8055962898688449, 364.6971507214555572 ) ) ;
#10897=CARTESIAN_POINT ( 'NONE',  ( 795.1360043628807261, 3.910851887033985896, 360.2193346964456282 ) ) ;
#10902=CARTESIAN_POINT ( 'NONE',  ( 801.1904061080336987, -20.08914811296592973, 368.3070685750235498 ) ) ;
#10903=CARTESIAN_POINT ( 'NONE',  ( 808.0189434323515343, -86.08914811296573077, 319.0252816721025511 ) ) ;
#10904=DIRECTION ( 'NONE',  ( 1.000000000000000000, -0.000000000000000000, -0.000000000000000000 ) ) ;
#10907=CARTESIAN_POINT ( 'NONE',  ( 745.1792804349281596, -350.1908817542433212, 343.7566961878542884 ) ) ;
#10909=CARTESIAN_POINT ( 'NONE',  ( 801.1904061080336987, -332.0891481129649492, 368.3070685750235498 ) ) ;
#10913=CARTESIAN_POINT ( 'NONE',  ( 754.8072714833581358, -436.8164208402372992, 338.1981804954720587 ) ) ;
#10914=CARTESIAN_POINT ( 'NONE',  ( 787.5531968255692163, -189.8272453906073736, 316.1348686366205811 ) ) ;
#10917=CARTESIAN_POINT ( 'NONE',  ( 746.7653713866222915, -89.26014174441463922, 351.0478386215610271 ) ) ;
#10918=CARTESIAN_POINT ( 'NONE',  ( 755.0636971347428243, -388.2709662947829656, 341.7834795799807353 ) ) ;
#10920=CARTESIAN_POINT ( 'NONE',  ( 800.2193346964447755, -450.9982390220554294, 355.1360043628815788 ) ) ;
#10925=CARTESIAN_POINT ( 'NONE',  ( 788.8264449731200330, -213.1800572038743553, 363.6646147819171233 ) ) ;
#10926=CARTESIAN_POINT ( 'NONE',  ( 794.9819416627830151, -228.9982390220561683, 319.9864689768909898 ) ) ;
#10931=CARTESIAN_POINT ( 'NONE',  ( 764.8639956371174549, -416.0891481129645513, 319.7806653035542013 ) ) ;
#10934=CARTESIAN_POINT ( 'NONE',  ( 808.3070685750232087, -138.9982390220564241, 361.1904061080339829 ) ) ;
#10935=CARTESIAN_POINT ( 'NONE',  ( 766.9102291470427417, -282.5545181178798657, 318.6633372737382501 ) ) ;
#10943=CARTESIAN_POINT ( 'NONE',  ( 800.7704444035546203, -220.1692326535051052, 326.0291762391768771 ) ) ;
#10952=CARTESIAN_POINT ( 'NONE',  ( 750.9282345327678740, -136.9181544815166376, 319.8311093483690115 ) ) ;
#10959=CARTESIAN_POINT ( 'NONE',  ( 745.1792804349281596, -374.1908817542432075, 343.7566961878542884 ) ) ;
#10964=CARTESIAN_POINT ( 'NONE',  ( 778.2165204200184689, 1.183579159761269040, 364.9363028652563230 ) ) ;
#10965=CARTESIAN_POINT ( 'NONE',  ( 810.4231160770870019, -240.5545181178798941, 321.9338519418446936 ) ) ;
#10967=CARTESIAN_POINT ( 'NONE',  ( 805.0032342141412300, -229.5436935675106440, 314.9967657858571783 ) ) ;
#10970=CARTESIAN_POINT ( 'NONE',  ( 756.3353852180819104, -341.9073299311465917, 331.1735550268788302 ) ) ;
#10971=CARTESIAN_POINT ( 'NONE',  ( 790.0220218866281812, -103.0999726633349525, 363.2186876482849129 ) ) ;
#10972=CARTESIAN_POINT ( 'NONE',  ( 763.8424801807145741, -90.00906357242590161, 320.5453621957614700 ) ) ;
#10976=CARTESIAN_POINT ( 'NONE',  ( 779.4709603349208464, -144.3510508353235764, 314.7162404726379918 ) ) ;
#10977=CARTESIAN_POINT ( 'NONE',  ( 771.1735550268778070, -345.1800572038739006, 316.3353852180827630 ) ) ;
#10981=CARTESIAN_POINT ( 'NONE',  ( 797.6776695296629214, -115.5436935675110988, 357.6776695296636603 ) ) ;
#10984=CARTESIAN_POINT ( 'NONE',  ( 744.8212110874229666, -426.8965053807771142, 336.2046728542121627 ) ) ;
#10986=CARTESIAN_POINT ( 'NONE',  ( 797.8594530101008786, -325.5436935675105019, 322.1405469898980982 ) ) ;
#10987=AXIS2_PLACEMENT_3D ( 'NONE', #30998, #1303, #16449 ) ;
#10991=CARTESIAN_POINT ( 'NONE',  ( 804.6798772138708955, -399.7255117493283478, 334.6312213355107019 ) ) ;
#10997=CARTESIAN_POINT ( 'NONE',  ( 769.9779781133707957, -451.0999726633339151, 316.7813123517150871 ) ) ;
#10998=CARTESIAN_POINT ( 'NONE',  ( 754.8983024940795303, -138.8965053807781374, 336.9254006560228163 ) ) ;
#11001=CARTESIAN_POINT ( 'NONE',  ( 754.0944755984390895, -375.6237781080501463, 364.1009440267246760 ) ) ;
#11006=CARTESIAN_POINT ( 'NONE',  ( 799.9636004259356241, -22.91815448151701062, 311.2241431872006956 ) ) ;
#11014=CARTESIAN_POINT ( 'NONE',  ( 780.5236548040995785, -356.7363362996978253, 314.9735926884559944 ) ) ;
#11015=CARTESIAN_POINT ( 'NONE',  ( 773.7305795820266212, -345.2817908451523863, 374.8230680027170365 ) ) ;
#11020=CARTESIAN_POINT ( 'NONE',  ( 795.8262568251477660, -142.3726999360620766, 308.3538107759623585 ) ) ;
#11022=CARTESIAN_POINT ( 'NONE',  ( 763.0537975583475827, -120.4527844766019484, 371.0346526505627480 ) ) ;
#11026=CARTESIAN_POINT ( 'NONE',  ( 755.5713283507202505, -221.3618753856925707, 334.6858677611754729 ) ) ;
#11027=CARTESIAN_POINT ( 'NONE',  ( 796.2681130854250569, -462.7578698805381237, 371.0719813302654870 ) ) ;
#11030=DIRECTION ( 'NONE',  ( -0.000000000000000000, 1.000000000000000000, -0.000000000000000000 ) ) ;
#11031=CARTESIAN_POINT ( 'NONE',  ( 798.0661480581538854, -2.532869017142183932, 309.5768839229118043 ) ) ;
#11035=CARTESIAN_POINT ( 'NONE',  ( 761.9338519418445230, -302.5328690171411949, 370.4231160770881957 ) ) ;
#11036=CARTESIAN_POINT ( 'NONE',  ( 781.8018195045267476, -142.2709662947837330, 365.1927285166407273 ) ) ;
#11038=CARTESIAN_POINT ( 'NONE',  ( 800.2193346964447755, -306.9982390220558273, 355.1360043628815788 ) ) ;
#11040=CARTESIAN_POINT ( 'NONE',  ( 814.9108240113580450, -88.27096629478390355, 337.5031285880265273 ) ) ;
#11044=AXIS2_PLACEMENT_3D ( 'NONE', #20406, #2628, #3319 ) ;
#11047=CARTESIAN_POINT ( 'NONE',  ( 792.1044303154645831, -36.45278447660223975, 317.8323909638837677 ) ) ;
#11049=CARTESIAN_POINT ( 'NONE',  ( 796.7737145352015204, -404.6346026584193396, 370.7187646348536987 ) ) ;
#11050=CARTESIAN_POINT ( 'NONE',  ( 807.5423716828161105, -273.0783235625958696, 362.2119215644372048 ) ) ;
#11051=CARTESIAN_POINT ( 'NONE',  ( 756.1443688327750579, -69.62377810805107003, 314.3581564841659315 ) ) ;
#11056=CARTESIAN_POINT ( 'NONE',  ( 745.0891759886404770, -388.2709662947829656, 342.4968714119734159 ) ) ;
#11062=CARTESIAN_POINT ( 'NONE',  ( 758.4439275373578084, -276.5545181178798657, 353.2243759319684386 ) ) ;
#11063=CARTESIAN_POINT ( 'NONE',  ( 802.1676090361156639, -158.6346026584199933, 327.8955696845344505 ) ) ;
#11067=CARTESIAN_POINT ( 'NONE',  ( 804.1601925771018387, -319.4419599262320730, 346.5483106153029098 ) ) ;
#11069=CARTESIAN_POINT ( 'NONE',  ( 815.3608509340175488, -26.73633629969882008, 341.2497674668889545 ) ) ;
#11071=CARTESIAN_POINT ( 'NONE',  ( 767.8955696845333705, -72.45278447660213317, 362.1676090361162323 ) ) ;
#11074=CARTESIAN_POINT ( 'NONE',  ( 744.6391490659812007, -446.7363362996975980, 338.7502325331110455 ) ) ;
#11077=CARTESIAN_POINT ( 'NONE',  ( 776.9566956441375396, -372.8965053807773415, 364.8461984189686405 ) ) ;
#11078=CARTESIAN_POINT ( 'NONE',  ( 805.0032342141413437, -37.54369356751133324, 314.9967657858572352 ) ) ;
#11080=CARTESIAN_POINT ( 'NONE',  ( 794.1144889064781864, -58.16923265350564520, 360.9840315886528401 ) ) ;
#11082=CARTESIAN_POINT ( 'NONE',  ( 811.6461892240364477, -220.7146871989596661, 324.1737431748509835 ) ) ;
#11083=CARTESIAN_POINT ( 'NONE',  ( 778.1981804954715471, -34.27096629478407408, 314.8072714833591021 ) ) ;
#11086=CARTESIAN_POINT ( 'NONE',  ( 788.8264449731200330, -213.1800572038743553, 363.6646147819171233 ) ) ;
#11089=CARTESIAN_POINT ( 'NONE',  ( 785.3687786644885591, -323.3618753856922581, 315.3201227861280813 ) ) ;
#11093=CARTESIAN_POINT ( 'NONE',  ( 773.3843516231979720, -61.44195992623291147, 364.4086373105754433 ) ) ;
#11096=CARTESIAN_POINT ( 'NONE',  ( 746.8695393053151292, -293.9073299311468759, 327.6429770376306578 ) ) ;
#11097=CARTESIAN_POINT ( 'NONE',  ( 812.6845335610512393, 16.01258552831230375, 353.5525998758768651 ) ) ;
#11103=CARTESIAN_POINT ( 'NONE',  ( 751.6929314249748586, -294.9982390220560546, 318.8095938919659034 ) ) ;
#11106=CARTESIAN_POINT ( 'NONE',  ( 800.9840315886518738, -172.9181544815165239, 354.1144889064786412 ) ) ;
#11107=CARTESIAN_POINT ( 'NONE',  ( 765.0180583372156207, -48.99823902205675807, 360.0135310231089534 ) ) ;
#11111=CARTESIAN_POINT ( 'NONE',  ( 764.1737431748507561, -274.3726999360617356, 371.6461892240376415 ) ) ;
#11112=CARTESIAN_POINT ( 'NONE',  ( 784.0799538623451781, -227.8055962898687596, 364.6971507214555572 ) ) ;
#11114=EDGE_CURVE ( 'NONE', #34493, #30414, #9551, .T. ) ;
#11115=CARTESIAN_POINT ( 'NONE',  ( 759.9864689768902508, -2.089148112965993231, 354.9819416627836404 ) ) ;
#11118=CARTESIAN_POINT ( 'NONE',  ( 787.4397851343537695, -21.72551174932956641, 374.2001403089903988 ) ) ;
#11119=CARTESIAN_POINT ( 'NONE',  ( 746.8695393053150156, -125.9073299311474159, 327.6429770376306010 ) ) ;
#11123=CARTESIAN_POINT ( 'NONE',  ( 754.3581564841646241, -353.4636090269705733, 316.1443688327762516 ) ) ;
#11124=CARTESIAN_POINT ( 'NONE',  ( 779.9999999999992042, 126.4563064324884465, 370.0000000000000568 ) ) ;
#11125=CARTESIAN_POINT ( 'NONE',  ( 754.9967657858570647, -337.5436935675102177, 365.0032342141425374 ) ) ;
#11129=CARTESIAN_POINT ( 'NONE',  ( 771.1735550268778070, -441.1800572038735027, 316.3353852180827630 ) ) ;
#11130=CARTESIAN_POINT ( 'NONE',  ( 805.2837595273609850, -194.7363362996982517, 340.5290396650784714 ) ) ;
#11133=CARTESIAN_POINT ( 'NONE',  ( 800.1688906516307043, -106.1692326535054889, 369.0717654672308186 ) ) ;
#11134=CARTESIAN_POINT ( 'NONE',  ( 762.3223304703356007, -415.5436935675102177, 322.3223304703362828 ) ) ;
#11142=CARTESIAN_POINT ( 'NONE',  ( 774.6858677611749044, -225.7255117493289163, 315.5713283507209894 ) ) ;
#11143=CARTESIAN_POINT ( 'NONE',  ( 767.8955696845334842, -216.4527844766016926, 362.1676090361161755 ) ) ;
#11147=CARTESIAN_POINT ( 'NONE',  ( 781.8018195045266339, -430.2709662947827383, 365.1927285166406705 ) ) ;
#11152=CARTESIAN_POINT ( 'NONE',  ( 772.5602148656447525, -177.7255117493290868, 305.7998596910095443 ) ) ;
#11153=CARTESIAN_POINT ( 'NONE',  ( 805.2837595273609850, -266.7363362996981095, 340.5290396650784714 ) ) ;
#11154=VERTEX_POINT ( 'NONE', #42464 ) ;
#11156=CARTESIAN_POINT ( 'NONE',  ( 815.0009284576459549, -198.3510508353234059, 338.7629533639073429 ) ) ;
#11161=CARTESIAN_POINT ( 'NONE',  ( 804.9511171171677688, -245.8055962898686460, 335.8780910478229202 ) ) ;
#11171=CARTESIAN_POINT ( 'NONE',  ( 757.7880784355613741, -186.0090635724255890, 312.4576283171834916 ) ) ;
#11178=CARTESIAN_POINT ( 'NONE',  ( 810.4231160770870019, -384.5545181178795247, 321.9338519418446936 ) ) ;
#11182=CARTESIAN_POINT ( 'NONE',  ( 804.9363028652555840, -16.27096629478413092, 338.2165204200192079 ) ) ;
#11183=CARTESIAN_POINT ( 'NONE',  ( 805.6418435158337843, -245.4636090269709143, 363.8556311672236916 ) ) ;
#11185=CARTESIAN_POINT ( 'NONE',  ( 792.2312462859673587, -227.9073299311471033, 307.2067596250082602 ) ) ;
#11188=CARTESIAN_POINT ( 'NONE',  ( 759.7806653035534055, -318.9982390220557704, 324.8639956371180801 ) ) ;
#11189=CARTESIAN_POINT ( 'NONE',  ( 757.4527132478984868, -88.37269993606226137, 329.1273215169538844 ) ) ;
#11190=CARTESIAN_POINT ( 'NONE',  ( 776.9254006560222479, -92.19088175424406018, 314.8983024940802125 ) ) ;
#11193=EDGE_CURVE ( 'NONE', #43717, #40029, #30982, .T. ) ;
#11195=CARTESIAN_POINT ( 'NONE',  ( 756.7813123517142913, -163.9874144716871456, 329.9779781133712504 ) ) ;
#11196=CARTESIAN_POINT ( 'NONE',  ( 768.0187753319979720, -344.6346026584195101, 318.0580252608186242 ) ) ;
#11197=VERTEX_POINT ( 'NONE', #37458 ) ;
#11201=CARTESIAN_POINT ( 'NONE',  ( 791.9812246680005501, -116.6346026584201780, 361.9419747391813189 ) ) ;
#11204=CARTESIAN_POINT ( 'NONE',  ( 808.3070685750230950, 5.001760977943074948, 361.1904061080339261 ) ) ;
#11205=ORIENTED_EDGE ( 'NONE', *, *, #34603, .F. ) ;
#11206=CARTESIAN_POINT ( 'NONE',  ( 795.1360043628807261, -308.0891481129650629, 360.2193346964456282 ) ) ;
#11209=CARTESIAN_POINT ( 'NONE',  ( 768.0187753319979720, -440.6346026584191122, 318.0580252608186242 ) ) ;
#11213=EDGE_LOOP ( 'NONE', ( #3071, #12666, #34020, #1315 ) ) ;
#11218=CARTESIAN_POINT ( 'NONE',  ( 771.1735550268778070, -9.180057203875058747, 316.3353852180827630 ) ) ;
#11219=CARTESIAN_POINT ( 'NONE',  ( 759.2295555964440155, -136.1692326535053894, 353.9708237608231229 ) ) ;
#11222=CARTESIAN_POINT ( 'NONE',  ( 759.8311093483677041, -406.1692326535045368, 310.9282345327691814 ) ) ;
#11227=CARTESIAN_POINT ( 'NONE',  ( 771.3260364891663130, -67.64542720878958448, 306.0683387631859773 ) ) ;
#11235=CARTESIAN_POINT ( 'NONE',  ( 790.9844846989617508, -358.3726999360613945, 317.2208543904092721 ) ) ;
#11236=CARTESIAN_POINT ( 'NONE',  ( 802.2119215644370342, -342.0090635724251342, 367.5423716828165084 ) ) ;
#11240=CARTESIAN_POINT ( 'NONE',  ( 799.9636004259356241, -142.9181544815166376, 311.2241431872006956 ) ) ;
#11242=CARTESIAN_POINT ( 'NONE',  ( 758.8095938919642549, -128.0891481129655176, 311.6929314249763365 ) ) ;
#11246=CARTESIAN_POINT ( 'NONE',  ( 802.1676090361156639, -230.6346026584197659, 327.8955696845344505 ) ) ;
#11248=CARTESIAN_POINT ( 'NONE',  ( 804.6971507214547046, -3.281790845153435221, 344.0799538623459739 ) ) ;
#11252=CARTESIAN_POINT ( 'NONE',  ( 798.0661480581538854, -26.53286901714210799, 309.5768839229118043 ) ) ;
#11255=CARTESIAN_POINT ( 'NONE',  ( 804.9363028652555840, -40.27096629478405987, 338.2165204200192079 ) ) ;
#11257=CARTESIAN_POINT ( 'NONE',  ( 803.8556311672234642, -297.6237781080502600, 365.6418435158340117 ) ) ;
#11258=CARTESIAN_POINT ( 'NONE',  ( 805.1927285166399315, -160.8164208402382371, 341.8018195045277707 ) ) ;
#11260=CARTESIAN_POINT ( 'NONE',  ( 792.1044303154645831, -324.4527844766013231, 317.8323909638837677 ) ) ;
#11263=CARTESIAN_POINT ( 'NONE',  ( 763.2262854647970016, -80.63460265842029173, 309.2812353651462445 ) ) ;
#11268=CARTESIAN_POINT ( 'NONE',  ( 771.2633955100217236, -47.90732993114767169, 363.4237431249939618 ) ) ;
#11269=CARTESIAN_POINT ( 'NONE',  ( 799.2566176426618085, -384.0090635724249637, 324.0069404352559559 ) ) ;
#11271=CARTESIAN_POINT ( 'NONE',  ( 745.7998596910086917, -389.3618753856919739, 332.5602148656461168 ) ) ;
#11272=CARTESIAN_POINT ( 'NONE',  ( 801.9858362298568863, -291.0783235625957559, 312.7379699480935642 ) ) ;
#11273=CARTESIAN_POINT ( 'NONE',  ( 746.7653713866222915, -65.26014174441471027, 351.0478386215610271 ) ) ;
#11279=CARTESIAN_POINT ( 'NONE',  ( 744.7301800767019131, -388.8164208402374129, 337.4774526936615757 ) ) ;
#11285=CARTESIAN_POINT ( 'NONE',  ( 804.6971507214547046, -267.2817908451526137, 344.0799538623459739 ) ) ;
#11286=CARTESIAN_POINT ( 'NONE',  ( 803.4237431249931660, -159.1800572038746111, 331.2633955100225194 ) ) ;
#11290=CARTESIAN_POINT ( 'NONE',  ( 761.2382568024794409, -327.6237781080502600, 356.9571628226838129 ) ) ;
#11292=CARTESIAN_POINT ( 'NONE',  ( 807.2620300519052989, -48.00906357242602951, 318.0141637701419768 ) ) ;
#11294=CARTESIAN_POINT ( 'NONE',  ( 746.8695393053150156, -197.9073299311472169, 327.6429770376306010 ) ) ;
#11295=CARTESIAN_POINT ( 'NONE',  ( 764.8639956371174549, -104.0891481129656881, 319.7806653035542013 ) ) ;
#11300=CARTESIAN_POINT ( 'NONE',  ( 746.4236121716829757, -447.8272453906067199, 328.8385539511384650 ) ) ;
#11303=CARTESIAN_POINT ( 'NONE',  ( 761.2382568024794409, -351.6237781080502032, 356.9571628226838129 ) ) ;
#11304=CARTESIAN_POINT ( 'NONE',  ( 815.2698199232962679, -64.81642084023852135, 342.5225473063383674 ) ) ;
#11306=CARTESIAN_POINT ( 'NONE',  ( 754.9735926884551418, -42.35105083532388193, 340.5236548041000333 ) ) ;
#11308=EDGE_CURVE ( 'NONE', #10247, #1373, #21443, .T. ) ;
#11310=CARTESIAN_POINT ( 'NONE',  ( 756.1443688327750579, -189.6237781080507148, 314.3581564841659315 ) ) ;
#11311=CARTESIAN_POINT ( 'NONE',  ( 758.0580252608178853, -54.45278447660219001, 328.0187753319985404 ) ) ;
#11312=ORIENTED_EDGE ( 'NONE', *, *, #12291, .F. ) ;
#11314=CARTESIAN_POINT ( 'NONE',  ( 803.4237431249931660, -183.1800572038744974, 331.2633955100225194 ) ) ;
#11316=CARTESIAN_POINT ( 'NONE',  ( 788.7366044899766848, -347.9073299311467053, 316.5762568750059813 ) ) ;
#11320=CARTESIAN_POINT ( 'NONE',  ( 770.0799878456142551, -37.98741447168752927, 362.9823548866085616 ) ) ;
#11322=CARTESIAN_POINT ( 'NONE',  ( 801.1904061080338124, -308.0891481129650629, 368.3070685750236066 ) ) ;
#11323=CARTESIAN_POINT ( 'NONE',  ( 781.2497674668890113, 11.64894916467595642, 375.3608509340180603 ) ) ;
#11330=CARTESIAN_POINT ( 'NONE',  ( 814.5518280994195948, -303.7255117493287457, 332.4837098697145734 ) ) ;
#11332=CARTESIAN_POINT ( 'NONE',  ( 786.6156483768007774, -361.4419599262319593, 315.5913626894246136 ) ) ;
#11334=CARTESIAN_POINT ( 'NONE',  ( 758.4439275373578084, -156.5545181178802636, 353.2243759319684386 ) ) ;
#11335=CARTESIAN_POINT ( 'NONE',  ( 803.4237431249931660, -63.18005720387488822, 331.2633955100225194 ) ) ;
#11339=CARTESIAN_POINT ( 'NONE',  ( 745.1792804349281596, -254.1908817542435770, 343.7566961878542884 ) ) ;
#11340=CARTESIAN_POINT ( 'NONE',  ( 803.2186876482843445, -223.9874144716869182, 350.0220218866286928 ) ) ;
#11343=CIRCLE ( 'NONE', #34901, 20.00000000000001776 ) ;
#11344=CARTESIAN_POINT ( 'NONE',  ( 804.8461984189677878, -458.1908817542429802, 336.9566956441385628 ) ) ;
#11347=CARTESIAN_POINT ( 'NONE',  ( 751.6929314249748586, -6.998239022056885972, 318.8095938919659034 ) ) ;
#11348=CARTESIAN_POINT ( 'NONE',  ( 813.1304606946830518, -113.9073299311474301, 352.3570229623690580 ) ) ;
#11351=CARTESIAN_POINT ( 'NONE',  ( 750.9282345327678740, -376.9181544815159555, 319.8311093483690115 ) ) ;
#11353=CARTESIAN_POINT ( 'NONE',  ( 758.8095938919642549, -344.0891481129647786, 311.6929314249763365 ) ) ;
#11357=CARTESIAN_POINT ( 'NONE',  ( 785.3687786644884454, -443.3618753856917465, 315.3201227861279676 ) ) ;
#11360=CARTESIAN_POINT ( 'NONE',  ( 801.5560724626406000, -192.5545181178801215, 326.7756240680316182 ) ) ;
#11363=CARTESIAN_POINT ( 'NONE',  ( 811.6461892240364477, -100.7146871989600356, 324.1737431748509835 ) ) ;
#11364=CARTESIAN_POINT ( 'NONE',  ( 755.0636971347428243, -436.2709662947827951, 341.7834795799807353 ) ) ;
#11369=CARTESIAN_POINT ( 'NONE',  ( 802.1676090361156639, -278.6346026584196807, 327.8955696845344505 ) ) ;
#11370=CARTESIAN_POINT ( 'NONE',  ( 759.9864689768902508, -242.0891481129652618, 354.9819416627836404 ) ) ;
#11373=CARTESIAN_POINT ( 'NONE',  ( 755.5713283507202505, -437.3618753856919170, 334.6858677611754729 ) ) ;
#11376=CARTESIAN_POINT ( 'NONE',  ( 744.7301800767020268, -172.8164208402381519, 337.4774526936615189 ) ) ;
#11377=CARTESIAN_POINT ( 'NONE',  ( 796.1575198192839480, -270.0090635724253048, 359.4546378042384163 ) ) ;
#11381=CARTESIAN_POINT ( 'NONE',  ( 754.0944755984390895, -231.6237781080504874, 364.1009440267246760 ) ) ;
#11386=CARTESIAN_POINT ( 'NONE',  ( 787.6308680596127942, -275.2601417444140566, 364.1105419155492768 ) ) ;
#11395=CARTESIAN_POINT ( 'NONE',  ( 755.8990559732751535, -155.4636090269711417, 365.9055244015606831 ) ) ;
#11405=CARTESIAN_POINT ( 'NONE',  ( 758.0580252608178853, -6.452784476602343666, 328.0187753319985404 ) ) ;
#11407=CARTESIAN_POINT ( 'NONE',  ( 766.4474001241216001, -283.0999726633344267, 307.3154664389482491 ) ) ;
#11409=CARTESIAN_POINT ( 'NONE',  ( 792.3570229623688874, -237.1800572038742985, 373.1304606946836202 ) ) ;
#11415=CARTESIAN_POINT ( 'NONE',  ( 758.0580252608178853, -318.4527844766014368, 328.0187753319985404 ) ) ;
#11416=CARTESIAN_POINT ( 'NONE',  ( 793.9708237608222134, -94.91815448151677970, 319.2295555964448681 ) ) ;
#11420=CARTESIAN_POINT ( 'NONE',  ( 795.9930595647434757, -147.0783235625962959, 320.7433823573372820 ) ) ;
#11421=CARTESIAN_POINT ( 'NONE',  ( 762.1405469898971887, -361.5436935675103882, 357.8594530101015607 ) ) ;
#11428=CARTESIAN_POINT ( 'NONE',  ( 813.1304606946830518, 6.092670068852159559, 352.3570229623690580 ) ) ;
#11431=CARTESIAN_POINT ( 'NONE',  ( 797.6776695296629214, -307.5436935675104451, 357.6776695296636603 ) ) ;
#11433=EDGE_CURVE ( 'NONE', #23783, #22578, #7591, .T. ) ;
#11435=CARTESIAN_POINT ( 'NONE',  ( 774.6858677611749044, -441.7255117493282910, 315.5713283507209894 ) ) ;
#11442=AXIS2_PLACEMENT_3D ( 'NONE', #26971, #36910, #41068 ) ;
#11443=CARTESIAN_POINT ( 'NONE',  ( 796.9571628226829034, -455.4636090269701754, 321.2382568024804641 ) ) ;
#11444=CARTESIAN_POINT ( 'NONE',  ( 763.2262854647970016, -224.6346026584198228, 309.2812353651462445 ) ) ;
#11445=CARTESIAN_POINT ( 'NONE',  ( 798.7617431975189675, -147.6237781080508285, 323.0428371773161871 ) ) ;
#11448=CARTESIAN_POINT ( 'NONE',  ( 814.8230680027162407, -389.8055962898682765, 333.7305795820267917 ) ) ;
#11455=CARTESIAN_POINT ( 'NONE',  ( 760.0363995740630116, -58.91815448151690759, 368.7758568127991907 ) ) ;
#11462=PLANE ( 'NONE',  #43670 ) ;
#11464=CARTESIAN_POINT ( 'NONE',  ( 769.0155153010367712, -394.3726999360613377, 362.7791456095907279 ) ) ;
#11467=CARTESIAN_POINT ( 'NONE',  ( 771.3260364891663130, -355.6454272087887603, 306.0683387631859773 ) ) ;
#11472=CIRCLE ( 'NONE', #32828, 10.00000000000000888 ) ;
#11473=CARTESIAN_POINT ( 'NONE',  ( 814.8207195650702488, -170.1908817542438328, 336.2433038121456548 ) ) ;
#11475=CARTESIAN_POINT ( 'NONE',  ( 746.8695393053150156, -101.9073299311474727, 327.6429770376306010 ) ) ;
#11480=CARTESIAN_POINT ( 'NONE',  ( 803.4237431249931660, -231.1800572038743553, 331.2633955100225194 ) ) ;
#11482=CARTESIAN_POINT ( 'NONE',  ( 810.4231160770870019, -456.5545181178792404, 321.9338519418446936 ) ) ;
#11487=CARTESIAN_POINT ( 'NONE',  ( 807.5423716828161105, -33.07832356259662987, 362.2119215644372048 ) ) ;
#11490=CARTESIAN_POINT ( 'NONE',  ( 755.5713283507202505, -29.36187538569318178, 334.6858677611754729 ) ) ;
#11493=CARTESIAN_POINT ( 'NONE',  ( 801.9858362298568863, -339.0783235625956422, 312.7379699480935642 ) ) ;
#11494=CARTESIAN_POINT ( 'NONE',  ( 788.8264449731201466, -141.1800572038746395, 363.6646147819170665 ) ) ;
#11497=CARTESIAN_POINT ( 'NONE',  ( 768.0187753319979720, -344.6346026584195101, 318.0580252608186242 ) ) ;
#11503=CARTESIAN_POINT ( 'NONE',  ( 797.8594530101008786, -61.54369356751124087, 322.1405469898980982 ) ) ;
#11504=CARTESIAN_POINT ( 'NONE',  ( 773.4516893846965786, -355.6454272087887603, 315.8398074228977066 ) ) ;
#11507=CARTESIAN_POINT ( 'NONE',  ( 804.7487373415286811, -403.5436935675101608, 364.7487373415288516 ) ) ;
#11508=CARTESIAN_POINT ( 'NONE',  ( 754.0944755984390895, -303.6237781080503169, 364.1009440267246760 ) ) ;
#11515=CARTESIAN_POINT ( 'NONE',  ( 745.4481719005789273, -435.7255117493282341, 347.5162901302853129 ) ) ;
#11523=VECTOR ( 'NONE', #20908, 1000.000000000000000 ) ;
#11524=CARTESIAN_POINT ( 'NONE',  ( 757.4527132478984868, -304.3726999360615082, 329.1273215169538844 ) ) ;
#11525=CARTESIAN_POINT ( 'NONE',  ( 778.2165204200184689, -142.8164208402382656, 364.9363028652563230 ) ) ;
#11528=CARTESIAN_POINT ( 'NONE',  ( 756.1348686366196716, -329.2601417444138860, 347.5531968255698416 ) ) ;
#11530=CARTESIAN_POINT ( 'NONE',  ( 788.6739635108323228, -31.64542720878970883, 373.9316612368139090 ) ) ;
#11533=CARTESIAN_POINT ( 'NONE',  ( 796.9462024416508257, -204.4527844766016926, 308.9653473494370246 ) ) ;
#11534=CARTESIAN_POINT ( 'NONE',  ( 781.8018195045266339, -118.2709662947837899, 365.1927285166406705 ) ) ;
#11538=CARTESIAN_POINT ( 'NONE',  ( 776.9254006560222479, -20.19088175424429110, 314.8983024940802125 ) ) ;
#11541=CARTESIAN_POINT ( 'NONE',  ( 802.7791456095903868, -412.7146871989590409, 329.0155153010375102 ) ) ;
#11547=CARTESIAN_POINT ( 'NONE',  ( 776.2433038121456548, -228.8965053807778816, 374.8207195650711014 ) ) ;
#11548=CARTESIAN_POINT ( 'NONE',  ( 756.3353852180820240, -53.90732993114765037, 331.1735550268787733 ) ) ;
#11552=CARTESIAN_POINT ( 'NONE',  ( 788.7366044899766848, -227.9073299311471033, 316.5762568750059813 ) ) ;
#11558=CARTESIAN_POINT ( 'NONE',  ( 815.2698199232962679, -280.8164208402378108, 342.5225473063383674 ) ) ;
#11559=CARTESIAN_POINT ( 'NONE',  ( 793.4146539503750546, -1.987414471687640294, 307.6481478633938877 ) ) ;
#11567=CARTESIAN_POINT ( 'NONE',  ( 808.3070685750230950, -330.9982390220558273, 361.1904061080339261 ) ) ;
#11569=CARTESIAN_POINT ( 'NONE',  ( 776.9254006560222479, -212.1908817542436623, 314.8983024940802125 ) ) ;
#11572=CARTESIAN_POINT ( 'NONE',  ( 796.1575198192839480, -150.0090635724257027, 359.4546378042384163 ) ) ;
#11573=CARTESIAN_POINT ( 'NONE',  ( 755.5713283507202505, -53.36187538569310362, 334.6858677611754729 ) ) ;
#11578=CARTESIAN_POINT ( 'NONE',  ( 788.6739635108323228, -271.6454272087889876, 373.9316612368139090 ) ) ;
#11579=CARTESIAN_POINT ( 'NONE',  ( 754.8983024940795303, -234.8965053807777963, 336.9254006560228163 ) ) ;
#11583=CARTESIAN_POINT ( 'NONE',  ( 756.3353852180819104, -5.907329931147798696, 331.1735550268788302 ) ) ;
#11587=CARTESIAN_POINT ( 'NONE',  ( 813.1304606946830518, -41.90732993114767169, 352.3570229623690580 ) ) ;
#11588=CARTESIAN_POINT ( 'NONE',  ( 777.5031285880264704, -118.8164208402383508, 374.9108240113588408 ) ) ;
#11589=DIRECTION ( 'NONE',  ( 0.000000000000000000, 0.000000000000000000, -1.000000000000000000 ) ) ;
#11591=CARTESIAN_POINT ( 'NONE',  ( 815.3608509340175488, -386.7363362996977116, 341.2497674668889545 ) ) ;
#11593=CARTESIAN_POINT ( 'NONE',  ( 808.3070685750230950, -354.9982390220557704, 361.1904061080339261 ) ) ;
#11596=CARTESIAN_POINT ( 'NONE',  ( 801.9419747391806368, -426.4527844766010389, 351.9812246680014027 ) ) ;
#11597=CARTESIAN_POINT ( 'NONE',  ( 761.4292242960306112, -185.4636090269710280, 323.2154366446414429 ) ) ;
#11600=CARTESIAN_POINT ( 'NONE',  ( 751.2241431872005251, -88.16923265350555994, 359.9636004259367610 ) ) ;
#11601=CARTESIAN_POINT ( 'NONE',  ( 755.3201227861273992, -435.7255117493282341, 345.3687786644892981 ) ) ;
#11608=CARTESIAN_POINT ( 'NONE',  ( 765.0180583372156207, -264.9982390220561115, 360.0135310231089534 ) ) ;
#11609=CARTESIAN_POINT ( 'NONE',  ( 797.8594530101009923, -277.5436935675105588, 322.1405469898982119 ) ) ;
#11612=CARTESIAN_POINT ( 'NONE',  ( 795.1360043628807261, -452.0891481129646650, 360.2193346964456282 ) ) ;
#11616=CARTESIAN_POINT ( 'NONE',  ( 810.7187646348534145, -186.4527844766017779, 356.7737145352016341 ) ) ;
#11617=CARTESIAN_POINT ( 'NONE',  ( 793.9708237608222134, -262.9181544815162965, 319.2295555964448681 ) ) ;
#11620=CARTESIAN_POINT ( 'NONE',  ( 752.4576283171824116, -213.0783235625960401, 317.7880784355627952 ) ) ;
#11625=CARTESIAN_POINT ( 'NONE',  ( 799.4546378042377910, -249.0783235625959549, 356.1575198192848006 ) ) ;
#11633=CARTESIAN_POINT ( 'NONE',  ( 747.6481478633932056, -157.0999726633347962, 353.4146539503763620 ) ) ;
#11639=CARTESIAN_POINT ( 'NONE',  ( 787.4397851343537695, -21.72551174932956641, 374.2001403089903988 ) ) ;
#11643=CARTESIAN_POINT ( 'NONE',  ( 756.5762568750052424, -27.18005720387500901, 348.7366044899774238 ) ) ;
#11645=CARTESIAN_POINT ( 'NONE',  ( 760.0363995740630116, -274.9181544815161828, 368.7758568127991907 ) ) ;
#11647=CARTESIAN_POINT ( 'NONE',  ( 808.3070685750230950, -210.9982390220561967, 361.1904061080339261 ) ) ;
#11650=EDGE_LOOP ( 'NONE', ( #28547, #3475 ) ) ;
#11652=CARTESIAN_POINT ( 'NONE',  ( 771.2633955100217236, -335.9073299311468190, 363.4237431249939618 ) ) ;
#11653=CARTESIAN_POINT ( 'NONE',  ( 790.9844846989617508, -70.37269993606230400, 317.2208543904092721 ) ) ;
#11657=CARTESIAN_POINT ( 'NONE',  ( 763.2154366446407039, -165.6237781080507716, 321.4292242960311228 ) ) ;
#11658=CARTESIAN_POINT ( 'NONE',  ( 754.8072714833581358, -364.8164208402374697, 338.1981804954720587 ) ) ;
#11661=CARTESIAN_POINT ( 'NONE',  ( 794.9819416627830151, -156.9982390220564241, 319.9864689768909898 ) ) ;
#11664=CARTESIAN_POINT ( 'NONE',  ( 758.8095938919642549, 15.91085188703394238, 311.6929314249763365 ) ) ;
#11666=CARTESIAN_POINT ( 'NONE',  ( 802.1676090361156639, -326.6346026584193396, 327.8955696845344505 ) ) ;
#11668=ORIENTED_EDGE ( 'NONE', *, *, #23205, .F. ) ;
#11669=CARTESIAN_POINT ( 'NONE',  ( 800.0135310231082713, -446.0891481129646081, 325.0180583372163028 ) ) ;
#11677=CARTESIAN_POINT ( 'NONE',  ( 762.1405469898971887, -1.543693567511449150, 357.8594530101015607 ) ) ;
#11678=CARTESIAN_POINT ( 'NONE',  ( 812.7932403749906598, -231.1800572038743553, 327.7687537140311633 ) ) ;
#11679=CARTESIAN_POINT ( 'NONE',  ( 761.2382568024794409, -159.6237781080508285, 356.9571628226838129 ) ) ;
#11682=CARTESIAN_POINT ( 'NONE',  ( 815.1787889125755555, -414.8965053807771710, 343.7953271457877804 ) ) ;
#11689=CARTESIAN_POINT ( 'NONE',  ( 762.1177392798416577, -66.55451811788050520, 309.8865473780659272 ) ) ;
#11690=DIRECTION ( 'NONE',  ( 0.000000000000000000, 0.000000000000000000, 1.000000000000000000 ) ) ;
#11697=CARTESIAN_POINT ( 'NONE',  ( 763.0428371773158460, -395.4636090269705164, 358.7617431975195359 ) ) ;
#11699=ADVANCED_FACE ( 'NONE', ( #1550, #16102 ), #2231, .F. ) ;
#11702=CARTESIAN_POINT ( 'NONE',  ( 757.7880784355613741, -186.0090635724255890, 312.4576283171834916 ) ) ;
#11705=CARTESIAN_POINT ( 'NONE',  ( 772.4837098697144029, -119.3618753856928691, 374.5518280994205611 ) ) ;
#11709=CARTESIAN_POINT ( 'NONE',  ( 768.0187753319979720, -224.6346026584198228, 318.0580252608186242 ) ) ;
#11710=CARTESIAN_POINT ( 'NONE',  ( 757.4527132478984868, -16.37269993606248519, 329.1273215169538844 ) ) ;
#11714=CARTESIAN_POINT ( 'NONE',  ( 764.3348316497523456, -22.71468719896029853, 308.6759233522265617 ) ) ;
#11717=CARTESIAN_POINT ( 'NONE',  ( 768.0187753319979720, -32.63460265842044095, 318.0580252608186242 ) ) ;
#11720=CARTESIAN_POINT ( 'NONE',  ( 807.5423716828161105, -345.0783235625956991, 362.2119215644372048 ) ) ;
#11721=CARTESIAN_POINT ( 'NONE',  ( 765.0180583372156207, -168.9982390220563673, 360.0135310231089534 ) ) ;
#11723=CARTESIAN_POINT ( 'NONE',  ( 801.9858362298568863, -435.0783235625953580, 312.7379699480935642 ) ) ;
#11725=CARTESIAN_POINT ( 'NONE',  ( 804.4286716492782716, -353.3618753856922012, 345.3141322388244703 ) ) ;
#11732=CARTESIAN_POINT ( 'NONE',  ( 767.8955696845333705, -72.45278447660213317, 362.1676090361162323 ) ) ;
#11733=CARTESIAN_POINT ( 'NONE',  ( 757.0176451133909268, -373.0999726633340856, 349.9200121543848354 ) ) ;
#11736=CARTESIAN_POINT ( 'NONE',  ( 813.1304606946831655, -401.9073299311464211, 352.3570229623691716 ) ) ;
#11737=CARTESIAN_POINT ( 'NONE',  ( 771.2368401574024119, -325.4419599262320162, 374.2805881961240857 ) ) ;
#11739=CARTESIAN_POINT ( 'NONE',  ( 798.0661480581538854, -98.53286901714187707, 309.5768839229118043 ) ) ;
#11746=CARTESIAN_POINT ( 'NONE',  ( 792.3570229623688874, -429.1800572038737869, 373.1304606946836202 ) ) ;
#11747=CARTESIAN_POINT ( 'NONE',  ( 774.2415430293718828, 19.23444159658009056, 310.5578503957772796 ) ) ;
#11752=CARTESIAN_POINT ( 'NONE',  ( 776.9254006560222479, -308.1908817542434349, 314.8983024940802125 ) ) ;
#11753=CARTESIAN_POINT ( 'NONE',  ( 759.9864689768902508, -146.0891481129655176, 354.9819416627836404 ) ) ;
#11756=CARTESIAN_POINT ( 'NONE',  ( 803.8651313633788504, -317.2601417444139429, 332.4468031744301015 ) ) ;
#11759=CARTESIAN_POINT ( 'NONE',  ( 797.8822607201568644, -78.55451811788046257, 370.1134526219340160 ) ) ;
#11762=CARTESIAN_POINT ( 'NONE',  ( 777.4774526936600978, -202.2709662947834772, 304.7301800767027657 ) ) ;
#11763=CARTESIAN_POINT ( 'NONE',  ( 759.9864689768902508, -98.08914811296568814, 354.9819416627836404 ) ) ;
#11765=CARTESIAN_POINT ( 'NONE',  ( 802.9823548866075953, -1.099972663335260226, 330.0799878456151077 ) ) ;
#11768=CARTESIAN_POINT ( 'NONE',  ( 757.2208543904082489, -400.7146871989590977, 350.9844846989624330 ) ) ;
#11773=CARTESIAN_POINT ( 'NONE',  ( 813.9316612368132837, -247.4419599262323004, 348.6739635108323228 ) ) ;
#11774=CARTESIAN_POINT ( 'NONE',  ( 757.8323909638828582, -50.63460265842038410, 352.1044303154654358 ) ) ;
#11777=CARTESIAN_POINT ( 'NONE',  ( 756.3353852180819104, -221.9073299311470464, 331.1735550268788302 ) ) ;
#11784=CARTESIAN_POINT ( 'NONE',  ( 796.9462024416508257, -300.4527844766013231, 308.9653473494370246 ) ) ;
#11785=CARTESIAN_POINT ( 'NONE',  ( 756.1443688327750579, -21.62377810805121570, 314.3581564841659315 ) ) ;
#11792=CARTESIAN_POINT ( 'NONE',  ( 792.2312462859673587, -323.9073299311468190, 307.2067596250082602 ) ) ;
#11793=FACE_OUTER_BOUND ( 'NONE', #4727, .T. ) ;
#11794=CARTESIAN_POINT ( 'NONE',  ( 754.8983024940795303, -354.8965053807774552, 336.9254006560228163 ) ) ;
#11796=CARTESIAN_POINT ( 'NONE',  ( 786.5483106153019435, -199.6454272087891582, 364.1601925771022366 ) ) ;
#11797=CARTESIAN_POINT ( 'NONE',  ( 764.8639956371174549, -32.08914811296588709, 319.7806653035542013 ) ) ;
#11801=CARTESIAN_POINT ( 'NONE',  ( 803.8651313633788504, -221.2601417444142271, 332.4468031744301015 ) ) ;
#11804=CARTESIAN_POINT ( 'NONE',  ( 811.0346526505616112, -446.6346026584189985, 323.0537975583477532 ) ) ;
#11808=CARTESIAN_POINT ( 'NONE',  ( 782.4968714119720516, -58.81642084023854267, 305.0891759886411023 ) ) ;
#11809=CARTESIAN_POINT ( 'NONE',  ( 815.2698199232961542, -112.8164208402383508, 342.5225473063383106 ) ) ;
#11812=CARTESIAN_POINT ( 'NONE',  ( 755.8990559732751535, -395.4636090269705164, 365.9055244015606831 ) ) ;
#11814=CARTESIAN_POINT ( 'NONE',  ( 813.1304606946830518, -377.9073299311466485, 352.3570229623690580 ) ) ;
#11816=CARTESIAN_POINT ( 'NONE',  ( 795.1360043628807261, -452.0891481129646650, 360.2193346964456282 ) ) ;
#11817=CARTESIAN_POINT ( 'NONE',  ( 804.4086373105744769, -193.6454272087891582, 333.3843516231986541 ) ) ;
#11820=CARTESIAN_POINT ( 'NONE',  ( 815.1787889125755555, -126.8965053807781516, 343.7953271457877804 ) ) ;
#11821=CARTESIAN_POINT ( 'NONE',  ( 805.1927285166399315, -448.8164208402372424, 341.8018195045277707 ) ) ;
#11826=CARTESIAN_POINT ( 'NONE',  ( 778.2165204200184689, -262.8164208402379245, 364.9363028652563230 ) ) ;
#11827=CARTESIAN_POINT ( 'NONE',  ( 756.3353852180820240, -245.9073299311469896, 331.1735550268787733 ) ) ;
#11828=CARTESIAN_POINT ( 'NONE',  ( 759.9999999999992042, 205.0000000000000568, 339.9999999999999432 ) ) ;
#11830=CARTESIAN_POINT ( 'NONE',  ( 757.2208543904082489, 7.285312801039605546, 350.9844846989624330 ) ) ;
#11833=CARTESIAN_POINT ( 'NONE',  ( 749.2812353651451076, -174.4527844766018063, 323.2262854647983090 ) ) ;
#11834=CARTESIAN_POINT ( 'NONE',  ( 754.7162404726377645, -278.7363362996980527, 339.4709603349214717 ) ) ;
#11835=CARTESIAN_POINT ( 'NONE',  ( 805.1016975059191054, -390.8965053807772279, 343.0745993439771837 ) ) ;
#11838=CARTESIAN_POINT ( 'NONE',  ( 810.1134526219336749, -224.5328690171415076, 357.8822607201570349 ) ) ;
#11843=CARTESIAN_POINT ( 'NONE',  ( 804.9511171171677688, -269.8055962898686175, 335.8780910478229202 ) ) ;
#11850=CARTESIAN_POINT ( 'NONE',  ( 773.7305795820266212, -177.2817908451528695, 374.8230680027170365 ) ) ;
#11855=CARTESIAN_POINT ( 'NONE',  ( 805.0032342141412300, -13.54369356751140785, 314.9967657858571783 ) ) ;
#11859=CARTESIAN_POINT ( 'NONE',  ( 804.4286716492782716, -41.36187538569314626, 345.3141322388244703 ) ) ;
#11860=CARTESIAN_POINT ( 'NONE',  ( 814.2805881961230625, -289.6454272087889308, 331.2368401574024119 ) ) ;
#11862=CARTESIAN_POINT ( 'NONE',  ( 787.5162901302840055, -251.3618753856923149, 305.4481719005792684 ) ) ;
#11866=CARTESIAN_POINT ( 'NONE',  ( 756.5762568750052424, -339.1800572038740142, 348.7366044899774238 ) ) ;
#11867=CARTESIAN_POINT ( 'NONE',  ( 787.5531968255692163, -93.82724539060770041, 316.1348686366205811 ) ) ;
#11871=CARTESIAN_POINT ( 'NONE',  ( 786.2056067578752163, -131.8055962898690439, 374.4686193811670023 ) ) ;
#11872=CARTESIAN_POINT ( 'NONE',  ( 771.2633955100217236, -407.9073299311465348, 363.4237431249939618 ) ) ;
#11875=CARTESIAN_POINT ( 'NONE',  ( 765.0180583372156207, -144.9982390220564525, 360.0135310231089534 ) ) ;
#11879=CARTESIAN_POINT ( 'NONE',  ( 814.2001403089898304, 6.638124614306706306, 347.4397851343538264 ) ) ;
#11881=CARTESIAN_POINT ( 'NONE',  ( 764.8639956371174549, -368.0891481129647786, 319.7806653035542013 ) ) ;
#11890=CARTESIAN_POINT ( 'NONE',  ( 800.0135310231082713, 9.910851887033969021, 325.0180583372163028 ) ) ;
#11891=CARTESIAN_POINT ( 'NONE',  ( 764.0069404352550464, -159.0783235625962391, 359.2566176426627180 ) ) ;
#11900=CARTESIAN_POINT ( 'NONE',  ( 805.6418435158337843, -77.46360902697138329, 363.8556311672236916 ) ) ;
#11902=CARTESIAN_POINT ( 'NONE',  ( 779.9999999999992042, -462.9681489794448339, 339.9999999999999432 ) ) ;
#11908=CARTESIAN_POINT ( 'NONE',  ( 755.8894580844503253, -399.8272453906067767, 332.3691319403863531 ) ) ;
#11910=CARTESIAN_POINT ( 'NONE',  ( 799.2566176426618085, -240.0090635724253900, 324.0069404352559559 ) ) ;
#11913=CARTESIAN_POINT ( 'NONE',  ( 776.2046728542105711, -188.1908817542437760, 304.8212110874238761 ) ) ;
#11915=CARTESIAN_POINT ( 'NONE',  ( 745.0891759886404770, -148.2709662947837330, 342.4968714119734159 ) ) ;
#11919=CARTESIAN_POINT ( 'NONE',  ( 797.8594530101008786, -229.5436935675106440, 322.1405469898980982 ) ) ;
#11920=CARTESIAN_POINT ( 'NONE',  ( 757.4527132478984868, -40.37269993606240348, 329.1273215169538844 ) ) ;
#11924=CARTESIAN_POINT ( 'NONE',  ( 744.9990715423526808, -18.35105083532395298, 341.2370466360926002 ) ) ;
#11929=CARTESIAN_POINT ( 'NONE',  ( 778.2165204200184689, -22.81642084023865280, 364.9363028652563230 ) ) ;
#11934=CARTESIAN_POINT ( 'NONE',  ( 812.6845335610512393, -343.9874144716865771, 353.5525998758768651 ) ) ;
#11936=CARTESIAN_POINT ( 'NONE',  ( 781.2497674668890113, -420.3510508353225532, 375.3608509340180603 ) ) ;
#11938=CARTESIAN_POINT ( 'NONE',  ( 795.1360043628807261, -356.0891481129647218, 360.2193346964456282 ) ) ;
#11946=CARTESIAN_POINT ( 'NONE',  ( 788.8264449731200330, -45.18005720387493085, 363.6646147819171233 ) ) ;
#11947=CARTESIAN_POINT ( 'NONE',  ( 773.4516893846965786, -379.6454272087886466, 315.8398074228977066 ) ) ;
#11949=CARTESIAN_POINT ( 'NONE',  ( 754.9967657858570647, -433.5436935675100472, 365.0032342141425943 ) ) ;
#11950=CARTESIAN_POINT ( 'NONE',  ( 811.6461892240364477, -316.7146871989593819, 324.1737431748509835 ) ) ;
#11951=CARTESIAN_POINT ( 'NONE',  ( 810.1134526219336749, -104.5328690171418913, 357.8822607201570349 ) ) ;
#11957=CARTESIAN_POINT ( 'NONE',  ( 810.7187646348534145, -426.4527844766010389, 356.7737145352016341 ) ) ;
#11963=CARTESIAN_POINT ( 'NONE',  ( 786.5483106153019435, -295.6454272087888739, 364.1601925771022366 ) ) ;
#11964=CARTESIAN_POINT ( 'NONE',  ( 804.4286716492782716, -137.3618753856928265, 345.3141322388244703 ) ) ;
#11965=EDGE_LOOP ( 'NONE', ( #5860, #24534, #32964, #33852 ) ) ;
#11968=CARTESIAN_POINT ( 'NONE',  ( 805.1016975059191054, -318.8965053807775121, 343.0745993439771837 ) ) ;
#11970=CARTESIAN_POINT ( 'NONE',  ( 781.2370466360911223, -68.73633629969867798, 304.9990715423533629 ) ) ;
#11973=CARTESIAN_POINT ( 'NONE',  ( 814.2001403089898304, -209.3618753856926276, 347.4397851343538264 ) ) ;
#11974=CARTESIAN_POINT ( 'NONE',  ( 804.6798772138708955, -111.7255117493293000, 334.6312213355107019 ) ) ;
#11978=CARTESIAN_POINT ( 'NONE',  ( 763.8424801807145741, -18.00906357242611477, 320.5453621957614700 ) ) ;
#11981=CARTESIAN_POINT ( 'NONE',  ( 758.6633372737375112, -404.5328690171409107, 326.9102291470432533 ) ) ;
#11982=ORIENTED_EDGE ( 'NONE', *, *, #30859, .F. ) ;
#11983=CARTESIAN_POINT ( 'NONE',  ( 770.0799878456142551, -85.98741447168738716, 362.9823548866085616 ) ) ;
#11990=CARTESIAN_POINT ( 'NONE',  ( 776.2433038121456548, -252.8965053807777394, 374.8207195650711014 ) ) ;
#11991=CARTESIAN_POINT ( 'NONE',  ( 797.8594530101009923, -37.54369356751133324, 322.1405469898982119 ) ) ;
#11994=CARTESIAN_POINT ( 'NONE',  ( 781.8018195045266339, -238.2709662947833920, 365.1927285166406705 ) ) ;
#12003=CARTESIAN_POINT ( 'NONE',  ( 744.7301800767020268, -292.8164208402378108, 337.4774526936615189 ) ) ;
#12004=CARTESIAN_POINT ( 'NONE',  ( 813.9316612368132837, -31.44195992623299674, 348.6739635108323228 ) ) ;
#12010=CARTESIAN_POINT ( 'NONE',  ( 764.8639956371174549, -200.0891481129653187, 319.7806653035542013 ) ) ;
#12013=CARTESIAN_POINT ( 'NONE',  ( 808.0189434323515343, -326.0891481129649492, 319.0252816721025511 ) ) ;
#12014=CARTESIAN_POINT ( 'NONE',  ( 779.9999999999992042, 126.4563064324884465, 309.9999999999998863 ) ) ;
#12017=CARTESIAN_POINT ( 'NONE',  ( 787.5531968255692163, -189.8272453906073736, 316.1348686366205811 ) ) ;
#12018=CARTESIAN_POINT ( 'NONE',  ( 762.3223304703356007, -55.54369356751127640, 322.3223304703362828 ) ) ;
#12023=CARTESIAN_POINT ( 'NONE',  ( 764.0069404352550464, -207.0783235625960685, 359.2566176426627180 ) ) ;
#12027=CARTESIAN_POINT ( 'NONE',  ( 782.4968714119720516, -418.8164208402374129, 305.0891759886411023 ) ) ;
#12032=CARTESIAN_POINT ( 'NONE',  ( 811.0346526505616112, -38.63460265842041252, 323.0537975583477532 ) ) ;
#12033=CARTESIAN_POINT ( 'NONE',  ( 782.5225473063381969, -118.2709662947837899, 375.2698199232970637 ) ) ;
#12036=CARTESIAN_POINT ( 'NONE',  ( 752.7379699480933368, -396.0090635724249637, 361.9858362298580232 ) ) ;
#12037=DIRECTION ( 'NONE',  ( -1.000000000000000000, -0.000000000000000000, 0.000000000000000000 ) ) ;
#12038=CARTESIAN_POINT ( 'NONE',  ( 792.3570229623688874, -357.1800572038739006, 373.1304606946836202 ) ) ;
#12041=CARTESIAN_POINT ( 'NONE',  ( 790.8050863131179540, -452.8379544210779954, 362.5841948692291226 ) ) ;
#12044=CARTESIAN_POINT ( 'NONE',  ( 781.2497674668890113, -132.3510508353235764, 375.3608509340180603 ) ) ;
#12045=CARTESIAN_POINT ( 'NONE',  ( 778.1981804954715471, -442.2709662947827383, 314.8072714833591021 ) ) ;
#12049=CARTESIAN_POINT ( 'NONE',  ( 757.8323909638827445, -122.6346026584201354, 352.1044303154654358 ) ) ;
#12051=CARTESIAN_POINT ( 'NONE',  ( 800.2193346964447755, -258.9982390220561115, 355.1360043628815788 ) ) ;
#12052=CARTESIAN_POINT ( 'NONE',  ( 757.8323909638828582, -266.6346026584197375, 352.1044303154654358 ) ) ;
#12053=DIRECTION ( 'NONE',  ( 0.000000000000000000, 0.000000000000000000, -1.000000000000000000 ) ) ;
#12055=CARTESIAN_POINT ( 'NONE',  ( 794.1144889064781864, 13.83076734649413098, 360.9840315886528401 ) ) ;
#12059=CARTESIAN_POINT ( 'NONE',  ( 755.2512626584698410, -199.5436935675108430, 315.2512626584710915 ) ) ;
#12060=CARTESIAN_POINT ( 'NONE',  ( 773.4516893846965786, -283.6454272087889308, 315.8398074228977066 ) ) ;
#12061=CARTESIAN_POINT ( 'NONE',  ( 754.8983024940795303, -402.8965053807773415, 336.9254006560228163 ) ) ;
#12069=CARTESIAN_POINT ( 'NONE',  ( 803.8651313633788504, -269.2601417444139997, 332.4468031744301015 ) ) ;
#12076=CARTESIAN_POINT ( 'NONE',  ( 764.1737431748507561, -154.3726999360620198, 371.6461892240376415 ) ) ;
#12082=CARTESIAN_POINT ( 'NONE',  ( 792.3570229623688874, -21.18005720387502677, 373.1304606946836202 ) ) ;
#12088=CARTESIAN_POINT ( 'NONE',  ( 756.3353852180819104, -29.90732993114771787, 331.1735550268788302 ) ) ;
#12089=CARTESIAN_POINT ( 'NONE',  ( 749.5768839229115201, -276.5545181178798657, 358.0661480581553064 ) ) ;
#12090=CARTESIAN_POINT ( 'NONE',  ( 749.2812353651451076, -270.4527844766014937, 323.2262854647983090 ) ) ;
#12094=CARTESIAN_POINT ( 'NONE',  ( 768.0187753319979720, -368.6346026584193964, 318.0580252608186242 ) ) ;
#12095=CARTESIAN_POINT ( 'NONE',  ( 763.8424801807145741, -114.0090635724258163, 320.5453621957614700 ) ) ;
#12100=CARTESIAN_POINT ( 'NONE',  ( 800.1688906516307043, -130.1692326535054463, 369.0717654672308186 ) ) ;
#12101=CARTESIAN_POINT ( 'NONE',  ( 802.1676090361156639, -398.6346026584193396, 327.8955696845344505 ) ) ;
#12104=CARTESIAN_POINT ( 'NONE',  ( 762.3223304703356007, -151.5436935675109851, 322.3223304703362828 ) ) ;
#12109=CARTESIAN_POINT ( 'NONE',  ( 755.5713283507202505, -341.3618753856922012, 334.6858677611754729 ) ) ;
#12111=CARTESIAN_POINT ( 'NONE',  ( 785.3141322388236176, -429.7255117493282910, 364.4286716492789537 ) ) ;
#12113=CARTESIAN_POINT ( 'NONE',  ( 772.4837098697145166, -71.36187538569303968, 374.5518280994205611 ) ) ;
#12119=CARTESIAN_POINT ( 'NONE',  ( 794.9819416627830151, 11.00176097794305541, 319.9864689768909898 ) ) ;
#12120=CARTESIAN_POINT ( 'NONE',  ( 800.7704444035546203, -148.1692326535053610, 326.0291762391768771 ) ) ;
#12127=CARTESIAN_POINT ( 'NONE',  ( 760.0363995740630116, -82.91815448151682233, 368.7758568127991907 ) ) ;
#12128=VECTOR ( 'NONE', #29085, 1000.000000000000000 ) ;
#12137=CARTESIAN_POINT ( 'NONE',  ( 786.5483106153019435, -415.6454272087885897, 364.1601925771022366 ) ) ;
#12140=CARTESIAN_POINT ( 'NONE',  ( 780.5236548040995785, -236.7363362996981380, 314.9735926884559944 ) ) ;
#12143=CARTESIAN_POINT ( 'NONE',  ( 810.4231160770870019, -192.5545181178801215, 321.9338519418446936 ) ) ;
#12145=CARTESIAN_POINT ( 'NONE',  ( 805.0032342141412300, -157.5436935675108998, 314.9967657858571783 ) ) ;
#12148=FACE_OUTER_BOUND ( 'NONE', #35052, .T. ) ;
#12149=CARTESIAN_POINT ( 'NONE',  ( 788.8264449731200330, -261.1800572038741848, 363.6646147819171233 ) ) ;
#12151=CARTESIAN_POINT ( 'NONE',  ( 801.5560724626406000, -24.55451811788064020, 326.7756240680316182 ) ) ;
#12157=CARTESIAN_POINT ( 'NONE',  ( 798.7617431975189675, -51.62377810805111267, 323.0428371773161871 ) ) ;
#12160=CARTESIAN_POINT ( 'NONE',  ( 762.1405469898971887, -25.54369356751136877, 357.8594530101015607 ) ) ;
#12163=CARTESIAN_POINT ( 'NONE',  ( 747.3154664389472828, -331.9874144716865203, 326.4474001241230781 ) ) ;
#12165=CIRCLE ( 'NONE', #6250, 20.00000000000001776 ) ;
#12167=CARTESIAN_POINT ( 'NONE',  ( 803.4237431249931660, -327.1800572038741279, 331.2633955100225194 ) ) ;
#12176=CARTESIAN_POINT ( 'NONE',  ( 791.9812246680005501, -68.63460265842033436, 361.9419747391813189 ) ) ;
#12177=CARTESIAN_POINT ( 'NONE',  ( 763.8424801807145741, -354.0090635724250774, 320.5453621957614700 ) ) ;
#12178=CARTESIAN_POINT ( 'NONE',  ( 804.7487373415286811, -427.5436935675101040, 364.7487373415288516 ) ) ;
#12180=CARTESIAN_POINT ( 'NONE',  ( 808.7758568127978833, -316.1692326535048210, 320.0363995740631822 ) ) ;
#12182=CARTESIAN_POINT ( 'NONE',  ( 749.8865473780648472, -92.53286901714190549, 322.1177392798429082 ) ) ;
#12187=CARTESIAN_POINT ( 'NONE',  ( 787.5162901302840055, -419.3618753856918033, 305.4481719005792684 ) ) ;
#12195=CARTESIAN_POINT ( 'NONE',  ( 796.9571628226829034, -311.4636090269706870, 321.2382568024804641 ) ) ;
#12196=CARTESIAN_POINT ( 'NONE',  ( 755.3201227861273992, -171.7255117493291152, 345.3687786644892981 ) ) ;
#12201=CARTESIAN_POINT ( 'NONE',  ( 771.3260364891663130, -67.64542720878958448, 306.0683387631859773 ) ) ;
#12205=CARTESIAN_POINT ( 'NONE',  ( 800.2193346964447755, -162.9982390220563673, 355.1360043628815788 ) ) ;
#12208=CARTESIAN_POINT ( 'NONE',  ( 796.1575198192839480, -30.00906357242607925, 359.4546378042384163 ) ) ;
#12211=CARTESIAN_POINT ( 'NONE',  ( 794.1144889064781864, -394.1692326535045368, 360.9840315886528401 ) ) ;
#12216=CARTESIAN_POINT ( 'NONE',  ( 787.4999999999992042, -512.9681489794448908, 309.9999999999998863 ) ) ;
#12217=CARTESIAN_POINT ( 'NONE',  ( 748.3538107759620743, -256.7146871989595525, 355.8262568251490165 ) ) ;
#12218=CARTESIAN_POINT ( 'NONE',  ( 792.1044303154646968, -60.45278447660216159, 317.8323909638837677 ) ) ;
#12222=CARTESIAN_POINT ( 'NONE',  ( 805.1927285166397041, -232.8164208402379245, 341.8018195045277707 ) ) ;
#12227=EDGE_LOOP ( 'NONE', ( #34181, #28538, #45472, #41876 ) ) ;
#12231=CARTESIAN_POINT ( 'NONE',  ( 815.2698199232962679, -328.8164208402375834, 342.5225473063383674 ) ) ;
#12233=CARTESIAN_POINT ( 'NONE',  ( 744.9990715423526808, -42.35105083532388193, 341.2370466360926002 ) ) ;
#12238=CARTESIAN_POINT ( 'NONE',  ( 791.9812246680005501, -212.6346026584198796, 361.9419747391813189 ) ) ;
#12241=CARTESIAN_POINT ( 'NONE',  ( 782.5225473063381969, -310.2709662947832499, 375.2698199232970637 ) ) ;
#12246=CARTESIAN_POINT ( 'NONE',  ( 755.1538015810308480, -182.1908817542437760, 343.0433043558613804 ) ) ;
#12247=CARTESIAN_POINT ( 'NONE',  ( 781.8018195045266339, -94.27096629478386092, 365.1927285166406705 ) ) ;
#12251=CARTESIAN_POINT ( 'NONE',  ( 757.2208543904082489, -256.7146871989595525, 350.9844846989624330 ) ) ;
#12254=CARTESIAN_POINT ( 'NONE',  ( 812.7932403749906598, -423.1800572038737300, 327.7687537140311633 ) ) ;
#12258=CARTESIAN_POINT ( 'NONE',  ( 812.7932403749906598, -39.18005720387496638, 327.7687537140311633 ) ) ;
#12259=CARTESIAN_POINT ( 'NONE',  ( 800.9747183278959710, -132.9982390220564810, 311.9810565676471583 ) ) ;
#12266=CARTESIAN_POINT ( 'NONE',  ( 801.1904061080336987, -356.0891481129647218, 368.3070685750235498 ) ) ;
#12269=CARTESIAN_POINT ( 'NONE',  ( 779.4709603349208464, 23.64894916467591912, 314.7162404726379918 ) ) ;
#12273=CARTESIAN_POINT ( 'NONE',  ( 764.3348316497523456, -118.7146871989600072, 308.6759233522265617 ) ) ;
#12274=CARTESIAN_POINT ( 'NONE',  ( 795.1360043628808398, -428.0891481129645513, 360.2193346964456282 ) ) ;
#12275=CARTESIAN_POINT ( 'NONE',  ( 752.4576283171824116, -165.0783235625962391, 317.7880784355627952 ) ) ;
#12279=CARTESIAN_POINT ( 'NONE',  ( 764.8639956371174549, -128.0891481129655176, 319.7806653035542013 ) ) ;
#12281=CARTESIAN_POINT ( 'NONE',  ( 781.7834795799800531, -250.8164208402379245, 315.0636971347436202 ) ) ;
#12282=CARTESIAN_POINT ( 'NONE',  ( 768.0187753319979720, -272.6346026584196807, 318.0580252608186242 ) ) ;
#12285=CARTESIAN_POINT ( 'NONE',  ( 797.6776695296629214, -451.5436935675099903, 357.6776695296636603 ) ) ;
#12290=CARTESIAN_POINT ( 'NONE',  ( 814.2001403089898304, -233.3618753856925423, 347.4397851343538264 ) ) ;
#12291=EDGE_CURVE ( 'NONE', #20106, #6763, #45431, .T. ) ;
#12292=CARTESIAN_POINT ( 'NONE',  ( 769.9779781133707957, -307.0999726633343130, 316.7813123517150871 ) ) ;
#12293=CARTESIAN_POINT ( 'NONE',  ( 765.8855110935204493, -382.1692326535045936, 319.0159684113471599 ) ) ;
#12301=CARTESIAN_POINT ( 'NONE',  ( 793.2243759319678702, -266.5328690171413655, 318.4439275373583200 ) ) ;
#12308=CARTESIAN_POINT ( 'NONE',  ( 797.6776695296629214, 4.456306432488530866, 357.6776695296636603 ) ) ;
#12311=CARTESIAN_POINT ( 'NONE',  ( 754.3581564841646241, -209.4636090269709996, 316.1443688327762516 ) ) ;
#12319=CARTESIAN_POINT ( 'NONE',  ( 797.6776695296629214, -43.54369356751131903, 357.6776695296636603 ) ) ;
#12321=CARTESIAN_POINT ( 'NONE',  ( 811.3240766477731540, -268.3726999360616787, 355.6651683502462902 ) ) ;
#12323=CARTESIAN_POINT ( 'NONE',  ( 792.2312462859673587, -275.9073299311469896, 307.2067596250082602 ) ) ;
#12328=CARTESIAN_POINT ( 'NONE',  ( 803.4237431249931660, -351.1800572038740142, 331.2633955100225194 ) ) ;
#12329=CARTESIAN_POINT ( 'NONE',  ( 796.9571628226829034, -119.4636090269712554, 321.2382568024804641 ) ) ;
#12331=AXIS2_PLACEMENT_3D ( 'NONE', #37217, #26593, #9046 ) ;
#12334=CARTESIAN_POINT ( 'NONE',  ( 781.7834795799800531, -394.8164208402374697, 315.0636971347436202 ) ) ;
#12338=CARTESIAN_POINT ( 'NONE',  ( 788.8264449731200330, -165.1800572038745258, 363.6646147819171233 ) ) ;
#12340=PLANE ( 'NONE',  #4265 ) ;
#12342=CARTESIAN_POINT ( 'NONE',  ( 774.6858677611749044, -369.7255117493284615, 315.5713283507209894 ) ) ;
#12344=ORIENTED_EDGE ( 'NONE', *, *, #2430, .T. ) ;
#12346=CARTESIAN_POINT ( 'NONE',  ( 808.3070685750232087, -66.99823902205670834, 361.1904061080339829 ) ) ;
#12351=CARTESIAN_POINT ( 'NONE',  ( 812.7932403749906598, -255.1800572038742700, 327.7687537140311633 ) ) ;
#12352=CARTESIAN_POINT ( 'NONE',  ( 798.7617431975189675, -171.6237781080507432, 323.0428371773161871 ) ) ;
#12353=EDGE_CURVE ( 'NONE', #16040, #17907, #4834, .T. ) ;
#12361=CARTESIAN_POINT ( 'NONE',  ( 814.2805881961230625, -97.64542720878949922, 331.2368401574024119 ) ) ;
#12363=DIRECTION ( 'NONE',  ( 0.000000000000000000, 0.000000000000000000, 1.000000000000000000 ) ) ;
#12371=CARTESIAN_POINT ( 'NONE',  ( 802.5472867521000353, -388.3726999360613945, 350.8726784830461156 ) ) ;
#12374=CARTESIAN_POINT ( 'NONE',  ( 791.7608162188021197, 240.0000000000000853, 360.0000000000000000 ) ) ;
#12376=CARTESIAN_POINT ( 'NONE',  ( 811.3240766477731540, -196.3726999360619061, 355.6651683502462902 ) ) ;
#12378=CARTESIAN_POINT ( 'NONE',  ( 808.0189434323515343, -158.0891481129655176, 319.0252816721025511 ) ) ;
#12381=CARTESIAN_POINT ( 'NONE',  ( 759.9864689768902508, -242.0891481129652618, 354.9819416627836404 ) ) ;
#12382=CARTESIAN_POINT ( 'NONE',  ( 755.3028492785439312, -15.28179084515340058, 335.9200461376539693 ) ) ;
#12387=CARTESIAN_POINT ( 'NONE',  ( 773.3843516231979720, -85.44195992623282621, 364.4086373105754433 ) ) ;
#12390=CARTESIAN_POINT ( 'NONE',  ( 771.2633955100217236, -71.90732993114760063, 363.4237431249939618 ) ) ;
#12393=CARTESIAN_POINT ( 'NONE',  ( 744.9990715423526808, -330.3510508353229511, 341.2370466360926002 ) ) ;
#12395=CARTESIAN_POINT ( 'NONE',  ( 783.7566961878529810, -432.8965053807771142, 305.1792804349288417 ) ) ;
#12396=CARTESIAN_POINT ( 'NONE',  ( 768.0187753319979720, -368.6346026584193964, 318.0580252608186242 ) ) ;
#12401=ORIENTED_EDGE ( 'NONE', *, *, #31257, .F. ) ;
#12403=CARTESIAN_POINT ( 'NONE',  ( 774.6858677611749044, -81.72551174932937101, 315.5713283507209894 ) ) ;
#12404=CARTESIAN_POINT ( 'NONE',  ( 786.5483106153019435, -415.6454272087885897, 364.1601925771022366 ) ) ;
#12405=CARTESIAN_POINT ( 'NONE',  ( 767.6429770376291799, -441.1800572038736163, 306.8695393053162093 ) ) ;
#12407=CARTESIAN_POINT ( 'NONE',  ( 746.7653713866222915, -305.2601417444139429, 351.0478386215610271 ) ) ;
#12408=CARTESIAN_POINT ( 'NONE',  ( 766.5853460496234675, -109.9874144716873019, 372.3518521366060554 ) ) ;
#12412=CARTESIAN_POINT ( 'NONE',  ( 749.2812353651451076, -438.4527844766009821, 323.2262854647983090 ) ) ;
#12418=CARTESIAN_POINT ( 'NONE',  ( 755.8894580844503253, -303.8272453906071178, 332.3691319403863531 ) ) ;
#12419=EDGE_LOOP ( 'NONE', ( #26629, #7700, #39977, #33907, #33198, #9491 ) ) ;
#12420=CARTESIAN_POINT ( 'NONE',  ( 754.3581564841646241, -281.4636090269706870, 316.1443688327762516 ) ) ;
#12424=CARTESIAN_POINT ( 'NONE',  ( 793.5525998758768083, -79.09997266333503774, 372.6845335610516941 ) ) ;
#12427=CARTESIAN_POINT ( 'NONE',  ( 768.0187753319979720, -152.6346026584200786, 318.0580252608186242 ) ) ;
#12431=CARTESIAN_POINT ( 'NONE',  ( 799.2566176426618085, -24.00906357242609346, 324.0069404352559559 ) ) ;
#12434=CARTESIAN_POINT ( 'NONE',  ( 776.9566956441375396, -396.8965053807772847, 364.8461984189686405 ) ) ;
#12439=CARTESIAN_POINT ( 'NONE',  ( 749.8865473780648472, -236.5328690171414792, 322.1177392798429082 ) ) ;
#12440=CARTESIAN_POINT ( 'NONE',  ( 781.7834795799800531, -82.81642084023846451, 315.0636971347436202 ) ) ;
#12441=ORIENTED_EDGE ( 'NONE', *, *, #14012, .T. ) ;
#12442=ORIENTED_EDGE ( 'NONE', *, *, #9964, .T. ) ;
#12444=CARTESIAN_POINT ( 'NONE',  ( 755.5713283507202505, -245.3618753856925139, 334.6858677611754729 ) ) ;
#12452=CARTESIAN_POINT ( 'NONE',  ( 749.2812353651451076, -342.4527844766013231, 323.2262854647983090 ) ) ;
#12453=CARTESIAN_POINT ( 'NONE',  ( 783.7566961878529810, -48.89650538077840025, 305.1792804349288417 ) ) ;
#12458=CARTESIAN_POINT ( 'NONE',  ( 759.7806653035534055, -198.9982390220562252, 324.8639956371180801 ) ) ;
#12461=CARTESIAN_POINT ( 'NONE',  ( 814.2001403089898304, -329.3618753856922581, 347.4397851343538264 ) ) ;
#12465=CARTESIAN_POINT ( 'NONE',  ( 755.5913626894240451, -205.6454272087891297, 346.6156483768012890 ) ) ;
#12466=CARTESIAN_POINT ( 'NONE',  ( 754.8072714833581358, -76.81642084023845030, 338.1981804954720587 ) ) ;
#12470=CARTESIAN_POINT ( 'NONE',  ( 793.2243759319678702, -266.5328690171413655, 318.4439275373583200 ) ) ;
#12473=CARTESIAN_POINT ( 'NONE',  ( 792.2312462859673587, -443.9073299311464780, 307.2067596250082602 ) ) ;
#12477=CARTESIAN_POINT ( 'NONE',  ( 782.5225473063381969, -94.27096629478386092, 375.2698199232970637 ) ) ;
#12478=CARTESIAN_POINT ( 'NONE',  ( 796.9462024416508257, -132.4527844766018916, 308.9653473494370246 ) ) ;
#12483=CARTESIAN_POINT ( 'NONE',  ( 767.7687537140311633, -359.9073299311467053, 372.7932403749916830 ) ) ;
#12486=CARTESIAN_POINT ( 'NONE',  ( 805.1927285166397041, -448.8164208402371855, 341.8018195045277707 ) ) ;
#12489=CARTESIAN_POINT ( 'NONE',  ( 773.7943932421234194, -119.8055962898690865, 305.5313806188329409 ) ) ;
#12494=CARTESIAN_POINT ( 'NONE',  ( 771.2633955100217236, -143.9073299311473590, 363.4237431249939618 ) ) ;
#12497=CARTESIAN_POINT ( 'NONE',  ( 765.0180583372156207, -288.9982390220559978, 360.0135310231089534 ) ) ;
#12498=CARTESIAN_POINT ( 'NONE',  ( 778.1981804954715471, -274.2709662947832499, 314.8072714833591021 ) ) ;
#12501=CARTESIAN_POINT ( 'NONE',  ( 794.9819416627830151, -444.9982390220554862, 319.9864689768909898 ) ) ;
#12505=CARTESIAN_POINT ( 'NONE',  ( 796.9462024416508257, -204.4527844766016926, 308.9653473494370246 ) ) ;
#12506=CARTESIAN_POINT ( 'NONE',  ( 802.9823548866075953, -313.0999726633342561, 330.0799878456151077 ) ) ;
#12507=CARTESIAN_POINT ( 'NONE',  ( 804.1601925771018387, -391.4419599262317888, 346.5483106153029098 ) ) ;
#12517=CARTESIAN_POINT ( 'NONE',  ( 803.8651313633788504, -317.2601417444139429, 332.4468031744301015 ) ) ;
#12523=CARTESIAN_POINT ( 'NONE',  ( 786.2694204179717872, -213.2817908451527842, 305.1769319972829067 ) ) ;
#12529=CARTESIAN_POINT ( 'NONE',  ( 749.2812353651451076, -30.45278447660226817, 323.2262854647983090 ) ) ;
#12532=CARTESIAN_POINT ( 'NONE',  ( 764.8639956371174549, -56.08914811296580893, 319.7806653035542013 ) ) ;
#12534=CARTESIAN_POINT ( 'NONE',  ( 795.8262568251477660, -310.3726999360616219, 308.3538107759623585 ) ) ;
#12535=CARTESIAN_POINT ( 'NONE',  ( 808.3070685750230950, -258.9982390220561115, 361.1904061080339261 ) ) ;
#12540=CARTESIAN_POINT ( 'NONE',  ( 755.5713283507202505, -365.3618753856920875, 334.6858677611754729 ) ) ;
#12541=CARTESIAN_POINT ( 'NONE',  ( 757.0176451133909268, -133.0999726633348246, 349.9200121543848354 ) ) ;
#12545=CARTESIAN_POINT ( 'NONE',  ( 755.3201227861273992, -411.7255117493282910, 345.3687786644892981 ) ) ;
#12549=CARTESIAN_POINT ( 'NONE',  ( 774.6858677611749044, -201.7255117493290015, 315.5713283507209894 ) ) ;
#12550=CARTESIAN_POINT ( 'NONE',  ( 800.0135310231082713, -158.0891481129655176, 325.0180583372163028 ) ) ;
#12555=CARTESIAN_POINT ( 'NONE',  ( 762.1405469898971887, -361.5436935675103882, 357.8594530101015607 ) ) ;
#12559=CARTESIAN_POINT ( 'NONE',  ( 758.8095938919644823, -104.0891481129656739, 311.6929314249762797 ) ) ;
#12566=CARTESIAN_POINT ( 'NONE',  ( 747.2067596250078623, -267.1800572038742985, 352.2312462859687230 ) ) ;
#12567=CARTESIAN_POINT ( 'NONE',  ( 784.0799538623451781, -179.8055962898688733, 364.6971507214555572 ) ) ;
#12574=CARTESIAN_POINT ( 'NONE',  ( 804.1009440267234822, -119.4636090269712554, 314.0944755984392600 ) ) ;
#12583=CARTESIAN_POINT ( 'NONE',  ( 760.7433823573367135, -444.0090635724249069, 355.9930595647440441 ) ) ;
#12586=CARTESIAN_POINT ( 'NONE',  ( 783.0745993439762742, -248.1908817542435202, 365.1016975059196739 ) ) ;
#12592=CARTESIAN_POINT ( 'NONE',  ( 773.7305795820266212, -225.2817908451527273, 374.8230680027170365 ) ) ;
#12594=CARTESIAN_POINT ( 'NONE',  ( 808.3070685750230950, -162.9982390220563673, 361.1904061080339261 ) ) ;
#12598=CARTESIAN_POINT ( 'NONE',  ( 802.1676090361156639, -254.6346026584196238, 327.8955696845344505 ) ) ;
#12599=CARTESIAN_POINT ( 'NONE',  ( 783.0745993439762742, -8.190881754244330182, 365.1016975059196739 ) ) ;
#12601=CARTESIAN_POINT ( 'NONE',  ( 779.9999999999992042, 166.4563064324884465, 350.0000000000000000 ) ) ;
#12604=CARTESIAN_POINT ( 'NONE',  ( 786.6156483768007774, -97.44195992623281199, 315.5913626894246136 ) ) ;
#12605=CARTESIAN_POINT ( 'NONE',  ( 797.6776695296629214, -307.5436935675104451, 357.6776695296636603 ) ) ;
#12610=CARTESIAN_POINT ( 'NONE',  ( 755.0636971347428243, -52.27096629478401724, 341.7834795799807353 ) ) ;
#12612=CARTESIAN_POINT ( 'NONE',  ( 815.0009284576459549, -390.3510508353227237, 338.7629533639073429 ) ) ;
#12614=CARTESIAN_POINT ( 'NONE',  ( 745.0891759886404770, -4.270966294784170003, 342.4968714119734159 ) ) ;
#12616=CARTESIAN_POINT ( 'NONE',  ( 774.6312213355099630, -383.3618753856921444, 364.6798772138717482 ) ) ;
#12623=CARTESIAN_POINT ( 'NONE',  ( 755.5713283507202505, -77.36187538569302546, 334.6858677611754729 ) ) ;
#12624=CARTESIAN_POINT ( 'NONE',  ( 766.9102291470427417, -402.5545181178795247, 318.6633372737382501 ) ) ;
#12625=CARTESIAN_POINT ( 'NONE',  ( 792.3570229623691148, -429.1800572038737300, 373.1304606946836770 ) ) ;
#12627=CARTESIAN_POINT ( 'NONE',  ( 801.9858362298568863, -339.0783235625956422, 312.7379699480935642 ) ) ;
#12631=CARTESIAN_POINT ( 'NONE',  ( 814.2001403089898304, -449.3618753856918602, 347.4397851343538264 ) ) ;
#12632=DIRECTION ( 'NONE',  ( -0.7014439490181307857, 0.1263042864341424876, 0.7014439490181749726 ) ) ;
#12638=CARTESIAN_POINT ( 'NONE',  ( 793.0897708529556667, -318.5545181178796952, 361.3366627262616362 ) ) ;
#12640=CARTESIAN_POINT ( 'NONE',  ( 768.9521613784389729, -297.8272453906070041, 373.2346286133773106 ) ) ;
#12643=CARTESIAN_POINT ( 'NONE',  ( 773.7305795820266212, -81.28179084515319630, 374.8230680027170365 ) ) ;
#12645=FACE_BOUND ( 'NONE', #7016, .T. ) ;
#12646=CARTESIAN_POINT ( 'NONE',  ( 795.1360043628807261, -164.0891481129655176, 360.2193346964456282 ) ) ;
#12650=CARTESIAN_POINT ( 'NONE',  ( 805.2837595273609850, -50.73633629969874193, 340.5290396650784714 ) ) ;
#12653=CARTESIAN_POINT ( 'NONE',  ( 755.8398074228967971, -427.4419599262317888, 333.4516893846970333 ) ) ;
#12655=CARTESIAN_POINT ( 'NONE',  ( 783.0433043558608688, -72.89650538077830788, 315.1538015810313027 ) ) ;
#12658=CARTESIAN_POINT ( 'NONE',  ( 744.8212110874229666, -258.8965053807777963, 336.2046728542121627 ) ) ;
#12659=CARTESIAN_POINT ( 'NONE',  ( 785.3687786644885591, -83.36187538569299704, 315.3201227861280813 ) ) ;
#12662=CARTESIAN_POINT ( 'NONE',  ( 804.9363028652555840, -280.2709662947833067, 338.2165204200192079 ) ) ;
#12664=CARTESIAN_POINT ( 'NONE',  ( 799.9999999999993179, -462.9681489794448339, 309.9999999999998863 ) ) ;
#12665=ORIENTED_EDGE ( 'NONE', *, *, #5460, .F. ) ;
#12666=ORIENTED_EDGE ( 'NONE', *, *, #11308, .T. ) ;
#12669=CARTESIAN_POINT ( 'NONE',  ( 808.0189434323515343, -326.0891481129649492, 319.0252816721025511 ) ) ;
#12670=CARTESIAN_POINT ( 'NONE',  ( 768.8385539511368734, -215.2601417444141987, 306.4236121716840557 ) ) ;
#12671=CARTESIAN_POINT ( 'NONE',  ( 744.8212110874229666, -42.89650538077842157, 336.2046728542121627 ) ) ;
#12676=CARTESIAN_POINT ( 'NONE',  ( 805.1927285166397041, -208.8164208402380666, 341.8018195045277707 ) ) ;
#12679=CARTESIAN_POINT ( 'NONE',  ( 772.4837098697144029, -359.3618753856920875, 374.5518280994205611 ) ) ;
#12681=CARTESIAN_POINT ( 'NONE',  ( 793.5727445751998630, 16.45630643248830793, 314.6726781324130684 ) ) ;
#12683=CARTESIAN_POINT ( 'NONE',  ( 802.9823548866075953, -193.0999726633346256, 330.0799878456151077 ) ) ;
#12684=CARTESIAN_POINT ( 'NONE',  ( 765.0180583372156207, -72.99823902205667991, 360.0135310231089534 ) ) ;
#12688=CARTESIAN_POINT ( 'NONE',  ( 804.1601925771018387, -271.4419599262321867, 346.5483106153029098 ) ) ;
#12691=CARTESIAN_POINT ( 'NONE',  ( 787.5162901302840055, -443.3618753856917465, 305.4481719005792684 ) ) ;
#12695=CARTESIAN_POINT ( 'NONE',  ( 763.2262854647970016, -80.63460265842029173, 309.2812353651462445 ) ) ;
#12696=CARTESIAN_POINT ( 'NONE',  ( 748.9653473494363425, -146.6346026584200217, 356.9462024416521331 ) ) ;
#12702=CARTESIAN_POINT ( 'NONE',  ( 749.2812353651451076, -390.4527844766011526, 323.2262854647983090 ) ) ;
#12703=CARTESIAN_POINT ( 'NONE',  ( 754.9967657858570647, -1.543693567511449594, 365.0032342141425943 ) ) ;
#12705=CARTESIAN_POINT ( 'NONE',  ( 761.2382568024794409, 8.376221891948691933, 356.9571628226838129 ) ) ;
#12709=CARTESIAN_POINT ( 'NONE',  ( 810.1134526219336749, -152.5328690171416781, 357.8822607201570349 ) ) ;
#12713=CARTESIAN_POINT ( 'NONE',  ( 754.8072714833581358, -172.8164208402381234, 338.1981804954720587 ) ) ;
#12715=CARTESIAN_POINT ( 'NONE',  ( 778.2165204200184689, -286.8164208402378677, 364.9363028652563230 ) ) ;
#12716=CARTESIAN_POINT ( 'NONE',  ( 797.6776695296629214, -307.5436935675104451, 357.6776695296636603 ) ) ;
#12719=CARTESIAN_POINT ( 'NONE',  ( 779.4709603349208464, -0.3510508353240099355, 314.7162404726379918 ) ) ;
#12723=CARTESIAN_POINT ( 'NONE',  ( 796.9462024416508257, -228.4527844766016074, 308.9653473494370246 ) ) ;
#12724=CARTESIAN_POINT ( 'NONE',  ( 798.5707757039680246, -293.4636090269707438, 356.7845633553585003 ) ) ;
#12725=CARTESIAN_POINT ( 'NONE',  ( 786.6156483768007774, -385.4419599262319593, 315.5913626894246136 ) ) ;
#12734=CARTESIAN_POINT ( 'NONE',  ( 790.8726784830453198, -298.7146871989593251, 362.5472867521010585 ) ) ;
#12740=CARTESIAN_POINT ( 'NONE',  ( 814.4686193811664907, -195.2817908451528410, 346.2056067578752732 ) ) ;
#12745=CARTESIAN_POINT ( 'NONE',  ( 772.4837098697144029, -47.36187538569312494, 374.5518280994205611 ) ) ;
#12748=DIRECTION ( 'NONE',  ( 0.000000000000000000, 0.000000000000000000, 1.000000000000000000 ) ) ;
#12749=CARTESIAN_POINT ( 'NONE',  ( 759.7806653035534055, -30.99823902205680071, 324.8639956371180801 ) ) ;
#12750=CARTESIAN_POINT ( 'NONE',  ( 754.3581564841646241, -329.4636090269706870, 316.1443688327762516 ) ) ;
#12751=CARTESIAN_POINT ( 'NONE',  ( 746.8695393053150156, -269.9073299311468190, 327.6429770376306010 ) ) ;
#12755=CARTESIAN_POINT ( 'NONE',  ( 756.3353852180819104, -365.9073299311465917, 331.1735550268788302 ) ) ;
#12757=CARTESIAN_POINT ( 'NONE',  ( 772.4468031744293057, -105.8272453906076578, 363.8651313633793620 ) ) ;
#12759=CARTESIAN_POINT ( 'NONE',  ( 759.8311093483677041, -46.16923265350568784, 310.9282345327691814 ) ) ;
#12760=CARTESIAN_POINT ( 'NONE',  ( 778.2165204200184689, -358.8164208402375834, 364.9363028652563230 ) ) ;
#12763=CARTESIAN_POINT ( 'NONE',  ( 764.8639956371174549, -392.0891481129648355, 319.7806653035542013 ) ) ;
#12766=CARTESIAN_POINT ( 'NONE',  ( 792.1044303154645831, -180.4527844766017211, 317.8323909638837677 ) ) ;
#12767=CARTESIAN_POINT ( 'NONE',  ( 778.2165204200184689, -190.8164208402381234, 364.9363028652563230 ) ) ;
#12771=CARTESIAN_POINT ( 'NONE',  ( 804.6798772138708955, -351.7255117493284047, 334.6312213355107019 ) ) ;
#12776=CARTESIAN_POINT ( 'NONE',  ( 777.5031285880264704, -118.8164208402383508, 374.9108240113588408 ) ) ;
#12782=CARTESIAN_POINT ( 'NONE',  ( 787.5162901302840055, -251.3618753856923149, 305.4481719005792684 ) ) ;
#12783=CARTESIAN_POINT ( 'NONE',  ( 780.5290396650775619, -180.3510508353234343, 365.2837595273619513 ) ) ;
#12784=PLANE ( 'NONE',  #38786 ) ;
#12793=VERTEX_POINT ( 'NONE', #40075 ) ;
#12795=AXIS2_PLACEMENT_3D ( 'NONE', #37404, #44560, #16379 ) ;
#12796=CARTESIAN_POINT ( 'NONE',  ( 776.2046728542105711, -116.1908817542440033, 304.8212110874238761 ) ) ;
#12806=CARTESIAN_POINT ( 'NONE',  ( 793.9708237608222134, -430.9181544815157849, 319.2295555964448681 ) ) ;
#12807=CARTESIAN_POINT ( 'NONE',  ( 791.0478386215596629, -357.8272453906068904, 306.7653713866226326 ) ) ;
#12815=CARTESIAN_POINT ( 'NONE',  ( 748.6759233522253680, -232.3726999360617924, 324.3348316497537098 ) ) ;
#12817=CARTESIAN_POINT ( 'NONE',  ( 815.2698199232961542, -160.8164208402382371, 342.5225473063383106 ) ) ;
#12820=CARTESIAN_POINT ( 'NONE',  ( 800.2193346964447755, -258.9982390220561115, 355.1360043628815788 ) ) ;
#12821=CARTESIAN_POINT ( 'NONE',  ( 776.9254006560222479, -44.19088175424421649, 314.8983024940802125 ) ) ;
#12825=CARTESIAN_POINT ( 'NONE',  ( 793.3938497862117174, -453.0432664090020580, 372.3358127763067955 ) ) ;
#12827=CARTESIAN_POINT ( 'NONE',  ( 804.9511171171677688, -101.8055962898691718, 335.8780910478229202 ) ) ;
#12831=CARTESIAN_POINT ( 'NONE',  ( 797.8594530101008786, -61.54369356751124087, 322.1405469898980982 ) ) ;
#12832=VECTOR ( 'NONE', #6346, 1000.000000000000000 ) ;
#12834=CARTESIAN_POINT ( 'NONE',  ( 751.2241431872005251, -376.1692326535046504, 359.9636004259367610 ) ) ;
#12836=CARTESIAN_POINT ( 'NONE',  ( 767.7687537140311633, 0.09267006885218045942, 372.7932403749916830 ) ) ;
#12839=CARTESIAN_POINT ( 'NONE',  ( 759.9864689768902508, -386.0891481129647786, 354.9819416627836404 ) ) ;
#12848=CARTESIAN_POINT ( 'NONE',  ( 801.9419747391806368, -90.45278447660209054, 351.9812246680014027 ) ) ;
#12849=CARTESIAN_POINT ( 'NONE',  ( 801.5560724626406000, -408.5545181178794110, 326.7756240680316182 ) ) ;
#12850=CARTESIAN_POINT ( 'NONE',  ( 795.9930595647434757, -99.07832356259642381, 320.7433823573372820 ) ) ;
#12851=CARTESIAN_POINT ( 'NONE',  ( 772.5602148656447525, -441.7255117493282910, 305.7998596910095443 ) ) ;
#12853=CARTESIAN_POINT ( 'NONE',  ( 745.1769319972822814, -353.8055962898683333, 346.2694204179732083 ) ) ;
#12856=CARTESIAN_POINT ( 'NONE',  ( 759.8311093483677041, -118.1692326535054463, 310.9282345327691814 ) ) ;
#12860=CARTESIAN_POINT ( 'NONE',  ( 791.0478386215596629, 2.172754609392001601, 306.7653713866226326 ) ) ;
#12862=DIRECTION ( 'NONE',  ( 0.000000000000000000, 0.000000000000000000, -1.000000000000000000 ) ) ;
#12868=CARTESIAN_POINT ( 'NONE',  ( 796.9571628226829034, -335.4636090269705733, 321.2382568024804641 ) ) ;
#12870=CARTESIAN_POINT ( 'NONE',  ( 785.3141322388236176, -189.7255117493290300, 364.4286716492789537 ) ) ;
#12872=CARTESIAN_POINT ( 'NONE',  ( 778.7629533639073998, -296.7363362996979390, 375.0009284576466371 ) ) ;
#12875=CARTESIAN_POINT ( 'NONE',  ( 781.2370466360911223, -116.7363362996985217, 304.9990715423533629 ) ) ;
#12878=CARTESIAN_POINT ( 'NONE',  ( 765.0180583372156207, -144.9982390220564525, 360.0135310231089534 ) ) ;
#12880=CARTESIAN_POINT ( 'NONE',  ( 768.9521613784389729, -417.8272453906067199, 373.2346286133773106 ) ) ;
#12884=CARTESIAN_POINT ( 'NONE',  ( 755.1538015810308480, -38.19088175424422360, 343.0433043558613804 ) ) ;
#12887=CARTESIAN_POINT ( 'NONE',  ( 788.4001350590139054, -443.1233509495419298, 363.5803521658918385 ) ) ;
#12889=CARTESIAN_POINT ( 'NONE',  ( 801.3366627262608972, -80.53286901714194812, 353.0897708529566899 ) ) ;
#12894=CARTESIAN_POINT ( 'NONE',  ( 754.0944755984390895, -279.6237781080503737, 364.1009440267246760 ) ) ;
#12895=CARTESIAN_POINT ( 'NONE',  ( 756.5762568750052424, -75.18005720387485269, 348.7366044899774238 ) ) ;
#12898=CARTESIAN_POINT ( 'NONE',  ( 797.8594530101008786, -277.5436935675105019, 322.1405469898980982 ) ) ;
#12899=CLOSED_SHELL ( 'NONE', ( #9161, #5465, #28901, #16248, #41046, #2047, #41289, #37100, #9051, #28925, #23522, #31474, #7758, #23576, #23006, #3744, #41360, #38827, #34309, #35280, #28661, #15958, #14434, #8650, #32602, #11699, #29669, #22647, #21316, #35381, #19329, #36813, #39663, #4436, #26113, #24140, #45577, #8897, #24415, #1901, #43841, #6598, #13670, #44165, #44140, #41085, #467, #26031, #4934, #7751 ) ) ;
#12907=CARTESIAN_POINT ( 'NONE',  ( 777.5031285880264704, -310.8164208402377540, 374.9108240113588408 ) ) ;
#12908=CARTESIAN_POINT ( 'NONE',  ( 798.0661480581538854, -218.5328690171414792, 309.5768839229118043 ) ) ;
#12916=CARTESIAN_POINT ( 'NONE',  ( 804.7487373415286811, -355.5436935675103882, 364.7487373415288516 ) ) ;
#12919=CARTESIAN_POINT ( 'NONE',  ( 791.3765159950071393, 16.45630643248849623, 314.4691821868552211 ) ) ;
#12920=FACE_OUTER_BOUND ( 'NONE', #29238, .T. ) ;
#12921=AXIS2_PLACEMENT_3D ( 'NONE', #2144, #33792, #23139 ) ;
#12922=CARTESIAN_POINT ( 'NONE',  ( 757.0176451133909268, -229.0999726633345404, 349.9200121543848354 ) ) ;
#12924=CARTESIAN_POINT ( 'NONE',  ( 767.8955696845333705, -96.45278447660203369, 362.1676090361162323 ) ) ;
#12927=CARTESIAN_POINT ( 'NONE',  ( 790.8726784830453198, -274.7146871989594388, 362.5472867521010585 ) ) ;
#12930=CARTESIAN_POINT ( 'NONE',  ( 804.7487373415286811, -451.5436935675099903, 364.7487373415288516 ) ) ;
#12934=CARTESIAN_POINT ( 'NONE',  ( 804.7487373415286811, -91.54369356751116982, 364.7487373415288516 ) ) ;
#12935=CARTESIAN_POINT ( 'NONE',  ( 782.4968714119720516, -130.8164208402383224, 305.0891759886411023 ) ) ;
#12936=DIRECTION ( 'NONE',  ( 0.7071067811865697772, 0.000000000000000000, 0.7071067811865252573 ) ) ;
#12941=CARTESIAN_POINT ( 'NONE',  ( 788.6739635108323228, -415.6454272087885897, 373.9316612368139090 ) ) ;
#12943=CARTESIAN_POINT ( 'NONE',  ( 759.9999999999992042, 166.4563064324884465, 319.9999999999999432 ) ) ;
#12944=CARTESIAN_POINT ( 'NONE',  ( 744.7301800767019131, -412.8164208402372992, 337.4774526936615757 ) ) ;
#12945=CARTESIAN_POINT ( 'NONE',  ( 801.1904061080338124, 3.910851887033986785, 368.3070685750236066 ) ) ;
#12948=CARTESIAN_POINT ( 'NONE',  ( 775.9200461376533440, -23.80559628986938847, 315.3028492785443291 ) ) ;
#12951=CARTESIAN_POINT ( 'NONE',  ( 800.1688906516307043, -154.1692326535053894, 369.0717654672308186 ) ) ;
#12952=CARTESIAN_POINT ( 'NONE',  ( 804.9363028652555840, 7.729033705215793582, 338.2165204200192079 ) ) ;
#12956=CARTESIAN_POINT ( 'NONE',  ( 756.3353852180819104, -173.9073299311472169, 331.1735550268788302 ) ) ;
#12960=CARTESIAN_POINT ( 'NONE',  ( 791.9812246680005501, -308.6346026584195670, 361.9419747391813189 ) ) ;
#12963=CARTESIAN_POINT ( 'NONE',  ( 799.4546378042377910, -9.078323562596708030, 356.1575198192848006 ) ) ;
#12967=CARTESIAN_POINT ( 'NONE',  ( 777.5031285880264704, -214.8164208402380666, 374.9108240113588408 ) ) ;
#12968=CARTESIAN_POINT ( 'NONE',  ( 754.7162404726377645, -302.7363362996979959, 339.4709603349214717 ) ) ;
#12969=CARTESIAN_POINT ( 'NONE',  ( 801.3366627262608972, -440.5328690171407970, 353.0897708529566899 ) ) ;
#12979=CARTESIAN_POINT ( 'NONE',  ( 769.1273215169530886, -310.7146871989593251, 317.4527132478988847 ) ) ;
#12983=CARTESIAN_POINT ( 'NONE',  ( 804.8461984189677878, -122.1908817542439749, 336.9566956441385628 ) ) ;
#12987=CARTESIAN_POINT ( 'NONE',  ( 786.2694204179717872, -189.2817908451528979, 305.1769319972829067 ) ) ;
#12991=CARTESIAN_POINT ( 'NONE',  ( 805.0032342141412300, -61.54369356751124087, 314.9967657858571783 ) ) ;
#12994=LINE ( 'NONE', #27081, #20250 ) ;
#12995=CARTESIAN_POINT ( 'NONE',  ( 762.1177392798416577, -330.5545181178796952, 309.8865473780659272 ) ) ;
#12997=CARTESIAN_POINT ( 'NONE',  ( 755.2512626584698410, -295.5436935675105588, 315.2512626584710915 ) ) ;
#13001=CARTESIAN_POINT ( 'NONE',  ( 755.3201227861273992, -387.7255117493283478, 345.3687786644892981 ) ) ;
#13002=CARTESIAN_POINT ( 'NONE',  ( 763.0428371773158460, -131.4636090269711985, 358.7617431975195359 ) ) ;
#13004=CARTESIAN_POINT ( 'NONE',  ( 754.0944755984390895, -63.62377810805107714, 364.1009440267246760 ) ) ;
#13005=CARTESIAN_POINT ( 'NONE',  ( 794.9819416627830151, -372.9982390220557704, 319.9864689768909898 ) ) ;
#13006=CARTESIAN_POINT ( 'NONE',  ( 758.8095938919644823, 15.91085188703394593, 311.6929314249762797 ) ) ;
#13008=CARTESIAN_POINT ( 'NONE',  ( 800.2193346964447755, -426.9982390220554862, 355.1360043628815788 ) ) ;
#13012=CARTESIAN_POINT ( 'NONE',  ( 803.4237431249931660, -183.1800572038744974, 331.2633955100225194 ) ) ;
#13013=CARTESIAN_POINT ( 'NONE',  ( 756.3353852180820240, -197.9073299311472169, 331.1735550268787733 ) ) ;
#13017=CARTESIAN_POINT ( 'NONE',  ( 756.3353852180819104, -389.9073299311465348, 331.1735550268788302 ) ) ;
#13021=CARTESIAN_POINT ( 'NONE',  ( 745.4481719005789273, -123.7255117493292289, 347.5162901302853697 ) ) ;
#13027=CARTESIAN_POINT ( 'NONE',  ( 800.9747183278959710, -252.9982390220560831, 311.9810565676471583 ) ) ;
#13028=CARTESIAN_POINT ( 'NONE',  ( 790.8726784830453198, -178.7146871989598083, 362.5472867521010585 ) ) ;
#13029=CARTESIAN_POINT ( 'NONE',  ( 809.6099558218720631, -452.9681489794449476, 335.1781210895659342 ) ) ;
#13034=PLANE ( 'NONE',  #43205 ) ;
#13038=CARTESIAN_POINT ( 'NONE',  ( 812.3518521366052028, -97.09997266333496668, 326.5853460496235243 ) ) ;
#13048=CARTESIAN_POINT ( 'NONE',  ( 783.0745993439762742, -440.1908817542430370, 365.1016975059196739 ) ) ;
#13058=CARTESIAN_POINT ( 'NONE',  ( 771.3260364891663130, -211.6454272087891582, 306.0683387631859773 ) ) ;
#13060=CARTESIAN_POINT ( 'NONE',  ( 812.7932403749906598, -183.1800572038744974, 327.7687537140311633 ) ) ;
#13062=AXIS2_PLACEMENT_3D ( 'NONE', #36673, #2004, #13102 ) ;
#13064=CARTESIAN_POINT ( 'NONE',  ( 756.5762568750052424, -267.1800572038742985, 348.7366044899774238 ) ) ;
#13065=CARTESIAN_POINT ( 'NONE',  ( 776.9254006560222479, -68.19088175424413123, 314.8983024940802125 ) ) ;
#13069=CARTESIAN_POINT ( 'NONE',  ( 760.5453621957607311, -93.07832356259645223, 323.8424801807151425 ) ) ;
#13070=CARTESIAN_POINT ( 'NONE',  ( 755.0636971347428243, -340.2709662947831362, 341.7834795799807353 ) ) ;
#13075=CARTESIAN_POINT ( 'NONE',  ( 792.1044303154645831, -60.45278447660215448, 317.8323909638837677 ) ) ;
#13077=DIRECTION ( 'NONE',  ( 1.000000000000000000, -0.000000000000000000, -0.000000000000000000 ) ) ;
#13078=CARTESIAN_POINT ( 'NONE',  ( 773.7943932421234194, -383.8055962898682765, 305.5313806188329409 ) ) ;
#13081=CARTESIAN_POINT ( 'NONE',  ( 804.4286716492782716, -305.3618753856922581, 345.3141322388244703 ) ) ;
#13082=CARTESIAN_POINT ( 'NONE',  ( 777.4774526936600978, 13.72903370521577138, 304.7301800767027657 ) ) ;
#13085=CARTESIAN_POINT ( 'NONE',  ( 758.0580252608178853, -390.4527844766011526, 328.0187753319985404 ) ) ;
#13093=CARTESIAN_POINT ( 'NONE',  ( 759.7806653035534055, -78.99823902205662307, 324.8639956371180801 ) ) ;
#13094=CARTESIAN_POINT ( 'NONE',  ( 772.4468031744293057, -393.8272453906067199, 363.8651313633793620 ) ) ;
#13095=CARTESIAN_POINT ( 'NONE',  ( 795.1271208383658404, -452.8379544210779954, 371.6178728169206238 ) ) ;
#13097=CARTESIAN_POINT ( 'NONE',  ( 746.7653713866222915, -353.2601417444137724, 351.0478386215610271 ) ) ;
#13101=CARTESIAN_POINT ( 'NONE',  ( 805.0032342141412300, -445.5436935675098766, 314.9967657858571783 ) ) ;
#13102=DIRECTION ( 'NONE',  ( 0.000000000000000000, 1.110223024625155554E-15, -1.000000000000000000 ) ) ;
#13109=CARTESIAN_POINT ( 'NONE',  ( 805.2837595273609850, -314.7363362996979959, 340.5290396650784714 ) ) ;
#13112=CARTESIAN_POINT ( 'NONE',  ( 807.2620300519052989, -288.0090635724252479, 318.0141637701419768 ) ) ;
#13115=CARTESIAN_POINT ( 'NONE',  ( 814.2805881961230625, -97.64542720878949922, 331.2368401574024119 ) ) ;
#13119=CARTESIAN_POINT ( 'NONE',  ( 758.0580252608178853, -150.4527844766018916, 328.0187753319985404 ) ) ;
#13121=CARTESIAN_POINT ( 'NONE',  ( 781.2370466360911223, -428.7363362996975980, 304.9990715423533629 ) ) ;
#13126=CARTESIAN_POINT ( 'NONE',  ( 799.2566176426618085, -48.00906357242602951, 324.0069404352559559 ) ) ;
#13128=DIRECTION ( 'NONE',  ( 0.000000000000000000, 0.000000000000000000, 1.000000000000000000 ) ) ;
#13129=CARTESIAN_POINT ( 'NONE',  ( 779.4709603349208464, -432.3510508353226669, 314.7162404726379918 ) ) ;
#13134=CARTESIAN_POINT ( 'NONE',  ( 783.7566961878529810, -264.8965053807776826, 305.1792804349288417 ) ) ;
#13135=CARTESIAN_POINT ( 'NONE',  ( 762.1405469898973024, -97.54369356751114140, 357.8594530101016176 ) ) ;
#13138=CARTESIAN_POINT ( 'NONE',  ( 788.7366044899766848, -275.9073299311469896, 316.5762568750059813 ) ) ;
#13141=CARTESIAN_POINT ( 'NONE',  ( 791.1616803454811588, -448.0882476894967112, 368.5954562921680235 ) ) ;
#13145=CARTESIAN_POINT ( 'NONE',  ( 782.5225473063383106, -310.2709662947832499, 375.2698199232970637 ) ) ;
#13146=CARTESIAN_POINT ( 'NONE',  ( 810.1134526219336749, -248.5328690171414223, 357.8822607201570349 ) ) ;
#13150=CARTESIAN_POINT ( 'NONE',  ( 805.1927285166397041, -232.8164208402379245, 341.8018195045277707 ) ) ;
#13151=ORIENTED_EDGE ( 'NONE', *, *, #1507, .T. ) ;
#13153=CARTESIAN_POINT ( 'NONE',  ( 810.7187646348534145, -354.4527844766012095, 356.7737145352016341 ) ) ;
#13157=CARTESIAN_POINT ( 'NONE',  ( 766.8731515446878575, 16.45630643248848912, 318.5849060538806725 ) ) ;
#13159=CARTESIAN_POINT ( 'NONE',  ( 769.9779781133707957, -235.0999726633344835, 316.7813123517150871 ) ) ;
#13160=CARTESIAN_POINT ( 'NONE',  ( 800.0135310231082713, -86.08914811296573077, 325.0180583372163028 ) ) ;
#13164=CARTESIAN_POINT ( 'NONE',  ( 779.4709603349208464, -240.3510508353232069, 314.7162404726379918 ) ) ;
#13167=CARTESIAN_POINT ( 'NONE',  ( 814.2805881961230625, -1.645427208789804308, 331.2368401574024119 ) ) ;
#13171=CARTESIAN_POINT ( 'NONE',  ( 748.9653473494363425, -98.63460265842024910, 356.9462024416521331 ) ) ;
#13172=CARTESIAN_POINT ( 'NONE',  ( 815.2698199232961542, -160.8164208402382371, 342.5225473063383106 ) ) ;
#13177=CARTESIAN_POINT ( 'NONE',  ( 809.0717654672305343, -412.9181544815157281, 360.1688906516309885 ) ) ;
#13180=CARTESIAN_POINT ( 'NONE',  ( 748.9653473494363425, -386.6346026584191691, 356.9462024416521331 ) ) ;
#13181=CARTESIAN_POINT ( 'NONE',  ( 763.2262854647970016, -8.634602658420517329, 309.2812353651462445 ) ) ;
#13184=CARTESIAN_POINT ( 'NONE',  ( 795.9930595647434757, -3.078323562596726681, 320.7433823573372820 ) ) ;
#13187=CARTESIAN_POINT ( 'NONE',  ( 791.1614460488616487, -179.2601417444143692, 373.5763878283158874 ) ) ;
#13188=CARTESIAN_POINT ( 'NONE',  ( 768.0187753319979720, 15.36539734157940629, 318.0580252608186242 ) ) ;
#13189=CARTESIAN_POINT ( 'NONE',  ( 786.2056067578752163, -179.8055962898688733, 374.4686193811670023 ) ) ;
#13194=CARTESIAN_POINT ( 'NONE',  ( 755.3201227861273992, -147.7255117493291152, 345.3687786644892981 ) ) ;
#13197=CARTESIAN_POINT ( 'NONE',  ( 805.1927285166397041, -280.8164208402378677, 341.8018195045277707 ) ) ;
#13198=CARTESIAN_POINT ( 'NONE',  ( 794.9819416627830151, -300.9982390220559409, 319.9864689768909898 ) ) ;
#13201=CARTESIAN_POINT ( 'NONE',  ( 802.7791456095903868, -4.714687198960358039, 329.0155153010375102 ) ) ;
#13204=CARTESIAN_POINT ( 'NONE',  ( 813.1304606946831655, -209.9073299311471317, 352.3570229623691716 ) ) ;
#13205=CARTESIAN_POINT ( 'NONE',  ( 776.9254006560222479, -332.1908817542433781, 314.8983024940802125 ) ) ;
#13206=CARTESIAN_POINT ( 'NONE',  ( 805.0264073115434940, -438.3510508353226669, 339.4763451958999099 ) ) ;
#13213=CARTESIAN_POINT ( 'NONE',  ( 754.8983024940795303, -282.8965053807776258, 336.9254006560228163 ) ) ;
#13216=CARTESIAN_POINT ( 'NONE',  ( 769.0155153010367712, -130.3726999360621619, 362.7791456095907279 ) ) ;
#13217=CARTESIAN_POINT ( 'NONE',  ( 805.1927285166397041, 7.183579159761247723, 341.8018195045277707 ) ) ;
#13220=CARTESIAN_POINT ( 'NONE',  ( 814.8207195650702488, -218.1908817542437191, 336.2433038121456548 ) ) ;
#13225=CARTESIAN_POINT ( 'NONE',  ( 745.7998596910086917, -53.36187538569310362, 332.5602148656461168 ) ) ;
#13226=CARTESIAN_POINT ( 'NONE',  ( 795.1526350630804245, -452.9681489794450044, 359.9976132353968410 ) ) ;
#13229=CARTESIAN_POINT ( 'NONE',  ( 793.5525998758768083, -319.0999726633342561, 372.6845335610516941 ) ) ;
#13231=CARTESIAN_POINT ( 'NONE',  ( 749.2812353651451076, -294.4527844766013800, 323.2262854647983090 ) ) ;
#13235=CARTESIAN_POINT ( 'NONE',  ( 802.1676090361156639, -398.6346026584193396, 327.8955696845344505 ) ) ;
#13236=CARTESIAN_POINT ( 'NONE',  ( 790.9844846989617508, -166.3726999360620198, 317.2208543904092721 ) ) ;
#13238=CARTESIAN_POINT ( 'NONE',  ( 751.2241431872005251, -64.16923265350563099, 359.9636004259367610 ) ) ;
#13239=CARTESIAN_POINT ( 'NONE',  ( 759.7806653035535192, -366.9982390220557136, 324.8639956371181370 ) ) ;
#13242=CARTESIAN_POINT ( 'NONE',  ( 795.1360043628807261, -428.0891481129644944, 360.2193346964456282 ) ) ;
#13246=CARTESIAN_POINT ( 'NONE',  ( 788.7366044899766848, -203.9073299311471885, 316.5762568750059813 ) ) ;
#13247=CARTESIAN_POINT ( 'NONE',  ( 774.6858677611749044, -201.7255117493290015, 315.5713283507209894 ) ) ;
#13251=CARTESIAN_POINT ( 'NONE',  ( 778.2165204200184689, -382.8164208402374697, 364.9363028652563230 ) ) ;
#13255=CARTESIAN_POINT ( 'NONE',  ( 751.6929314249750860, -102.9982390220565662, 318.8095938919659034 ) ) ;
#13261=CARTESIAN_POINT ( 'NONE',  ( 775.9200461376533440, -191.8055962898689017, 315.3028492785443291 ) ) ;
#13267=CARTESIAN_POINT ( 'NONE',  ( 779.9999999999992042, -462.9681489794448339, 339.9999999999999432 ) ) ;
#13268=CARTESIAN_POINT ( 'NONE',  ( 799.9999999999993179, 166.4563064324884465, 319.9999999999999432 ) ) ;
#13270=CARTESIAN_POINT ( 'NONE',  ( 762.1177392798416577, -90.55451811788041994, 309.8865473780659272 ) ) ;
#13278=CARTESIAN_POINT ( 'NONE',  ( 769.0155153010367712, -442.3726999360611103, 362.7791456095907279 ) ) ;
#13285=CARTESIAN_POINT ( 'NONE',  ( 764.1737431748507561, -226.3726999360617924, 371.6461892240376415 ) ) ;
#13287=CARTESIAN_POINT ( 'NONE',  ( 767.6429770376289525, -201.1800572038744690, 306.8695393053162093 ) ) ;
#13290=CARTESIAN_POINT ( 'NONE',  ( 768.0187753319979720, -272.6346026584196807, 318.0580252608186242 ) ) ;
#13292=CARTESIAN_POINT ( 'NONE',  ( 801.5560724626406000, -72.55451811788049099, 326.7756240680316182 ) ) ;
#13296=CARTESIAN_POINT ( 'NONE',  ( 772.3691319403857278, -95.26014174441461080, 315.8894580844506663 ) ) ;
#13297=CARTESIAN_POINT ( 'NONE',  ( 774.6312213355099630, -311.3618753856922581, 364.6798772138717482 ) ) ;
#13301=CARTESIAN_POINT ( 'NONE',  ( 785.3141322388236176, -45.72551174932949181, 364.4286716492789537 ) ) ;
#13304=CARTESIAN_POINT ( 'NONE',  ( 795.6651683502461765, -394.7146871989591546, 371.3240766477733814 ) ) ;
#13306=CARTESIAN_POINT ( 'NONE',  ( 755.0636971347428243, -292.2709662947831930, 341.7834795799807353 ) ) ;
#13309=CARTESIAN_POINT ( 'NONE',  ( 774.6312213355099630, -359.3618753856920875, 364.6798772138717482 ) ) ;
#13316=CARTESIAN_POINT ( 'NONE',  ( 778.1981804954714335, -106.2709662947838467, 314.8072714833589885 ) ) ;
#13317=CARTESIAN_POINT ( 'NONE',  ( 796.1575198192839480, -414.0090635724249637, 359.4546378042384163 ) ) ;
#13318=CARTESIAN_POINT ( 'NONE',  ( 804.9511171171677688, -101.8055962898691718, 335.8780910478229202 ) ) ;
#13320=LINE ( 'NONE', #20685, #9285 ) ;
#13321=CARTESIAN_POINT ( 'NONE',  ( 812.6845335610512393, -367.9874144716865203, 353.5525998758768651 ) ) ;
#13325=CARTESIAN_POINT ( 'NONE',  ( 811.0346526505616112, -446.6346026584189985, 323.0537975583477532 ) ) ;
#13331=CARTESIAN_POINT ( 'NONE',  ( 783.0745993439762742, -344.1908817542433212, 365.1016975059196739 ) ) ;
#13333=CARTESIAN_POINT ( 'NONE',  ( 814.4686193811664907, -315.2817908451525000, 346.2056067578752732 ) ) ;
#13337=CARTESIAN_POINT ( 'NONE',  ( 797.8822607201568644, -126.5545181178803205, 370.1134526219340160 ) ) ;
#13343=CARTESIAN_POINT ( 'NONE',  ( 765.0180583372156207, -192.9982390220562820, 360.0135310231089534 ) ) ;
#13345=CARTESIAN_POINT ( 'NONE',  ( 814.2805881961230625, -433.6454272087884760, 331.2368401574024119 ) ) ;
#13348=CARTESIAN_POINT ( 'NONE',  ( 757.4527132478984868, -40.37269993606240348, 329.1273215169538844 ) ) ;
#13351=CARTESIAN_POINT ( 'NONE',  ( 757.2208543904082489, -424.7146871989589840, 350.9844846989624330 ) ) ;
#13355=CARTESIAN_POINT ( 'NONE',  ( 813.2346286133761168, -269.2601417444139997, 328.9521613784389160 ) ) ;
#13356=CARTESIAN_POINT ( 'NONE',  ( 759.9864689768902508, -74.08914811296577341, 354.9819416627836404 ) ) ;
#13359=CARTESIAN_POINT ( 'NONE',  ( 759.7806653035534055, -270.9982390220561115, 324.8639956371180801 ) ) ;
#13366=CARTESIAN_POINT ( 'NONE',  ( 792.1044303154645831, -300.4527844766012663, 317.8323909638837677 ) ) ;
#13368=CARTESIAN_POINT ( 'NONE',  ( 763.2262854647970016, -344.6346026584195101, 309.2812353651462445 ) ) ;
#13369=CARTESIAN_POINT ( 'NONE',  ( 812.6845335610512393, -247.9874144716867761, 353.5525998758768651 ) ) ;
#13370=CARTESIAN_POINT ( 'NONE',  ( 811.6461892240364477, -52.71468719896020616, 324.1737431748509835 ) ) ;
#13374=CARTESIAN_POINT ( 'NONE',  ( 804.4286716492782716, -233.3618753856925423, 345.3141322388244703 ) ) ;
#13376=CARTESIAN_POINT ( 'NONE',  ( 763.2262854647970016, -344.6346026584195101, 309.2812353651462445 ) ) ;
#13379=CARTESIAN_POINT ( 'NONE',  ( 764.4978033197144214, 16.45630643248849267, 320.3127214678681867 ) ) ;
#13382=CARTESIAN_POINT ( 'NONE',  ( 804.1105419155481968, -243.8272453906072030, 347.6308680596136469 ) ) ;
#13383=CARTESIAN_POINT ( 'NONE',  ( 778.2165204200184689, -118.8164208402383508, 364.9363028652563230 ) ) ;
#13388=CARTESIAN_POINT ( 'NONE',  ( 760.5453621957607311, -285.0783235625958127, 323.8424801807151425 ) ) ;
#13391=CARTESIAN_POINT ( 'NONE',  ( 766.4474001241216001, 4.900027336664720679, 307.3154664389482491 ) ) ;
#13395=CARTESIAN_POINT ( 'NONE',  ( 810.7187646348534145, -90.45278447660209054, 356.7737145352016341 ) ) ;
#13396=CARTESIAN_POINT ( 'NONE',  ( 777.5031285880264704, -190.8164208402381234, 374.9108240113588408 ) ) ;
#13400=CARTESIAN_POINT ( 'NONE',  ( 811.3240766477731540, -412.3726999360612808, 355.6651683502462902 ) ) ;
#13403=CARTESIAN_POINT ( 'NONE',  ( 805.0032342141412300, -397.5436935675100472, 314.9967657858571783 ) ) ;
#13404=CARTESIAN_POINT ( 'NONE',  ( 754.9967657858570647, -25.54369356751137232, 365.0032342141425943 ) ) ;
#13406=CARTESIAN_POINT ( 'NONE',  ( 773.3843516231979720, -13.44195992623305713, 364.4086373105754433 ) ) ;
#13410=CARTESIAN_POINT ( 'NONE',  ( 803.8556311672234642, -177.6237781080507148, 365.6418435158340117 ) ) ;
#13411=CARTESIAN_POINT ( 'NONE',  ( 803.6646147819162707, 6.092670068852160448, 348.8264449731211130 ) ) ;
#13413=CARTESIAN_POINT ( 'NONE',  ( 815.1787889125755555, -174.8965053807779952, 343.7953271457877804 ) ) ;
#13417=CARTESIAN_POINT ( 'NONE',  ( 785.3687786644884454, -155.3618753856927128, 315.3201227861279676 ) ) ;
#13419=CARTESIAN_POINT ( 'NONE',  ( 785.3687786644885591, -299.3618753856923149, 315.3201227861280813 ) ) ;
#13423=CARTESIAN_POINT ( 'NONE',  ( 789.9200121543843807, -1.987414471687640294, 317.0176451133914384 ) ) ;
#13426=CARTESIAN_POINT ( 'NONE',  ( 746.8695393053151292, -245.9073299311469896, 327.6429770376306578 ) ) ;
#13427=CARTESIAN_POINT ( 'NONE',  ( 796.1575198192839480, -342.0090635724251342, 359.4546378042384163 ) ) ;
#13428=CARTESIAN_POINT ( 'NONE',  ( 798.7617431975189675, -435.6237781080499190, 323.0428371773161871 ) ) ;
#13434=CARTESIAN_POINT ( 'NONE',  ( 799.4546378042377910, -297.0783235625957559, 356.1575198192848006 ) ) ;
#13437=CARTESIAN_POINT ( 'NONE',  ( 757.4527132478984868, -136.3726999360621051, 329.1273215169538844 ) ) ;
#13438=CARTESIAN_POINT ( 'NONE',  ( 792.1044303154645831, -12.45278447660232146, 317.8323909638837677 ) ) ;
#13441=CARTESIAN_POINT ( 'NONE',  ( 805.6418435158337843, -245.4636090269709143, 363.8556311672236916 ) ) ;
#13447=CARTESIAN_POINT ( 'NONE',  ( 815.2698199232961542, -88.81642084023842187, 342.5225473063383106 ) ) ;
#13449=CARTESIAN_POINT ( 'NONE',  ( 796.3364271039121149, -452.9681489794448339, 359.1033184105688747 ) ) ;
#13452=CARTESIAN_POINT ( 'NONE',  ( 778.7629533639073998, -320.7363362996979390, 375.0009284576466371 ) ) ;
#13454=CARTESIAN_POINT ( 'NONE',  ( 808.0189434323515343, -302.0891481129650629, 319.0252816721025511 ) ) ;
#13458=CARTESIAN_POINT ( 'NONE',  ( 797.6776695296629214, -403.5436935675101608, 357.6776695296636603 ) ) ;
#13459=CARTESIAN_POINT ( 'NONE',  ( 798.5707757039680246, -149.4636090269711417, 356.7845633553585003 ) ) ;
#13462=CARTESIAN_POINT ( 'NONE',  ( 788.7631598425961101, -73.44195992623286884, 305.7194118038759143 ) ) ;
#13463=CARTESIAN_POINT ( 'NONE',  ( 804.9363028652555840, -376.2709662947829656, 338.2165204200192079 ) ) ;
#13464=DIRECTION ( 'NONE',  ( 0.000000000000000000, 1.000000000000000000, 0.000000000000000000 ) ) ;
#13466=CARTESIAN_POINT ( 'NONE',  ( 759.7806653035534055, -438.9982390220553157, 324.8639956371180801 ) ) ;
#13470=CARTESIAN_POINT ( 'NONE',  ( 803.6646147819161570, -209.9073299311470748, 348.8264449731210561 ) ) ;
#13471=CARTESIAN_POINT ( 'NONE',  ( 785.3687786644885591, -179.3618753856927128, 315.3201227861280813 ) ) ;
#13476=CARTESIAN_POINT ( 'NONE',  ( 788.8264449731200330, -405.1800572038737300, 363.6646147819171233 ) ) ;
#13477=VERTEX_POINT ( 'NONE', #44909 ) ;
#13480=CARTESIAN_POINT ( 'NONE',  ( 804.7487373415286811, -115.5436935675110988, 364.7487373415288516 ) ) ;
#13486=CARTESIAN_POINT ( 'NONE',  ( 766.7756240680305382, -206.5328690171415360, 361.5560724626415663 ) ) ;
#13487=CARTESIAN_POINT ( 'NONE',  ( 779.9999999999992042, -462.9681489794448339, 309.9999999999998863 ) ) ;
#13492=DIRECTION ( 'NONE',  ( -1.000000000000000000, 0.000000000000000000, -0.000000000000000000 ) ) ;
#13503=CARTESIAN_POINT ( 'NONE',  ( 804.1105419155481968, -435.8272453906066062, 347.6308680596136469 ) ) ;
#13504=CARTESIAN_POINT ( 'NONE',  ( 814.8207195650702488, -362.1908817542432644, 336.2433038121456548 ) ) ;
#13510=CARTESIAN_POINT ( 'NONE',  ( 800.0135310231082713, 9.910851887033969021, 325.0180583372163028 ) ) ;
#13512=CARTESIAN_POINT ( 'NONE',  ( 787.5531968255692163, 2.172754609392001601, 316.1348686366205811 ) ) ;
#13513=CARTESIAN_POINT ( 'NONE',  ( 810.4231160770870019, -216.5545181178800931, 321.9338519418446936 ) ) ;
#13515=CARTESIAN_POINT ( 'NONE',  ( 744.7301800767019131, -172.8164208402381234, 337.4774526936615757 ) ) ;
#13518=CARTESIAN_POINT ( 'NONE',  ( 795.1360043628807261, -284.0891481129650629, 360.2193346964456282 ) ) ;
#13519=CARTESIAN_POINT ( 'NONE',  ( 790.0220218866281812, -55.09997266333508747, 363.2186876482849129 ) ) ;
#13523=CARTESIAN_POINT ( 'NONE',  ( 796.7845633553578182, -129.6237781080508853, 358.5707757039688204 ) ) ;
#13524=CARTESIAN_POINT ( 'NONE',  ( 755.0636971347428243, -316.2709662947832499, 341.7834795799807353 ) ) ;
#13527=CARTESIAN_POINT ( 'NONE',  ( 803.4237431249931660, -87.18005720387481006, 331.2633955100225194 ) ) ;
#13530=CARTESIAN_POINT ( 'NONE',  ( 781.2497674668890113, -372.3510508353228374, 375.3608509340180603 ) ) ;
#13532=CARTESIAN_POINT ( 'NONE',  ( 788.7366044899766848, -275.9073299311469896, 316.5762568750059813 ) ) ;
#13534=CARTESIAN_POINT ( 'NONE',  ( 788.8264449731200330, -405.1800572038737300, 363.6646147819171233 ) ) ;
#13542=CARTESIAN_POINT ( 'NONE',  ( 781.8018195045266339, -118.2709662947837899, 365.1927285166406705 ) ) ;
#13543=CARTESIAN_POINT ( 'NONE',  ( 760.7433823573367135, -444.0090635724249069, 355.9930595647440441 ) ) ;
#13544=CARTESIAN_POINT ( 'NONE',  ( 779.4709603349208464, -96.35105083532370429, 314.7162404726379918 ) ) ;
#13546=DIRECTION ( 'NONE',  ( -1.000000000000000000, -0.000000000000000000, 0.000000000000000000 ) ) ;
#13547=CARTESIAN_POINT ( 'NONE',  ( 773.7943932421234194, -359.8055962898683333, 305.5313806188329409 ) ) ;
#13552=CARTESIAN_POINT ( 'NONE',  ( 800.9747183278959710, -444.9982390220554862, 311.9810565676471583 ) ) ;
#13559=CARTESIAN_POINT ( 'NONE',  ( 763.0428371773158460, -347.4636090269705733, 358.7617431975195359 ) ) ;
#13560=CARTESIAN_POINT ( 'NONE',  ( 802.2119215644370342, -294.0090635724253048, 367.5423716828165084 ) ) ;
#13563=CARTESIAN_POINT ( 'NONE',  ( 745.1792804349281596, -110.1908817542440033, 343.7566961878542884 ) ) ;
#13567=CARTESIAN_POINT ( 'NONE',  ( 759.7806653035534055, -198.9982390220562252, 324.8639956371180801 ) ) ;
#13570=CARTESIAN_POINT ( 'NONE',  ( 788.6739635108323228, -439.6454272087884760, 373.9316612368139090 ) ) ;
#13573=CARTESIAN_POINT ( 'NONE',  ( 755.8894580844503253, -63.82724539060779279, 332.3691319403863531 ) ) ;
#13576=CARTESIAN_POINT ( 'NONE',  ( 794.1144889064781864, -442.1692326535044231, 360.9840315886528401 ) ) ;
#13580=CARTESIAN_POINT ( 'NONE',  ( 788.7631598425961101, -265.4419599262323004, 305.7194118038759143 ) ) ;
#13581=CARTESIAN_POINT ( 'NONE',  ( 802.1676090361155502, -110.6346026584201923, 327.8955696845344505 ) ) ;
#13584=CARTESIAN_POINT ( 'NONE',  ( 774.6858677611749044, -273.7255117493288026, 315.5713283507209894 ) ) ;
#13590=CARTESIAN_POINT ( 'NONE',  ( 804.9363028652555840, -40.27096629478405987, 338.2165204200192079 ) ) ;
#13592=CARTESIAN_POINT ( 'NONE',  ( 755.2512626584698410, -367.5436935675102745, 315.2512626584710915 ) ) ;
#13593=CARTESIAN_POINT ( 'NONE',  ( 776.2433038121456548, -252.8965053807777394, 374.8207195650711014 ) ) ;
#13599=CARTESIAN_POINT ( 'NONE',  ( 804.6798772138708955, -231.7255117493288310, 334.6312213355107019 ) ) ;
#13601=CARTESIAN_POINT ( 'NONE',  ( 748.9653473494363425, -362.6346026584194533, 356.9462024416521331 ) ) ;
#13606=CARTESIAN_POINT ( 'NONE',  ( 804.4086373105744769, -217.6454272087891582, 333.3843516231986541 ) ) ;
#13607=CARTESIAN_POINT ( 'NONE',  ( 756.5762568750052424, -123.1800572038747106, 348.7366044899774238 ) ) ;
#13608=VERTEX_POINT ( 'NONE', #13268 ) ;
#13611=CARTESIAN_POINT ( 'NONE',  ( 789.9200121543843807, -289.9874144716866908, 317.0176451133914384 ) ) ;
#13615=CARTESIAN_POINT ( 'NONE',  ( 805.6418435158337843, -5.463609026971610660, 363.8556311672236916 ) ) ;
#13617=AXIS2_PLACEMENT_3D ( 'NONE', #24345, #19757, #38449 ) ;
#13618=CARTESIAN_POINT ( 'NONE',  ( 763.0537975583475827, -168.4527844766018347, 371.0346526505627480 ) ) ;
#13619=CARTESIAN_POINT ( 'NONE',  ( 792.1044303154645831, -84.45278447660206211, 317.8323909638837677 ) ) ;
#13623=CARTESIAN_POINT ( 'NONE',  ( 786.2694204179717872, -429.2817908451521021, 305.1769319972829067 ) ) ;
#13626=CARTESIAN_POINT ( 'NONE',  ( 810.7187646348534145, -402.4527844766010389, 356.7737145352016341 ) ) ;
#13627=CARTESIAN_POINT ( 'NONE',  ( 749.2812353651451076, -30.45278447660226817, 323.2262854647983090 ) ) ;
#13629=VECTOR ( 'NONE', #30537, 1000.000000000000000 ) ;
#13630=CARTESIAN_POINT ( 'NONE',  ( 802.7791456095903868, -4.714687198960358039, 329.0155153010375102 ) ) ;
#13633=CARTESIAN_POINT ( 'NONE',  ( 744.8212110874229666, -186.8965053807779668, 336.2046728542121627 ) ) ;
#13634=CARTESIAN_POINT ( 'NONE',  ( 756.5762568750052424, -3.180057203875080063, 348.7366044899774238 ) ) ;
#13635=CARTESIAN_POINT ( 'NONE',  ( 807.5423716828161105, -177.0783235625961538, 362.2119215644372048 ) ) ;
#13639=CARTESIAN_POINT ( 'NONE',  ( 758.0580252608178853, -150.4527844766018916, 328.0187753319985404 ) ) ;
#13642=CARTESIAN_POINT ( 'NONE',  ( 754.8072714833583632, -292.8164208402378108, 338.1981804954721156 ) ) ;
#13645=CARTESIAN_POINT ( 'NONE',  ( 803.8651313633788504, -5.260141744414903897, 332.4468031744301015 ) ) ;
#13650=CARTESIAN_POINT ( 'NONE',  ( 811.0346526505617248, -254.6346026584197091, 323.0537975583478101 ) ) ;
#13651=CARTESIAN_POINT ( 'NONE',  ( 804.4086373105744769, -337.6454272087888171, 333.3843516231986541 ) ) ;
#13652=CARTESIAN_POINT ( 'NONE',  ( 784.0799538623451781, -419.8055962898681059, 364.6971507214555572 ) ) ;
#13657=CARTESIAN_POINT ( 'NONE',  ( 803.8651313633788504, -341.2601417444138292, 332.4468031744301015 ) ) ;
#13660=CARTESIAN_POINT ( 'NONE',  ( 757.0176451133909268, -133.0999726633348246, 349.9200121543848354 ) ) ;
#13661=CARTESIAN_POINT ( 'NONE',  ( 788.8264449731200330, 2.819942796124898177, 363.6646147819171233 ) ) ;
#13665=LINE ( 'NONE', #20800, #18841 ) ;
#13667=CARTESIAN_POINT ( 'NONE',  ( 771.3260364891663130, -235.6454272087890729, 306.0683387631859773 ) ) ;
#13668=CARTESIAN_POINT ( 'NONE',  ( 795.9930595647434757, -195.0783235625961538, 320.7433823573372820 ) ) ;
#13670=ADVANCED_FACE ( 'NONE', ( #31035, #35189 ), #45134, .T. ) ;
#13673=CARTESIAN_POINT ( 'NONE',  ( 767.7687537140311633, -71.90732993114760063, 372.7932403749916830 ) ) ;
#13679=CARTESIAN_POINT ( 'NONE',  ( 776.2046728542105711, -356.1908817542432075, 304.8212110874238761 ) ) ;
#13681=CARTESIAN_POINT ( 'NONE',  ( 796.9462024416508257, -276.4527844766013800, 308.9653473494370246 ) ) ;
#13685=CYLINDRICAL_SURFACE ( 'NONE', #41695, 10.00000000000000888 ) ;
#13686=CARTESIAN_POINT ( 'NONE',  ( 762.1405469898971887, -409.5436935675101040, 357.8594530101015607 ) ) ;
#13687=CARTESIAN_POINT ( 'NONE',  ( 755.1538015810308480, -158.1908817542438612, 343.0433043558613804 ) ) ;
#13690=CARTESIAN_POINT ( 'NONE',  ( 783.7566961878529810, -48.89650538077840025, 305.1792804349288417 ) ) ;
#13691=CARTESIAN_POINT ( 'NONE',  ( 774.6312213355098493, -383.3618753856920875, 364.6798772138717482 ) ) ;
#13692=FACE_OUTER_BOUND ( 'NONE', #5737, .T. ) ;
#13694=CARTESIAN_POINT ( 'NONE',  ( 774.6858677611749044, -441.7255117493282910, 315.5713283507209894 ) ) ;
#13699=CARTESIAN_POINT ( 'NONE',  ( 785.3141322388236176, -237.7255117493289163, 364.4286716492789537 ) ) ;
#13700=CARTESIAN_POINT ( 'NONE',  ( 804.6798772138710092, -183.7255117493290300, 334.6312213355106451 ) ) ;
#13706=CARTESIAN_POINT ( 'NONE',  ( 803.4237431249931660, -399.1800572038738437, 331.2633955100225194 ) ) ;
#13712=CARTESIAN_POINT ( 'NONE',  ( 763.2262854647970016, -152.6346026584200786, 309.2812353651462445 ) ) ;
#13714=CARTESIAN_POINT ( 'NONE',  ( 812.6845335610512393, -199.9874144716870603, 353.5525998758768651 ) ) ;
#13720=CARTESIAN_POINT ( 'NONE',  ( 793.2243759319678702, -242.5328690171414507, 318.4439275373583200 ) ) ;
#13721=LINE ( 'NONE', #41665, #8566 ) ;
#13723=AXIS2_PLACEMENT_3D ( 'NONE', #31765, #8209, #42393 ) ;
#13731=CARTESIAN_POINT ( 'NONE',  ( 814.8207195650702488, -146.1908817542438896, 336.2433038121456548 ) ) ;
#13739=CARTESIAN_POINT ( 'NONE',  ( 805.6418435158337843, -389.4636090269704027, 363.8556311672236916 ) ) ;
#13744=CARTESIAN_POINT ( 'NONE',  ( 781.7834795799800531, 13.18357915976123174, 315.0636971347436202 ) ) ;
#13747=CARTESIAN_POINT ( 'NONE',  ( 807.2620300519052989, -264.0090635724253616, 318.0141637701419768 ) ) ;
#13749=CARTESIAN_POINT ( 'NONE',  ( 763.0537975583475827, -192.4527844766016926, 371.0346526505627480 ) ) ;
#13752=CARTESIAN_POINT ( 'NONE',  ( 804.6798772138708955, -279.7255117493288026, 334.6312213355107019 ) ) ;
#13753=CARTESIAN_POINT ( 'NONE',  ( 796.1575198192839480, -54.00906357242601530, 359.4546378042384163 ) ) ;
#13759=CARTESIAN_POINT ( 'NONE',  ( 805.0264073115434940, -126.3510508353236048, 339.4763451958999099 ) ) ;
#13760=CARTESIAN_POINT ( 'NONE',  ( 785.3141322388236176, -309.7255117493287457, 364.4286716492789537 ) ) ;
#13765=CARTESIAN_POINT ( 'NONE',  ( 774.6312213355099630, -95.36187538569294020, 364.6798772138717482 ) ) ;
#13768=CARTESIAN_POINT ( 'NONE',  ( 768.8385539511368734, -407.2601417444137155, 306.4236121716840557 ) ) ;
#13773=CARTESIAN_POINT ( 'NONE',  ( 803.6646147819161570, -425.9073299311463074, 348.8264449731210561 ) ) ;
#13776=ORIENTED_EDGE ( 'NONE', *, *, #17400, .T. ) ;
#13780=CARTESIAN_POINT ( 'NONE',  ( 795.1360043628807261, -116.0891481129656029, 360.2193346964456282 ) ) ;
#13781=CARTESIAN_POINT ( 'NONE',  ( 783.0745993439762742, -440.1908817542430370, 365.1016975059196739 ) ) ;
#13785=CARTESIAN_POINT ( 'NONE',  ( 781.2497674668890113, -348.3510508353228943, 375.3608509340180603 ) ) ;
#13791=CARTESIAN_POINT ( 'NONE',  ( 814.2805881961230625, -25.64542720878973014, 331.2368401574024119 ) ) ;
#13800=CARTESIAN_POINT ( 'NONE',  ( 804.1105419155481968, -363.8272453906068336, 347.6308680596136469 ) ) ;
#13801=CARTESIAN_POINT ( 'NONE',  ( 755.8990559732751535, -323.4636090269706301, 365.9055244015606831 ) ) ;
#13804=CARTESIAN_POINT ( 'NONE',  ( 804.1009440267234822, -119.4636090269712554, 314.0944755984392600 ) ) ;
#13808=CARTESIAN_POINT ( 'NONE',  ( 803.6646147819161570, -185.9073299311472454, 348.8264449731210561 ) ) ;
#13810=CARTESIAN_POINT ( 'NONE',  ( 783.7953271457878373, -440.1908817542430370, 375.1787889125761239 ) ) ;
#13815=CARTESIAN_POINT ( 'NONE',  ( 800.1688906516307043, 13.83076734649413098, 369.0717654672308186 ) ) ;
#13819=CARTESIAN_POINT ( 'NONE',  ( 808.7758568127978833, -316.1692326535048210, 320.0363995740631822 ) ) ;
#13820=CARTESIAN_POINT ( 'NONE',  ( 771.2633955100217236, -119.9073299311474443, 363.4237431249939618 ) ) ;
#13823=CARTESIAN_POINT ( 'NONE',  ( 797.6776695296629214, -307.5436935675104451, 357.6776695296636603 ) ) ;
#13824=CIRCLE ( 'NONE', #45298, 10.00000000000000888 ) ;
#13826=DIRECTION ( 'NONE',  ( 0.000000000000000000, 0.000000000000000000, -1.000000000000000000 ) ) ;
#13830=CARTESIAN_POINT ( 'NONE',  ( 802.1676090361156639, -38.63460265842041252, 327.8955696845344505 ) ) ;
#13832=CARTESIAN_POINT ( 'NONE',  ( 751.6929314249750860, -366.9982390220557136, 318.8095938919659034 ) ) ;
#13833=CARTESIAN_POINT ( 'NONE',  ( 756.1443688327750579, -237.6237781080505442, 314.3581564841659315 ) ) ;
#13838=CARTESIAN_POINT ( 'NONE',  ( 754.8072714833581358, -244.8164208402378961, 338.1981804954720587 ) ) ;
#13839=CARTESIAN_POINT ( 'NONE',  ( 796.9462024416508257, -396.4527844766010389, 308.9653473494370246 ) ) ;
#13845=CARTESIAN_POINT ( 'NONE',  ( 804.6971507214547046, -219.2817908451527558, 344.0799538623459739 ) ) ;
#13846=CARTESIAN_POINT ( 'NONE',  ( 755.0636971347428243, -124.2709662947837899, 341.7834795799807353 ) ) ;
#13850=CARTESIAN_POINT ( 'NONE',  ( 770.0799878456142551, -301.9874144716867477, 362.9823548866085616 ) ) ;
#13853=CARTESIAN_POINT ( 'NONE',  ( 771.3260364891663130, -19.64542720878974791, 306.0683387631859773 ) ) ;
#13855=CARTESIAN_POINT ( 'NONE',  ( 751.9810565676468741, -170.0891481129654608, 360.9747183278973921 ) ) ;
#13856=CARTESIAN_POINT ( 'NONE',  ( 804.4286716492782716, -65.36187538569306810, 345.3141322388244703 ) ) ;
#13859=CARTESIAN_POINT ( 'NONE',  ( 810.4231160770870019, -432.5545181178793541, 321.9338519418446936 ) ) ;
#13861=CARTESIAN_POINT ( 'NONE',  ( 809.6099558218720631, -452.9681489794449476, 335.1781210895659342 ) ) ;
#13862=CARTESIAN_POINT ( 'NONE',  ( 783.0433043558608688, -360.8965053807773984, 315.1538015810313027 ) ) ;
#13863=CARTESIAN_POINT ( 'NONE',  ( 763.2262854647970016, -56.63460265842036279, 309.2812353651462445 ) ) ;
#13866=CARTESIAN_POINT ( 'NONE',  ( 798.7617431975189675, -27.62377810805120149, 323.0428371773161871 ) ) ;
#13870=CARTESIAN_POINT ( 'NONE',  ( 748.3538107759620743, -160.7146871989598651, 355.8262568251490165 ) ) ;
#13871=CARTESIAN_POINT ( 'NONE',  ( 762.1405469898973024, -1.543693567511449594, 357.8594530101016176 ) ) ;
#13874=CARTESIAN_POINT ( 'NONE',  ( 758.0580252608178853, -198.4527844766017495, 328.0187753319985404 ) ) ;
#13876=CARTESIAN_POINT ( 'NONE',  ( 759.9864689768902508, -314.0891481129650629, 354.9819416627836404 ) ) ;
#13879=CARTESIAN_POINT ( 'NONE',  ( 786.6156483768007774, -49.44195992623295410, 315.5913626894246136 ) ) ;
#13882=CARTESIAN_POINT ( 'NONE',  ( 763.2262854647970016, -272.6346026584196807, 309.2812353651462445 ) ) ;
#13883=CARTESIAN_POINT ( 'NONE',  ( 757.4527132478984868, -328.3726999360615650, 329.1273215169538844 ) ) ;
#13884=CARTESIAN_POINT ( 'NONE',  ( 805.1016975059191054, -438.8965053807771710, 343.0745993439771837 ) ) ;
#13889=VERTEX_POINT ( 'NONE', #14410 ) ;
#13890=CARTESIAN_POINT ( 'NONE',  ( 758.8095938919642549, -248.0891481129651481, 311.6929314249763365 ) ) ;
#13891=CARTESIAN_POINT ( 'NONE',  ( 805.0264073115434940, -342.3510508353228943, 339.4763451958999099 ) ) ;
#13893=CARTESIAN_POINT ( 'NONE',  ( 772.4468031744293057, -129.8272453906075725, 363.8651313633793620 ) ) ;
#13894=CARTESIAN_POINT ( 'NONE',  ( 795.1360043628807261, -20.08914811296592973, 360.2193346964456282 ) ) ;
#13898=CARTESIAN_POINT ( 'NONE',  ( 760.7433823573367135, -228.0090635724254753, 355.9930595647440441 ) ) ;
#13899=CARTESIAN_POINT ( 'NONE',  ( 793.5525998758768083, -223.0999726633346256, 372.6845335610516941 ) ) ;
#13900=CARTESIAN_POINT ( 'NONE',  ( 804.9511171171677688, -173.8055962898689302, 335.8780910478229202 ) ) ;
#13904=CARTESIAN_POINT ( 'NONE',  ( 767.7687537140311633, -23.90732993114773919, 372.7932403749916830 ) ) ;
#13905=CARTESIAN_POINT ( 'NONE',  ( 745.0891759886404770, -76.27096629478394618, 342.4968714119734159 ) ) ;
#13906=LINE ( 'NONE', #3515, #29881 ) ;
#13910=CARTESIAN_POINT ( 'NONE',  ( 815.3608509340175488, -338.7363362996978822, 341.2497674668889545 ) ) ;
#13912=CARTESIAN_POINT ( 'NONE',  ( 782.5225473063381969, -310.2709662947832499, 375.2698199232970637 ) ) ;
#13917=CARTESIAN_POINT ( 'NONE',  ( 759.9864689768902508, -410.0891481129647218, 354.9819416627836404 ) ) ;
#13918=CARTESIAN_POINT ( 'NONE',  ( 766.0291762391763086, -154.9181544815165523, 360.7704444035551319 ) ) ;
#13921=CARTESIAN_POINT ( 'NONE',  ( 758.0141637701419768, -63.07832356259653750, 367.2620300519063790 ) ) ;
#13922=CARTESIAN_POINT ( 'NONE',  ( 791.9812246680005501, -404.6346026584193396, 361.9419747391813189 ) ) ;
#13924=CARTESIAN_POINT ( 'NONE',  ( 771.2633955100217236, -431.9073299311464211, 363.4237431249939618 ) ) ;
#13928=CARTESIAN_POINT ( 'NONE',  ( 765.0180583372156207, -216.9982390220562252, 360.0135310231089534 ) ) ;
#13929=CARTESIAN_POINT ( 'NONE',  ( 791.9812246680005501, -212.6346026584198796, 361.9419747391813189 ) ) ;
#13933=CARTESIAN_POINT ( 'NONE',  ( 762.1405469898971887, -409.5436935675101040, 357.8594530101015607 ) ) ;
#13936=CARTESIAN_POINT ( 'NONE',  ( 777.5031285880264704, -142.8164208402382656, 374.9108240113588408 ) ) ;
#13938=CARTESIAN_POINT ( 'NONE',  ( 811.6461892240364477, -196.7146871989598083, 324.1737431748509835 ) ) ;
#13944=CARTESIAN_POINT ( 'NONE',  ( 775.9200461376533440, -215.8055962898687881, 315.3028492785443291 ) ) ;
#13951=ORIENTED_EDGE ( 'NONE', *, *, #7772, .T. ) ;
#13953=CARTESIAN_POINT ( 'NONE',  ( 757.7880784355613741, -138.0090635724257311, 312.4576283171834916 ) ) ;
#13962=CARTESIAN_POINT ( 'NONE',  ( 768.9521613784389729, -393.8272453906067199, 373.2346286133773106 ) ) ;
#13967=CARTESIAN_POINT ( 'NONE',  ( 771.1735550268778070, 14.81994279612486309, 316.3353852180827630 ) ) ;
#13969=CARTESIAN_POINT ( 'NONE',  ( 762.1177392798416577, -258.5545181178799226, 309.8865473780659272 ) ) ;
#13971=CARTESIAN_POINT ( 'NONE',  ( 796.7737145352015204, -188.6346026584199365, 370.7187646348536987 ) ) ;
#13976=CARTESIAN_POINT ( 'NONE',  ( 803.4237431249931660, -303.1800572038740711, 331.2633955100225194 ) ) ;
#13977=CARTESIAN_POINT ( 'NONE',  ( 784.1219089521767955, -93.28179084515315367, 315.0488828828318333 ) ) ;
#13982=CARTESIAN_POINT ( 'NONE',  ( 759.2295555964440155, -136.1692326535053894, 353.9708237608231229 ) ) ;
#13983=CARTESIAN_POINT ( 'NONE',  ( 778.1981804954714335, -322.2709662947830225, 314.8072714833589885 ) ) ;
#13986=CARTESIAN_POINT ( 'NONE',  ( 778.2165204200184689, -94.81642084023843609, 364.9363028652563230 ) ) ;
#13989=CARTESIAN_POINT ( 'NONE',  ( 808.7758568127978833, -412.1692326535045936, 320.0363995740631822 ) ) ;
#13991=ORIENTED_EDGE ( 'NONE', *, *, #44755, .T. ) ;
#13992=CARTESIAN_POINT ( 'NONE',  ( 759.7806653035534055, -294.9982390220560546, 324.8639956371180801 ) ) ;
#13997=CARTESIAN_POINT ( 'NONE',  ( 771.2633955100217236, -407.9073299311465348, 363.4237431249939618 ) ) ;
#14002=CARTESIAN_POINT ( 'NONE',  ( 755.0636971347428243, -124.2709662947837899, 341.7834795799807353 ) ) ;
#14003=CARTESIAN_POINT ( 'NONE',  ( 755.8894580844503253, -423.8272453906067199, 332.3691319403863531 ) ) ;
#14004=CARTESIAN_POINT ( 'NONE',  ( 783.0433043558608688, -120.8965053807781800, 315.1538015810313027 ) ) ;
#14005=CARTESIAN_POINT ( 'NONE',  ( 787.4999999999992042, -462.9681489794447202, 270.0000000000000568 ) ) ;
#14007=CARTESIAN_POINT ( 'NONE',  ( 744.9990715423526808, -402.3510508353228374, 341.2370466360926002 ) ) ;
#14012=EDGE_CURVE ( 'NONE', #32527, #24990, #29570, .T. ) ;
#14013=CARTESIAN_POINT ( 'NONE',  ( 815.3608509340175488, -26.73633629969882008, 341.2497674668889545 ) ) ;
#14022=CARTESIAN_POINT ( 'NONE',  ( 799.2566176426618085, -384.0090635724249637, 324.0069404352559559 ) ) ;
#14024=CARTESIAN_POINT ( 'NONE',  ( 752.7379699480933368, -324.0090635724251911, 361.9858362298580232 ) ) ;
#14028=CARTESIAN_POINT ( 'NONE',  ( 814.8207195650702488, -146.1908817542438896, 336.2433038121456548 ) ) ;
#14034=CARTESIAN_POINT ( 'NONE',  ( 771.2633955100217236, -191.9073299311471885, 363.4237431249939618 ) ) ;
#14036=CARTESIAN_POINT ( 'NONE',  ( 747.6481478633932056, -445.0999726633338582, 353.4146539503763620 ) ) ;
#14041=CARTESIAN_POINT ( 'NONE',  ( 778.7502325331095108, -0.3510508353240099355, 304.6391490659818828 ) ) ;
#14043=CARTESIAN_POINT ( 'NONE',  ( 765.0180583372156207, -264.9982390220561115, 360.0135310231089534 ) ) ;
#14046=CARTESIAN_POINT ( 'NONE',  ( 776.2433038121456548, -300.8965053807775689, 374.8207195650711014 ) ) ;
#14047=CARTESIAN_POINT ( 'NONE',  ( 762.3223304703356007, -127.5436935675110561, 322.3223304703362828 ) ) ;
#14049=CARTESIAN_POINT ( 'NONE',  ( 781.8018195045266339, -310.2709662947832499, 365.1927285166406705 ) ) ;
#14055=CARTESIAN_POINT ( 'NONE',  ( 762.1405469898971887, -25.54369356751136877, 357.8594530101015607 ) ) ;
#14057=CARTESIAN_POINT ( 'NONE',  ( 812.7932403749906598, -351.1800572038740142, 327.7687537140311633 ) ) ;
#14058=CARTESIAN_POINT ( 'NONE',  ( 786.2056067578752163, -251.8055962898686744, 374.4686193811670023 ) ) ;
#14059=CARTESIAN_POINT ( 'NONE',  ( 749.8865473780648472, -68.53286901714197654, 322.1177392798429082 ) ) ;
#14063=CARTESIAN_POINT ( 'NONE',  ( 805.1927285166397041, -256.8164208402379245, 341.8018195045277707 ) ) ;
#14065=CARTESIAN_POINT ( 'NONE',  ( 808.3070685750230950, -378.9982390220555999, 361.1904061080339261 ) ) ;
#14071=CARTESIAN_POINT ( 'NONE',  ( 779.4763451958990572, -248.7363362996981380, 365.0264073115438919 ) ) ;
#14072=CARTESIAN_POINT ( 'NONE',  ( 762.3223304703356007, -127.5436935675110561, 322.3223304703362828 ) ) ;
#14076=CARTESIAN_POINT ( 'NONE',  ( 754.8983024940795303, -306.8965053807775689, 336.9254006560228163 ) ) ;
#14078=CARTESIAN_POINT ( 'NONE',  ( 813.5763878283155464, -27.82724539060790292, 351.1614460488615350 ) ) ;
#14080=CARTESIAN_POINT ( 'NONE',  ( 787.5162901302840055, -179.3618753856927128, 305.4481719005792684 ) ) ;
#14081=CARTESIAN_POINT ( 'NONE',  ( 794.9819416627830151, -84.99823902205663728, 319.9864689768909898 ) ) ;
#14084=CARTESIAN_POINT ( 'NONE',  ( 790.9844846989617508, 1.627300063937458408, 317.2208543904092721 ) ) ;
#14087=CARTESIAN_POINT ( 'NONE',  ( 784.0799538623451781, -347.8055962898683333, 364.6971507214555572 ) ) ;
#14088=CARTESIAN_POINT ( 'NONE',  ( 787.4397851343537695, -45.72551174932949181, 374.2001403089903988 ) ) ;
#14090=CARTESIAN_POINT ( 'NONE',  ( 761.2382568024794409, -39.62377810805116951, 356.9571628226838129 ) ) ;
#14094=CARTESIAN_POINT ( 'NONE',  ( 768.8385539511368734, -191.2601417444143976, 306.4236121716840557 ) ) ;
#14095=CARTESIAN_POINT ( 'NONE',  ( 803.4237431249931660, -15.18005720387504631, 331.2633955100225194 ) ) ;
#14098=CARTESIAN_POINT ( 'NONE',  ( 762.3223304703356007, -199.5436935675108430, 322.3223304703362828 ) ) ;
#14101=CARTESIAN_POINT ( 'NONE',  ( 767.8955696845334842, -312.4527844766013800, 362.1676090361161755 ) ) ;
#14102=CARTESIAN_POINT ( 'NONE',  ( 759.0860845406687076, 19.76315572498245743, 318.4906424660488256 ) ) ;
#14104=CARTESIAN_POINT ( 'NONE',  ( 776.9566956441375396, -60.89650538077837894, 364.8461984189686405 ) ) ;
#14106=CARTESIAN_POINT ( 'NONE',  ( 814.2001403089898304, -257.3618753856924286, 347.4397851343538264 ) ) ;
#14107=CARTESIAN_POINT ( 'NONE',  ( 807.5423716828161105, 14.92167643740321381, 362.2119215644372048 ) ) ;
#14110=AXIS2_PLACEMENT_3D ( 'NONE', #29184, #4691, #40929 ) ;
#14113=CARTESIAN_POINT ( 'NONE',  ( 754.9967657858570647, -289.5436935675103882, 365.0032342141425374 ) ) ;
#14115=CARTESIAN_POINT ( 'NONE',  ( 804.1601925771018387, -343.4419599262320162, 346.5483106153029098 ) ) ;
#14117=CARTESIAN_POINT ( 'NONE',  ( 787.5531968255692163, -141.8272453906075157, 316.1348686366205811 ) ) ;
#14118=CARTESIAN_POINT ( 'NONE',  ( 759.9864689768902508, -2.089148112965993231, 354.9819416627836404 ) ) ;
#14123=CARTESIAN_POINT ( 'NONE',  ( 809.0717654672305343, -244.9181544815162681, 360.1688906516309885 ) ) ;
#14124=CARTESIAN_POINT ( 'NONE',  ( 779.4709603349208464, -192.3510508353233774, 314.7162404726379918 ) ) ;
#14128=CARTESIAN_POINT ( 'NONE',  ( 767.7687537140311633, 0.09267006885218045942, 372.7932403749916830 ) ) ;
#14129=CARTESIAN_POINT ( 'NONE',  ( 801.1904061080336987, -68.08914811296575920, 368.3070685750235498 ) ) ;
#14133=CARTESIAN_POINT ( 'NONE',  ( 773.7305795820266212, -345.2817908451523863, 374.8230680027170365 ) ) ;
#14135=CARTESIAN_POINT ( 'NONE',  ( 796.7737145352015204, -332.6346026584195101, 370.7187646348536987 ) ) ;
#14139=CARTESIAN_POINT ( 'NONE',  ( 759.7806653035534055, -414.9982390220555430, 324.8639956371180801 ) ) ;
#14141=CARTESIAN_POINT ( 'NONE',  ( 769.9779781133707957, -139.0999726633348530, 316.7813123517150871 ) ) ;
#14144=CARTESIAN_POINT ( 'NONE',  ( 814.8230680027162407, -101.8055962898691718, 333.7305795820267917 ) ) ;
#14145=CARTESIAN_POINT ( 'NONE',  ( 764.8639956371174549, -416.0891481129646650, 319.7806653035542581 ) ) ;
#14147=CARTESIAN_POINT ( 'NONE',  ( 789.5670355615794733, -453.0432664090020012, 363.0970091259334822 ) ) ;
#14152=CARTESIAN_POINT ( 'NONE',  ( 801.9419747391806368, -234.4527844766016358, 351.9812246680014027 ) ) ;
#14153=CARTESIAN_POINT ( 'NONE',  ( 804.6798772138710092, -231.7255117493288594, 334.6312213355106451 ) ) ;
#14155=CARTESIAN_POINT ( 'NONE',  ( 800.1688906516307043, -442.1692326535044231, 369.0717654672308186 ) ) ;
#14158=CARTESIAN_POINT ( 'NONE',  ( 756.3353852180819104, -413.9073299311465348, 331.1735550268788302 ) ) ;
#14161=CARTESIAN_POINT ( 'NONE',  ( 812.7932403749906598, -159.1800572038746111, 327.7687537140311633 ) ) ;
#14167=CARTESIAN_POINT ( 'NONE',  ( 755.8398074228967971, -235.4419599262323857, 333.4516893846970333 ) ) ;
#14177=CARTESIAN_POINT ( 'NONE',  ( 812.3518521366052028, -121.0999726633348956, 326.5853460496235243 ) ) ;
#14183=CARTESIAN_POINT ( 'NONE',  ( 807.2620300519052989, -384.0090635724249637, 318.0141637701419768 ) ) ;
#14187=CARTESIAN_POINT ( 'NONE',  ( 759.9999999999992042, 205.0000000000000568, 350.0000000000000000 ) ) ;
#14188=CARTESIAN_POINT ( 'NONE',  ( 756.3353852180819104, -5.907329931147798696, 331.1735550268788302 ) ) ;
#14190=CARTESIAN_POINT ( 'NONE',  ( 809.0717654672305343, -244.9181544815162681, 360.1688906516309885 ) ) ;
#14192=CARTESIAN_POINT ( 'NONE',  ( 751.6929314249748586, -222.9982390220561399, 318.8095938919659034 ) ) ;
#14195=EDGE_CURVE ( 'NONE', #20161, #18157, #43224, .T. ) ;
#14196=CARTESIAN_POINT ( 'NONE',  ( 774.6858677611749044, -297.7255117493286889, 315.5713283507209894 ) ) ;
#14198=CARTESIAN_POINT ( 'NONE',  ( 804.1105419155481968, -99.82724539060768620, 347.6308680596136469 ) ) ;
#14202=CARTESIAN_POINT ( 'NONE',  ( 766.7756240680305382, -110.5328690171418629, 361.5560724626415663 ) ) ;
#14203=CARTESIAN_POINT ( 'NONE',  ( 803.6646147819161570, -353.9073299311467053, 348.8264449731210561 ) ) ;
#14206=CARTESIAN_POINT ( 'NONE',  ( 792.1044303154645831, -108.4527844766019911, 317.8323909638837677 ) ) ;
#14209=CARTESIAN_POINT ( 'NONE',  ( 778.7502325331095108, -408.3510508353227806, 304.6391490659818828 ) ) ;
#14211=CARTESIAN_POINT ( 'NONE',  ( 803.6646147819161570, -329.9073299311467053, 348.8264449731210561 ) ) ;
#14215=CARTESIAN_POINT ( 'NONE',  ( 771.1735550268778070, -393.1800572038737300, 316.3353852180827630 ) ) ;
#14221=CARTESIAN_POINT ( 'NONE',  ( 791.9812246680005501, -116.6346026584201780, 361.9419747391813189 ) ) ;
#14222=CARTESIAN_POINT ( 'NONE',  ( 784.1219089521767955, -429.2817908451521021, 315.0488828828318333 ) ) ;
#14223=CARTESIAN_POINT ( 'NONE',  ( 755.0488828828309806, -113.8055962898691149, 344.1219089521771934 ) ) ;
#14224=PLANE ( 'NONE',  #43937 ) ;
#14226=CARTESIAN_POINT ( 'NONE',  ( 758.0141637701419768, -399.0783235625955285, 367.2620300519063790 ) ) ;
#14233=CARTESIAN_POINT ( 'NONE',  ( 764.1737431748507561, -34.37269993606243901, 371.6461892240376415 ) ) ;
#14240=DIRECTION ( 'NONE',  ( -0.000000000000000000, 1.000000000000000000, -0.000000000000000000 ) ) ;
#14241=CARTESIAN_POINT ( 'NONE',  ( 793.0897708529556667, -366.5545181178795815, 361.3366627262616362 ) ) ;
#14242=CARTESIAN_POINT ( 'NONE',  ( 764.1737431748507561, -322.3726999360615082, 371.6461892240376415 ) ) ;
#14247=CARTESIAN_POINT ( 'NONE',  ( 776.2046728542105711, -140.1908817542438896, 304.8212110874238761 ) ) ;
#14250=CARTESIAN_POINT ( 'NONE',  ( 744.7301800767019131, -124.8164208402383508, 337.4774526936615757 ) ) ;
#14255=CARTESIAN_POINT ( 'NONE',  ( 778.1981804954714335, -178.2709662947835625, 314.8072714833589885 ) ) ;
#14256=CARTESIAN_POINT ( 'NONE',  ( 780.5236548040995785, 3.263663700301089765, 314.9735926884559944 ) ) ;
#14260=CARTESIAN_POINT ( 'NONE',  ( 808.7758568127978833, 19.83076734649410966, 320.0363995740631822 ) ) ;
#14264=CARTESIAN_POINT ( 'NONE',  ( 776.2433038121456548, -324.8965053807775121, 374.8207195650711014 ) ) ;
#14265=CARTESIAN_POINT ( 'NONE',  ( 778.2165204200184689, -118.8164208402383508, 364.9363028652563230 ) ) ;
#14268=EDGE_CURVE ( 'NONE', #29782, #30209, #23374, .T. ) ;
#14269=CARTESIAN_POINT ( 'NONE',  ( 759.9864689768902508, -290.0891481129650629, 354.9819416627836404 ) ) ;
#14272=CARTESIAN_POINT ( 'NONE',  ( 815.2698199232962679, -88.81642084023843609, 342.5225473063383674 ) ) ;
#14276=CARTESIAN_POINT ( 'NONE',  ( 792.1044303154645831, -12.45278447660232146, 317.8323909638837677 ) ) ;
#14279=CARTESIAN_POINT ( 'NONE',  ( 813.1304606946831655, -377.9073299311465917, 352.3570229623691716 ) ) ;
#14280=CARTESIAN_POINT ( 'NONE',  ( 812.6845335610512393, -295.9874144716866908, 353.5525998758768651 ) ) ;
#14281=EDGE_CURVE ( 'NONE', #11197, #17401, #18953, .T. ) ;
#14282=CARTESIAN_POINT ( 'NONE',  ( 786.2056067578752163, -83.80559628986920018, 374.4686193811670023 ) ) ;
#14288=CARTESIAN_POINT ( 'NONE',  ( 811.0346526505616112, -398.6346026584193396, 323.0537975583477532 ) ) ;
#14294=CARTESIAN_POINT ( 'NONE',  ( 796.1575198192839480, -270.0090635724253048, 359.4546378042384163 ) ) ;
#14296=CARTESIAN_POINT ( 'NONE',  ( 785.3141322388236176, -117.7255117493292715, 364.4286716492789537 ) ) ;
#14302=CARTESIAN_POINT ( 'NONE',  ( 776.9566956441375396, -300.8965053807775689, 364.8461984189686405 ) ) ;
#14304=CARTESIAN_POINT ( 'NONE',  ( 809.0717654672305343, -28.91815448151699286, 360.1688906516309885 ) ) ;
#14306=CARTESIAN_POINT ( 'NONE',  ( 808.3070685750230950, -186.9982390220563104, 361.1904061080339261 ) ) ;
#14307=CARTESIAN_POINT ( 'NONE',  ( 781.7834795799800531, -82.81642084023846451, 315.0636971347436202 ) ) ;
#14310=VECTOR ( 'NONE', #1222, 1000.000000000000000 ) ;
#14311=CARTESIAN_POINT ( 'NONE',  ( 752.7379699480933368, -444.0090635724249069, 361.9858362298580232 ) ) ;
#14314=CARTESIAN_POINT ( 'NONE',  ( 763.2154366446407039, -357.6237781080501463, 321.4292242960311228 ) ) ;
#14315=CARTESIAN_POINT ( 'NONE',  ( 782.4968714119720516, -34.81642084023861372, 305.0891759886411023 ) ) ;
#14317=CARTESIAN_POINT ( 'NONE',  ( 776.9566956441375396, -36.89650538077844288, 364.8461984189686405 ) ) ;
#14319=CARTESIAN_POINT ( 'NONE',  ( 798.0661480581538854, -218.5328690171414792, 309.5768839229118043 ) ) ;
#14320=CARTESIAN_POINT ( 'NONE',  ( 756.5762568750052424, -27.18005720387500901, 348.7366044899774238 ) ) ;
#14325=CARTESIAN_POINT ( 'NONE',  ( 805.1927285166397041, -184.8164208402380950, 341.8018195045277707 ) ) ;
#14327=CARTESIAN_POINT ( 'NONE',  ( 755.5713283507202505, -341.3618753856922012, 334.6858677611754729 ) ) ;
#14329=CARTESIAN_POINT ( 'NONE',  ( 779.9999999999992042, 166.4563064324884465, 329.9999999999999432 ) ) ;
#14332=CARTESIAN_POINT ( 'NONE',  ( 795.9930595647434757, -51.07832356259657303, 320.7433823573372820 ) ) ;
#14335=CARTESIAN_POINT ( 'NONE',  ( 745.0891759886404770, -268.2709662947833067, 342.4968714119734159 ) ) ;
#14336=CARTESIAN_POINT ( 'NONE',  ( 813.2346286133761168, 18.73985825558501972, 328.9521613784389160 ) ) ;
#14341=CARTESIAN_POINT ( 'NONE',  ( 792.2312462859673587, -299.9073299311468759, 307.2067596250082602 ) ) ;
#14342=VECTOR ( 'NONE', #26745, 1000.000000000000000 ) ;
#14343=CARTESIAN_POINT ( 'NONE',  ( 804.6401732501814195, -455.9581923679652391, 357.6484231659003967 ) ) ;
#14344=CARTESIAN_POINT ( 'NONE',  ( 769.1273215169530886, -334.7146871989593251, 317.4527132478988847 ) ) ;
#14347=CARTESIAN_POINT ( 'NONE',  ( 793.9708237608222134, -142.9181544815166376, 319.2295555964448681 ) ) ;
#14348=CARTESIAN_POINT ( 'NONE',  ( 757.8323909638827445, -26.63460265842045871, 352.1044303154654358 ) ) ;
#14352=CARTESIAN_POINT ( 'NONE',  ( 811.3240766477731540, -220.3726999360618208, 355.6651683502462902 ) ) ;
#14353=CARTESIAN_POINT ( 'NONE',  ( 783.0433043558608688, -192.8965053807779668, 315.1538015810313027 ) ) ;
#14355=CARTESIAN_POINT ( 'NONE',  ( 797.8594530101008786, 10.45630643248850866, 322.1405469898980982 ) ) ;
#14359=CARTESIAN_POINT ( 'NONE',  ( 815.2698199232961542, -16.81642084023866701, 342.5225473063383106 ) ) ;
#14365=CARTESIAN_POINT ( 'NONE',  ( 773.7305795820266212, -369.2817908451523294, 374.8230680027170365 ) ) ;
#14367=CARTESIAN_POINT ( 'NONE',  ( 751.9810565676468741, -338.0891481129649492, 360.9747183278973921 ) ) ;
#14371=CARTESIAN_POINT ( 'NONE',  ( 785.3141322388236176, -429.7255117493282910, 364.4286716492789537 ) ) ;
#14372=CARTESIAN_POINT ( 'NONE',  ( 754.7162404726377645, -206.7363362996982801, 339.4709603349214717 ) ) ;
#14375=CARTESIAN_POINT ( 'NONE',  ( 747.3154664389472828, -115.9874144716872877, 326.4474001241230781 ) ) ;
#14376=CARTESIAN_POINT ( 'NONE',  ( 785.3687786644885591, -419.3618753856918602, 315.3201227861280813 ) ) ;
#14378=CARTESIAN_POINT ( 'NONE',  ( 810.1134526219336749, -152.5328690171416781, 357.8822607201570349 ) ) ;
#14385=CARTESIAN_POINT ( 'NONE',  ( 781.8018195045266339, -214.2709662947834488, 365.1927285166406705 ) ) ;
#14386=CARTESIAN_POINT ( 'NONE',  ( 800.2193346964446619, -234.9982390220561683, 355.1360043628816925 ) ) ;
#14390=CARTESIAN_POINT ( 'NONE',  ( 758.0580252608178853, -414.4527844766010389, 328.0187753319985404 ) ) ;
#14393=CARTESIAN_POINT ( 'NONE',  ( 777.5031285880264704, -166.8164208402382087, 374.9108240113588408 ) ) ;
#14395=CARTESIAN_POINT ( 'NONE',  ( 761.4292242960306112, -281.4636090269706870, 323.2154366446414429 ) ) ;
#14396=ORIENTED_EDGE ( 'NONE', *, *, #14961, .T. ) ;
#14397=CARTESIAN_POINT ( 'NONE',  ( 788.7631598425961101, -193.4419599262325278, 305.7194118038759143 ) ) ;
#14404=CARTESIAN_POINT ( 'NONE',  ( 784.0799538623451781, -227.8055962898687596, 364.6971507214555572 ) ) ;
#14410=CARTESIAN_POINT ( 'NONE',  ( 787.4999999999992042, -462.9681489794447771, 309.9999999999998863 ) ) ;
#14414=CARTESIAN_POINT ( 'NONE',  ( 804.1009440267234822, -143.4636090269711701, 314.0944755984392600 ) ) ;
#14426=CARTESIAN_POINT ( 'NONE',  ( 755.0636971347428243, -4.270966294784170003, 341.7834795799807353 ) ) ;
#14427=CARTESIAN_POINT ( 'NONE',  ( 814.4686193811664907, -267.2817908451526137, 346.2056067578752732 ) ) ;
#14429=CARTESIAN_POINT ( 'NONE',  ( 792.3570229623688874, -213.1800572038743553, 373.1304606946836202 ) ) ;
#14432=CARTESIAN_POINT ( 'NONE',  ( 788.8264449731200330, -309.1800572038740711, 363.6646147819171233 ) ) ;
#14433=CARTESIAN_POINT ( 'NONE',  ( 793.0897708529556667, -78.55451811788046257, 361.3366627262616362 ) ) ;
#14434=ADVANCED_FACE ( 'NONE', ( #3200, #35521 ), #42016, .F. ) ;
#14435=CARTESIAN_POINT ( 'NONE',  ( 769.0155153010367712, -82.37269993606227558, 362.7791456095907279 ) ) ;
#14441=CARTESIAN_POINT ( 'NONE',  ( 758.6633372737375112, -164.5328690171416781, 326.9102291470432533 ) ) ;
#14442=CARTESIAN_POINT ( 'NONE',  ( 794.9819416627830151, -348.9982390220558273, 319.9864689768909898 ) ) ;
#14445=CARTESIAN_POINT ( 'NONE',  ( 759.9864689768902508, -122.0891481129656171, 354.9819416627836404 ) ) ;
#14448=CARTESIAN_POINT ( 'NONE',  ( 813.9316612368132837, -415.4419599262318457, 348.6739635108323228 ) ) ;
#14450=CARTESIAN_POINT ( 'NONE',  ( 785.3141322388236176, -333.7255117493286320, 364.4286716492789537 ) ) ;
#14452=( BOUNDED_SURFACE ( )  B_SPLINE_SURFACE ( 3, 2, ( 
 ( #6794, #44695, #23874, #13967, #10262, #3101, #13744, #37994, #16974, #31050, #17436, #45149, #13510, #27583, #41688, #10042, #31516, #28040, #785, #39833, #25252, #561, #39362, #322, #21565, #18356, #7493, #42821, #10964, #36118, #8176, #35890, #17666, #22241, #42355, #36338, #29193, #28256, #14426, #32437, #24803, #14188, #11405, #7716, #22029, #7961, #31728, #43043, #10724, #25033, #32199, #14885, #96, #21797, #14664, #4264, #28505, #35648, #28963, #4020, #11182, #39143, #4483, #38923, #25493, #7275, #21346, #35422, #3794, #43272, #17885, #42603, #39605, #31952, #18121, #18575, #32658, #1000, #15103, #28740, #11643, #25721, #43712, #25932, #9301, #12088, #26165, #12749, #33322, #16222, #43943, #40039, #1232, #26394, #1452, #19689, #43492, #19455, #8395, #44394, #8847, #40279, #40495, #33781, #4696, #1666, #11859, #8633, #22464, #22695, #12319, #36572, #36794, #9061, #4926, #1897, #15553, #19024, #40707, #33116, #5360, #22915, #29420, #15771, #16005, #37005, #5151, #19235, #32887, #29857, #15338, #33548, #30086, #12532, #5598, #44170, #26829, #29633, #26607, #23129, #37232, #2132, #30299, #40935, #23369, #18797, #19919, #34638, #14550, #3690, #13856, #3457, #45500, #37472, #35083, #24450, #3909, #42481, #18004, #32077, #20991, #213, #445, #11071, #7381, #17777, #31624, #30463, #45258, #27932, #42028, #31843, #20759, #17084, #2995, #10374, #38554, #21457, #17552, #31162, #6910, #5834, #14307, #35313, #28629, #13619, #14081, #28379, #28156, #10153, #10847, #24918, #24683, #39032, #35535, #41805, #27701, #38337, #24229, #6683, #34851, #3215, #17306, #42707, #31395, #42248, #10605, #38800, #7157, #21233, #11763, #32544, #21683, #18682, #890, #19137, #39943, #40152, #1120, #32772, #5046, #11295, #25829, #29740, #42930, #14992, #22584, #18465, #43819, #32323, #18919, #15662, #39492, #25139, #33225, #11974, #39252, #7605, #15232, #8287, #1564, #29079, #18247, #35776, #43167, #4153, #677, #11534, #4590, #14778, #28849, #8518, #25374, #7848, #29322, #29533, #25616, #36454, #36011, #21926, #36686, #33014, #39728, #4375, #8076, #43396, #15456, #4818, #22139, #36228, #22350, #1353, #43607, #26040, #44762, #37120, #16582, #37819, #41292, #16814, #30421, #40395, #44519, #26283, #5258, #36905, #22813, #2474, #34350, #33671, #8746, #30665, #19350, #26726, #6168, #9643, #12878, #33433, #2719, #20258, #34108, #5940, #1778, #9185, #23708, #5478, #13119, #44061, #9418, #23027, #12427, #27199, #26506, #26964, #2246, #15890, #23260, #23486, #41060, #30201, #40827, #29975, #44291, #40607, #33892, #2020, #20030, #30892, #5722, #12205, #8958, #12646, #19576, #37361, #37586, #16115, #19809, #16340, #24868, #27418, #41515, #21411, #10546, #20707, #10325, #6634, #44987, #41984, #31340, #10795, #3643, #38985, #7335, #27886, #7104, #35487, #17951, #14255, #24623, #38500, #6853, #6414, #34800, #3163, #38744, #27643, #23937, #9865, #17253, #45448, #38287, #13808, #28102, #3861, #20933, #24399, #35030, #41753, #3407, #45681, #17500, #31578, #14034, #17730, #13343, #42198, #38058, #20496, #34586, #2942, #17031, #31107, #10104, #21184, #45205, #13567, #35264, #31794, #163, #28322, #24180, #42423, #42663, #25321, #7557, #36641, #39434, #7788, #40098, #14942, #43553, #25560, #21634, #28575, #8021, #28801, #1304, #25092, #1066, #35716, #25990, #36180, #21868, #22090, #15400, #32021, #29026, #39206, #35956, #4095, #4323, #39674, #18192, #42879, #32720, #32267, #11026, #25781, #4540, #36400, #22303, #393, #11709, #625, #18414, #14727, #4996, #32493, #843, #8460, #43111, #11919, #18633, #11246, #11480, #15176, #29265, #29482, #43341, #39892, #8234, #22531, #4762, #18866, #32958, #14498, #19089, #16066, #26233, #22974, #40346, #8908, #26676, #5208, #12381, #23436, #19297, #16290, #29923, #33381, #9369, #1726, #19758, #9129, #43769, #30149, #30372, #37305, #37070, #33616, #1514, #5423, #15609, #40771, #40560, #26900, #19985, #12598, #27150, #8698, #19517, #44008, #1968, #5667, #15830, #12820, #26458, #44703, #29693, #12149, #41237, #44464, #44239, #23196, #33844, #33177, #2198, #41008, #30603, #37537, #13064, #9596, #5896, #34061, #23656, #37767, #2422, #16523, #22763, #36858, #13290, #27591, #10053, #17444, #34531, #30838, #2660, #24123, #41696, #45156, #20656, #34976, #28264, #13752, #34748, #27832, #2889, #38231, #6801, #6578, #31286, #13518, #24567, #42364, #24346, #6116, #10731, #44932, #24811, #17675, #16758, #20879, #27367, #41462, #45628, #41927, #10492, #42142, #20207, #31525, #9815, #3108, #23882, #34289, #17198, #45390, #14196, #10269, #31736, #38450, #38004, #6358, #3351, #16981, #21128, #20440, #13976, #31057, #103, #28047, #38684, #7042, #35212, #3587, #35898, #330, #42827, #14432, #28746, #792, #25039, #32206, #43281, #39149, #36125, #4028, #7501, #29202, #21573, #39613, #28970, #17891, #4272, #4490, #11415, #11188, #7724, #21352, #25260, #35430, #14892, #14670, #1008, #39841, #32444, #1242, #28513, #39370, #18127, #21803, #25500, #35655, #32665, #568, #18806, #3801, #31959, #15346, #18582, #18363, #43053, #7969, #38931, #22036, #15114, #4704, #11652, #32896, #29426, #25728, #8183, #43499, #11866, #22248, #36345, #7282, #42610, #10970, #1672, #29866, #37241, #8640, #4936, #22472, #43949, #15777, #19241, #40503, #9068, #2356, #33556, #8854, #1904, #22703, #12328, #26614, #26401, #5366, #33328, #44401, #16455, #44176, #25939, #30538, #19032, #44640, #37480, #36579, #36801, #40046, #5604, #23135, #8403, #33123, #16013, #2139, #22921, #43718, #30307, #19698, #12540, #12755, #26835, #29639, #1459, #26173, #12094, #15559, #40285, #5157, #37013, #33788, #19461, #30094, #16228, #40713, #40944, #9307, #23377, #5841, #19927, #34002, #34471, #6979, #27765, #27989, #34695, #20600, #38618, #44873, #45324, #17610, #30782, #2831, #10434, #6290, #31679, #20144, #6743, #3524, #27313, #13001, #21064, #45564, #27089, #41181, #3053, #41867, #35147, #20375, #6054, #9535, #16923, #23599, #37705, #31003, #38173, #2596, #34221, #42084, #16697, #13235, #6522, #17378, #45101, #24288, #23820, #41406, #24510, #20818, #13458, #9756, #27527, #17143, #3283, #38394, #41627, #37932, #9986, #24055, #31227, #13686, #13917, #10211, #31461, #34918, #29141, #4649, #18310, #28211, #32389, #14139, #38868, #24753, #10669, #36073, #22199, #21515, #42305, #4440, #7223, #14618, #25674, #43225, #740, #21294, #36290, #39787, #21984, #39559, #35372, #42768, #11596, #15053, #25200, #3747, #7442, #18744, #14371, #46, #8135, #32607, #17834, #31902, #35842, #14839, #274, #39092, #28452, #42551, #35594, #10913, #24981, #3970, #39312, #18065, #32147, #510, #28690, #11129, #7666, #18526, #21744, #11357, #4217, #28911, #42993, #7914, #25437, #949, #40224, #26345, #23085, #12486, #19192, #33070, #22412, #4878, #22870, #11816, #19643, #12041, #37184 ),
 ( #26563, #39997, #29810, #30257, #2084, #12269, #25885, #8584, #1185, #44120, #30038, #9257, #8346, #40449, #9014, #22648, #18980, #5548, #40661, #19411, #33735, #16176, #36516, #1409, #15512, #29592, #43669, #26108, #36746, #5104, #44349, #33278, #1624, #12705, #37430, #26785, #8803, #33499, #15723, #29377, #36962, #43889, #40890, #1849, #23327, #5315, #15955, #5786, #32834, #15293, #43449, #37650, #41354, #17316, #13184, #24460, #27034, #13630, #2304, #3226, #27941, #9485, #45052, #24239, #27266, #31174, #30731, #42038, #34865, #27713, #9704, #5999, #23768, #13406, #10163, #45270, #6230, #20092, #23547, #34167, #9929, #44587, #6693, #44825, #38348, #45513, #31407, #38568, #38124, #16403, #6476, #33953, #12948, #41133, #30483, #20772, #10384, #37881, #2539, #13866, #16643, #34416, #19875, #20321, #20553, #2783, #16875, #30958, #41818, #27478, #41576, #24002, #34649, #3008, #17096, #45725, #14317, #21000, #18260, #4164, #29700, #14090, #14563, #28858, #42493, #24694, #11306, #686, #39260, #39502, #7859, #10617, #31633, #7168, #38812, #42258, #28165, #35321, #21241, #14786, #3699, #17786, #32333, #12157, #42939, #28637, #7615, #28391, #3470, #458, #10859, #1520, #21692, #21938, #42716, #11080, #32554, #31851, #35785, #26240, #223, #24927, #4386, #39041, #6922, #7390, #25384, #43775, #21466, #35093, #15615, #36023, #17561, #35544, #25148, #18475, #3919, #18014, #32086, #40352, #1974, #16763, #20212, #16072, #19764, #29930, #30843, #34296, #16528, #34067, #1733, #37311, #37773, #9601, #33850, #33388, #30156, #8704, #5901, #37543, #44939, #15838, #2203, #30612, #44246, #12387, #44709, #2427, #26907, #27155, #41244, #44014, #19303, #40566, #26465, #8914, #22982, #37077, #5429, #13069, #19524, #33623, #19990, #13296, #23661, #16296, #41014, #12604, #36864, #30377, #26682, #2667, #9374, #6122, #44470, #12827, #22770, #40779, #23441, #5216, #9135, #23202, #5673, #20661, #31966, #34536, #21133, #17899, #41704, #336, #7287, #14202, #41467, #9820, #17449, #42147, #3807, #34753, #20447, #27372, #3114, #23888, #21360, #17204, #6806, #16986, #38010, #10738, #35436, #31063, #20885, #31741, #31291, #38690, #38238, #6364, #42369, #35217, #45396, #45161, #13759, #34980, #17681, #7049, #27837, #27596, #13523, #10058, #31532, #2895, #28270, #6584, #110, #24128, #24816, #41932, #45633, #10277, #13982, #24351, #38455, #3358, #28054, #38936, #10498, #24573, #3593, #43288, #42616, #4277, #4710, #22254, #39620, #10976, #18135, #29209, #32213, #22041, #11420, #25046, #32449, #18587, #7974, #21809, #18369, #28520, #35904, #39156, #43058, #25267, #15119, #39846, #28978, #18813, #7507, #797, #42833, #14897, #36133, #575, #1016, #28753, #32904, #21579, #35662, #1249, #32671, #39377, #25507, #11195, #14441, #4495, #11657, #4035, #14676, #7731, #25733, #8188, #36352, #15352, #29431, #24963, #21276, #3508, #17593, #17127, #31443, #13900, #35356, #38380, #34681, #6509, #27974, #45549, #3265, #24495, #38852, #32128, #31664, #38602, #31, #6728, #42069, #10652, #10419, #35129, #17359, #28432, #494, #28196, #9969, #14599, #3039, #28672, #21498, #20587, #20802, #24732, #31212, #45307, #3730, #14124, #14353, #256, #24038, #17818, #13668, #6959, #27749, #38159, #21043, #42289, #18047, #7204, #35576, #31886, #41851, #10196, #42530, #34899, #39076, #24274, #10895, #7425, #3954, #1167, #32590, #18728, #12023, #42751, #39772, #4200, #933, #18292, #15036, #4632, #28893, #36057, #1393, #42975, #39981, #7897, #35821, #32367, #8330, #1610, #22393, #32816, #29363, #4421, #39294, #36275, #18510, #36730, #11801, #26090, #15276, #43433, #22631, #11340, #25870, #15709, #14820, #29124, #40204, #43208, #11112, #722, #36497, #33264, #25419, #25182, #5088, #29577, #7648, #21727, #4860, #18961, #19179, #11579, #39540, #21971, #25659, #8120, #22181, #33056, #15497, #43653, #8565, #13164, #37864, #19397, #9237, #34148, #37168, #41112, #40647, #6210, #44807, #37630, #19622, #1828, #5527, #23308, #20073, #9465, #16159, #30020, #33482, #15936, #19855, #8787, #16624, #9000, #2518, #9685, #27243, #34394, #2286, #12251, #16385, #43872, #22855, #36948, #40435, #30710, #20303, #33718, #26330, #41335, #5301, #44333, #23749, #2765, #30464, #44106, #29792, #12470, #5981, #23528, #26549, #26768, #23070, #2067, #37409, #30241, #12688, #40873, #5767, #27013, #33935, #44566, #12927, #38794, #6677, #34632, #21227, #10601, #3450, #3685, #17772, #20538, #41558, #17076, #2989, #6459, #38103, #45252, #31154, #24675, #23983, #13388, #7150, #6903, #35308, #31838, #16859, #42243, #27460, #10148, #13611, #21452, #24223, #38331, #24912, #45494, #28372, #10369, #27695, #9911, #38549, #41798, #208, #20754, #31620, #34844, #10840, #20982, #3209, #35078, #14302, #30939, #13850, #17299, #31389, #27928, #42023, #24445, #17547, #45723, #42474, #14076, #28151, #39026, #7376, #35529, #45032, #4586, #39721, #28621, #886, #15228, #22133, #21918, #18459, #32069, #36006, #441, #25611, #25369, #11756, #4810, #43161, #11968, #11067, #4369, #28844, #32539, #36222, #4147, #43389, #671, #29527, #14543, #42703, #26036, #29315, #39483, #14988, #11290, #3904, #29075, #11528, #15451, #8280, #43602, #40149, #8071, #25823, #8512, #22580, #18914, #39935, #18677, #32768, #25134, #7843, #1113, #22344, #32315, #39248, #7600, #36447, #33007, #42924, #1347, #17999, #21678, #35769, #18241, #14773, #3465, #24689, #21463, #10613, #220, #14087, #39257, #42936, #39038, #20768, #25381, #45509, #11303, #32329, #31404, #17558, #35541, #39498, #28162, #42255, #28855, #3696, #683, #14314, #10380, #17313, #42488, #31630, #35782, #13862, #3916, #42034, #14783, #24924, #38808, #10855, #4160, #34859, #17783, #27938, #7164, #24456, #21238, #28386, #6917, #35318, #25145, #20997, #18011, #8363, #35090, #11077, #31848, #32083, #7387, #38563, #453, #14557, #28634, #42713, #7612, #3223, #21689, #18255, #29540, #29328, #15669, #8753, #1359, #15896, #14999, #39948, #32779, #8293, #26049, #8083, #1571, #4595, #33443, #36018, #4381, #29982, #19144, #43402, #18926, #15239, #7855, #4824, #22357, #19357, #12211, #1786, #44069, #36462, #29749, #12434, #26513, #22819, #33231, #15462, #43615, #29086, #11768, #25836, #43827, #36234, #32550, #18471, #33021, #11981, #1126, #40160, #36694, #21933, #8525, #22590, #5053, #18690, #26290, #40403, #36911, #5265, #896, #43173, #11541, #25623, #39734, #22145, #19583, #17039, #6423, #5486, #37369, #41301, #2028, #37129, #34358, #30673, #44995, #30901, #40614, #20267, #33678, #33900, #16122, #34116, #13351, #2727, #26972, #40836, #30208, #12653, #44770, #44298, #27426, #19817, #41523, #20506, #23946, #45213, #13129, #23034, #27207, #8965, #26733, #9194, #23269, #9875, #31117, #16349, #5731, #38066, #2254, #9427, #34594, #2951, #9651, #30429, #13576, #44529, #16823, #12887 ),
 ( #41069, #23494, #37594, #5948, #20039, #2483, #16591, #23716, #37827, #6178, #38990, #35271, #14260, #35038, #24189, #21191, #3414, #21638, #42429, #42669, #3649, #17736, #7563, #13815, #28328, #32273, #45455, #17508, #25097, #20942, #631, #34809, #21416, #18197, #41990, #27653, #35725, #14503, #41762, #10112, #31799, #10800, #4102, #31586, #20715, #38296, #45688, #6642, #3170, #14041, #7111, #17261, #31348, #11031, #27893, #10333, #170, #32028, #28110, #7340, #38509, #24406, #39211, #35492, #42206, #6860, #10554, #24874, #24632, #3867, #38753, #17958, #399, #28581, #18639, #35961, #4545, #22308, #848, #8027, #19095, #14948, #11924, #25567, #29031, #5002, #43118, #15408, #4768, #39441, #11714, #25995, #32963, #32725, #29271, #42884, #1073, #11252, #36405, #36185, #22537, #16231, #8239, #23380, #21873, #15182, #39679, #43348, #1309, #11487, #8467, #22095, #40947, #25326, #7797, #37483, #40103, #25785, #39897, #18872, #14733, #29487, #43558, #26838, #33184, #9310, #5844, #36646, #2142, #19930, #34005, #30310, #44404, #12759, #28806, #4329, #18419, #32498, #13690, #30785, #27092, #44643, #20378, #37935, #41409, #16927, #31232, #24514, #9990, #31007, #24059, #44876, #6293, #3058, #34475, #27531, #9759, #20822, #38623, #20604, #2359, #6983, #41184, #21068, #13921, #13004, #13238, #17147, #9538, #23602, #41871, #38177, #6748, #38398, #16458, #27769, #37708, #23824, #6057, #30541, #2835, #45105, #10439, #13462, #27993, #41631, #20148, #34224, #6525, #27316, #17382, #2599, #45328, #16700, #42088, #10215, #3287, #34699, #24292, #34923, #31464, #45569, #35598, #7671, #35376, #28916, #31906, #15059, #17614, #31683, #11600, #744, #10917, #514, #42555, #35151, #32151, #21521, #953, #39563, #29145, #43229, #18069, #42997, #25678, #8139, #4444, #14843, #28694, #42773, #42309, #24986, #39096, #11363, #17839, #14144, #50, #7446, #3975, #28456, #14622, #18314, #39791, #11133, #25205, #39315, #278, #21749, #35846, #4221, #32393, #25442, #7918, #3528, #21988, #28215, #10673, #24757, #38872, #7227, #21298, #14375, #36077, #3751, #18530, #32612, #12273, #26566, #12489, #22203, #1852, #32838, #15515, #43453, #26788, #29595, #43673, #30260, #5107, #33739, #15726, #11820, #18750, #43894, #18983, #37188, #15297, #36965, #25888, #16179, #26348, #12044, #40452, #5552, #36295, #19195, #29381, #26114, #40001, #40228, #29814, #8349, #8587, #40664, #22417, #19414, #33073, #36520, #9018, #4881, #22874, #8806, #1189, #33282, #33504, #5319, #22651, #36749, #4653, #1627, #1412, #15959, #30042, #44123, #23088, #19646, #2088, #44352, #12709, #40893, #41821, #12951, #33956, #9488, #27037, #44591, #30486, #37654, #23551, #3011, #2307, #41136, #6479, #13870, #20556, #16878, #41579, #16647, #5790, #2786, #30734, #3231, #24006, #24242, #30961, #45055, #34868, #6002, #9933, #27945, #20095, #44828, #6696, #2543, #9261, #16406, #17099, #45517, #34170, #23330, #17320, #10166, #37433, #19879, #13410, #38128, #31410, #13187, #27269, #41358, #9708, #23771, #37884, #6234, #34419, #20324, #27481, #38351, #34652, #31179, #45274, #13633, #27716, #20775, #7170, #4389, #11310, #4166, #31854, #14094, #3702, #35546, #32336, #21694, #28395, #42260, #31636, #28168, #32090, #21006, #28861, #21244, #690, #21940, #25387, #902, #14565, #24463, #28640, #10388, #35097, #3473, #6925, #14788, #18480, #17789, #38571, #42942, #17564, #10863, #36026, #39506, #42718, #3, #32558, #15005, #18262, #35789, #10620, #39044, #7862, #42042, #21468, #24697, #226, #38815, #7618, #39262, #35324, #14319, #3922, #42495, #24930, #11082, #7394, #18017, #460, #25152, #22363, #33683, #36241, #22823, #19588, #43407, #2033, #8970, #15900, #43178, #11547, #19149, #43833, #5493, #36468, #22152, #29093, #4830, #25630, #23039, #18933, #8532, #18695, #39740, #12439, #37134, #32785, #22596, #33449, #33028, #40408, #39955, #8090, #44073, #36917, #1365, #1135, #15469, #36699, #19364, #8757, #29547, #29335, #15246, #11773, #33235, #4601, #29987, #8299, #1793, #25843, #26519, #43623, #1576, #11990, #15676, #26056, #40167, #5057, #29756, #40619, #12217, #26296, #5271, #20510, #12658, #30678, #41766, #45218, #34363, #26738, #6646, #10117, #38070, #9879, #23274, #13134, #13580, #31122, #41306, #9200, #23499, #30212, #27429, #13355, #38300, #37377, #23720, #6429, #5953, #33905, #34598, #23951, #2734, #2956, #17043, #19822, #40840, #16355, #2258, #5735, #30435, #44534, #12894, #27659, #26978, #41078, #41527, #20720, #24193, #37832, #16827, #37600, #9434, #9657, #20043, #34814, #30906, #16127, #6182, #20272, #44303, #45000, #34121, #2487, #16596, #44776, #27212, #10560, #25333, #28811, #24637, #28332, #38514, #31354, #32279, #11257, #6866, #42435, #7568, #38758, #14508, #14046, #39447, #18203, #11035, #7115, #20946, #21195, #10804, #39216, #28586, #35275, #3417, #35043, #17512, #38994, #27898, #35730, #28116, #21644, #42891, #635, #7804, #21421, #45459, #35497, #17265, #41994, #10337, #13819, #4108, #21879, #3653, #24410, #14737, #31590, #17741, #3175, #45693, #3871, #42210, #31804, #173, #25101, #42672, #14264, #24879, #7344, #17963, #32032, #405, #43353, #4336, #1526, #33190, #12393, #29038, #43565, #12163, #25791, #8034, #40358, #29707, #22545, #22777, #36871, #39686, #14954, #36190, #22100, #25573, #11493, #18643, #4552, #43783, #43123, #32732, #15623, #40573, #26247, #11934, #36651, #11720, #32505, #29493, #39905, #29937, #5010, #5222, #26001, #40111, #15845, #1078, #19101, #8919, #15191, #8246, #33396, #29276, #35968, #22313, #8710, #26472, #36413, #18425, #44020, #19311, #854, #4774, #18879, #32970, #8474, #1314, #1742, #15415, #2903, #5438, #19531, #45170, #34304, #44477, #34074, #30385, #22989, #19996, #9381, #34543, #27380, #16994, #31070, #5907, #30852, #13530, #41711, #38018, #2676, #16537, #30620, #30162, #12834, #26914, #16771, #5680, #1980, #33630, #41022, #23448, #16302, #37549, #6129, #27604, #44717, #2435, #13078, #19771, #27163, #23668, #41251, #9607, #37781, #41476, #37082, #20220, #16078, #44253, #12612, #26689, #40786, #9143, #33857, #44948, #23211, #37322, #13304, #9828, #23898, #6373, #2211, #20455, #20669, #3365, #31298, #14683, #17457, #31540, #18142, #38698, #21587, #3602, #45404, #6591, #31748, #6814, #25053, #3122, #24824, #13768, #4044, #14209, #45641, #119, #39165, #10067, #7057, #17211, #13989, #27845, #28061, #17689, #41939, #42154, #14448, #10284, #7294, #20892, #24358, #345, #38462, #10746, #28277, #34760, #21141, #21369, #42378, #10505, #24581, #38246, #35224, #34990, #38944, #35445, #17906, #10984, #3814, #32222, #31974, #582, #35669, #28528, #42623, #7515, #28760, #24135, #36359, #29217, #32914, #1257, #42840, #4718, #39386, #25514, #4284, #36595, #39628, #7982, #8417, #18594, #25950, #15128, #18375, #7740, #43297, #28985, #43512 ),
 ( #39854, #11664, #21818, #32678, #18822, #25740, #22049, #4502, #25276, #36140, #35911, #8195, #1025, #15360, #29438, #22262, #22485, #32455, #11879, #11428, #40057, #11204, #803, #14903, #43066, #18298, #20806, #34906, #14826, #3959, #14128, #3735, #35, #38384, #35360, #24741, #4206, #42755, #32376, #729, #21282, #499, #28900, #11347, #7654, #18052, #31890, #262, #45553, #28200, #42294, #32134, #21051, #17363, #3271, #10658, #38858, #31668, #7209, #21503, #42981, #14359, #17823, #28439, #35134, #42538, #39082, #10902, #24968, #7430, #11118, #6732, #35581, #31449, #13904, #27978, #21732, #14606, #42073, #10422, #24499, #28678, #25187, #38607, #39299, #35829, #6966, #3513, #17597, #32823, #39548, #36737, #22640, #1838, #18517, #33063, #1617, #15284, #43213, #29802, #19185, #12032, #12258, #26339, #29129, #4429, #25665, #11587, #15043, #939, #8126, #39778, #33271, #32596, #22189, #5095, #30029, #15716, #1400, #26100, #1175, #21976, #18970, #29369, #19404, #40212, #40442, #15504, #29584, #5308, #36282, #8575, #44113, #4638, #43440, #22862, #18736, #25425, #11808, #43881, #15947, #25877, #7905, #33490, #8794, #36062, #39990, #43660, #36955, #8338, #22401, #36505, #4868, #19862, #35260, #38110, #33942, #37637, #2074, #40654, #41563, #21180, #16166, #5988, #16864, #2294, #23756, #23315, #3639, #27465, #20309, #16392, #30248, #30471, #20080, #2772, #37870, #44575, #12695, #44340, #26775, #2527, #37176, #45040, #37419, #30945, #6465, #9917, #17726, #30719, #9007, #44814, #26556, #5535, #19632, #23077, #13395, #31789, #12934, #33727, #23988, #40881, #27022, #12477, #41121, #9245, #9474, #23536, #5776, #34155, #16631, #13171, #27252, #34402, #41343, #9692, #6218, #11475, #39428, #7784, #7331, #21629, #4091, #25555, #28570, #24864, #42418, #18187, #35712, #39202, #14723, #29022, #22299, #21862, #28797, #35952, #42659, #32262, #839, #620, #25316, #7553, #18629, #36396, #18410, #159, #4758, #38981, #18862, #11705, #10789, #11022, #14938, #21407, #35482, #39669, #4318, #4536, #36176, #14250, #8017, #3856, #42875, #17947, #28318, #11242, #32489, #8230, #43106, #25777, #22086, #32017, #389, #32716, #25088, #15171, #14491, #1062, #29260, #39888, #43337, #22759, #8904, #2195, #32952, #29919, #40094, #36854, #8455, #5205, #40556, #19083, #26228, #37302, #33173, #30146, #43765, #1510, #23193, #15605, #33612, #22971, #11915, #44004, #44236, #5420, #19293, #1723, #15396, #33378, #29477, #37067, #8694, #40768, #33841, #26455, #41005, #22526, #15827, #12145, #12378, #19513, #29689, #26671, #40342, #12817, #43549, #25986, #9365, #12594, #1964, #16063, #36636, #16287, #23433, #4991, #9126, #5663, #19755, #30368, #44460, #37534, #26897, #5893, #1298, #37764, #27364, #13515, #10266, #45386, #6352, #20203, #9593, #6113, #10048, #44699, #6798, #44929, #24343, #45624, #3347, #24564, #38228, #2418, #6574, #34058, #13060, #27147, #30599, #38447, #42138, #41459, #16518, #20876, #41234, #34528, #13971, #17440, #20653, #23653, #10489, #28044, #41922, #13749, #34283, #16978, #31521, #34973, #45153, #2656, #9812, #16754, #31283, #17195, #38680, #30835, #27588, #19982, #23879, #13287, #37999, #27827, #34745, #20436, #2886, #31054, #41692, #24117, #3105, #42360, #28261, #35426, #7279, #788, #100, #10728, #4268, #11647, #18359, #14667, #39366, #14429, #3584, #565, #28509, #1004, #21800, #22032, #28743, #42824, #32661, #38928, #7720, #25724, #24807, #42607, #4486, #326, #7038, #14192, #14888, #43276, #21349, #21124, #15108, #39608, #35208, #17671, #11185, #35893, #29196, #10967, #3797, #31732, #25036, #17888, #31956, #39146, #32202, #7497, #21568, #43048, #35652, #4023, #18124, #11409, #25256, #32440, #28966, #36121, #25496, #7965, #18578, #19692, #16008, #33550, #1236, #36796, #37235, #9063, #19237, #32891, #1455, #8179, #5362, #37008, #16224, #15342, #1668, #30090, #29635, #11862, #44172, #1899, #26397, #26609, #40709, #43495, #18801, #40042, #25935, #29423, #8399, #22467, #36575, #12535, #4930, #19027, #19457, #44396, #23131, #15773, #40498, #15555, #36341, #33324, #43714, #33784, #8849, #5600, #29860, #43945, #2135, #33119, #22917, #12751, #12090, #26168, #30302, #40281, #39837, #8635, #22244, #4700, #22698, #5153, #12323, #13681, #40938, #9303, #16919, #41623, #3279, #20139, #19923, #26831, #34216, #17373, #6739, #2591, #6284, #16450, #23372, #10207, #34913, #30534, #20371, #31223, #16692, #38169, #37701, #31457, #41862, #34691, #30778, #44633, #44869, #34466, #45320, #6518, #13231, #27084, #12997, #41177, #30999, #5837, #27760, #6050, #38390, #20814, #45559, #37476, #45096, #33998, #13454, #2351, #9531, #23595, #9752, #2827, #27308, #41402, #27523, #23816, #9980, #37927, #24050, #20596, #3049, #13912, #18523, #38614, #36070, #25434, #24506, #10665, #14613, #21059, #10429, #7662, #3966, #18306, #4213, #27985, #39307, #6974, #7218, #35143, #32604, #21290, #35367, #21981, #42545, #39556, #7437, #3520, #17605, #35590, #24748, #28908, #31674, #28686, #42, #7911, #18061, #3742, #32142, #42989, #42080, #10909, #14135, #17830, #28207, #31898, #21510, #42301, #270, #32384, #38864, #11125, #14367, #28447, #736, #24977, #42764, #506, #39088, #25194, #21740, #35837, #14835, #11353, #4435, #18977, #29137, #22645, #22410, #8800, #1845, #40222, #9012, #8133, #33068, #25883, #1407, #19190, #1181, #40446, #43447, #26561, #43220, #11593, #23083, #12266, #36514, #12038, #8344, #946, #43667, #15510, #12483, #5313, #40659, #37181, #29590, #22868, #5544, #19638, #15953, #26343, #8581, #36743, #22195, #4875, #26106, #36960, #29375, #25671, #39784, #5102, #33276, #39995, #1622, #29807, #15049, #15721, #19409, #43887, #33496, #36288, #30036, #44118, #4647, #11814, #18742, #32831, #15291, #23544, #27030, #2535, #16872, #10160, #41351, #16640, #9701, #16400, #37647, #34411, #5996, #13180, #41129, #6473, #24236, #6226, #33732, #38345, #12702, #6690, #45267, #44346, #30480, #2780, #40887, #30254, #27475, #23765, #38120, #23998, #2081, #13403, #26782, #9481, #9254, #16173, #20089, #34164, #41814, #30728, #13626, #27261, #23322, #37426, #37878, #44583, #3003, #5783, #30954, #19872, #27710, #20318, #44822, #45048, #17091, #33950, #41573, #2301, #9925, #12944, #20549, #34646, #31170, #36733, #2070, #29580, #40650, #8569, #43656, #33721, #12027, #44109, #33486, #22397, #40438, #9003, #15940, #15712, #12254, #25873, #29797, #39985, #19400, #33267, #5530, #44336, #36951, #5770, #4864, #43875, #22635, #26334, #30024, #26094, #37172, #40207, #23311, #8333, #36500, #19858, #23073, #1613, #8790, #5091, #43436, #22858, #5304, #9240, #16162, #37414, #33938, #1832, #19627, #2290, #16388, #12691, #12473, #30244, #26552, #26771, #40877, #11804, #18965, #33059, #1396, #15500, #41802, #2992, #2769, #45036, #12930, #16862, #27017, #6463, #6214 ),
 ( #34847, #10371, #42025, #13391, #38334, #24447, #3453, #45496, #10151, #23986, #38107, #37633, #20306, #34398, #24226, #13167, #9469, #41116, #30942, #27463, #23752, #41561, #13615, #6906, #20541, #9915, #34635, #27247, #17080, #31157, #45255, #27698, #37867, #3211, #20985, #6680, #30467, #35080, #23531, #44570, #38551, #5984, #41338, #20756, #20076, #34151, #17302, #31391, #13853, #27930, #2522, #16627, #30714, #44810, #9688, #22136, #10842, #39028, #25613, #443, #29077, #11069, #7152, #14078, #39250, #14304, #32541, #10603, #32319, #38796, #11530, #21680, #7378, #7602, #888, #17549, #14546, #24679, #21454, #21230, #35531, #25136, #3687, #24915, #21921, #28153, #7845, #39724, #3906, #40078, #36009, #42245, #32072, #43164, #14990, #35771, #35310, #8073, #36224, #39486, #11292, #17774, #28624, #31622, #31840, #42705, #210, #18001, #28375, #28846, #14775, #42477, #4149, #18244, #4372, #673, #42926, #18461, #25371, #36902, #37116, #5475, #8282, #29317, #4813, #22347, #39939, #25826, #33011, #18916, #44056, #43392, #36450, #1774, #9181, #15885, #12201, #5255, #11970, #1116, #43815, #26037, #44287, #19346, #19571, #26280, #40392, #30197, #1351, #33430, #23256, #15454, #40150, #2016, #43604, #4588, #11759, #12424, #40824, #29529, #18679, #12643, #33667, #32770, #15230, #8743, #29972, #26723, #8514, #22581, #36683, #5043, #19134, #33222, #1560, #29736, #15659, #22810, #16112, #26503, #40604, #8955, #23024, #44757, #2938, #2470, #45443, #6629, #45201, #27194, #9414, #13115, #30888, #27639, #17025, #23703, #37583, #26958, #23482, #27414, #16337, #24175, #16577, #41747, #17249, #20703, #41980, #9861, #19806, #23933, #5718, #30418, #44515, #34795, #13563, #41287, #5937, #9639, #44982, #10100, #31102, #37815, #20027, #41057, #34104, #41511, #12875, #38283, #30659, #3158, #31336, #13804, #10321, #38052, #33889, #6410, #2242, #6164, #20254, #34345, #27882, #37357, #2714, #16808, #13337, #20492, #34580, #4316, #7782, #42657, #20928, #14936, #18408, #618, #18185, #31574, #21405, #21859, #39426, #3854, #17496, #31787, #38496, #35710, #21627, #837, #45676, #32014, #14721, #14247, #42192, #28795, #32260, #11020, #11240, #25314, #28097, #3402, #24617, #10541, #14028, #38738, #7098, #21178, #42873, #35258, #3637, #4088, #29020, #35950, #387, #25086, #157, #35026, #17945, #28316, #32487, #39200, #43104, #14489, #28568, #24393, #17724, #7551, #6848, #42416, #10787, #24862, #38979, #7329, #35480, #5203, #1962, #25775, #16061, #37064, #44002, #25553, #39666, #1506, #26226, #33610, #4756, #4534, #11473, #18860, #30144, #5418, #32950, #36634, #1060, #8015, #40554, #19511, #15169, #4989, #15825, #1296, #22757, #22297, #22084, #18627, #40340, #32714, #36174, #15603, #15394, #33171, #26453, #29258, #8453, #43335, #29474, #11702, #43547, #19081, #39886, #11913, #29917, #8228, #8692, #36394, #25984, #1721, #40092, #12143, #29687, #22524, #43763, #36852, #19290, #33376, #12376, #8902, #22969, #26669, #20201, #19980, #6350, #45151, #37762, #6572, #5661, #30597, #23431, #44697, #16752, #44458, #37997, #41003, #24115, #40766, #9124, #20651, #9810, #34056, #9591, #5891, #44234, #41232, #13058, #10046, #2884, #38226, #34743, #27145, #20434, #3103, #17193, #13513, #23877, #6111, #34281, #19753, #2416, #16516, #34526, #26895, #23191, #37300, #23651, #2654, #37532, #30833, #27362, #12592, #44927, #13285, #41457, #9363, #16976, #31052, #27586, #41690, #33839, #2193, #16285, #30366, #12815, #35891, #10264, #7718, #42822, #41920, #28042, #31954, #38445, #27825, #25034, #21347, #35650, #21566, #31281, #10965, #24341, #24562, #6796, #4266, #38678, #7036, #39364, #14190, #11183, #24805, #20874, #34971, #7277, #42136, #563, #21122, #45384, #42605, #28507, #21798, #3345, #38926, #7495, #35206, #17438, #4021, #39144, #17886, #18122, #32200, #31519, #45622, #13969, #10487, #3582, #17669, #31730, #98, #14665, #28259, #42358, #28741, #13747, #25254, #35424, #324, #10726, #3795, #14427, #39834, #12321, #33117, #33323, #40040, #25933, #43944, #4484, #4928, #22916, #36119, #8177, #15772, #11645, #37006, #25494, #12089, #8848, #32659, #18357, #26396, #5152, #32438, #786, #8397, #1453, #40497, #25722, #11407, #14886, #22242, #28964, #43046, #36339, #43493, #7963, #39606, #1667, #22030, #18576, #11860, #22697, #4698, #29634, #29194, #1002, #29859, #26167, #18799, #15106, #32889, #22465, #8634, #43713, #1233, #43274, #15340, #29421, #36573, #19025, #19236, #15554, #36795, #40280, #34464, #9978, #23593, #33549, #37698, #19456, #44171, #30088, #16007, #41400, #27520, #26830, #1898, #9749, #12534, #19920, #30996, #2825, #6048, #26608, #41621, #45094, #27306, #44867, #40708, #2349, #16917, #20369, #30532, #9062, #13229, #6283, #44631, #13452, #23130, #37474, #30301, #5835, #20137, #5599, #23814, #2133, #24048, #37234, #19691, #5361, #16690, #40937, #16448, #12750, #33783, #12995, #33996, #16223, #37925, #44395, #9302, #27082, #23370, #41175, #9529, #34214, #30776, #2589, #40, #45317, #13910, #42078, #3740, #20812, #17138, #34689, #10427, #27983, #31455, #6972, #21288, #14611, #14133, #21057, #28205, #34911, #24504, #38863, #38612, #17603, #45557, #10907, #28684, #10663, #38167, #42761, #31221, #11123, #3964, #3047, #3277, #7215, #13679, #27758, #31896, #42299, #42543, #28445, #6516, #17828, #41860, #35140, #10205, #20594, #3518, #31672, #504, #24746, #18059, #35365, #24282, #38388, #268, #17370, #7435, #6737, #14365, #24974, #32140, #39086, #21508, #35588, #40219, #25192, #22193, #32382, #29135, #734, #15047, #32829, #11351, #18521, #29588, #25432, #22406, #36067, #39554, #15508, #7909, #25880, #15289, #4211, #36286, #36512, #43445, #43218, #39782, #7660, #11591, #21738, #1179, #944, #32601, #39305, #4873, #18975, #2248, #18303, #29373, #1405, #25669, #42987, #43664, #33066, #11812, #12036, #26104, #28906, #14832, #21979, #4433, #8130, #4643, #18740, #39993, #9187, #8341, #23262, #37363, #30423, #5724, #19811, #33894, #16343, #35835, #44522, #34352, #6855, #27645, #27887, #34588, #20498, #38503, #44764, #45207, #17502, #30667, #2721, #10327, #6171, #31580, #20033, #6636, #3409, #27201, #12880, #20937, #45450, #26966, #41062, #2944, #41756, #35032, #20260, #5942, #9420, #16816, #23488, #37588, #30894, #38060, #2477, #34110, #41985, #16584, #13121, #6416, #17256, #44989, #24182, #23710, #41295, #24401, #20709, #13345, #9645, #27420, #17033, #3165, #38289, #41517, #37821, #9869, #23939, #31111, #13570, #13810, #10106, #31342, #34803, #29027, #4541, #18193, #28104, #32268, #14036, #38747, #24627, #10548, #35957, #22091, #21412, #42201, #4324, #7106, #14499, #25561, #43114, #626, #21186, #36181, #39675, #21869, #39437, #35265, #42664, #11482, #14944, #25093, #3644, #14728, #17731, #8022, #4097, #35488, #21635, #18635, #45683, #11027, #31795 ),
 ( #35719, #3863, #7790, #844, #39207, #165, #14256, #32024, #24869, #394, #28802, #28324, #18415, #42424, #10796, #38986, #7336, #17952, #11248, #28576, #7559, #42880, #25322, #32494, #19090, #44240, #37072, #12599, #26677, #15610, #40561, #40772, #5668, #1969, #44009, #26234, #40347, #39893, #8462, #36642, #12382, #15401, #11710, #29266, #4997, #22532, #25991, #1515, #15832, #9130, #8699, #29694, #22764, #29483, #33178, #33383, #43770, #12151, #40099, #5424, #23197, #5209, #32721, #37306, #25782, #1069, #15177, #43342, #43554, #1727, #8235, #22304, #26459, #36859, #19519, #22975, #36401, #8909, #4764, #19298, #18867, #32959, #29924, #33617, #1305, #16067, #11920, #30150, #9370, #16291, #41463, #16524, #34749, #12821, #6359, #33845, #26902, #44466, #30373, #10054, #41928, #41239, #2199, #24124, #41009, #34291, #45391, #3110, #38005, #23437, #10270, #13753, #41698, #13519, #37538, #16759, #17199, #31287, #44933, #5897, #27151, #19986, #31059, #16982, #24347, #34062, #27368, #38232, #9597, #2423, #6579, #27592, #20441, #20657, #27833, #30605, #44704, #13065, #23657, #37768, #6117, #20208, #2661, #38451, #30839, #13292, #45157, #19759, #9816, #23883, #34532, #2890, #3353, #7283, #17676, #42828, #14433, #32208, #35431, #21353, #28747, #10494, #331, #39371, #42143, #31737, #570, #3588, #7725, #45629, #25040, #6802, #7044, #20880, #11189, #14671, #17445, #31526, #31960, #42611, #34977, #42365, #38686, #13977, #24812, #28048, #24568, #28515, #21574, #10733, #104, #21129, #35213, #3802, #25262, #14198, #39150, #28265, #7502, #38932, #17893, #10971, #35656, #4030, #18129, #41605, #38373, #27742, #34449, #2571, #37686, #20125, #38152, #27071, #34893, #27293, #6721, #27967, #31436, #6952, #20580, #30516, #21036, #34201, #23800, #45542, #41387, #2335, #9515, #41845, #38595, #16677, #16435, #42063, #3259, #44618, #12983, #6501, #17121, #24488, #9735, #41164, #23581, #37912, #6033, #10412, #6266, #27507, #30763, #44854, #13893, #13216, #20353, #9962, #20796, #2812, #13660, #16903, #30984, #17351, #10189, #45081, #13437, #24032, #34676, #3033, #24265, #31206, #45302, #24724, #7198, #25176, #14117, #21965, #14347, #39533, #15030, #18505, #39766, #7642, #17587, #21721, #3501, #28190, #42283, #25, #25413, #11572, #10889, #31658, #7890, #10645, #3946, #29118, #32584, #35814, #38845, #25653, #43201, #11334, #28887, #21269, #32121, #926, #4413, #14593, #35348, #42523, #3724, #716, #32360, #8114, #17812, #42744, #36051, #24956, #31878, #35123, #42967, #4193, #250, #28424, #39070, #7418, #21492, #35569, #18041, #486, #28666, #11106, #39287, #18286, #14814, #19390, #26762, #33477, #29787, #8782, #29572, #18722, #15702, #43648, #16154, #36943, #37163, #43866, #12246, #2062, #8324, #22850, #30236, #5296, #5521, #26325, #40430, #44328, #22388, #1823, #40868, #39975, #12017, #19617, #15492, #22174, #29356, #15931, #12683, #36492, #36269, #4625, #8995, #32809, #1162, #30015, #44101, #15270, #26085, #43428, #11796, #40199, #25865, #4855, #8560, #1605, #18955, #33051, #33713, #1388, #22624, #12465, #26544, #36725, #40642, #5083, #19174, #33259, #23063, #44802, #27008, #16619, #2760, #45246, #34627, #41331, #9460, #44561, #41107, #45028, #33930, #41793, #34142, #13606, #34839, #38326, #13845, #27455, #37405, #41552, #23303, #2281, #16380, #19849, #27689, #31384, #30706, #5762, #10143, #30457, #23744, #3203, #6672, #9905, #12922, #45488, #17294, #31149, #2984, #23523, #6205, #20747, #24218, #34389, #37625, #13159, #5976, #20533, #6454, #27923, #20067, #16854, #9231, #27238, #2513, #9680, #17071, #23978, #37856, #20298, #30934, #13382, #38099, #45718, #31615, #17541, #24670, #42238, #35763, #35073, #14071, #39242, #881, #7595, #3899, #28616, #3680, #38544, #35523, #17767, #42469, #14538, #10594, #4142, #38788, #21914, #24439, #6896, #18456, #21671, #31832, #7371, #203, #42018, #39021, #28367, #7839, #666, #36001, #4365, #24907, #18235, #32535, #14984, #11285, #32310, #17992, #32064, #3445, #14294, #10835, #14767, #7144, #20976, #28144, #21447, #436, #35303, #42698, #25129, #10364, #11062, #28839, #42919, #21222, #25362, #39479, #18910, #8507, #22340, #1767, #5469, #1554, #29069, #33661, #8067, #19564, #40599, #39717, #25819, #29732, #36218, #25607, #22804, #19130, #33425, #19340, #43157, #8738, #22129, #36441, #4582, #2010, #4805, #33003, #37111, #11963, #8948, #22576, #18673, #32762, #5038, #39931, #44050, #1109, #43811, #15224, #23018, #33218, #1342, #15652, #12418, #11524, #26032, #29311, #15447, #43385, #29523, #36678, #11752, #43597, #15878, #8275, #26275, #40143, #12195, #29967, #40387, #36897, #5251, #26499, #13109, #27408, #34338, #34098, #30654, #44281, #2465, #12638, #37810, #37576, #23926, #17021, #9634, #24170, #23248, #16569, #41051, #37351, #26717, #9856, #6159, #20488, #6405, #16107, #41505, #40818, #9408, #5712, #20699, #23476, #5931, #38279, #44751, #27632, #23698, #19799, #9171, #20247, #12868, #31098, #33883, #30881, #2236, #10095, #2709, #20022, #16802, #45197, #30191, #27190, #16331, #41281, #30413, #44977, #13331, #44508, #38047, #34574, #26951, #2934, #13559, #41742, #6624, #34790, #3848, #38974, #27877, #152, #14483, #21400, #21173, #17718, #31330, #35253, #45438, #24857, #24612, #11014, #4079, #42408, #11235, #10317, #3631, #28092, #31781, #35474, #3398, #42652, #45670, #28790, #13800, #41974, #25308, #28562, #38729, #14241, #10536, #3153, #28310, #10780, #14714, #7545, #42868, #39420, #7324, #25081, #7774, #21852, #18179, #39195, #17940, #32008, #24388, #7092, #379, #21621, #31570, #38492, #6844, #35705, #32255, #42186, #613, #17244, #20924, #35020, #17492, #14022, #18622, #39882, #36629, #25770, #29468, #29253, #8687, #12371, #8448, #35944, #40546, #14932, #26447, #1715, #833, #32709, #4983, #43331, #11464, #8896, #11697, #8223, #43995, #18854, #15819, #43541, #25548, #32483, #11908, #1055, #5198, #29015, #19076, #39661, #29909, #40087, #22292, #25979, #19283, #4311, #32945, #43098, #36388, #22078, #4750, #22518, #36169, #1290, #40335, #4530, #33165, #15161, #1501, #26219, #15599, #29681, #43759, #12137, #22751, #36846, #33370, #18403, #37525, #5409, #40994, #19505, #44689, #44449, #30826, #23869, #16507, #31045, #30137, #9355, #2186, #23424, #41226, #23184, #16744, #19746, #2877, #33602, #1954, #45144, #34273, #12806, #34049, #30357, #22963, #19973, #5884, #34518, #27355, #16968, #13503, #2406, #44920, #27577, #42292, #37986, #2647, #30588, #13048, #44225, #26887, #27137, #13278, #5653, #16055, #12583, #9583, #23643, #16278, #37754, #6103, #37057, #20193, #41450, #9801, #33833, #6341, #20425, #26660, #40757, #9115, #37292, #32819, #28897, #10654, #15280, #35358, #1171, #22185, #21279, #7427, #11344, #17820, #7206, #4425, #725, #15040, #936, #24736, #36060, #3732, #35825 ),
 ( #3956, #32131, #18733, #39296, #36278, #4203, #259, #31888, #32372, #21500, #25662, #14355, #25422, #28435, #4635, #14823, #496, #42978, #39775, #38854, #7651, #42533, #14602, #10897, #28674, #18295, #24965, #18049, #29126, #39079, #7901, #35578, #42753, #43211, #11115, #39544, #21974, #25184, #21730, #18513, #32593, #11583, #8123, #29366, #25570, #35727, #29274, #29035, #15412, #8471, #1076, #15620, #14735, #39683, #32502, #8031, #25789, #7801, #1312, #4333, #33187, #4105, #18200, #29704, #18876, #43121, #18641, #14951, #7565, #4548, #22098, #19098, #11929, #1523, #43779, #36188, #29490, #12160, #26244, #22541, #32967, #15188, #43351, #28809, #11490, #32729, #43562, #35966, #32276, #633, #11717, #39903, #851, #8242, #36410, #21641, #22311, #4771, #25998, #18422, #40108, #36649, #5007, #42888, #11255, #25330, #39445, #21876, #44714, #20216, #6126, #23207, #2432, #34300, #13301, #9604, #5904, #33854, #2208, #1738, #16075, #44250, #19993, #22986, #19307, #36868, #12610, #30159, #33627, #9139, #23445, #16768, #16299, #37319, #30382, #37080, #26686, #41019, #40783, #19768, #1978, #13075, #30849, #12831, #40355, #44945, #33393, #8707, #2673, #5219, #5434, #9379, #15842, #29934, #34070, #44474, #27160, #30617, #22774, #16534, #44017, #5677, #12390, #26469, #26910, #37546, #40570, #41248, #8917, #23665, #19528, #37777, #3362, #24132, #42373, #20452, #42151, #2900, #21366, #31537, #17208, #17454, #10742, #27377, #24355, #34540, #31295, #16991, #45400, #34986, #13527, #20666, #31745, #27600, #24577, #38243, #41708, #17686, #10064, #28058, #45638, #6370, #38459, #38695, #13986, #13765, #41936, #9825, #27842, #23894, #10502, #3118, #35221, #28274, #20889, #35442, #31067, #10281, #6588, #6810, #7054, #34757, #21138, #3599, #7291, #38015, #45165, #3811, #116, #14206, #24821, #38941, #17903, #31970, #341, #41472, #36527, #23093, #43678, #26571, #8592, #4040, #10981, #36756, #11201, #30047, #7512, #29820, #35666, #9023, #19200, #4886, #5111, #44129, #14445, #12049, #21583, #18988, #18139, #33080, #22658, #579, #7736, #19419, #14680, #12279, #25273, #28757, #5324, #42837, #15731, #33287, #39162, #26121, #26354, #1632, #1417, #29600, #42620, #15520, #25050, #43901, #40235, #22879, #15966, #40458, #37193, #32218, #8811, #39383, #36971, #33511, #21815, #1858, #12494, #40668, #5559, #19651, #33745, #28525, #23557, #13194, #9494, #2095, #44833, #34176, #13639, #6484, #27722, #41826, #30739, #9940, #10171, #20780, #17104, #13417, #41366, #9713, #9265, #37659, #6008, #27487, #30491, #26793, #44357, #20101, #2548, #41141, #16653, #30966, #24249, #23777, #27274, #37890, #44596, #6242, #2792, #20330, #34425, #16884, #20564, #38357, #45061, #16184, #6703, #40898, #30265, #12713, #23333, #12956, #41584, #37437, #5797, #24011, #38133, #34658, #3018, #19883, #31186, #45280, #33960, #2312, #16411, #27043, #34874, #42265, #11314, #14792, #10625, #14325, #24469, #17327, #18267, #42946, #38576, #28402, #39266, #24702, #465, #8, #25391, #4172, #42723, #38822, #6930, #7176, #42500, #25156, #14569, #21249, #35101, #21013, #3478, #24934, #13874, #21698, #14098, #7622, #28865, #32340, #39511, #7398, #31414, #21472, #3237, #27950, #42046, #45521, #35794, #7867, #35329, #10393, #696, #17568, #3707, #31640, #28172, #35550, #17793, #31859, #230, #11086, #28645, #10868, #39049, #3926, #18021, #32098, #15010, #29338, #36031, #33239, #19153, #44078, #29097, #29551, #43838, #11777, #39745, #26300, #15680, #8535, #8761, #22828, #25634, #906, #22156, #8095, #11552, #43183, #4604, #36245, #29761, #18699, #32789, #1580, #26524, #12222, #43626, #22600, #43410, #18485, #15473, #25848, #15906, #36703, #36922, #11994, #26060, #1797, #1140, #5061, #40623, #15249, #39957, #19369, #8303, #21945, #22367, #40411, #12444, #36471, #4394, #29991, #5276, #32562, #4833, #18936, #33453, #33031, #1369, #40171, #33689, #5957, #20276, #27216, #26984, #23502, #37140, #41083, #5498, #30683, #30438, #16832, #9883, #2492, #17046, #16131, #9437, #33909, #37604, #41310, #9205, #2738, #5739, #34602, #19592, #2038, #31125, #34368, #44539, #20046, #16358, #8974, #34125, #16599, #20513, #13359, #2959, #45222, #44782, #30910, #13584, #27664, #23954, #45004, #13138, #9660, #30218, #12898, #23724, #27433, #37381, #44308, #12662, #37837, #6186, #2261, #41531, #38075, #23042, #6434, #26742, #40844, #19826, #23280, #42439, #31593, #21198, #35047, #14512, #18206, #14269, #41771, #638, #20724, #32283, #7571, #6650, #38518, #10808, #3179, #38303, #35500, #31808, #408, #32037, #10120, #21424, #34817, #3422, #17269, #14740, #17517, #45696, #4113, #24642, #21648, #35278, #31357, #45463, #17744, #6870, #11038, #13823, #24883, #27901, #35734, #176, #14049, #28337, #25104, #24196, #38761, #41997, #28119, #10340, #42214, #3656, #24414, #10565, #28590, #20950, #38997, #7118, #7347, #3874, #17967, #42675, #39219, #7807, #39451, #19106, #5226, #4558, #11260, #33193, #25336, #43360, #8715, #12167, #1318, #21884, #19316, #22781, #5015, #22550, #35974, #25794, #26250, #43786, #8250, #4339, #36194, #42894, #40115, #26005, #33399, #18429, #36417, #1529, #18648, #858, #15625, #36654, #15420, #29709, #40362, #32509, #14958, #29044, #43129, #11497, #25577, #39692, #8039, #36876, #22105, #32738, #8479, #1745, #28814, #4779, #29497, #1083, #15197, #22316, #29282, #11725, #43569, #39909, #18882, #32975, #11938, #1985, #2440, #20461, #33633, #37326, #13309, #9148, #34549, #22993, #9613, #6380, #30167, #15849, #41481, #2682, #29940, #44023, #5910, #30626, #38024, #23217, #8923, #12396, #5686, #26475, #9834, #19777, #41025, #5442, #40577, #44953, #23903, #19537, #9385, #20225, #33861, #27169, #26694, #37086, #30858, #23674, #2214, #16083, #16307, #23452, #6134, #41257, #30390, #44257, #12616, #40790, #20000, #44482, #16778, #12839, #34312, #26920, #27386, #37552, #34077, #16543, #44722, #13085, #37786, #38704, #27609, #45648, #14215, #21147, #20898, #17463, #31075, #34996, #45174, #24587, #24364, #10753, #3822, #42159, #10991, #10072, #3372, #27851, #31545, #35229, #3128, #42384, #45411, #28534, #13534, #41716, #25059, #28284, #38467, #13997, #10289, #2908, #28065, #10511, #14456, #7300, #42629, #39171, #7064, #24830, #7521, #21595, #17912, #38950, #3608, #17695, #24143, #6820, #31756, #21375, #31304, #38252, #6597, #125, #35451, #41948, #31980, #351, #16999, #20675, #34766, #17217, #13773, #39632, #36364, #25519, #15134, #28989, #8422, #12111, #8200, #35675, #40306, #14690, #26191, #1474, #588, #32459, #4725, #42845, #32228, #29444, #25746, #40062, #25955, #4051, #15364, #28766, #43070, #11209, #8658, #11435, #7987, #43733, #18598, #15574, #29225, #25281, #39392, #11669, #807, #4956, #7745, #18828, #21822, #29656, #39859, #22054, #22267, #19048, #18149, #32684, #35916, #36144 ) ),
 .UNSPECIFIED., .T., .F., .T. ) 
 B_SPLINE_SURFACE_WITH_KNOTS ( ( 4, 3, 4 ),
 ( 3, 2, 2, 2, 2, 2, 2, 2, 2, 2, 2, 2, 2, 2, 2, 2, 2, 2, 2, 2, 2, 2, 2, 2, 2, 2, 2, 2, 2, 2, 2, 2, 2, 2, 2, 2, 2, 2, 2, 2, 2, 2, 2, 2, 2, 2, 2, 2, 2, 2, 2, 2, 2, 2, 2, 2, 2, 2, 2, 2, 2, 2, 2, 2, 2, 2, 2, 2, 2, 2, 2, 2, 2, 2, 2, 2, 2, 2, 2, 2, 2, 2, 2, 2, 2, 2, 2, 2, 2, 2, 2, 2, 2, 2, 2, 2, 2, 2, 2, 2, 2, 2, 2, 2, 2, 2, 2, 2, 2, 2, 2, 2, 2, 2, 2, 2, 2, 2, 2, 2, 2, 2, 2, 2, 2, 2, 2, 2, 2, 2, 2, 2, 2, 2, 2, 2, 2, 2, 2, 2, 2, 2, 2, 2, 2, 2, 2, 2, 2, 2, 2, 2, 2, 2, 2, 2, 2, 2, 2, 2, 2, 2, 2, 2, 2, 2, 2, 2, 2, 2, 2, 2, 2, 2, 2, 2, 2, 2, 2, 2, 2, 2, 2, 2, 2, 2, 2, 2, 2, 2, 2, 2, 2, 2, 2, 2, 2, 2, 2, 2, 2, 2, 2, 2, 2, 2, 2, 2, 2, 2, 2, 2, 2, 2, 2, 2, 2, 2, 2, 2, 2, 2, 2, 2, 2, 2, 2, 2, 2, 2, 2, 2, 2, 2, 2, 2, 2, 2, 2, 2, 2, 2, 2, 2, 2, 2, 2, 2, 2, 2, 2, 2, 2, 2, 2, 2, 2, 2, 2, 2, 2, 2, 2, 2, 2, 2, 2, 2, 2, 2, 2, 2, 2, 2, 2, 2, 2, 2, 2, 2, 2, 2, 2, 2, 2, 2, 2, 2, 2, 2, 2, 2, 2, 2, 2, 2, 2, 2, 2, 2, 2, 2, 2, 2, 2, 2, 2, 2, 2, 2, 2, 2, 2, 2, 2, 2, 2, 2, 2, 2, 2, 2, 2, 2, 2, 2, 2, 2, 2, 2, 2, 2, 2, 2, 2, 2, 2, 2, 2, 2, 2, 2, 2, 2, 2, 2, 2, 2, 2, 2, 2, 2, 2, 2, 2, 2, 2, 2, 2, 2, 2, 2, 2, 2, 2, 2, 2, 2, 2, 2, 2, 2, 2, 2, 2, 2, 2, 2, 2, 2, 2, 2, 2, 2, 2, 2, 2, 2, 2, 2, 2, 2, 2, 2, 2, 2, 2, 2, 2, 2, 2, 2, 2, 2, 2, 2, 2, 2, 2, 2, 2, 2, 2, 2, 2, 2, 2, 2, 2, 2, 2, 2, 2, 2, 2, 2, 2, 2, 2, 2, 2, 3 ),
 ( 0.000000000000000000, 0.5000000000000000000, 1.000000000000000000 ),
 ( 0.000000000000000000, 0.002272727272727272617, 0.004545454545454545234, 0.006818181818181817851, 0.009090909090909090468, 0.01136363636363636395, 0.01363636363636363570, 0.01590909090909090745, 0.01818181818181818094, 0.02045454545454545442, 0.02272727272727272790, 0.02500000000000000139, 0.02727272727272727140, 0.02954545454545454489, 0.03181818181818181490, 0.03409090909090908839, 0.03636363636363636187, 0.03863636363636363535, 0.04090909090909090884, 0.04318181818181818232, 0.04545454545454545581, 0.04772727272727272929, 0.05000000000000000278, 0.05227272727272726932, 0.05454545454545454281, 0.05681818181818181629, 0.05909090909090908977, 0.06136363636363636326, 0.06363636363636362980, 0.06590909090909090329, 0.06818181818181817677, 0.07045454545454545026, 0.07272727272727272374, 0.07499999999999999722, 0.07727272727272727071, 0.07954545454545454419, 0.08181818181818181768, 0.08409090909090909116, 0.08636363636363636465, 0.08863636363636363813, 0.09090909090909091161, 0.09318181818181818510, 0.09545454545454545858, 0.09772727272727273207, 0.1000000000000000056, 0.1022727272727272790, 0.1045454545454545386, 0.1068181818181818121, 0.1090909090909090856, 0.1113636363636363591, 0.1136363636363636326, 0.1159090909090909061, 0.1181818181818181795, 0.1204545454545454530, 0.1227272727272727265, 0.1250000000000000000, 0.1272727272727272596, 0.1295454545454545470, 0.1318181818181818066, 0.1340909090909090939, 0.1363636363636363535, 0.1386363636363636409, 0.1409090909090909005, 0.1431818181818181879, 0.1454545454545454475, 0.1477272727272727348, 0.1499999999999999944, 0.1522727272727272818, 0.1545454545454545414, 0.1568181818181818288, 0.1590909090909090884, 0.1613636363636363757, 0.1636363636363636354, 0.1659090909090909227, 0.1681818181818181823, 0.1704545454545454419, 0.1727272727272727293, 0.1749999999999999889, 0.1772727272727272763, 0.1795454545454545359, 0.1818181818181818232, 0.1840909090909090828, 0.1863636363636363702, 0.1886363636363636298, 0.1909090909090909172, 0.1931818181818181768, 0.1954545454545454641, 0.1977272727272727237, 0.2000000000000000111, 0.2022727272727272707, 0.2045454545454545581, 0.2068181818181818177, 0.2090909090909090773, 0.2113636363636363646, 0.2136363636363636243, 0.2159090909090909116, 0.2181818181818181712, 0.2204545454545454586, 0.2227272727272727182, 0.2250000000000000056, 0.2272727272727272652, 0.2295454545454545525, 0.2318181818181818121, 0.2340909090909090995, 0.2363636363636363591, 0.2386363636363636465, 0.2409090909090909061, 0.2431818181818181934, 0.2454545454545454530, 0.2477272727272727404, 0.2500000000000000000, 0.2522727272727272596, 0.2545454545454545192, 0.2568181818181818343, 0.2590909090909090939, 0.2613636363636363535, 0.2636363636363636131, 0.2659090909090909283, 0.2681818181818181879, 0.2704545454545454475, 0.2727272727272727071, 0.2750000000000000222, 0.2772727272727272818, 0.2795454545454545414, 0.2818181818181818010, 0.2840909090909091161, 0.2863636363636363757, 0.2886363636363636354, 0.2909090909090908950, 0.2931818181818181546, 0.2954545454545454697, 0.2977272727272727293, 0.2999999999999999889, 0.3022727272727272485, 0.3045454545454545636, 0.3068181818181818232, 0.3090909090909090828, 0.3113636363636363424, 0.3136363636363636576, 0.3159090909090909172, 0.3181818181818181768, 0.3204545454545454364, 0.3227272727272727515, 0.3250000000000000111, 0.3272727272727272707, 0.3295454545454545303, 0.3318181818181818454, 0.3340909090909091050, 0.3363636363636363646, 0.3386363636363636243, 0.3409090909090908839, 0.3431818181818181990, 0.3454545454545454586, 0.3477272727272727182, 0.3499999999999999778, 0.3522727272727272929, 0.3545454545454545525, 0.3568181818181818121, 0.3590909090909090717, 0.3613636363636363869, 0.3636363636363636465, 0.3659090909090909061, 0.3681818181818181657, 0.3704545454545454808, 0.3727272727272727404, 0.3750000000000000000, 0.3772727272727272596, 0.3795454545454545192, 0.3818181818181818343, 0.3840909090909090939, 0.3863636363636363535, 0.3886363636363636131, 0.3909090909090909283, 0.3931818181818181879, 0.3954545454545454475, 0.3977272727272727071, 0.4000000000000000222, 0.4022727272727272818, 0.4045454545454545414, 0.4068181818181818010, 0.4090909090909091161, 0.4113636363636363757, 0.4136363636363636354, 0.4159090909090908950, 0.4181818181818181546, 0.4204545454545454697, 0.4227272727272727293, 0.4249999999999999889, 0.4272727272727272485, 0.4295454545454545636, 0.4318181818181818232, 0.4340909090909090828, 0.4363636363636363424, 0.4386363636363636576, 0.4409090909090909172, 0.4431818181818181768, 0.4454545454545454364, 0.4477272727272727515, 0.4500000000000000111, 0.4522727272727272707, 0.4545454545454545303, 0.4568181818181818454, 0.4590909090909091050, 0.4613636363636363646, 0.4636363636363636243, 0.4659090909090908839, 0.4681818181818181990, 0.4704545454545454586, 0.4727272727272727182, 0.4749999999999999778, 0.4772727272727272929, 0.4795454545454545525, 0.4818181818181818121, 0.4840909090909090717, 0.4863636363636363869, 0.4886363636363636465, 0.4909090909090909061, 0.4931818181818181657, 0.4954545454545454808, 0.4977272727272727404, 0.5000000000000000000, 0.5022727272727273151, 0.5045454545454545192, 0.5068181818181818343, 0.5090909090909090384, 0.5113636363636363535, 0.5136363636363636687, 0.5159090909090908728, 0.5181818181818181879, 0.5204545454545455030, 0.5227272727272727071, 0.5250000000000000222, 0.5272727272727272263, 0.5295454545454545414, 0.5318181818181818565, 0.5340909090909090606, 0.5363636363636363757, 0.5386363636363636909, 0.5409090909090908950, 0.5431818181818182101, 0.5454545454545454142, 0.5477272727272727293, 0.5500000000000000444, 0.5522727272727272485, 0.5545454545454545636, 0.5568181818181817677, 0.5590909090909090828, 0.5613636363636363980, 0.5636363636363636020, 0.5659090909090909172, 0.5681818181818182323, 0.5704545454545454364, 0.5727272727272727515, 0.5749999999999999556, 0.5772727272727272707, 0.5795454545454545858, 0.5818181818181817899, 0.5840909090909091050, 0.5863636363636363091, 0.5886363636363636243, 0.5909090909090909394, 0.5931818181818181435, 0.5954545454545454586, 0.5977272727272727737, 0.5999999999999999778, 0.6022727272727272929, 0.6045454545454544970, 0.6068181818181818121, 0.6090909090909091272, 0.6113636363636363313, 0.6136363636363636465, 0.6159090909090909616, 0.6181818181818181657, 0.6204545454545454808, 0.6227272727272726849, 0.6250000000000000000, 0.6272727272727273151, 0.6295454545454545192, 0.6318181818181818343, 0.6340909090909090384, 0.6363636363636363535, 0.6386363636363636687, 0.6409090909090908728, 0.6431818181818181879, 0.6454545454545455030, 0.6477272727272727071, 0.6500000000000000222, 0.6522727272727272263, 0.6545454545454545414, 0.6568181818181818565, 0.6590909090909090606, 0.6613636363636363757, 0.6636363636363636909, 0.6659090909090908950, 0.6681818181818182101, 0.6704545454545454142, 0.6727272727272727293, 0.6750000000000000444, 0.6772727272727272485, 0.6795454545454545636, 0.6818181818181817677, 0.6840909090909090828, 0.6863636363636363980, 0.6886363636363636020, 0.6909090909090909172, 0.6931818181818182323, 0.6954545454545454364, 0.6977272727272727515, 0.6999999999999999556, 0.7022727272727272707, 0.7045454545454545858, 0.7068181818181817899, 0.7090909090909091050, 0.7113636363636363091, 0.7136363636363636243, 0.7159090909090909394, 0.7181818181818181435, 0.7204545454545454586, 0.7227272727272727737, 0.7249999999999999778, 0.7272727272727272929, 0.7295454545454544970, 0.7318181818181818121, 0.7340909090909091272, 0.7363636363636363313, 0.7386363636363636465, 0.7409090909090909616, 0.7431818181818181657, 0.7454545454545454808, 0.7477272727272726849, 0.7500000000000000000, 0.7522727272727273151, 0.7545454545454545192, 0.7568181818181818343, 0.7590909090909090384, 0.7613636363636363535, 0.7636363636363636687, 0.7659090909090908728, 0.7681818181818181879, 0.7704545454545455030, 0.7727272727272727071, 0.7750000000000000222, 0.7772727272727272263, 0.7795454545454545414, 0.7818181818181818565, 0.7840909090909090606, 0.7863636363636363757, 0.7886363636363636909, 0.7909090909090908950, 0.7931818181818182101, 0.7954545454545454142, 0.7977272727272727293, 0.8000000000000000444, 0.8022727272727272485, 0.8045454545454545636, 0.8068181818181817677, 0.8090909090909090828, 0.8113636363636363980, 0.8136363636363636020, 0.8159090909090909172, 0.8181818181818182323, 0.8204545454545454364, 0.8227272727272727515, 0.8249999999999999556, 0.8272727272727272707, 0.8295454545454545858, 0.8318181818181817899, 0.8340909090909091050, 0.8363636363636363091, 0.8386363636363636243, 0.8409090909090909394, 0.8431818181818181435, 0.8454545454545454586, 0.8477272727272727737, 0.8499999999999999778, 0.8522727272727272929, 0.8545454545454544970, 0.8568181818181818121, 0.8590909090909091272, 0.8613636363636363313, 0.8636363636363636465, 0.8659090909090909616, 0.8681818181818181657, 0.8704545454545454808, 0.8727272727272726849, 0.8750000000000000000, 0.8772727272727273151, 0.8795454545454545192, 0.8818181818181818343, 0.8840909090909090384, 0.8863636363636363535, 0.8886363636363636687, 0.8909090909090908728, 0.8931818181818181879, 0.8954545454545455030, 0.8977272727272727071, 0.9000000000000000222, 0.9022727272727272263, 0.9045454545454545414, 0.9068181818181818565, 0.9090909090909090606, 0.9113636363636363757, 0.9136363636363636909, 0.9159090909090908950, 0.9181818181818182101, 0.9204545454545454142, 0.9227272727272727293, 0.9250000000000000444, 0.9272727272727272485, 0.9295454545454545636, 0.9318181818181817677, 0.9340909090909090828, 0.9363636363636363980, 0.9386363636363636020, 0.9409090909090909172, 0.9431818181818182323, 0.9454545454545454364, 0.9477272727272727515, 0.9499999999999999556, 0.9522727272727272707, 0.9545454545454545858, 0.9568181818181817899, 0.9590909090909091050, 0.9613636363636363091, 0.9636363636363636243, 0.9659090909090909394, 0.9681818181818181435, 0.9704545454545454586, 0.9727272727272727737, 0.9749999999999999778, 0.9772727272727272929, 0.9781254700864303597 ),
 .UNSPECIFIED. ) 
 GEOMETRIC_REPRESENTATION_ITEM ( )  RATIONAL_B_SPLINE_SURFACE ( (
 ( 1.000000000000000000, 0.9898214418809326842, 1.000000000000000000, 0.9898214418809326842, 1.000000000000000000, 0.9898214418809326842, 1.000000000000000000, 0.9898214418809326842, 1.000000000000000000, 0.9898214418809326842, 1.000000000000000000, 0.9898214418809326842, 1.000000000000000000, 0.9898214418809326842, 1.000000000000000000, 0.9898214418809326842, 1.000000000000000000, 0.9898214418809326842, 1.000000000000000000, 0.9898214418809326842, 1.000000000000000000, 0.9898214418809326842, 1.000000000000000000, 0.9898214418809326842, 1.000000000000000000, 0.9898214418809326842, 1.000000000000000000, 0.9898214418809326842, 1.000000000000000000, 0.9898214418809326842, 1.000000000000000000, 0.9898214418809326842, 1.000000000000000000, 0.9898214418809326842, 1.000000000000000000, 0.9898214418809326842, 1.000000000000000000, 0.9898214418809326842, 1.000000000000000000, 0.9898214418809326842, 1.000000000000000000, 0.9898214418809326842, 1.000000000000000000, 0.9898214418809326842, 1.000000000000000000, 0.9898214418809326842, 1.000000000000000000, 0.9898214418809326842, 1.000000000000000000, 0.9898214418809326842, 1.000000000000000000, 0.9898214418809326842, 1.000000000000000000, 0.9898214418809326842, 1.000000000000000000, 0.9898214418809326842, 1.000000000000000000, 0.9898214418809326842, 1.000000000000000000, 0.9898214418809326842, 1.000000000000000000, 0.9898214418809326842, 1.000000000000000000, 0.9898214418809326842, 1.000000000000000000, 0.9898214418809326842, 1.000000000000000000, 0.9898214418809326842, 1.000000000000000000, 0.9898214418809326842, 1.000000000000000000, 0.9898214418809326842, 1.000000000000000000, 0.9898214418809326842, 1.000000000000000000, 0.9898214418809326842, 1.000000000000000000, 0.9898214418809326842, 1.000000000000000000, 0.9898214418809326842, 1.000000000000000000, 0.9898214418809326842, 1.000000000000000000, 0.9898214418809326842, 1.000000000000000000, 0.9898214418809326842, 1.000000000000000000, 0.9898214418809326842, 1.000000000000000000, 0.9898214418809326842, 1.000000000000000000, 0.9898214418809326842, 1.000000000000000000, 0.9898214418809326842, 1.000000000000000000, 0.9898214418809326842, 1.000000000000000000, 0.9898214418809326842, 1.000000000000000000, 0.9898214418809326842, 1.000000000000000000, 0.9898214418809326842, 1.000000000000000000, 0.9898214418809326842, 1.000000000000000000, 0.9898214418809326842, 1.000000000000000000, 0.9898214418809326842, 1.000000000000000000, 0.9898214418809326842, 1.000000000000000000, 0.9898214418809326842, 1.000000000000000000, 0.9898214418809326842, 1.000000000000000000, 0.9898214418809326842, 1.000000000000000000, 0.9898214418809326842, 1.000000000000000000, 0.9898214418809326842, 1.000000000000000000, 0.9898214418809326842, 1.000000000000000000, 0.9898214418809326842, 1.000000000000000000, 0.9898214418809326842, 1.000000000000000000, 0.9898214418809326842, 1.000000000000000000, 0.9898214418809326842, 1.000000000000000000, 0.9898214418809326842, 1.000000000000000000, 0.9898214418809326842, 1.000000000000000000, 0.9898214418809326842, 1.000000000000000000, 0.9898214418809326842, 1.000000000000000000, 0.9898214418809326842, 1.000000000000000000, 0.9898214418809326842, 1.000000000000000000, 0.9898214418809326842, 1.000000000000000000, 0.9898214418809326842, 1.000000000000000000, 0.9898214418809326842, 1.000000000000000000, 0.9898214418809326842, 1.000000000000000000, 0.9898214418809326842, 1.000000000000000000, 0.9898214418809326842, 1.000000000000000000, 0.9898214418809326842, 1.000000000000000000, 0.9898214418809326842, 1.000000000000000000, 0.9898214418809326842, 1.000000000000000000, 0.9898214418809326842, 1.000000000000000000, 0.9898214418809326842, 1.000000000000000000, 0.9898214418809326842, 1.000000000000000000, 0.9898214418809326842, 1.000000000000000000, 0.9898214418809326842, 1.000000000000000000, 0.9898214418809326842, 1.000000000000000000, 0.9898214418809326842, 1.000000000000000000, 0.9898214418809326842, 1.000000000000000000, 0.9898214418809326842, 1.000000000000000000, 0.9898214418809326842, 1.000000000000000000, 0.9898214418809326842, 1.000000000000000000, 0.9898214418809326842, 1.000000000000000000, 0.9898214418809326842, 1.000000000000000000, 0.9898214418809326842, 1.000000000000000000, 0.9898214418809326842, 1.000000000000000000, 0.9898214418809326842, 1.000000000000000000, 0.9898214418809326842, 1.000000000000000000, 0.9898214418809326842, 1.000000000000000000, 0.9898214418809326842, 1.000000000000000000, 0.9898214418809326842, 1.000000000000000000, 0.9898214418809326842, 1.000000000000000000, 0.9898214418809326842, 1.000000000000000000, 0.9898214418809326842, 1.000000000000000000, 0.9898214418809326842, 1.000000000000000000, 0.9898214418809326842, 1.000000000000000000, 0.9898214418809326842, 1.000000000000000000, 0.9898214418809326842, 1.000000000000000000, 0.9898214418809326842, 1.000000000000000000, 0.9898214418809326842, 1.000000000000000000, 0.9898214418809326842, 1.000000000000000000, 0.9898214418809326842, 1.000000000000000000, 0.9898214418809326842, 1.000000000000000000, 0.9898214418809326842, 1.000000000000000000, 0.9898214418809326842, 1.000000000000000000, 0.9898214418809326842, 1.000000000000000000, 0.9898214418809326842, 1.000000000000000000, 0.9898214418809326842, 1.000000000000000000, 0.9898214418809326842, 1.000000000000000000, 0.9898214418809326842, 1.000000000000000000, 0.9898214418809326842, 1.000000000000000000, 0.9898214418809326842, 1.000000000000000000, 0.9898214418809326842, 1.000000000000000000, 0.9898214418809326842, 1.000000000000000000, 0.9898214418809326842, 1.000000000000000000, 0.9898214418809326842, 1.000000000000000000, 0.9898214418809326842, 1.000000000000000000, 0.9898214418809326842, 1.000000000000000000, 0.9898214418809326842, 1.000000000000000000, 0.9898214418809326842, 1.000000000000000000, 0.9898214418809326842, 1.000000000000000000, 0.9898214418809326842, 1.000000000000000000, 0.9898214418809326842, 1.000000000000000000, 0.9898214418809326842, 1.000000000000000000, 0.9898214418809326842, 1.000000000000000000, 0.9898214418809326842, 1.000000000000000000, 0.9898214418809326842, 1.000000000000000000, 0.9898214418809326842, 1.000000000000000000, 0.9898214418809326842, 1.000000000000000000, 0.9898214418809326842, 1.000000000000000000, 0.9898214418809326842, 1.000000000000000000, 0.9898214418809326842, 1.000000000000000000, 0.9898214418809326842, 1.000000000000000000, 0.9898214418809326842, 1.000000000000000000, 0.9898214418809326842, 1.000000000000000000, 0.9898214418809326842, 1.000000000000000000, 0.9898214418809326842, 1.000000000000000000, 0.9898214418809326842, 1.000000000000000000, 0.9898214418809326842, 1.000000000000000000, 0.9898214418809326842, 1.000000000000000000, 0.9898214418809326842, 1.000000000000000000, 0.9898214418809326842, 1.000000000000000000, 0.9898214418809326842, 1.000000000000000000, 0.9898214418809326842, 1.000000000000000000, 0.9898214418809326842, 1.000000000000000000, 0.9898214418809326842, 1.000000000000000000, 0.9898214418809326842, 1.000000000000000000, 0.9898214418809326842, 1.000000000000000000, 0.9898214418809326842, 1.000000000000000000, 0.9898214418809326842, 1.000000000000000000, 0.9898214418809326842, 1.000000000000000000, 0.9898214418809326842, 1.000000000000000000, 0.9898214418809326842, 1.000000000000000000, 0.9898214418809326842, 1.000000000000000000, 0.9898214418809326842, 1.000000000000000000, 0.9898214418809326842, 1.000000000000000000, 0.9898214418809326842, 1.000000000000000000, 0.9898214418809326842, 1.000000000000000000, 0.9898214418809326842, 1.000000000000000000, 0.9898214418809326842, 1.000000000000000000, 0.9898214418809326842, 1.000000000000000000, 0.9898214418809326842, 1.000000000000000000, 0.9898214418809326842, 1.000000000000000000, 0.9898214418809326842, 1.000000000000000000, 0.9898214418809326842, 1.000000000000000000, 0.9898214418809326842, 1.000000000000000000, 0.9898214418809326842, 1.000000000000000000, 0.9898214418809326842, 1.000000000000000000, 0.9898214418809326842, 1.000000000000000000, 0.9898214418809326842, 1.000000000000000000, 0.9898214418809326842, 1.000000000000000000, 0.9898214418809326842, 1.000000000000000000, 0.9898214418809326842, 1.000000000000000000, 0.9898214418809326842, 1.000000000000000000, 0.9898214418809326842, 1.000000000000000000, 0.9898214418809326842, 1.000000000000000000, 0.9898214418809326842, 1.000000000000000000, 0.9898214418809326842, 1.000000000000000000, 0.9898214418809326842, 1.000000000000000000, 0.9898214418809326842, 1.000000000000000000, 0.9898214418809326842, 1.000000000000000000, 0.9898214418809326842, 1.000000000000000000, 0.9898214418809326842, 1.000000000000000000, 0.9898214418809326842, 1.000000000000000000, 0.9898214418809326842, 1.000000000000000000, 0.9898214418809326842, 1.000000000000000000, 0.9898214418809326842, 1.000000000000000000, 0.9898214418809326842, 1.000000000000000000, 0.9898214418809326842, 1.000000000000000000, 0.9898214418809326842, 1.000000000000000000, 0.9898214418809326842, 1.000000000000000000, 0.9898214418809326842, 1.000000000000000000, 0.9898214418809326842, 1.000000000000000000, 0.9898214418809326842, 1.000000000000000000, 0.9898214418809326842, 1.000000000000000000, 0.9898214418809326842, 1.000000000000000000, 0.9898214418809326842, 1.000000000000000000, 0.9898214418809326842, 1.000000000000000000, 0.9898214418809326842, 1.000000000000000000, 0.9898214418809326842, 1.000000000000000000, 0.9898214418809326842, 1.000000000000000000, 0.9898214418809326842, 1.000000000000000000, 0.9898214418809326842, 1.000000000000000000, 0.9898214418809326842, 1.000000000000000000, 0.9898214418809326842, 1.000000000000000000, 0.9898214418809326842, 1.000000000000000000, 0.9898214418809326842, 1.000000000000000000, 0.9898214418809326842, 1.000000000000000000, 0.9898214418809326842, 1.000000000000000000, 0.9898214418809326842, 1.000000000000000000, 0.9898214418809326842, 1.000000000000000000, 0.9898214418809326842, 1.000000000000000000, 0.9898214418809326842, 1.000000000000000000, 0.9898214418809326842, 1.000000000000000000, 0.9898214418809326842, 1.000000000000000000, 0.9898214418809326842, 1.000000000000000000, 0.9898214418809326842, 1.000000000000000000, 0.9898214418809326842, 1.000000000000000000, 0.9898214418809326842, 1.000000000000000000, 0.9898214418809326842, 1.000000000000000000, 0.9898214418809326842, 1.000000000000000000, 0.9898214418809326842, 1.000000000000000000, 0.9898214418809326842, 1.000000000000000000, 0.9898214418809326842, 1.000000000000000000, 0.9898214418809326842, 1.000000000000000000, 0.9898214418809326842, 1.000000000000000000, 0.9898214418809326842, 1.000000000000000000, 0.9898214418809326842, 1.000000000000000000, 0.9898214418809326842, 1.000000000000000000, 0.9898214418809326842, 1.000000000000000000, 0.9898214418809326842, 1.000000000000000000, 0.9898214418809326842, 1.000000000000000000, 0.9898214418809326842, 1.000000000000000000, 0.9898214418809326842, 1.000000000000000000, 0.9898214418809326842, 1.000000000000000000, 0.9898214418809326842, 1.000000000000000000, 0.9898214418809326842, 1.000000000000000000, 0.9898214418809326842, 1.000000000000000000, 0.9898214418809326842, 1.000000000000000000, 0.9898214418809326842, 1.000000000000000000, 0.9898214418809326842, 1.000000000000000000, 0.9898214418809326842, 1.000000000000000000, 0.9898214418809326842, 1.000000000000000000, 0.9898214418809326842, 1.000000000000000000, 0.9898214418809326842, 1.000000000000000000, 0.9898214418809326842, 1.000000000000000000, 0.9898214418809326842, 1.000000000000000000, 0.9898214418809326842, 1.000000000000000000, 0.9898214418809326842, 1.000000000000000000, 0.9898214418809326842, 1.000000000000000000, 0.9898214418809326842, 1.000000000000000000, 0.9898214418809326842, 1.000000000000000000, 0.9898214418809326842, 1.000000000000000000, 0.9898214418809326842, 1.000000000000000000, 0.9898214418809326842, 1.000000000000000000, 0.9898214418809326842, 1.000000000000000000, 0.9898214418809326842, 1.000000000000000000, 0.9898214418809326842, 1.000000000000000000, 0.9898214418809326842, 1.000000000000000000, 0.9898214418809326842, 1.000000000000000000, 0.9898214418809326842, 1.000000000000000000, 0.9898214418809326842, 1.000000000000000000, 0.9898214418809326842, 1.000000000000000000, 0.9898214418809326842, 1.000000000000000000, 0.9898214418809326842, 1.000000000000000000, 0.9898214418809326842, 1.000000000000000000, 0.9898214418809326842, 1.000000000000000000, 0.9898214418809326842, 1.000000000000000000, 0.9898214418809326842, 1.000000000000000000, 0.9898214418809326842, 1.000000000000000000, 0.9898214418809326842, 1.000000000000000000, 0.9898214418809326842, 1.000000000000000000, 0.9898214418809326842, 1.000000000000000000, 0.9898214418809326842, 1.000000000000000000, 0.9898214418809326842, 1.000000000000000000, 0.9898214418809326842, 1.000000000000000000, 0.9898214418809326842, 1.000000000000000000, 0.9898214418809326842, 1.000000000000000000, 0.9898214418809326842, 1.000000000000000000, 0.9898214418809326842, 1.000000000000000000, 0.9898214418809326842, 1.000000000000000000, 0.9898214418809326842, 1.000000000000000000, 0.9898214418809326842, 1.000000000000000000, 0.9898214418809326842, 1.000000000000000000, 0.9898214418809326842, 1.000000000000000000, 0.9898214418809326842, 1.000000000000000000, 0.9898214418809326842, 1.000000000000000000, 0.9898214418809326842, 1.000000000000000000, 0.9898214418809326842, 1.000000000000000000, 0.9898214418809326842, 1.000000000000000000, 0.9898214418809326842, 1.000000000000000000, 0.9898214418809326842, 1.000000000000000000, 0.9898214418809326842, 1.000000000000000000, 0.9898214418809326842, 1.000000000000000000, 0.9898214418809326842, 1.000000000000000000, 0.9898214418809326842, 1.000000000000000000, 0.9898214418809326842, 1.000000000000000000, 0.9898214418809326842, 1.000000000000000000, 0.9898214418809326842, 1.000000000000000000, 0.9898214418809326842, 1.000000000000000000, 0.9898214418809326842, 1.000000000000000000, 0.9898214418809326842, 1.000000000000000000, 0.9898214418809326842, 1.000000000000000000, 0.9898214418809326842, 1.000000000000000000, 0.9898214418809326842, 1.000000000000000000, 0.9898214418809326842, 1.000000000000000000, 0.9898214418809326842, 1.000000000000000000, 0.9898214418809326842, 1.000000000000000000, 0.9898214418809326842, 1.000000000000000000, 0.9898214418809326842, 1.000000000000000000, 0.9898214418809326842, 1.000000000000000000, 0.9898214418809326842, 1.000000000000000000, 0.9898214418809326842, 1.000000000000000000, 0.9898214418809326842, 1.000000000000000000, 0.9898214418809326842, 1.000000000000000000, 0.9898214418809326842, 1.000000000000000000, 0.9898214418809326842, 1.000000000000000000, 0.9898214418809326842, 1.000000000000000000, 0.9898214418809326842, 1.000000000000000000, 0.9898214418809326842, 1.000000000000000000, 0.9898214418809326842, 1.000000000000000000, 0.9898214418809326842, 1.000000000000000000, 0.9898214418809326842, 1.000000000000000000, 0.9898214418809326842, 1.000000000000000000, 0.9898214418809326842, 1.000000000000000000, 0.9898214418809326842, 1.000000000000000000, 0.9898214418809326842, 1.000000000000000000, 0.9898214418809326842, 1.000000000000000000, 0.9898214418809326842, 1.000000000000000000, 0.9898214418809326842, 1.000000000000000000, 0.9898214418809326842, 1.000000000000000000, 0.9898214418809326842, 1.000000000000000000, 0.9898214418809326842, 1.000000000000000000, 0.9898214418809326842, 1.000000000000000000, 0.9898214418809326842, 1.000000000000000000, 0.9898214418809326842, 1.000000000000000000, 0.9898214418809326842, 1.000000000000000000, 0.9898214418809326842, 1.000000000000000000, 0.9898214418809326842, 1.000000000000000000, 0.9898214418809326842, 1.000000000000000000, 0.9898214418809326842, 1.000000000000000000, 0.9898214418809326842, 1.000000000000000000, 0.9898214418809326842, 1.000000000000000000, 0.9898214418809326842, 1.000000000000000000, 0.9898214418809326842, 1.000000000000000000, 0.9898214418809326842, 1.000000000000000000, 0.9898214418809326842, 1.000000000000000000, 0.9898214418809326842, 1.000000000000000000, 0.9898214418809326842, 1.000000000000000000, 0.9898214418809326842, 1.000000000000000000, 0.9898214418809326842, 1.000000000000000000, 0.9898214418809326842, 1.000000000000000000, 0.9898214418809326842, 1.000000000000000000, 0.9898214418809326842, 1.000000000000000000, 0.9898214418809326842, 1.000000000000000000, 0.9898214418809326842, 1.000000000000000000, 0.9898214418809326842, 1.000000000000000000, 0.9898214418809326842, 1.000000000000000000, 0.9898214418809326842, 1.000000000000000000, 0.9898214418809326842, 1.000000000000000000, 0.9898214418809326842, 1.000000000000000000, 0.9898214418809326842, 1.000000000000000000, 0.9898214418809326842, 1.000000000000000000, 0.9898214418809326842, 1.000000000000000000, 0.9898214418809326842, 1.000000000000000000, 0.9898214418809326842, 1.000000000000000000, 0.9898214418809326842, 1.000000000000000000, 0.9898214418809326842, 1.000000000000000000, 0.9898214418809326842, 1.000000000000000000, 0.9898214418809326842, 1.000000000000000000, 0.9898214418809326842, 1.000000000000000000, 0.9898214418809326842, 1.000000000000000000, 0.9898214418809326842, 1.000000000000000000, 0.9898214418809326842, 1.000000000000000000, 0.9898214418809326842, 1.000000000000000000, 0.9898214418809326842, 1.000000000000000000, 0.9898214418809326842, 1.000000000000000000, 0.9898214418809326842, 1.000000000000000000, 0.9898214418809326842, 1.000000000000000000, 0.9898214418809326842, 1.000000000000000000, 0.9898214418809326842, 1.000000000000000000, 0.9898214418809326842, 1.000000000000000000, 0.9898214418809326842, 1.000000000000000000, 0.9898214418809326842, 1.000000000000000000, 0.9898214418809326842, 1.000000000000000000, 0.9898214418809326842, 1.000000000000000000, 0.9898214418809326842, 1.000000000000000000, 0.9898214418809326842, 1.000000000000000000, 0.9898214418809326842, 1.000000000000000000, 0.9898214418809326842, 1.000000000000000000, 0.9898214418809326842, 1.000000000000000000, 0.9898214418809326842, 1.000000000000000000, 0.9898214418809326842, 1.000000000000000000, 0.9898214418809326842, 1.000000000000000000, 0.9898214418809326842, 1.000000000000000000, 0.9898214418809326842, 1.000000000000000000, 0.9898214418809326842, 1.000000000000000000, 0.9898214418809326842, 1.000000000000000000, 0.9898214418809326842, 1.000000000000000000, 0.9898214418809326842, 1.000000000000000000, 0.9898214418809326842, 1.000000000000000000, 0.9898214418809326842, 1.000000000000000000, 0.9898214418809326842, 1.000000000000000000, 0.9898214418809326842, 1.000000000000000000, 0.9898214418809326842, 1.000000000000000000, 0.9898214418809326842, 1.000000000000000000, 0.9898214418809326842, 1.000000000000000000, 0.9898214418809326842, 1.000000000000000000, 0.9898214418809326842, 1.000000000000000000, 0.9898214418809326842, 1.000000000000000000, 0.9898214418809326842, 1.000000000000000000, 0.9898214418809326842, 1.000000000000000000, 0.9898214418809326842, 1.000000000000000000, 0.9898214418809326842, 1.000000000000000000, 0.9898214418809326842, 1.000000000000000000, 0.9898214418809326842, 1.000000000000000000, 0.9898214418809326842, 1.000000000000000000, 0.9898214418809326842, 1.000000000000000000, 0.9898214418809326842, 1.000000000000000000, 0.9898214418809326842, 1.000000000000000000, 0.9898214418809326842, 1.000000000000000000, 0.9961809353924466759, 0.9952277490961531914),
 ( 0.3333333333333333703, 0.3299404806269776169, 0.3333333333333333703, 0.3299404806269776169, 0.3333333333333333703, 0.3299404806269776169, 0.3333333333333333703, 0.3299404806269776169, 0.3333333333333333703, 0.3299404806269776169, 0.3333333333333333703, 0.3299404806269776169, 0.3333333333333333703, 0.3299404806269776169, 0.3333333333333333703, 0.3299404806269776169, 0.3333333333333333703, 0.3299404806269776169, 0.3333333333333333703, 0.3299404806269776169, 0.3333333333333333703, 0.3299404806269776169, 0.3333333333333333703, 0.3299404806269776169, 0.3333333333333333703, 0.3299404806269776169, 0.3333333333333333703, 0.3299404806269776169, 0.3333333333333333703, 0.3299404806269776169, 0.3333333333333333703, 0.3299404806269776169, 0.3333333333333333703, 0.3299404806269776169, 0.3333333333333333703, 0.3299404806269776169, 0.3333333333333333703, 0.3299404806269776169, 0.3333333333333333703, 0.3299404806269776169, 0.3333333333333333703, 0.3299404806269776169, 0.3333333333333333703, 0.3299404806269776169, 0.3333333333333333703, 0.3299404806269776169, 0.3333333333333333703, 0.3299404806269776169, 0.3333333333333333703, 0.3299404806269776169, 0.3333333333333333703, 0.3299404806269776169, 0.3333333333333333703, 0.3299404806269776169, 0.3333333333333333703, 0.3299404806269776169, 0.3333333333333333703, 0.3299404806269776169, 0.3333333333333333703, 0.3299404806269776169, 0.3333333333333333703, 0.3299404806269776169, 0.3333333333333333703, 0.3299404806269776169, 0.3333333333333333703, 0.3299404806269776169, 0.3333333333333333703, 0.3299404806269776169, 0.3333333333333333703, 0.3299404806269776169, 0.3333333333333333703, 0.3299404806269776169, 0.3333333333333333703, 0.3299404806269776169, 0.3333333333333333703, 0.3299404806269776169, 0.3333333333333333703, 0.3299404806269776169, 0.3333333333333333703, 0.3299404806269776169, 0.3333333333333333703, 0.3299404806269776169, 0.3333333333333333703, 0.3299404806269776169, 0.3333333333333333703, 0.3299404806269776169, 0.3333333333333333703, 0.3299404806269776169, 0.3333333333333333703, 0.3299404806269776169, 0.3333333333333333703, 0.3299404806269776169, 0.3333333333333333703, 0.3299404806269776169, 0.3333333333333333703, 0.3299404806269776169, 0.3333333333333333703, 0.3299404806269776169, 0.3333333333333333703, 0.3299404806269776169, 0.3333333333333333703, 0.3299404806269776169, 0.3333333333333333703, 0.3299404806269776169, 0.3333333333333333703, 0.3299404806269776169, 0.3333333333333333703, 0.3299404806269776169, 0.3333333333333333703, 0.3299404806269776169, 0.3333333333333333703, 0.3299404806269776169, 0.3333333333333333703, 0.3299404806269776169, 0.3333333333333333703, 0.3299404806269776169, 0.3333333333333333703, 0.3299404806269776169, 0.3333333333333333703, 0.3299404806269776169, 0.3333333333333333703, 0.3299404806269776169, 0.3333333333333333703, 0.3299404806269776169, 0.3333333333333333703, 0.3299404806269776169, 0.3333333333333333703, 0.3299404806269776169, 0.3333333333333333703, 0.3299404806269776169, 0.3333333333333333703, 0.3299404806269776169, 0.3333333333333333703, 0.3299404806269776169, 0.3333333333333333703, 0.3299404806269776169, 0.3333333333333333703, 0.3299404806269776169, 0.3333333333333333703, 0.3299404806269776169, 0.3333333333333333703, 0.3299404806269776169, 0.3333333333333333703, 0.3299404806269776169, 0.3333333333333333703, 0.3299404806269776169, 0.3333333333333333703, 0.3299404806269776169, 0.3333333333333333703, 0.3299404806269776169, 0.3333333333333333703, 0.3299404806269776169, 0.3333333333333333703, 0.3299404806269776169, 0.3333333333333333703, 0.3299404806269776169, 0.3333333333333333703, 0.3299404806269776169, 0.3333333333333333703, 0.3299404806269776169, 0.3333333333333333703, 0.3299404806269776169, 0.3333333333333333703, 0.3299404806269776169, 0.3333333333333333703, 0.3299404806269776169, 0.3333333333333333703, 0.3299404806269776169, 0.3333333333333333703, 0.3299404806269776169, 0.3333333333333333703, 0.3299404806269776169, 0.3333333333333333703, 0.3299404806269776169, 0.3333333333333333703, 0.3299404806269776169, 0.3333333333333333703, 0.3299404806269776169, 0.3333333333333333703, 0.3299404806269776169, 0.3333333333333333703, 0.3299404806269776169, 0.3333333333333333703, 0.3299404806269776169, 0.3333333333333333703, 0.3299404806269776169, 0.3333333333333333703, 0.3299404806269776169, 0.3333333333333333703, 0.3299404806269776169, 0.3333333333333333703, 0.3299404806269776169, 0.3333333333333333703, 0.3299404806269776169, 0.3333333333333333703, 0.3299404806269776169, 0.3333333333333333703, 0.3299404806269776169, 0.3333333333333333703, 0.3299404806269776169, 0.3333333333333333703, 0.3299404806269776169, 0.3333333333333333703, 0.3299404806269776169, 0.3333333333333333703, 0.3299404806269776169, 0.3333333333333333703, 0.3299404806269776169, 0.3333333333333333703, 0.3299404806269776169, 0.3333333333333333703, 0.3299404806269776169, 0.3333333333333333703, 0.3299404806269776169, 0.3333333333333333703, 0.3299404806269776169, 0.3333333333333333703, 0.3299404806269776169, 0.3333333333333333703, 0.3299404806269776169, 0.3333333333333333703, 0.3299404806269776169, 0.3333333333333333703, 0.3299404806269776169, 0.3333333333333333703, 0.3299404806269776169, 0.3333333333333333703, 0.3299404806269776169, 0.3333333333333333703, 0.3299404806269776169, 0.3333333333333333703, 0.3299404806269776169, 0.3333333333333333703, 0.3299404806269776169, 0.3333333333333333703, 0.3299404806269776169, 0.3333333333333333703, 0.3299404806269776169, 0.3333333333333333703, 0.3299404806269776169, 0.3333333333333333703, 0.3299404806269776169, 0.3333333333333333703, 0.3299404806269776169, 0.3333333333333333703, 0.3299404806269776169, 0.3333333333333333703, 0.3299404806269776169, 0.3333333333333333703, 0.3299404806269776169, 0.3333333333333333703, 0.3299404806269776169, 0.3333333333333333703, 0.3299404806269776169, 0.3333333333333333703, 0.3299404806269776169, 0.3333333333333333703, 0.3299404806269776169, 0.3333333333333333703, 0.3299404806269776169, 0.3333333333333333703, 0.3299404806269776169, 0.3333333333333333703, 0.3299404806269776169, 0.3333333333333333703, 0.3299404806269776169, 0.3333333333333333703, 0.3299404806269776169, 0.3333333333333333703, 0.3299404806269776169, 0.3333333333333333703, 0.3299404806269776169, 0.3333333333333333703, 0.3299404806269776169, 0.3333333333333333703, 0.3299404806269776169, 0.3333333333333333703, 0.3299404806269776169, 0.3333333333333333703, 0.3299404806269776169, 0.3333333333333333703, 0.3299404806269776169, 0.3333333333333333703, 0.3299404806269776169, 0.3333333333333333703, 0.3299404806269776169, 0.3333333333333333703, 0.3299404806269776169, 0.3333333333333333703, 0.3299404806269776169, 0.3333333333333333703, 0.3299404806269776169, 0.3333333333333333703, 0.3299404806269776169, 0.3333333333333333703, 0.3299404806269776169, 0.3333333333333333703, 0.3299404806269776169, 0.3333333333333333703, 0.3299404806269776169, 0.3333333333333333703, 0.3299404806269776169, 0.3333333333333333703, 0.3299404806269776169, 0.3333333333333333703, 0.3299404806269776169, 0.3333333333333333703, 0.3299404806269776169, 0.3333333333333333703, 0.3299404806269776169, 0.3333333333333333703, 0.3299404806269776169, 0.3333333333333333703, 0.3299404806269776169, 0.3333333333333333703, 0.3299404806269776169, 0.3333333333333333703, 0.3299404806269776169, 0.3333333333333333703, 0.3299404806269776169, 0.3333333333333333703, 0.3299404806269776169, 0.3333333333333333703, 0.3299404806269776169, 0.3333333333333333703, 0.3299404806269776169, 0.3333333333333333703, 0.3299404806269776169, 0.3333333333333333703, 0.3299404806269776169, 0.3333333333333333703, 0.3299404806269776169, 0.3333333333333333703, 0.3299404806269776169, 0.3333333333333333703, 0.3299404806269776169, 0.3333333333333333703, 0.3299404806269776169, 0.3333333333333333703, 0.3299404806269776169, 0.3333333333333333703, 0.3299404806269776169, 0.3333333333333333703, 0.3299404806269776169, 0.3333333333333333703, 0.3299404806269776169, 0.3333333333333333703, 0.3299404806269776169, 0.3333333333333333703, 0.3299404806269776169, 0.3333333333333333703, 0.3299404806269776169, 0.3333333333333333703, 0.3299404806269776169, 0.3333333333333333703, 0.3299404806269776169, 0.3333333333333333703, 0.3299404806269776169, 0.3333333333333333703, 0.3299404806269776169, 0.3333333333333333703, 0.3299404806269776169, 0.3333333333333333703, 0.3299404806269776169, 0.3333333333333333703, 0.3299404806269776169, 0.3333333333333333703, 0.3299404806269776169, 0.3333333333333333703, 0.3299404806269776169, 0.3333333333333333703, 0.3299404806269776169, 0.3333333333333333703, 0.3299404806269776169, 0.3333333333333333703, 0.3299404806269776169, 0.3333333333333333703, 0.3299404806269776169, 0.3333333333333333703, 0.3299404806269776169, 0.3333333333333333703, 0.3299404806269776169, 0.3333333333333333703, 0.3299404806269776169, 0.3333333333333333703, 0.3299404806269776169, 0.3333333333333333703, 0.3299404806269776169, 0.3333333333333333703, 0.3299404806269776169, 0.3333333333333333703, 0.3299404806269776169, 0.3333333333333333703, 0.3299404806269776169, 0.3333333333333333703, 0.3299404806269776169, 0.3333333333333333703, 0.3299404806269776169, 0.3333333333333333703, 0.3299404806269776169, 0.3333333333333333703, 0.3299404806269776169, 0.3333333333333333703, 0.3299404806269776169, 0.3333333333333333703, 0.3299404806269776169, 0.3333333333333333703, 0.3299404806269776169, 0.3333333333333333703, 0.3299404806269776169, 0.3333333333333333703, 0.3299404806269776169, 0.3333333333333333703, 0.3299404806269776169, 0.3333333333333333703, 0.3299404806269776169, 0.3333333333333333703, 0.3299404806269776169, 0.3333333333333333703, 0.3299404806269776169, 0.3333333333333333703, 0.3299404806269776169, 0.3333333333333333703, 0.3299404806269776169, 0.3333333333333333703, 0.3299404806269776169, 0.3333333333333333703, 0.3299404806269776169, 0.3333333333333333703, 0.3299404806269776169, 0.3333333333333333703, 0.3299404806269776169, 0.3333333333333333703, 0.3299404806269776169, 0.3333333333333333703, 0.3299404806269776169, 0.3333333333333333703, 0.3299404806269776169, 0.3333333333333333703, 0.3299404806269776169, 0.3333333333333333703, 0.3299404806269776169, 0.3333333333333333703, 0.3299404806269776169, 0.3333333333333333703, 0.3299404806269776169, 0.3333333333333333703, 0.3299404806269776169, 0.3333333333333333703, 0.3299404806269776169, 0.3333333333333333703, 0.3299404806269776169, 0.3333333333333333703, 0.3299404806269776169, 0.3333333333333333703, 0.3299404806269776169, 0.3333333333333333703, 0.3299404806269776169, 0.3333333333333333703, 0.3299404806269776169, 0.3333333333333333703, 0.3299404806269776169, 0.3333333333333333703, 0.3299404806269776169, 0.3333333333333333703, 0.3299404806269776169, 0.3333333333333333703, 0.3299404806269776169, 0.3333333333333333703, 0.3299404806269776169, 0.3333333333333333703, 0.3299404806269776169, 0.3333333333333333703, 0.3299404806269776169, 0.3333333333333333703, 0.3299404806269776169, 0.3333333333333333703, 0.3299404806269776169, 0.3333333333333333703, 0.3299404806269776169, 0.3333333333333333703, 0.3299404806269776169, 0.3333333333333333703, 0.3299404806269776169, 0.3333333333333333703, 0.3299404806269776169, 0.3333333333333333703, 0.3299404806269776169, 0.3333333333333333703, 0.3299404806269776169, 0.3333333333333333703, 0.3299404806269776169, 0.3333333333333333703, 0.3299404806269776169, 0.3333333333333333703, 0.3299404806269776169, 0.3333333333333333703, 0.3299404806269776169, 0.3333333333333333703, 0.3299404806269776169, 0.3333333333333333703, 0.3299404806269776169, 0.3333333333333333703, 0.3299404806269776169, 0.3333333333333333703, 0.3299404806269776169, 0.3333333333333333703, 0.3299404806269776169, 0.3333333333333333703, 0.3299404806269776169, 0.3333333333333333703, 0.3299404806269776169, 0.3333333333333333703, 0.3299404806269776169, 0.3333333333333333703, 0.3299404806269776169, 0.3333333333333333703, 0.3299404806269776169, 0.3333333333333333703, 0.3299404806269776169, 0.3333333333333333703, 0.3299404806269776169, 0.3333333333333333703, 0.3299404806269776169, 0.3333333333333333703, 0.3299404806269776169, 0.3333333333333333703, 0.3299404806269776169, 0.3333333333333333703, 0.3299404806269776169, 0.3333333333333333703, 0.3299404806269776169, 0.3333333333333333703, 0.3299404806269776169, 0.3333333333333333703, 0.3299404806269776169, 0.3333333333333333703, 0.3299404806269776169, 0.3333333333333333703, 0.3299404806269776169, 0.3333333333333333703, 0.3299404806269776169, 0.3333333333333333703, 0.3299404806269776169, 0.3333333333333333703, 0.3299404806269776169, 0.3333333333333333703, 0.3299404806269776169, 0.3333333333333333703, 0.3299404806269776169, 0.3333333333333333703, 0.3299404806269776169, 0.3333333333333333703, 0.3299404806269776169, 0.3333333333333333703, 0.3299404806269776169, 0.3333333333333333703, 0.3299404806269776169, 0.3333333333333333703, 0.3299404806269776169, 0.3333333333333333703, 0.3299404806269776169, 0.3333333333333333703, 0.3299404806269776169, 0.3333333333333333703, 0.3299404806269776169, 0.3333333333333333703, 0.3299404806269776169, 0.3333333333333333703, 0.3299404806269776169, 0.3333333333333333703, 0.3299404806269776169, 0.3333333333333333703, 0.3299404806269776169, 0.3333333333333333703, 0.3299404806269776169, 0.3333333333333333703, 0.3299404806269776169, 0.3333333333333333703, 0.3299404806269776169, 0.3333333333333333703, 0.3299404806269776169, 0.3333333333333333703, 0.3299404806269776169, 0.3333333333333333703, 0.3299404806269776169, 0.3333333333333333703, 0.3299404806269776169, 0.3333333333333333703, 0.3299404806269776169, 0.3333333333333333703, 0.3299404806269776169, 0.3333333333333333703, 0.3299404806269776169, 0.3333333333333333703, 0.3299404806269776169, 0.3333333333333333703, 0.3299404806269776169, 0.3333333333333333703, 0.3299404806269776169, 0.3333333333333333703, 0.3299404806269776169, 0.3333333333333333703, 0.3299404806269776169, 0.3333333333333333703, 0.3299404806269776169, 0.3333333333333333703, 0.3299404806269776169, 0.3333333333333333703, 0.3299404806269776169, 0.3333333333333333703, 0.3299404806269776169, 0.3333333333333333703, 0.3299404806269776169, 0.3333333333333333703, 0.3299404806269776169, 0.3333333333333333703, 0.3299404806269776169, 0.3333333333333333703, 0.3299404806269776169, 0.3333333333333333703, 0.3299404806269776169, 0.3333333333333333703, 0.3299404806269776169, 0.3333333333333333703, 0.3299404806269776169, 0.3333333333333333703, 0.3299404806269776169, 0.3333333333333333703, 0.3299404806269776169, 0.3333333333333333703, 0.3299404806269776169, 0.3333333333333333703, 0.3299404806269776169, 0.3333333333333333703, 0.3299404806269776169, 0.3333333333333333703, 0.3299404806269776169, 0.3333333333333333703, 0.3299404806269776169, 0.3333333333333333703, 0.3299404806269776169, 0.3333333333333333703, 0.3299404806269776169, 0.3333333333333333703, 0.3299404806269776169, 0.3333333333333333703, 0.3299404806269776169, 0.3333333333333333703, 0.3299404806269776169, 0.3333333333333333703, 0.3299404806269776169, 0.3333333333333333703, 0.3299404806269776169, 0.3333333333333333703, 0.3299404806269776169, 0.3333333333333333703, 0.3299404806269776169, 0.3333333333333333703, 0.3299404806269776169, 0.3333333333333333703, 0.3299404806269776169, 0.3333333333333333703, 0.3299404806269776169, 0.3333333333333333703, 0.3299404806269776169, 0.3333333333333333703, 0.3299404806269776169, 0.3333333333333333703, 0.3299404806269776169, 0.3333333333333333703, 0.3299404806269776169, 0.3333333333333333703, 0.3299404806269776169, 0.3333333333333333703, 0.3299404806269776169, 0.3333333333333333703, 0.3299404806269776169, 0.3333333333333333703, 0.3299404806269776169, 0.3333333333333333703, 0.3299404806269776169, 0.3333333333333333703, 0.3299404806269776169, 0.3333333333333333703, 0.3299404806269776169, 0.3333333333333333703, 0.3299404806269776169, 0.3333333333333333703, 0.3299404806269776169, 0.3333333333333333703, 0.3299404806269776169, 0.3333333333333333703, 0.3299404806269776169, 0.3333333333333333703, 0.3299404806269776169, 0.3333333333333333703, 0.3299404806269776169, 0.3333333333333333703, 0.3299404806269776169, 0.3333333333333333703, 0.3299404806269776169, 0.3333333333333333703, 0.3299404806269776169, 0.3333333333333333703, 0.3299404806269776169, 0.3333333333333333703, 0.3299404806269776169, 0.3333333333333333703, 0.3299404806269776169, 0.3333333333333333703, 0.3299404806269776169, 0.3333333333333333703, 0.3299404806269776169, 0.3333333333333333703, 0.3299404806269776169, 0.3333333333333333703, 0.3299404806269776169, 0.3333333333333333703, 0.3299404806269776169, 0.3333333333333333703, 0.3299404806269776169, 0.3333333333333333703, 0.3299404806269776169, 0.3333333333333333703, 0.3299404806269776169, 0.3333333333333333703, 0.3299404806269776169, 0.3333333333333333703, 0.3299404806269776169, 0.3333333333333333703, 0.3299404806269776169, 0.3333333333333333703, 0.3299404806269776169, 0.3333333333333333703, 0.3299404806269776169, 0.3333333333333333703, 0.3299404806269776169, 0.3333333333333333703, 0.3299404806269776169, 0.3333333333333333703, 0.3299404806269776169, 0.3333333333333333703, 0.3299404806269776169, 0.3333333333333333703, 0.3299404806269776169, 0.3333333333333333703, 0.3299404806269776169, 0.3333333333333333703, 0.3299404806269776169, 0.3333333333333333703, 0.3299404806269776169, 0.3333333333333333703, 0.3299404806269776169, 0.3333333333333333703, 0.3299404806269776169, 0.3333333333333333703, 0.3299404806269776169, 0.3333333333333333703, 0.3299404806269776169, 0.3333333333333333703, 0.3299404806269776169, 0.3333333333333333703, 0.3299404806269776169, 0.3333333333333333703, 0.3299404806269776169, 0.3333333333333333703, 0.3299404806269776169, 0.3333333333333333703, 0.3299404806269776169, 0.3333333333333333703, 0.3299404806269776169, 0.3333333333333333703, 0.3299404806269776169, 0.3333333333333333703, 0.3299404806269776169, 0.3333333333333333703, 0.3299404806269776169, 0.3333333333333333703, 0.3299404806269776169, 0.3333333333333333703, 0.3299404806269776169, 0.3333333333333333703, 0.3299404806269776169, 0.3333333333333333703, 0.3299404806269776169, 0.3333333333333333703, 0.3299404806269776169, 0.3333333333333333703, 0.3299404806269776169, 0.3333333333333333703, 0.3299404806269776169, 0.3333333333333333703, 0.3299404806269776169, 0.3333333333333333703, 0.3299404806269776169, 0.3333333333333333703, 0.3299404806269776169, 0.3333333333333333703, 0.3299404806269776169, 0.3333333333333333703, 0.3299404806269776169, 0.3333333333333333703, 0.3299404806269776169, 0.3333333333333333703, 0.3299404806269776169, 0.3333333333333333703, 0.3299404806269776169, 0.3333333333333333703, 0.3299404806269776169, 0.3333333333333333703, 0.3299404806269776169, 0.3333333333333333703, 0.3299404806269776169, 0.3333333333333333703, 0.3299404806269776169, 0.3333333333333333703, 0.3299404806269776169, 0.3333333333333333703, 0.3299404806269776169, 0.3333333333333333703, 0.3299404806269776169, 0.3333333333333333703, 0.3299404806269776169, 0.3333333333333333703, 0.3299404806269776169, 0.3333333333333333703, 0.3299404806269776169, 0.3333333333333333703, 0.3299404806269776169, 0.3333333333333333703, 0.3299404806269776169, 0.3333333333333333703, 0.3299404806269776169, 0.3333333333333333703, 0.3299404806269776169, 0.3333333333333333703, 0.3299404806269776169, 0.3333333333333333703, 0.3299404806269776169, 0.3333333333333333703, 0.3299404806269776169, 0.3333333333333333703, 0.3299404806269776169, 0.3333333333333333703, 0.3299404806269776169, 0.3333333333333333703, 0.3299404806269776169, 0.3333333333333333703, 0.3299404806269776169, 0.3333333333333333703, 0.3299404806269776169, 0.3333333333333333703, 0.3299404806269776169, 0.3333333333333333703, 0.3299404806269776169, 0.3333333333333333703, 0.3299404806269776169, 0.3333333333333333703, 0.3299404806269776169, 0.3333333333333333703, 0.3320603117974822438, 0.3317425830320511193),
 ( 0.3333333333333333703, 0.3299404806269776169, 0.3333333333333333703, 0.3299404806269776169, 0.3333333333333333703, 0.3299404806269776169, 0.3333333333333333703, 0.3299404806269776169, 0.3333333333333333703, 0.3299404806269776169, 0.3333333333333333703, 0.3299404806269776169, 0.3333333333333333703, 0.3299404806269776169, 0.3333333333333333703, 0.3299404806269776169, 0.3333333333333333703, 0.3299404806269776169, 0.3333333333333333703, 0.3299404806269776169, 0.3333333333333333703, 0.3299404806269776169, 0.3333333333333333703, 0.3299404806269776169, 0.3333333333333333703, 0.3299404806269776169, 0.3333333333333333703, 0.3299404806269776169, 0.3333333333333333703, 0.3299404806269776169, 0.3333333333333333703, 0.3299404806269776169, 0.3333333333333333703, 0.3299404806269776169, 0.3333333333333333703, 0.3299404806269776169, 0.3333333333333333703, 0.3299404806269776169, 0.3333333333333333703, 0.3299404806269776169, 0.3333333333333333703, 0.3299404806269776169, 0.3333333333333333703, 0.3299404806269776169, 0.3333333333333333703, 0.3299404806269776169, 0.3333333333333333703, 0.3299404806269776169, 0.3333333333333333703, 0.3299404806269776169, 0.3333333333333333703, 0.3299404806269776169, 0.3333333333333333703, 0.3299404806269776169, 0.3333333333333333703, 0.3299404806269776169, 0.3333333333333333703, 0.3299404806269776169, 0.3333333333333333703, 0.3299404806269776169, 0.3333333333333333703, 0.3299404806269776169, 0.3333333333333333703, 0.3299404806269776169, 0.3333333333333333703, 0.3299404806269776169, 0.3333333333333333703, 0.3299404806269776169, 0.3333333333333333703, 0.3299404806269776169, 0.3333333333333333703, 0.3299404806269776169, 0.3333333333333333703, 0.3299404806269776169, 0.3333333333333333703, 0.3299404806269776169, 0.3333333333333333703, 0.3299404806269776169, 0.3333333333333333703, 0.3299404806269776169, 0.3333333333333333703, 0.3299404806269776169, 0.3333333333333333703, 0.3299404806269776169, 0.3333333333333333703, 0.3299404806269776169, 0.3333333333333333703, 0.3299404806269776169, 0.3333333333333333703, 0.3299404806269776169, 0.3333333333333333703, 0.3299404806269776169, 0.3333333333333333703, 0.3299404806269776169, 0.3333333333333333703, 0.3299404806269776169, 0.3333333333333333703, 0.3299404806269776169, 0.3333333333333333703, 0.3299404806269776169, 0.3333333333333333703, 0.3299404806269776169, 0.3333333333333333703, 0.3299404806269776169, 0.3333333333333333703, 0.3299404806269776169, 0.3333333333333333703, 0.3299404806269776169, 0.3333333333333333703, 0.3299404806269776169, 0.3333333333333333703, 0.3299404806269776169, 0.3333333333333333703, 0.3299404806269776169, 0.3333333333333333703, 0.3299404806269776169, 0.3333333333333333703, 0.3299404806269776169, 0.3333333333333333703, 0.3299404806269776169, 0.3333333333333333703, 0.3299404806269776169, 0.3333333333333333703, 0.3299404806269776169, 0.3333333333333333703, 0.3299404806269776169, 0.3333333333333333703, 0.3299404806269776169, 0.3333333333333333703, 0.3299404806269776169, 0.3333333333333333703, 0.3299404806269776169, 0.3333333333333333703, 0.3299404806269776169, 0.3333333333333333703, 0.3299404806269776169, 0.3333333333333333703, 0.3299404806269776169, 0.3333333333333333703, 0.3299404806269776169, 0.3333333333333333703, 0.3299404806269776169, 0.3333333333333333703, 0.3299404806269776169, 0.3333333333333333703, 0.3299404806269776169, 0.3333333333333333703, 0.3299404806269776169, 0.3333333333333333703, 0.3299404806269776169, 0.3333333333333333703, 0.3299404806269776169, 0.3333333333333333703, 0.3299404806269776169, 0.3333333333333333703, 0.3299404806269776169, 0.3333333333333333703, 0.3299404806269776169, 0.3333333333333333703, 0.3299404806269776169, 0.3333333333333333703, 0.3299404806269776169, 0.3333333333333333703, 0.3299404806269776169, 0.3333333333333333703, 0.3299404806269776169, 0.3333333333333333703, 0.3299404806269776169, 0.3333333333333333703, 0.3299404806269776169, 0.3333333333333333703, 0.3299404806269776169, 0.3333333333333333703, 0.3299404806269776169, 0.3333333333333333703, 0.3299404806269776169, 0.3333333333333333703, 0.3299404806269776169, 0.3333333333333333703, 0.3299404806269776169, 0.3333333333333333703, 0.3299404806269776169, 0.3333333333333333703, 0.3299404806269776169, 0.3333333333333333703, 0.3299404806269776169, 0.3333333333333333703, 0.3299404806269776169, 0.3333333333333333703, 0.3299404806269776169, 0.3333333333333333703, 0.3299404806269776169, 0.3333333333333333703, 0.3299404806269776169, 0.3333333333333333703, 0.3299404806269776169, 0.3333333333333333703, 0.3299404806269776169, 0.3333333333333333703, 0.3299404806269776169, 0.3333333333333333703, 0.3299404806269776169, 0.3333333333333333703, 0.3299404806269776169, 0.3333333333333333703, 0.3299404806269776169, 0.3333333333333333703, 0.3299404806269776169, 0.3333333333333333703, 0.3299404806269776169, 0.3333333333333333703, 0.3299404806269776169, 0.3333333333333333703, 0.3299404806269776169, 0.3333333333333333703, 0.3299404806269776169, 0.3333333333333333703, 0.3299404806269776169, 0.3333333333333333703, 0.3299404806269776169, 0.3333333333333333703, 0.3299404806269776169, 0.3333333333333333703, 0.3299404806269776169, 0.3333333333333333703, 0.3299404806269776169, 0.3333333333333333703, 0.3299404806269776169, 0.3333333333333333703, 0.3299404806269776169, 0.3333333333333333703, 0.3299404806269776169, 0.3333333333333333703, 0.3299404806269776169, 0.3333333333333333703, 0.3299404806269776169, 0.3333333333333333703, 0.3299404806269776169, 0.3333333333333333703, 0.3299404806269776169, 0.3333333333333333703, 0.3299404806269776169, 0.3333333333333333703, 0.3299404806269776169, 0.3333333333333333703, 0.3299404806269776169, 0.3333333333333333703, 0.3299404806269776169, 0.3333333333333333703, 0.3299404806269776169, 0.3333333333333333703, 0.3299404806269776169, 0.3333333333333333703, 0.3299404806269776169, 0.3333333333333333703, 0.3299404806269776169, 0.3333333333333333703, 0.3299404806269776169, 0.3333333333333333703, 0.3299404806269776169, 0.3333333333333333703, 0.3299404806269776169, 0.3333333333333333703, 0.3299404806269776169, 0.3333333333333333703, 0.3299404806269776169, 0.3333333333333333703, 0.3299404806269776169, 0.3333333333333333703, 0.3299404806269776169, 0.3333333333333333703, 0.3299404806269776169, 0.3333333333333333703, 0.3299404806269776169, 0.3333333333333333703, 0.3299404806269776169, 0.3333333333333333703, 0.3299404806269776169, 0.3333333333333333703, 0.3299404806269776169, 0.3333333333333333703, 0.3299404806269776169, 0.3333333333333333703, 0.3299404806269776169, 0.3333333333333333703, 0.3299404806269776169, 0.3333333333333333703, 0.3299404806269776169, 0.3333333333333333703, 0.3299404806269776169, 0.3333333333333333703, 0.3299404806269776169, 0.3333333333333333703, 0.3299404806269776169, 0.3333333333333333703, 0.3299404806269776169, 0.3333333333333333703, 0.3299404806269776169, 0.3333333333333333703, 0.3299404806269776169, 0.3333333333333333703, 0.3299404806269776169, 0.3333333333333333703, 0.3299404806269776169, 0.3333333333333333703, 0.3299404806269776169, 0.3333333333333333703, 0.3299404806269776169, 0.3333333333333333703, 0.3299404806269776169, 0.3333333333333333703, 0.3299404806269776169, 0.3333333333333333703, 0.3299404806269776169, 0.3333333333333333703, 0.3299404806269776169, 0.3333333333333333703, 0.3299404806269776169, 0.3333333333333333703, 0.3299404806269776169, 0.3333333333333333703, 0.3299404806269776169, 0.3333333333333333703, 0.3299404806269776169, 0.3333333333333333703, 0.3299404806269776169, 0.3333333333333333703, 0.3299404806269776169, 0.3333333333333333703, 0.3299404806269776169, 0.3333333333333333703, 0.3299404806269776169, 0.3333333333333333703, 0.3299404806269776169, 0.3333333333333333703, 0.3299404806269776169, 0.3333333333333333703, 0.3299404806269776169, 0.3333333333333333703, 0.3299404806269776169, 0.3333333333333333703, 0.3299404806269776169, 0.3333333333333333703, 0.3299404806269776169, 0.3333333333333333703, 0.3299404806269776169, 0.3333333333333333703, 0.3299404806269776169, 0.3333333333333333703, 0.3299404806269776169, 0.3333333333333333703, 0.3299404806269776169, 0.3333333333333333703, 0.3299404806269776169, 0.3333333333333333703, 0.3299404806269776169, 0.3333333333333333703, 0.3299404806269776169, 0.3333333333333333703, 0.3299404806269776169, 0.3333333333333333703, 0.3299404806269776169, 0.3333333333333333703, 0.3299404806269776169, 0.3333333333333333703, 0.3299404806269776169, 0.3333333333333333703, 0.3299404806269776169, 0.3333333333333333703, 0.3299404806269776169, 0.3333333333333333703, 0.3299404806269776169, 0.3333333333333333703, 0.3299404806269776169, 0.3333333333333333703, 0.3299404806269776169, 0.3333333333333333703, 0.3299404806269776169, 0.3333333333333333703, 0.3299404806269776169, 0.3333333333333333703, 0.3299404806269776169, 0.3333333333333333703, 0.3299404806269776169, 0.3333333333333333703, 0.3299404806269776169, 0.3333333333333333703, 0.3299404806269776169, 0.3333333333333333703, 0.3299404806269776169, 0.3333333333333333703, 0.3299404806269776169, 0.3333333333333333703, 0.3299404806269776169, 0.3333333333333333703, 0.3299404806269776169, 0.3333333333333333703, 0.3299404806269776169, 0.3333333333333333703, 0.3299404806269776169, 0.3333333333333333703, 0.3299404806269776169, 0.3333333333333333703, 0.3299404806269776169, 0.3333333333333333703, 0.3299404806269776169, 0.3333333333333333703, 0.3299404806269776169, 0.3333333333333333703, 0.3299404806269776169, 0.3333333333333333703, 0.3299404806269776169, 0.3333333333333333703, 0.3299404806269776169, 0.3333333333333333703, 0.3299404806269776169, 0.3333333333333333703, 0.3299404806269776169, 0.3333333333333333703, 0.3299404806269776169, 0.3333333333333333703, 0.3299404806269776169, 0.3333333333333333703, 0.3299404806269776169, 0.3333333333333333703, 0.3299404806269776169, 0.3333333333333333703, 0.3299404806269776169, 0.3333333333333333703, 0.3299404806269776169, 0.3333333333333333703, 0.3299404806269776169, 0.3333333333333333703, 0.3299404806269776169, 0.3333333333333333703, 0.3299404806269776169, 0.3333333333333333703, 0.3299404806269776169, 0.3333333333333333703, 0.3299404806269776169, 0.3333333333333333703, 0.3299404806269776169, 0.3333333333333333703, 0.3299404806269776169, 0.3333333333333333703, 0.3299404806269776169, 0.3333333333333333703, 0.3299404806269776169, 0.3333333333333333703, 0.3299404806269776169, 0.3333333333333333703, 0.3299404806269776169, 0.3333333333333333703, 0.3299404806269776169, 0.3333333333333333703, 0.3299404806269776169, 0.3333333333333333703, 0.3299404806269776169, 0.3333333333333333703, 0.3299404806269776169, 0.3333333333333333703, 0.3299404806269776169, 0.3333333333333333703, 0.3299404806269776169, 0.3333333333333333703, 0.3299404806269776169, 0.3333333333333333703, 0.3299404806269776169, 0.3333333333333333703, 0.3299404806269776169, 0.3333333333333333703, 0.3299404806269776169, 0.3333333333333333703, 0.3299404806269776169, 0.3333333333333333703, 0.3299404806269776169, 0.3333333333333333703, 0.3299404806269776169, 0.3333333333333333703, 0.3299404806269776169, 0.3333333333333333703, 0.3299404806269776169, 0.3333333333333333703, 0.3299404806269776169, 0.3333333333333333703, 0.3299404806269776169, 0.3333333333333333703, 0.3299404806269776169, 0.3333333333333333703, 0.3299404806269776169, 0.3333333333333333703, 0.3299404806269776169, 0.3333333333333333703, 0.3299404806269776169, 0.3333333333333333703, 0.3299404806269776169, 0.3333333333333333703, 0.3299404806269776169, 0.3333333333333333703, 0.3299404806269776169, 0.3333333333333333703, 0.3299404806269776169, 0.3333333333333333703, 0.3299404806269776169, 0.3333333333333333703, 0.3299404806269776169, 0.3333333333333333703, 0.3299404806269776169, 0.3333333333333333703, 0.3299404806269776169, 0.3333333333333333703, 0.3299404806269776169, 0.3333333333333333703, 0.3299404806269776169, 0.3333333333333333703, 0.3299404806269776169, 0.3333333333333333703, 0.3299404806269776169, 0.3333333333333333703, 0.3299404806269776169, 0.3333333333333333703, 0.3299404806269776169, 0.3333333333333333703, 0.3299404806269776169, 0.3333333333333333703, 0.3299404806269776169, 0.3333333333333333703, 0.3299404806269776169, 0.3333333333333333703, 0.3299404806269776169, 0.3333333333333333703, 0.3299404806269776169, 0.3333333333333333703, 0.3299404806269776169, 0.3333333333333333703, 0.3299404806269776169, 0.3333333333333333703, 0.3299404806269776169, 0.3333333333333333703, 0.3299404806269776169, 0.3333333333333333703, 0.3299404806269776169, 0.3333333333333333703, 0.3299404806269776169, 0.3333333333333333703, 0.3299404806269776169, 0.3333333333333333703, 0.3299404806269776169, 0.3333333333333333703, 0.3299404806269776169, 0.3333333333333333703, 0.3299404806269776169, 0.3333333333333333703, 0.3299404806269776169, 0.3333333333333333703, 0.3299404806269776169, 0.3333333333333333703, 0.3299404806269776169, 0.3333333333333333703, 0.3299404806269776169, 0.3333333333333333703, 0.3299404806269776169, 0.3333333333333333703, 0.3299404806269776169, 0.3333333333333333703, 0.3299404806269776169, 0.3333333333333333703, 0.3299404806269776169, 0.3333333333333333703, 0.3299404806269776169, 0.3333333333333333703, 0.3299404806269776169, 0.3333333333333333703, 0.3299404806269776169, 0.3333333333333333703, 0.3299404806269776169, 0.3333333333333333703, 0.3299404806269776169, 0.3333333333333333703, 0.3299404806269776169, 0.3333333333333333703, 0.3299404806269776169, 0.3333333333333333703, 0.3299404806269776169, 0.3333333333333333703, 0.3299404806269776169, 0.3333333333333333703, 0.3299404806269776169, 0.3333333333333333703, 0.3299404806269776169, 0.3333333333333333703, 0.3299404806269776169, 0.3333333333333333703, 0.3299404806269776169, 0.3333333333333333703, 0.3299404806269776169, 0.3333333333333333703, 0.3299404806269776169, 0.3333333333333333703, 0.3299404806269776169, 0.3333333333333333703, 0.3299404806269776169, 0.3333333333333333703, 0.3299404806269776169, 0.3333333333333333703, 0.3299404806269776169, 0.3333333333333333703, 0.3299404806269776169, 0.3333333333333333703, 0.3299404806269776169, 0.3333333333333333703, 0.3299404806269776169, 0.3333333333333333703, 0.3299404806269776169, 0.3333333333333333703, 0.3299404806269776169, 0.3333333333333333703, 0.3299404806269776169, 0.3333333333333333703, 0.3299404806269776169, 0.3333333333333333703, 0.3299404806269776169, 0.3333333333333333703, 0.3299404806269776169, 0.3333333333333333703, 0.3299404806269776169, 0.3333333333333333703, 0.3299404806269776169, 0.3333333333333333703, 0.3299404806269776169, 0.3333333333333333703, 0.3299404806269776169, 0.3333333333333333703, 0.3299404806269776169, 0.3333333333333333703, 0.3299404806269776169, 0.3333333333333333703, 0.3299404806269776169, 0.3333333333333333703, 0.3299404806269776169, 0.3333333333333333703, 0.3299404806269776169, 0.3333333333333333703, 0.3299404806269776169, 0.3333333333333333703, 0.3299404806269776169, 0.3333333333333333703, 0.3299404806269776169, 0.3333333333333333703, 0.3299404806269776169, 0.3333333333333333703, 0.3299404806269776169, 0.3333333333333333703, 0.3299404806269776169, 0.3333333333333333703, 0.3299404806269776169, 0.3333333333333333703, 0.3299404806269776169, 0.3333333333333333703, 0.3299404806269776169, 0.3333333333333333703, 0.3299404806269776169, 0.3333333333333333703, 0.3299404806269776169, 0.3333333333333333703, 0.3299404806269776169, 0.3333333333333333703, 0.3299404806269776169, 0.3333333333333333703, 0.3299404806269776169, 0.3333333333333333703, 0.3299404806269776169, 0.3333333333333333703, 0.3299404806269776169, 0.3333333333333333703, 0.3299404806269776169, 0.3333333333333333703, 0.3299404806269776169, 0.3333333333333333703, 0.3299404806269776169, 0.3333333333333333703, 0.3299404806269776169, 0.3333333333333333703, 0.3299404806269776169, 0.3333333333333333703, 0.3299404806269776169, 0.3333333333333333703, 0.3299404806269776169, 0.3333333333333333703, 0.3299404806269776169, 0.3333333333333333703, 0.3299404806269776169, 0.3333333333333333703, 0.3299404806269776169, 0.3333333333333333703, 0.3299404806269776169, 0.3333333333333333703, 0.3299404806269776169, 0.3333333333333333703, 0.3299404806269776169, 0.3333333333333333703, 0.3299404806269776169, 0.3333333333333333703, 0.3299404806269776169, 0.3333333333333333703, 0.3299404806269776169, 0.3333333333333333703, 0.3299404806269776169, 0.3333333333333333703, 0.3299404806269776169, 0.3333333333333333703, 0.3299404806269776169, 0.3333333333333333703, 0.3299404806269776169, 0.3333333333333333703, 0.3299404806269776169, 0.3333333333333333703, 0.3299404806269776169, 0.3333333333333333703, 0.3299404806269776169, 0.3333333333333333703, 0.3299404806269776169, 0.3333333333333333703, 0.3299404806269776169, 0.3333333333333333703, 0.3299404806269776169, 0.3333333333333333703, 0.3299404806269776169, 0.3333333333333333703, 0.3299404806269776169, 0.3333333333333333703, 0.3299404806269776169, 0.3333333333333333703, 0.3299404806269776169, 0.3333333333333333703, 0.3299404806269776169, 0.3333333333333333703, 0.3299404806269776169, 0.3333333333333333703, 0.3299404806269776169, 0.3333333333333333703, 0.3299404806269776169, 0.3333333333333333703, 0.3299404806269776169, 0.3333333333333333703, 0.3299404806269776169, 0.3333333333333333703, 0.3299404806269776169, 0.3333333333333333703, 0.3299404806269776169, 0.3333333333333333703, 0.3299404806269776169, 0.3333333333333333703, 0.3299404806269776169, 0.3333333333333333703, 0.3299404806269776169, 0.3333333333333333703, 0.3299404806269776169, 0.3333333333333333703, 0.3299404806269776169, 0.3333333333333333703, 0.3299404806269776169, 0.3333333333333333703, 0.3299404806269776169, 0.3333333333333333703, 0.3299404806269776169, 0.3333333333333333703, 0.3299404806269776169, 0.3333333333333333703, 0.3299404806269776169, 0.3333333333333333703, 0.3299404806269776169, 0.3333333333333333703, 0.3299404806269776169, 0.3333333333333333703, 0.3299404806269776169, 0.3333333333333333703, 0.3299404806269776169, 0.3333333333333333703, 0.3299404806269776169, 0.3333333333333333703, 0.3299404806269776169, 0.3333333333333333703, 0.3299404806269776169, 0.3333333333333333703, 0.3299404806269776169, 0.3333333333333333703, 0.3299404806269776169, 0.3333333333333333703, 0.3299404806269776169, 0.3333333333333333703, 0.3299404806269776169, 0.3333333333333333703, 0.3299404806269776169, 0.3333333333333333703, 0.3299404806269776169, 0.3333333333333333703, 0.3299404806269776169, 0.3333333333333333703, 0.3299404806269776169, 0.3333333333333333703, 0.3299404806269776169, 0.3333333333333333703, 0.3299404806269776169, 0.3333333333333333703, 0.3299404806269776169, 0.3333333333333333703, 0.3299404806269776169, 0.3333333333333333703, 0.3299404806269776169, 0.3333333333333333703, 0.3299404806269776169, 0.3333333333333333703, 0.3299404806269776169, 0.3333333333333333703, 0.3299404806269776169, 0.3333333333333333703, 0.3299404806269776169, 0.3333333333333333703, 0.3299404806269776169, 0.3333333333333333703, 0.3299404806269776169, 0.3333333333333333703, 0.3299404806269776169, 0.3333333333333333703, 0.3299404806269776169, 0.3333333333333333703, 0.3299404806269776169, 0.3333333333333333703, 0.3299404806269776169, 0.3333333333333333703, 0.3299404806269776169, 0.3333333333333333703, 0.3299404806269776169, 0.3333333333333333703, 0.3299404806269776169, 0.3333333333333333703, 0.3299404806269776169, 0.3333333333333333703, 0.3299404806269776169, 0.3333333333333333703, 0.3299404806269776169, 0.3333333333333333703, 0.3299404806269776169, 0.3333333333333333703, 0.3299404806269776169, 0.3333333333333333703, 0.3299404806269776169, 0.3333333333333333703, 0.3299404806269776169, 0.3333333333333333703, 0.3299404806269776169, 0.3333333333333333703, 0.3299404806269776169, 0.3333333333333333703, 0.3299404806269776169, 0.3333333333333333703, 0.3299404806269776169, 0.3333333333333333703, 0.3299404806269776169, 0.3333333333333333703, 0.3320603117974822438, 0.3317425830320511193),
 ( 1.000000000000000000, 0.9898214418809326842, 1.000000000000000000, 0.9898214418809326842, 1.000000000000000000, 0.9898214418809326842, 1.000000000000000000, 0.9898214418809326842, 1.000000000000000000, 0.9898214418809326842, 1.000000000000000000, 0.9898214418809326842, 1.000000000000000000, 0.9898214418809326842, 1.000000000000000000, 0.9898214418809326842, 1.000000000000000000, 0.9898214418809326842, 1.000000000000000000, 0.9898214418809326842, 1.000000000000000000, 0.9898214418809326842, 1.000000000000000000, 0.9898214418809326842, 1.000000000000000000, 0.9898214418809326842, 1.000000000000000000, 0.9898214418809326842, 1.000000000000000000, 0.9898214418809326842, 1.000000000000000000, 0.9898214418809326842, 1.000000000000000000, 0.9898214418809326842, 1.000000000000000000, 0.9898214418809326842, 1.000000000000000000, 0.9898214418809326842, 1.000000000000000000, 0.9898214418809326842, 1.000000000000000000, 0.9898214418809326842, 1.000000000000000000, 0.9898214418809326842, 1.000000000000000000, 0.9898214418809326842, 1.000000000000000000, 0.9898214418809326842, 1.000000000000000000, 0.9898214418809326842, 1.000000000000000000, 0.9898214418809326842, 1.000000000000000000, 0.9898214418809326842, 1.000000000000000000, 0.9898214418809326842, 1.000000000000000000, 0.9898214418809326842, 1.000000000000000000, 0.9898214418809326842, 1.000000000000000000, 0.9898214418809326842, 1.000000000000000000, 0.9898214418809326842, 1.000000000000000000, 0.9898214418809326842, 1.000000000000000000, 0.9898214418809326842, 1.000000000000000000, 0.9898214418809326842, 1.000000000000000000, 0.9898214418809326842, 1.000000000000000000, 0.9898214418809326842, 1.000000000000000000, 0.9898214418809326842, 1.000000000000000000, 0.9898214418809326842, 1.000000000000000000, 0.9898214418809326842, 1.000000000000000000, 0.9898214418809326842, 1.000000000000000000, 0.9898214418809326842, 1.000000000000000000, 0.9898214418809326842, 1.000000000000000000, 0.9898214418809326842, 1.000000000000000000, 0.9898214418809326842, 1.000000000000000000, 0.9898214418809326842, 1.000000000000000000, 0.9898214418809326842, 1.000000000000000000, 0.9898214418809326842, 1.000000000000000000, 0.9898214418809326842, 1.000000000000000000, 0.9898214418809326842, 1.000000000000000000, 0.9898214418809326842, 1.000000000000000000, 0.9898214418809326842, 1.000000000000000000, 0.9898214418809326842, 1.000000000000000000, 0.9898214418809326842, 1.000000000000000000, 0.9898214418809326842, 1.000000000000000000, 0.9898214418809326842, 1.000000000000000000, 0.9898214418809326842, 1.000000000000000000, 0.9898214418809326842, 1.000000000000000000, 0.9898214418809326842, 1.000000000000000000, 0.9898214418809326842, 1.000000000000000000, 0.9898214418809326842, 1.000000000000000000, 0.9898214418809326842, 1.000000000000000000, 0.9898214418809326842, 1.000000000000000000, 0.9898214418809326842, 1.000000000000000000, 0.9898214418809326842, 1.000000000000000000, 0.9898214418809326842, 1.000000000000000000, 0.9898214418809326842, 1.000000000000000000, 0.9898214418809326842, 1.000000000000000000, 0.9898214418809326842, 1.000000000000000000, 0.9898214418809326842, 1.000000000000000000, 0.9898214418809326842, 1.000000000000000000, 0.9898214418809326842, 1.000000000000000000, 0.9898214418809326842, 1.000000000000000000, 0.9898214418809326842, 1.000000000000000000, 0.9898214418809326842, 1.000000000000000000, 0.9898214418809326842, 1.000000000000000000, 0.9898214418809326842, 1.000000000000000000, 0.9898214418809326842, 1.000000000000000000, 0.9898214418809326842, 1.000000000000000000, 0.9898214418809326842, 1.000000000000000000, 0.9898214418809326842, 1.000000000000000000, 0.9898214418809326842, 1.000000000000000000, 0.9898214418809326842, 1.000000000000000000, 0.9898214418809326842, 1.000000000000000000, 0.9898214418809326842, 1.000000000000000000, 0.9898214418809326842, 1.000000000000000000, 0.9898214418809326842, 1.000000000000000000, 0.9898214418809326842, 1.000000000000000000, 0.9898214418809326842, 1.000000000000000000, 0.9898214418809326842, 1.000000000000000000, 0.9898214418809326842, 1.000000000000000000, 0.9898214418809326842, 1.000000000000000000, 0.9898214418809326842, 1.000000000000000000, 0.9898214418809326842, 1.000000000000000000, 0.9898214418809326842, 1.000000000000000000, 0.9898214418809326842, 1.000000000000000000, 0.9898214418809326842, 1.000000000000000000, 0.9898214418809326842, 1.000000000000000000, 0.9898214418809326842, 1.000000000000000000, 0.9898214418809326842, 1.000000000000000000, 0.9898214418809326842, 1.000000000000000000, 0.9898214418809326842, 1.000000000000000000, 0.9898214418809326842, 1.000000000000000000, 0.9898214418809326842, 1.000000000000000000, 0.9898214418809326842, 1.000000000000000000, 0.9898214418809326842, 1.000000000000000000, 0.9898214418809326842, 1.000000000000000000, 0.9898214418809326842, 1.000000000000000000, 0.9898214418809326842, 1.000000000000000000, 0.9898214418809326842, 1.000000000000000000, 0.9898214418809326842, 1.000000000000000000, 0.9898214418809326842, 1.000000000000000000, 0.9898214418809326842, 1.000000000000000000, 0.9898214418809326842, 1.000000000000000000, 0.9898214418809326842, 1.000000000000000000, 0.9898214418809326842, 1.000000000000000000, 0.9898214418809326842, 1.000000000000000000, 0.9898214418809326842, 1.000000000000000000, 0.9898214418809326842, 1.000000000000000000, 0.9898214418809326842, 1.000000000000000000, 0.9898214418809326842, 1.000000000000000000, 0.9898214418809326842, 1.000000000000000000, 0.9898214418809326842, 1.000000000000000000, 0.9898214418809326842, 1.000000000000000000, 0.9898214418809326842, 1.000000000000000000, 0.9898214418809326842, 1.000000000000000000, 0.9898214418809326842, 1.000000000000000000, 0.9898214418809326842, 1.000000000000000000, 0.9898214418809326842, 1.000000000000000000, 0.9898214418809326842, 1.000000000000000000, 0.9898214418809326842, 1.000000000000000000, 0.9898214418809326842, 1.000000000000000000, 0.9898214418809326842, 1.000000000000000000, 0.9898214418809326842, 1.000000000000000000, 0.9898214418809326842, 1.000000000000000000, 0.9898214418809326842, 1.000000000000000000, 0.9898214418809326842, 1.000000000000000000, 0.9898214418809326842, 1.000000000000000000, 0.9898214418809326842, 1.000000000000000000, 0.9898214418809326842, 1.000000000000000000, 0.9898214418809326842, 1.000000000000000000, 0.9898214418809326842, 1.000000000000000000, 0.9898214418809326842, 1.000000000000000000, 0.9898214418809326842, 1.000000000000000000, 0.9898214418809326842, 1.000000000000000000, 0.9898214418809326842, 1.000000000000000000, 0.9898214418809326842, 1.000000000000000000, 0.9898214418809326842, 1.000000000000000000, 0.9898214418809326842, 1.000000000000000000, 0.9898214418809326842, 1.000000000000000000, 0.9898214418809326842, 1.000000000000000000, 0.9898214418809326842, 1.000000000000000000, 0.9898214418809326842, 1.000000000000000000, 0.9898214418809326842, 1.000000000000000000, 0.9898214418809326842, 1.000000000000000000, 0.9898214418809326842, 1.000000000000000000, 0.9898214418809326842, 1.000000000000000000, 0.9898214418809326842, 1.000000000000000000, 0.9898214418809326842, 1.000000000000000000, 0.9898214418809326842, 1.000000000000000000, 0.9898214418809326842, 1.000000000000000000, 0.9898214418809326842, 1.000000000000000000, 0.9898214418809326842, 1.000000000000000000, 0.9898214418809326842, 1.000000000000000000, 0.9898214418809326842, 1.000000000000000000, 0.9898214418809326842, 1.000000000000000000, 0.9898214418809326842, 1.000000000000000000, 0.9898214418809326842, 1.000000000000000000, 0.9898214418809326842, 1.000000000000000000, 0.9898214418809326842, 1.000000000000000000, 0.9898214418809326842, 1.000000000000000000, 0.9898214418809326842, 1.000000000000000000, 0.9898214418809326842, 1.000000000000000000, 0.9898214418809326842, 1.000000000000000000, 0.9898214418809326842, 1.000000000000000000, 0.9898214418809326842, 1.000000000000000000, 0.9898214418809326842, 1.000000000000000000, 0.9898214418809326842, 1.000000000000000000, 0.9898214418809326842, 1.000000000000000000, 0.9898214418809326842, 1.000000000000000000, 0.9898214418809326842, 1.000000000000000000, 0.9898214418809326842, 1.000000000000000000, 0.9898214418809326842, 1.000000000000000000, 0.9898214418809326842, 1.000000000000000000, 0.9898214418809326842, 1.000000000000000000, 0.9898214418809326842, 1.000000000000000000, 0.9898214418809326842, 1.000000000000000000, 0.9898214418809326842, 1.000000000000000000, 0.9898214418809326842, 1.000000000000000000, 0.9898214418809326842, 1.000000000000000000, 0.9898214418809326842, 1.000000000000000000, 0.9898214418809326842, 1.000000000000000000, 0.9898214418809326842, 1.000000000000000000, 0.9898214418809326842, 1.000000000000000000, 0.9898214418809326842, 1.000000000000000000, 0.9898214418809326842, 1.000000000000000000, 0.9898214418809326842, 1.000000000000000000, 0.9898214418809326842, 1.000000000000000000, 0.9898214418809326842, 1.000000000000000000, 0.9898214418809326842, 1.000000000000000000, 0.9898214418809326842, 1.000000000000000000, 0.9898214418809326842, 1.000000000000000000, 0.9898214418809326842, 1.000000000000000000, 0.9898214418809326842, 1.000000000000000000, 0.9898214418809326842, 1.000000000000000000, 0.9898214418809326842, 1.000000000000000000, 0.9898214418809326842, 1.000000000000000000, 0.9898214418809326842, 1.000000000000000000, 0.9898214418809326842, 1.000000000000000000, 0.9898214418809326842, 1.000000000000000000, 0.9898214418809326842, 1.000000000000000000, 0.9898214418809326842, 1.000000000000000000, 0.9898214418809326842, 1.000000000000000000, 0.9898214418809326842, 1.000000000000000000, 0.9898214418809326842, 1.000000000000000000, 0.9898214418809326842, 1.000000000000000000, 0.9898214418809326842, 1.000000000000000000, 0.9898214418809326842, 1.000000000000000000, 0.9898214418809326842, 1.000000000000000000, 0.9898214418809326842, 1.000000000000000000, 0.9898214418809326842, 1.000000000000000000, 0.9898214418809326842, 1.000000000000000000, 0.9898214418809326842, 1.000000000000000000, 0.9898214418809326842, 1.000000000000000000, 0.9898214418809326842, 1.000000000000000000, 0.9898214418809326842, 1.000000000000000000, 0.9898214418809326842, 1.000000000000000000, 0.9898214418809326842, 1.000000000000000000, 0.9898214418809326842, 1.000000000000000000, 0.9898214418809326842, 1.000000000000000000, 0.9898214418809326842, 1.000000000000000000, 0.9898214418809326842, 1.000000000000000000, 0.9898214418809326842, 1.000000000000000000, 0.9898214418809326842, 1.000000000000000000, 0.9898214418809326842, 1.000000000000000000, 0.9898214418809326842, 1.000000000000000000, 0.9898214418809326842, 1.000000000000000000, 0.9898214418809326842, 1.000000000000000000, 0.9898214418809326842, 1.000000000000000000, 0.9898214418809326842, 1.000000000000000000, 0.9898214418809326842, 1.000000000000000000, 0.9898214418809326842, 1.000000000000000000, 0.9898214418809326842, 1.000000000000000000, 0.9898214418809326842, 1.000000000000000000, 0.9898214418809326842, 1.000000000000000000, 0.9898214418809326842, 1.000000000000000000, 0.9898214418809326842, 1.000000000000000000, 0.9898214418809326842, 1.000000000000000000, 0.9898214418809326842, 1.000000000000000000, 0.9898214418809326842, 1.000000000000000000, 0.9898214418809326842, 1.000000000000000000, 0.9898214418809326842, 1.000000000000000000, 0.9898214418809326842, 1.000000000000000000, 0.9898214418809326842, 1.000000000000000000, 0.9898214418809326842, 1.000000000000000000, 0.9898214418809326842, 1.000000000000000000, 0.9898214418809326842, 1.000000000000000000, 0.9898214418809326842, 1.000000000000000000, 0.9898214418809326842, 1.000000000000000000, 0.9898214418809326842, 1.000000000000000000, 0.9898214418809326842, 1.000000000000000000, 0.9898214418809326842, 1.000000000000000000, 0.9898214418809326842, 1.000000000000000000, 0.9898214418809326842, 1.000000000000000000, 0.9898214418809326842, 1.000000000000000000, 0.9898214418809326842, 1.000000000000000000, 0.9898214418809326842, 1.000000000000000000, 0.9898214418809326842, 1.000000000000000000, 0.9898214418809326842, 1.000000000000000000, 0.9898214418809326842, 1.000000000000000000, 0.9898214418809326842, 1.000000000000000000, 0.9898214418809326842, 1.000000000000000000, 0.9898214418809326842, 1.000000000000000000, 0.9898214418809326842, 1.000000000000000000, 0.9898214418809326842, 1.000000000000000000, 0.9898214418809326842, 1.000000000000000000, 0.9898214418809326842, 1.000000000000000000, 0.9898214418809326842, 1.000000000000000000, 0.9898214418809326842, 1.000000000000000000, 0.9898214418809326842, 1.000000000000000000, 0.9898214418809326842, 1.000000000000000000, 0.9898214418809326842, 1.000000000000000000, 0.9898214418809326842, 1.000000000000000000, 0.9898214418809326842, 1.000000000000000000, 0.9898214418809326842, 1.000000000000000000, 0.9898214418809326842, 1.000000000000000000, 0.9898214418809326842, 1.000000000000000000, 0.9898214418809326842, 1.000000000000000000, 0.9898214418809326842, 1.000000000000000000, 0.9898214418809326842, 1.000000000000000000, 0.9898214418809326842, 1.000000000000000000, 0.9898214418809326842, 1.000000000000000000, 0.9898214418809326842, 1.000000000000000000, 0.9898214418809326842, 1.000000000000000000, 0.9898214418809326842, 1.000000000000000000, 0.9898214418809326842, 1.000000000000000000, 0.9898214418809326842, 1.000000000000000000, 0.9898214418809326842, 1.000000000000000000, 0.9898214418809326842, 1.000000000000000000, 0.9898214418809326842, 1.000000000000000000, 0.9898214418809326842, 1.000000000000000000, 0.9898214418809326842, 1.000000000000000000, 0.9898214418809326842, 1.000000000000000000, 0.9898214418809326842, 1.000000000000000000, 0.9898214418809326842, 1.000000000000000000, 0.9898214418809326842, 1.000000000000000000, 0.9898214418809326842, 1.000000000000000000, 0.9898214418809326842, 1.000000000000000000, 0.9898214418809326842, 1.000000000000000000, 0.9898214418809326842, 1.000000000000000000, 0.9898214418809326842, 1.000000000000000000, 0.9898214418809326842, 1.000000000000000000, 0.9898214418809326842, 1.000000000000000000, 0.9898214418809326842, 1.000000000000000000, 0.9898214418809326842, 1.000000000000000000, 0.9898214418809326842, 1.000000000000000000, 0.9898214418809326842, 1.000000000000000000, 0.9898214418809326842, 1.000000000000000000, 0.9898214418809326842, 1.000000000000000000, 0.9898214418809326842, 1.000000000000000000, 0.9898214418809326842, 1.000000000000000000, 0.9898214418809326842, 1.000000000000000000, 0.9898214418809326842, 1.000000000000000000, 0.9898214418809326842, 1.000000000000000000, 0.9898214418809326842, 1.000000000000000000, 0.9898214418809326842, 1.000000000000000000, 0.9898214418809326842, 1.000000000000000000, 0.9898214418809326842, 1.000000000000000000, 0.9898214418809326842, 1.000000000000000000, 0.9898214418809326842, 1.000000000000000000, 0.9898214418809326842, 1.000000000000000000, 0.9898214418809326842, 1.000000000000000000, 0.9898214418809326842, 1.000000000000000000, 0.9898214418809326842, 1.000000000000000000, 0.9898214418809326842, 1.000000000000000000, 0.9898214418809326842, 1.000000000000000000, 0.9898214418809326842, 1.000000000000000000, 0.9898214418809326842, 1.000000000000000000, 0.9898214418809326842, 1.000000000000000000, 0.9898214418809326842, 1.000000000000000000, 0.9898214418809326842, 1.000000000000000000, 0.9898214418809326842, 1.000000000000000000, 0.9898214418809326842, 1.000000000000000000, 0.9898214418809326842, 1.000000000000000000, 0.9898214418809326842, 1.000000000000000000, 0.9898214418809326842, 1.000000000000000000, 0.9898214418809326842, 1.000000000000000000, 0.9898214418809326842, 1.000000000000000000, 0.9898214418809326842, 1.000000000000000000, 0.9898214418809326842, 1.000000000000000000, 0.9898214418809326842, 1.000000000000000000, 0.9898214418809326842, 1.000000000000000000, 0.9898214418809326842, 1.000000000000000000, 0.9898214418809326842, 1.000000000000000000, 0.9898214418809326842, 1.000000000000000000, 0.9898214418809326842, 1.000000000000000000, 0.9898214418809326842, 1.000000000000000000, 0.9898214418809326842, 1.000000000000000000, 0.9898214418809326842, 1.000000000000000000, 0.9898214418809326842, 1.000000000000000000, 0.9898214418809326842, 1.000000000000000000, 0.9898214418809326842, 1.000000000000000000, 0.9898214418809326842, 1.000000000000000000, 0.9898214418809326842, 1.000000000000000000, 0.9898214418809326842, 1.000000000000000000, 0.9898214418809326842, 1.000000000000000000, 0.9898214418809326842, 1.000000000000000000, 0.9898214418809326842, 1.000000000000000000, 0.9898214418809326842, 1.000000000000000000, 0.9898214418809326842, 1.000000000000000000, 0.9898214418809326842, 1.000000000000000000, 0.9898214418809326842, 1.000000000000000000, 0.9898214418809326842, 1.000000000000000000, 0.9898214418809326842, 1.000000000000000000, 0.9898214418809326842, 1.000000000000000000, 0.9898214418809326842, 1.000000000000000000, 0.9898214418809326842, 1.000000000000000000, 0.9898214418809326842, 1.000000000000000000, 0.9898214418809326842, 1.000000000000000000, 0.9898214418809326842, 1.000000000000000000, 0.9898214418809326842, 1.000000000000000000, 0.9898214418809326842, 1.000000000000000000, 0.9898214418809326842, 1.000000000000000000, 0.9898214418809326842, 1.000000000000000000, 0.9898214418809326842, 1.000000000000000000, 0.9898214418809326842, 1.000000000000000000, 0.9898214418809326842, 1.000000000000000000, 0.9898214418809326842, 1.000000000000000000, 0.9898214418809326842, 1.000000000000000000, 0.9898214418809326842, 1.000000000000000000, 0.9898214418809326842, 1.000000000000000000, 0.9898214418809326842, 1.000000000000000000, 0.9898214418809326842, 1.000000000000000000, 0.9898214418809326842, 1.000000000000000000, 0.9898214418809326842, 1.000000000000000000, 0.9898214418809326842, 1.000000000000000000, 0.9898214418809326842, 1.000000000000000000, 0.9898214418809326842, 1.000000000000000000, 0.9898214418809326842, 1.000000000000000000, 0.9898214418809326842, 1.000000000000000000, 0.9898214418809326842, 1.000000000000000000, 0.9898214418809326842, 1.000000000000000000, 0.9898214418809326842, 1.000000000000000000, 0.9898214418809326842, 1.000000000000000000, 0.9898214418809326842, 1.000000000000000000, 0.9898214418809326842, 1.000000000000000000, 0.9898214418809326842, 1.000000000000000000, 0.9898214418809326842, 1.000000000000000000, 0.9898214418809326842, 1.000000000000000000, 0.9898214418809326842, 1.000000000000000000, 0.9898214418809326842, 1.000000000000000000, 0.9898214418809326842, 1.000000000000000000, 0.9898214418809326842, 1.000000000000000000, 0.9898214418809326842, 1.000000000000000000, 0.9898214418809326842, 1.000000000000000000, 0.9898214418809326842, 1.000000000000000000, 0.9898214418809326842, 1.000000000000000000, 0.9898214418809326842, 1.000000000000000000, 0.9898214418809326842, 1.000000000000000000, 0.9898214418809326842, 1.000000000000000000, 0.9898214418809326842, 1.000000000000000000, 0.9898214418809326842, 1.000000000000000000, 0.9898214418809326842, 1.000000000000000000, 0.9898214418809326842, 1.000000000000000000, 0.9898214418809326842, 1.000000000000000000, 0.9898214418809326842, 1.000000000000000000, 0.9898214418809326842, 1.000000000000000000, 0.9898214418809326842, 1.000000000000000000, 0.9898214418809326842, 1.000000000000000000, 0.9898214418809326842, 1.000000000000000000, 0.9961809353924466759, 0.9952277490961531914),
 ( 0.3333333333333333703, 0.3299404806269776169, 0.3333333333333333703, 0.3299404806269776169, 0.3333333333333333703, 0.3299404806269776169, 0.3333333333333333703, 0.3299404806269776169, 0.3333333333333333703, 0.3299404806269776169, 0.3333333333333333703, 0.3299404806269776169, 0.3333333333333333703, 0.3299404806269776169, 0.3333333333333333703, 0.3299404806269776169, 0.3333333333333333703, 0.3299404806269776169, 0.3333333333333333703, 0.3299404806269776169, 0.3333333333333333703, 0.3299404806269776169, 0.3333333333333333703, 0.3299404806269776169, 0.3333333333333333703, 0.3299404806269776169, 0.3333333333333333703, 0.3299404806269776169, 0.3333333333333333703, 0.3299404806269776169, 0.3333333333333333703, 0.3299404806269776169, 0.3333333333333333703, 0.3299404806269776169, 0.3333333333333333703, 0.3299404806269776169, 0.3333333333333333703, 0.3299404806269776169, 0.3333333333333333703, 0.3299404806269776169, 0.3333333333333333703, 0.3299404806269776169, 0.3333333333333333703, 0.3299404806269776169, 0.3333333333333333703, 0.3299404806269776169, 0.3333333333333333703, 0.3299404806269776169, 0.3333333333333333703, 0.3299404806269776169, 0.3333333333333333703, 0.3299404806269776169, 0.3333333333333333703, 0.3299404806269776169, 0.3333333333333333703, 0.3299404806269776169, 0.3333333333333333703, 0.3299404806269776169, 0.3333333333333333703, 0.3299404806269776169, 0.3333333333333333703, 0.3299404806269776169, 0.3333333333333333703, 0.3299404806269776169, 0.3333333333333333703, 0.3299404806269776169, 0.3333333333333333703, 0.3299404806269776169, 0.3333333333333333703, 0.3299404806269776169, 0.3333333333333333703, 0.3299404806269776169, 0.3333333333333333703, 0.3299404806269776169, 0.3333333333333333703, 0.3299404806269776169, 0.3333333333333333703, 0.3299404806269776169, 0.3333333333333333703, 0.3299404806269776169, 0.3333333333333333703, 0.3299404806269776169, 0.3333333333333333703, 0.3299404806269776169, 0.3333333333333333703, 0.3299404806269776169, 0.3333333333333333703, 0.3299404806269776169, 0.3333333333333333703, 0.3299404806269776169, 0.3333333333333333703, 0.3299404806269776169, 0.3333333333333333703, 0.3299404806269776169, 0.3333333333333333703, 0.3299404806269776169, 0.3333333333333333703, 0.3299404806269776169, 0.3333333333333333703, 0.3299404806269776169, 0.3333333333333333703, 0.3299404806269776169, 0.3333333333333333703, 0.3299404806269776169, 0.3333333333333333703, 0.3299404806269776169, 0.3333333333333333703, 0.3299404806269776169, 0.3333333333333333703, 0.3299404806269776169, 0.3333333333333333703, 0.3299404806269776169, 0.3333333333333333703, 0.3299404806269776169, 0.3333333333333333703, 0.3299404806269776169, 0.3333333333333333703, 0.3299404806269776169, 0.3333333333333333703, 0.3299404806269776169, 0.3333333333333333703, 0.3299404806269776169, 0.3333333333333333703, 0.3299404806269776169, 0.3333333333333333703, 0.3299404806269776169, 0.3333333333333333703, 0.3299404806269776169, 0.3333333333333333703, 0.3299404806269776169, 0.3333333333333333703, 0.3299404806269776169, 0.3333333333333333703, 0.3299404806269776169, 0.3333333333333333703, 0.3299404806269776169, 0.3333333333333333703, 0.3299404806269776169, 0.3333333333333333703, 0.3299404806269776169, 0.3333333333333333703, 0.3299404806269776169, 0.3333333333333333703, 0.3299404806269776169, 0.3333333333333333703, 0.3299404806269776169, 0.3333333333333333703, 0.3299404806269776169, 0.3333333333333333703, 0.3299404806269776169, 0.3333333333333333703, 0.3299404806269776169, 0.3333333333333333703, 0.3299404806269776169, 0.3333333333333333703, 0.3299404806269776169, 0.3333333333333333703, 0.3299404806269776169, 0.3333333333333333703, 0.3299404806269776169, 0.3333333333333333703, 0.3299404806269776169, 0.3333333333333333703, 0.3299404806269776169, 0.3333333333333333703, 0.3299404806269776169, 0.3333333333333333703, 0.3299404806269776169, 0.3333333333333333703, 0.3299404806269776169, 0.3333333333333333703, 0.3299404806269776169, 0.3333333333333333703, 0.3299404806269776169, 0.3333333333333333703, 0.3299404806269776169, 0.3333333333333333703, 0.3299404806269776169, 0.3333333333333333703, 0.3299404806269776169, 0.3333333333333333703, 0.3299404806269776169, 0.3333333333333333703, 0.3299404806269776169, 0.3333333333333333703, 0.3299404806269776169, 0.3333333333333333703, 0.3299404806269776169, 0.3333333333333333703, 0.3299404806269776169, 0.3333333333333333703, 0.3299404806269776169, 0.3333333333333333703, 0.3299404806269776169, 0.3333333333333333703, 0.3299404806269776169, 0.3333333333333333703, 0.3299404806269776169, 0.3333333333333333703, 0.3299404806269776169, 0.3333333333333333703, 0.3299404806269776169, 0.3333333333333333703, 0.3299404806269776169, 0.3333333333333333703, 0.3299404806269776169, 0.3333333333333333703, 0.3299404806269776169, 0.3333333333333333703, 0.3299404806269776169, 0.3333333333333333703, 0.3299404806269776169, 0.3333333333333333703, 0.3299404806269776169, 0.3333333333333333703, 0.3299404806269776169, 0.3333333333333333703, 0.3299404806269776169, 0.3333333333333333703, 0.3299404806269776169, 0.3333333333333333703, 0.3299404806269776169, 0.3333333333333333703, 0.3299404806269776169, 0.3333333333333333703, 0.3299404806269776169, 0.3333333333333333703, 0.3299404806269776169, 0.3333333333333333703, 0.3299404806269776169, 0.3333333333333333703, 0.3299404806269776169, 0.3333333333333333703, 0.3299404806269776169, 0.3333333333333333703, 0.3299404806269776169, 0.3333333333333333703, 0.3299404806269776169, 0.3333333333333333703, 0.3299404806269776169, 0.3333333333333333703, 0.3299404806269776169, 0.3333333333333333703, 0.3299404806269776169, 0.3333333333333333703, 0.3299404806269776169, 0.3333333333333333703, 0.3299404806269776169, 0.3333333333333333703, 0.3299404806269776169, 0.3333333333333333703, 0.3299404806269776169, 0.3333333333333333703, 0.3299404806269776169, 0.3333333333333333703, 0.3299404806269776169, 0.3333333333333333703, 0.3299404806269776169, 0.3333333333333333703, 0.3299404806269776169, 0.3333333333333333703, 0.3299404806269776169, 0.3333333333333333703, 0.3299404806269776169, 0.3333333333333333703, 0.3299404806269776169, 0.3333333333333333703, 0.3299404806269776169, 0.3333333333333333703, 0.3299404806269776169, 0.3333333333333333703, 0.3299404806269776169, 0.3333333333333333703, 0.3299404806269776169, 0.3333333333333333703, 0.3299404806269776169, 0.3333333333333333703, 0.3299404806269776169, 0.3333333333333333703, 0.3299404806269776169, 0.3333333333333333703, 0.3299404806269776169, 0.3333333333333333703, 0.3299404806269776169, 0.3333333333333333703, 0.3299404806269776169, 0.3333333333333333703, 0.3299404806269776169, 0.3333333333333333703, 0.3299404806269776169, 0.3333333333333333703, 0.3299404806269776169, 0.3333333333333333703, 0.3299404806269776169, 0.3333333333333333703, 0.3299404806269776169, 0.3333333333333333703, 0.3299404806269776169, 0.3333333333333333703, 0.3299404806269776169, 0.3333333333333333703, 0.3299404806269776169, 0.3333333333333333703, 0.3299404806269776169, 0.3333333333333333703, 0.3299404806269776169, 0.3333333333333333703, 0.3299404806269776169, 0.3333333333333333703, 0.3299404806269776169, 0.3333333333333333703, 0.3299404806269776169, 0.3333333333333333703, 0.3299404806269776169, 0.3333333333333333703, 0.3299404806269776169, 0.3333333333333333703, 0.3299404806269776169, 0.3333333333333333703, 0.3299404806269776169, 0.3333333333333333703, 0.3299404806269776169, 0.3333333333333333703, 0.3299404806269776169, 0.3333333333333333703, 0.3299404806269776169, 0.3333333333333333703, 0.3299404806269776169, 0.3333333333333333703, 0.3299404806269776169, 0.3333333333333333703, 0.3299404806269776169, 0.3333333333333333703, 0.3299404806269776169, 0.3333333333333333703, 0.3299404806269776169, 0.3333333333333333703, 0.3299404806269776169, 0.3333333333333333703, 0.3299404806269776169, 0.3333333333333333703, 0.3299404806269776169, 0.3333333333333333703, 0.3299404806269776169, 0.3333333333333333703, 0.3299404806269776169, 0.3333333333333333703, 0.3299404806269776169, 0.3333333333333333703, 0.3299404806269776169, 0.3333333333333333703, 0.3299404806269776169, 0.3333333333333333703, 0.3299404806269776169, 0.3333333333333333703, 0.3299404806269776169, 0.3333333333333333703, 0.3299404806269776169, 0.3333333333333333703, 0.3299404806269776169, 0.3333333333333333703, 0.3299404806269776169, 0.3333333333333333703, 0.3299404806269776169, 0.3333333333333333703, 0.3299404806269776169, 0.3333333333333333703, 0.3299404806269776169, 0.3333333333333333703, 0.3299404806269776169, 0.3333333333333333703, 0.3299404806269776169, 0.3333333333333333703, 0.3299404806269776169, 0.3333333333333333703, 0.3299404806269776169, 0.3333333333333333703, 0.3299404806269776169, 0.3333333333333333703, 0.3299404806269776169, 0.3333333333333333703, 0.3299404806269776169, 0.3333333333333333703, 0.3299404806269776169, 0.3333333333333333703, 0.3299404806269776169, 0.3333333333333333703, 0.3299404806269776169, 0.3333333333333333703, 0.3299404806269776169, 0.3333333333333333703, 0.3299404806269776169, 0.3333333333333333703, 0.3299404806269776169, 0.3333333333333333703, 0.3299404806269776169, 0.3333333333333333703, 0.3299404806269776169, 0.3333333333333333703, 0.3299404806269776169, 0.3333333333333333703, 0.3299404806269776169, 0.3333333333333333703, 0.3299404806269776169, 0.3333333333333333703, 0.3299404806269776169, 0.3333333333333333703, 0.3299404806269776169, 0.3333333333333333703, 0.3299404806269776169, 0.3333333333333333703, 0.3299404806269776169, 0.3333333333333333703, 0.3299404806269776169, 0.3333333333333333703, 0.3299404806269776169, 0.3333333333333333703, 0.3299404806269776169, 0.3333333333333333703, 0.3299404806269776169, 0.3333333333333333703, 0.3299404806269776169, 0.3333333333333333703, 0.3299404806269776169, 0.3333333333333333703, 0.3299404806269776169, 0.3333333333333333703, 0.3299404806269776169, 0.3333333333333333703, 0.3299404806269776169, 0.3333333333333333703, 0.3299404806269776169, 0.3333333333333333703, 0.3299404806269776169, 0.3333333333333333703, 0.3299404806269776169, 0.3333333333333333703, 0.3299404806269776169, 0.3333333333333333703, 0.3299404806269776169, 0.3333333333333333703, 0.3299404806269776169, 0.3333333333333333703, 0.3299404806269776169, 0.3333333333333333703, 0.3299404806269776169, 0.3333333333333333703, 0.3299404806269776169, 0.3333333333333333703, 0.3299404806269776169, 0.3333333333333333703, 0.3299404806269776169, 0.3333333333333333703, 0.3299404806269776169, 0.3333333333333333703, 0.3299404806269776169, 0.3333333333333333703, 0.3299404806269776169, 0.3333333333333333703, 0.3299404806269776169, 0.3333333333333333703, 0.3299404806269776169, 0.3333333333333333703, 0.3299404806269776169, 0.3333333333333333703, 0.3299404806269776169, 0.3333333333333333703, 0.3299404806269776169, 0.3333333333333333703, 0.3299404806269776169, 0.3333333333333333703, 0.3299404806269776169, 0.3333333333333333703, 0.3299404806269776169, 0.3333333333333333703, 0.3299404806269776169, 0.3333333333333333703, 0.3299404806269776169, 0.3333333333333333703, 0.3299404806269776169, 0.3333333333333333703, 0.3299404806269776169, 0.3333333333333333703, 0.3299404806269776169, 0.3333333333333333703, 0.3299404806269776169, 0.3333333333333333703, 0.3299404806269776169, 0.3333333333333333703, 0.3299404806269776169, 0.3333333333333333703, 0.3299404806269776169, 0.3333333333333333703, 0.3299404806269776169, 0.3333333333333333703, 0.3299404806269776169, 0.3333333333333333703, 0.3299404806269776169, 0.3333333333333333703, 0.3299404806269776169, 0.3333333333333333703, 0.3299404806269776169, 0.3333333333333333703, 0.3299404806269776169, 0.3333333333333333703, 0.3299404806269776169, 0.3333333333333333703, 0.3299404806269776169, 0.3333333333333333703, 0.3299404806269776169, 0.3333333333333333703, 0.3299404806269776169, 0.3333333333333333703, 0.3299404806269776169, 0.3333333333333333703, 0.3299404806269776169, 0.3333333333333333703, 0.3299404806269776169, 0.3333333333333333703, 0.3299404806269776169, 0.3333333333333333703, 0.3299404806269776169, 0.3333333333333333703, 0.3299404806269776169, 0.3333333333333333703, 0.3299404806269776169, 0.3333333333333333703, 0.3299404806269776169, 0.3333333333333333703, 0.3299404806269776169, 0.3333333333333333703, 0.3299404806269776169, 0.3333333333333333703, 0.3299404806269776169, 0.3333333333333333703, 0.3299404806269776169, 0.3333333333333333703, 0.3299404806269776169, 0.3333333333333333703, 0.3299404806269776169, 0.3333333333333333703, 0.3299404806269776169, 0.3333333333333333703, 0.3299404806269776169, 0.3333333333333333703, 0.3299404806269776169, 0.3333333333333333703, 0.3299404806269776169, 0.3333333333333333703, 0.3299404806269776169, 0.3333333333333333703, 0.3299404806269776169, 0.3333333333333333703, 0.3299404806269776169, 0.3333333333333333703, 0.3299404806269776169, 0.3333333333333333703, 0.3299404806269776169, 0.3333333333333333703, 0.3299404806269776169, 0.3333333333333333703, 0.3299404806269776169, 0.3333333333333333703, 0.3299404806269776169, 0.3333333333333333703, 0.3299404806269776169, 0.3333333333333333703, 0.3299404806269776169, 0.3333333333333333703, 0.3299404806269776169, 0.3333333333333333703, 0.3299404806269776169, 0.3333333333333333703, 0.3299404806269776169, 0.3333333333333333703, 0.3299404806269776169, 0.3333333333333333703, 0.3299404806269776169, 0.3333333333333333703, 0.3299404806269776169, 0.3333333333333333703, 0.3299404806269776169, 0.3333333333333333703, 0.3299404806269776169, 0.3333333333333333703, 0.3299404806269776169, 0.3333333333333333703, 0.3299404806269776169, 0.3333333333333333703, 0.3299404806269776169, 0.3333333333333333703, 0.3299404806269776169, 0.3333333333333333703, 0.3299404806269776169, 0.3333333333333333703, 0.3299404806269776169, 0.3333333333333333703, 0.3299404806269776169, 0.3333333333333333703, 0.3299404806269776169, 0.3333333333333333703, 0.3299404806269776169, 0.3333333333333333703, 0.3299404806269776169, 0.3333333333333333703, 0.3299404806269776169, 0.3333333333333333703, 0.3299404806269776169, 0.3333333333333333703, 0.3299404806269776169, 0.3333333333333333703, 0.3299404806269776169, 0.3333333333333333703, 0.3299404806269776169, 0.3333333333333333703, 0.3299404806269776169, 0.3333333333333333703, 0.3299404806269776169, 0.3333333333333333703, 0.3299404806269776169, 0.3333333333333333703, 0.3299404806269776169, 0.3333333333333333703, 0.3299404806269776169, 0.3333333333333333703, 0.3299404806269776169, 0.3333333333333333703, 0.3299404806269776169, 0.3333333333333333703, 0.3299404806269776169, 0.3333333333333333703, 0.3299404806269776169, 0.3333333333333333703, 0.3299404806269776169, 0.3333333333333333703, 0.3299404806269776169, 0.3333333333333333703, 0.3299404806269776169, 0.3333333333333333703, 0.3299404806269776169, 0.3333333333333333703, 0.3299404806269776169, 0.3333333333333333703, 0.3299404806269776169, 0.3333333333333333703, 0.3299404806269776169, 0.3333333333333333703, 0.3299404806269776169, 0.3333333333333333703, 0.3299404806269776169, 0.3333333333333333703, 0.3299404806269776169, 0.3333333333333333703, 0.3299404806269776169, 0.3333333333333333703, 0.3299404806269776169, 0.3333333333333333703, 0.3299404806269776169, 0.3333333333333333703, 0.3299404806269776169, 0.3333333333333333703, 0.3299404806269776169, 0.3333333333333333703, 0.3299404806269776169, 0.3333333333333333703, 0.3299404806269776169, 0.3333333333333333703, 0.3299404806269776169, 0.3333333333333333703, 0.3299404806269776169, 0.3333333333333333703, 0.3299404806269776169, 0.3333333333333333703, 0.3299404806269776169, 0.3333333333333333703, 0.3299404806269776169, 0.3333333333333333703, 0.3299404806269776169, 0.3333333333333333703, 0.3299404806269776169, 0.3333333333333333703, 0.3299404806269776169, 0.3333333333333333703, 0.3299404806269776169, 0.3333333333333333703, 0.3299404806269776169, 0.3333333333333333703, 0.3299404806269776169, 0.3333333333333333703, 0.3299404806269776169, 0.3333333333333333703, 0.3299404806269776169, 0.3333333333333333703, 0.3299404806269776169, 0.3333333333333333703, 0.3299404806269776169, 0.3333333333333333703, 0.3299404806269776169, 0.3333333333333333703, 0.3299404806269776169, 0.3333333333333333703, 0.3299404806269776169, 0.3333333333333333703, 0.3299404806269776169, 0.3333333333333333703, 0.3299404806269776169, 0.3333333333333333703, 0.3299404806269776169, 0.3333333333333333703, 0.3299404806269776169, 0.3333333333333333703, 0.3299404806269776169, 0.3333333333333333703, 0.3299404806269776169, 0.3333333333333333703, 0.3299404806269776169, 0.3333333333333333703, 0.3299404806269776169, 0.3333333333333333703, 0.3299404806269776169, 0.3333333333333333703, 0.3299404806269776169, 0.3333333333333333703, 0.3299404806269776169, 0.3333333333333333703, 0.3299404806269776169, 0.3333333333333333703, 0.3299404806269776169, 0.3333333333333333703, 0.3299404806269776169, 0.3333333333333333703, 0.3299404806269776169, 0.3333333333333333703, 0.3299404806269776169, 0.3333333333333333703, 0.3299404806269776169, 0.3333333333333333703, 0.3299404806269776169, 0.3333333333333333703, 0.3299404806269776169, 0.3333333333333333703, 0.3299404806269776169, 0.3333333333333333703, 0.3299404806269776169, 0.3333333333333333703, 0.3299404806269776169, 0.3333333333333333703, 0.3299404806269776169, 0.3333333333333333703, 0.3299404806269776169, 0.3333333333333333703, 0.3299404806269776169, 0.3333333333333333703, 0.3299404806269776169, 0.3333333333333333703, 0.3299404806269776169, 0.3333333333333333703, 0.3299404806269776169, 0.3333333333333333703, 0.3299404806269776169, 0.3333333333333333703, 0.3299404806269776169, 0.3333333333333333703, 0.3299404806269776169, 0.3333333333333333703, 0.3299404806269776169, 0.3333333333333333703, 0.3299404806269776169, 0.3333333333333333703, 0.3299404806269776169, 0.3333333333333333703, 0.3299404806269776169, 0.3333333333333333703, 0.3299404806269776169, 0.3333333333333333703, 0.3299404806269776169, 0.3333333333333333703, 0.3299404806269776169, 0.3333333333333333703, 0.3299404806269776169, 0.3333333333333333703, 0.3299404806269776169, 0.3333333333333333703, 0.3299404806269776169, 0.3333333333333333703, 0.3299404806269776169, 0.3333333333333333703, 0.3299404806269776169, 0.3333333333333333703, 0.3299404806269776169, 0.3333333333333333703, 0.3299404806269776169, 0.3333333333333333703, 0.3299404806269776169, 0.3333333333333333703, 0.3299404806269776169, 0.3333333333333333703, 0.3299404806269776169, 0.3333333333333333703, 0.3299404806269776169, 0.3333333333333333703, 0.3299404806269776169, 0.3333333333333333703, 0.3299404806269776169, 0.3333333333333333703, 0.3299404806269776169, 0.3333333333333333703, 0.3299404806269776169, 0.3333333333333333703, 0.3299404806269776169, 0.3333333333333333703, 0.3299404806269776169, 0.3333333333333333703, 0.3299404806269776169, 0.3333333333333333703, 0.3299404806269776169, 0.3333333333333333703, 0.3299404806269776169, 0.3333333333333333703, 0.3299404806269776169, 0.3333333333333333703, 0.3299404806269776169, 0.3333333333333333703, 0.3299404806269776169, 0.3333333333333333703, 0.3299404806269776169, 0.3333333333333333703, 0.3299404806269776169, 0.3333333333333333703, 0.3299404806269776169, 0.3333333333333333703, 0.3299404806269776169, 0.3333333333333333703, 0.3299404806269776169, 0.3333333333333333703, 0.3299404806269776169, 0.3333333333333333703, 0.3299404806269776169, 0.3333333333333333703, 0.3299404806269776169, 0.3333333333333333703, 0.3299404806269776169, 0.3333333333333333703, 0.3299404806269776169, 0.3333333333333333703, 0.3299404806269776169, 0.3333333333333333703, 0.3299404806269776169, 0.3333333333333333703, 0.3299404806269776169, 0.3333333333333333703, 0.3299404806269776169, 0.3333333333333333703, 0.3299404806269776169, 0.3333333333333333703, 0.3299404806269776169, 0.3333333333333333703, 0.3299404806269776169, 0.3333333333333333703, 0.3299404806269776169, 0.3333333333333333703, 0.3320603117974822438, 0.3317425830320511193),
 ( 0.3333333333333333703, 0.3299404806269776169, 0.3333333333333333703, 0.3299404806269776169, 0.3333333333333333703, 0.3299404806269776169, 0.3333333333333333703, 0.3299404806269776169, 0.3333333333333333703, 0.3299404806269776169, 0.3333333333333333703, 0.3299404806269776169, 0.3333333333333333703, 0.3299404806269776169, 0.3333333333333333703, 0.3299404806269776169, 0.3333333333333333703, 0.3299404806269776169, 0.3333333333333333703, 0.3299404806269776169, 0.3333333333333333703, 0.3299404806269776169, 0.3333333333333333703, 0.3299404806269776169, 0.3333333333333333703, 0.3299404806269776169, 0.3333333333333333703, 0.3299404806269776169, 0.3333333333333333703, 0.3299404806269776169, 0.3333333333333333703, 0.3299404806269776169, 0.3333333333333333703, 0.3299404806269776169, 0.3333333333333333703, 0.3299404806269776169, 0.3333333333333333703, 0.3299404806269776169, 0.3333333333333333703, 0.3299404806269776169, 0.3333333333333333703, 0.3299404806269776169, 0.3333333333333333703, 0.3299404806269776169, 0.3333333333333333703, 0.3299404806269776169, 0.3333333333333333703, 0.3299404806269776169, 0.3333333333333333703, 0.3299404806269776169, 0.3333333333333333703, 0.3299404806269776169, 0.3333333333333333703, 0.3299404806269776169, 0.3333333333333333703, 0.3299404806269776169, 0.3333333333333333703, 0.3299404806269776169, 0.3333333333333333703, 0.3299404806269776169, 0.3333333333333333703, 0.3299404806269776169, 0.3333333333333333703, 0.3299404806269776169, 0.3333333333333333703, 0.3299404806269776169, 0.3333333333333333703, 0.3299404806269776169, 0.3333333333333333703, 0.3299404806269776169, 0.3333333333333333703, 0.3299404806269776169, 0.3333333333333333703, 0.3299404806269776169, 0.3333333333333333703, 0.3299404806269776169, 0.3333333333333333703, 0.3299404806269776169, 0.3333333333333333703, 0.3299404806269776169, 0.3333333333333333703, 0.3299404806269776169, 0.3333333333333333703, 0.3299404806269776169, 0.3333333333333333703, 0.3299404806269776169, 0.3333333333333333703, 0.3299404806269776169, 0.3333333333333333703, 0.3299404806269776169, 0.3333333333333333703, 0.3299404806269776169, 0.3333333333333333703, 0.3299404806269776169, 0.3333333333333333703, 0.3299404806269776169, 0.3333333333333333703, 0.3299404806269776169, 0.3333333333333333703, 0.3299404806269776169, 0.3333333333333333703, 0.3299404806269776169, 0.3333333333333333703, 0.3299404806269776169, 0.3333333333333333703, 0.3299404806269776169, 0.3333333333333333703, 0.3299404806269776169, 0.3333333333333333703, 0.3299404806269776169, 0.3333333333333333703, 0.3299404806269776169, 0.3333333333333333703, 0.3299404806269776169, 0.3333333333333333703, 0.3299404806269776169, 0.3333333333333333703, 0.3299404806269776169, 0.3333333333333333703, 0.3299404806269776169, 0.3333333333333333703, 0.3299404806269776169, 0.3333333333333333703, 0.3299404806269776169, 0.3333333333333333703, 0.3299404806269776169, 0.3333333333333333703, 0.3299404806269776169, 0.3333333333333333703, 0.3299404806269776169, 0.3333333333333333703, 0.3299404806269776169, 0.3333333333333333703, 0.3299404806269776169, 0.3333333333333333703, 0.3299404806269776169, 0.3333333333333333703, 0.3299404806269776169, 0.3333333333333333703, 0.3299404806269776169, 0.3333333333333333703, 0.3299404806269776169, 0.3333333333333333703, 0.3299404806269776169, 0.3333333333333333703, 0.3299404806269776169, 0.3333333333333333703, 0.3299404806269776169, 0.3333333333333333703, 0.3299404806269776169, 0.3333333333333333703, 0.3299404806269776169, 0.3333333333333333703, 0.3299404806269776169, 0.3333333333333333703, 0.3299404806269776169, 0.3333333333333333703, 0.3299404806269776169, 0.3333333333333333703, 0.3299404806269776169, 0.3333333333333333703, 0.3299404806269776169, 0.3333333333333333703, 0.3299404806269776169, 0.3333333333333333703, 0.3299404806269776169, 0.3333333333333333703, 0.3299404806269776169, 0.3333333333333333703, 0.3299404806269776169, 0.3333333333333333703, 0.3299404806269776169, 0.3333333333333333703, 0.3299404806269776169, 0.3333333333333333703, 0.3299404806269776169, 0.3333333333333333703, 0.3299404806269776169, 0.3333333333333333703, 0.3299404806269776169, 0.3333333333333333703, 0.3299404806269776169, 0.3333333333333333703, 0.3299404806269776169, 0.3333333333333333703, 0.3299404806269776169, 0.3333333333333333703, 0.3299404806269776169, 0.3333333333333333703, 0.3299404806269776169, 0.3333333333333333703, 0.3299404806269776169, 0.3333333333333333703, 0.3299404806269776169, 0.3333333333333333703, 0.3299404806269776169, 0.3333333333333333703, 0.3299404806269776169, 0.3333333333333333703, 0.3299404806269776169, 0.3333333333333333703, 0.3299404806269776169, 0.3333333333333333703, 0.3299404806269776169, 0.3333333333333333703, 0.3299404806269776169, 0.3333333333333333703, 0.3299404806269776169, 0.3333333333333333703, 0.3299404806269776169, 0.3333333333333333703, 0.3299404806269776169, 0.3333333333333333703, 0.3299404806269776169, 0.3333333333333333703, 0.3299404806269776169, 0.3333333333333333703, 0.3299404806269776169, 0.3333333333333333703, 0.3299404806269776169, 0.3333333333333333703, 0.3299404806269776169, 0.3333333333333333703, 0.3299404806269776169, 0.3333333333333333703, 0.3299404806269776169, 0.3333333333333333703, 0.3299404806269776169, 0.3333333333333333703, 0.3299404806269776169, 0.3333333333333333703, 0.3299404806269776169, 0.3333333333333333703, 0.3299404806269776169, 0.3333333333333333703, 0.3299404806269776169, 0.3333333333333333703, 0.3299404806269776169, 0.3333333333333333703, 0.3299404806269776169, 0.3333333333333333703, 0.3299404806269776169, 0.3333333333333333703, 0.3299404806269776169, 0.3333333333333333703, 0.3299404806269776169, 0.3333333333333333703, 0.3299404806269776169, 0.3333333333333333703, 0.3299404806269776169, 0.3333333333333333703, 0.3299404806269776169, 0.3333333333333333703, 0.3299404806269776169, 0.3333333333333333703, 0.3299404806269776169, 0.3333333333333333703, 0.3299404806269776169, 0.3333333333333333703, 0.3299404806269776169, 0.3333333333333333703, 0.3299404806269776169, 0.3333333333333333703, 0.3299404806269776169, 0.3333333333333333703, 0.3299404806269776169, 0.3333333333333333703, 0.3299404806269776169, 0.3333333333333333703, 0.3299404806269776169, 0.3333333333333333703, 0.3299404806269776169, 0.3333333333333333703, 0.3299404806269776169, 0.3333333333333333703, 0.3299404806269776169, 0.3333333333333333703, 0.3299404806269776169, 0.3333333333333333703, 0.3299404806269776169, 0.3333333333333333703, 0.3299404806269776169, 0.3333333333333333703, 0.3299404806269776169, 0.3333333333333333703, 0.3299404806269776169, 0.3333333333333333703, 0.3299404806269776169, 0.3333333333333333703, 0.3299404806269776169, 0.3333333333333333703, 0.3299404806269776169, 0.3333333333333333703, 0.3299404806269776169, 0.3333333333333333703, 0.3299404806269776169, 0.3333333333333333703, 0.3299404806269776169, 0.3333333333333333703, 0.3299404806269776169, 0.3333333333333333703, 0.3299404806269776169, 0.3333333333333333703, 0.3299404806269776169, 0.3333333333333333703, 0.3299404806269776169, 0.3333333333333333703, 0.3299404806269776169, 0.3333333333333333703, 0.3299404806269776169, 0.3333333333333333703, 0.3299404806269776169, 0.3333333333333333703, 0.3299404806269776169, 0.3333333333333333703, 0.3299404806269776169, 0.3333333333333333703, 0.3299404806269776169, 0.3333333333333333703, 0.3299404806269776169, 0.3333333333333333703, 0.3299404806269776169, 0.3333333333333333703, 0.3299404806269776169, 0.3333333333333333703, 0.3299404806269776169, 0.3333333333333333703, 0.3299404806269776169, 0.3333333333333333703, 0.3299404806269776169, 0.3333333333333333703, 0.3299404806269776169, 0.3333333333333333703, 0.3299404806269776169, 0.3333333333333333703, 0.3299404806269776169, 0.3333333333333333703, 0.3299404806269776169, 0.3333333333333333703, 0.3299404806269776169, 0.3333333333333333703, 0.3299404806269776169, 0.3333333333333333703, 0.3299404806269776169, 0.3333333333333333703, 0.3299404806269776169, 0.3333333333333333703, 0.3299404806269776169, 0.3333333333333333703, 0.3299404806269776169, 0.3333333333333333703, 0.3299404806269776169, 0.3333333333333333703, 0.3299404806269776169, 0.3333333333333333703, 0.3299404806269776169, 0.3333333333333333703, 0.3299404806269776169, 0.3333333333333333703, 0.3299404806269776169, 0.3333333333333333703, 0.3299404806269776169, 0.3333333333333333703, 0.3299404806269776169, 0.3333333333333333703, 0.3299404806269776169, 0.3333333333333333703, 0.3299404806269776169, 0.3333333333333333703, 0.3299404806269776169, 0.3333333333333333703, 0.3299404806269776169, 0.3333333333333333703, 0.3299404806269776169, 0.3333333333333333703, 0.3299404806269776169, 0.3333333333333333703, 0.3299404806269776169, 0.3333333333333333703, 0.3299404806269776169, 0.3333333333333333703, 0.3299404806269776169, 0.3333333333333333703, 0.3299404806269776169, 0.3333333333333333703, 0.3299404806269776169, 0.3333333333333333703, 0.3299404806269776169, 0.3333333333333333703, 0.3299404806269776169, 0.3333333333333333703, 0.3299404806269776169, 0.3333333333333333703, 0.3299404806269776169, 0.3333333333333333703, 0.3299404806269776169, 0.3333333333333333703, 0.3299404806269776169, 0.3333333333333333703, 0.3299404806269776169, 0.3333333333333333703, 0.3299404806269776169, 0.3333333333333333703, 0.3299404806269776169, 0.3333333333333333703, 0.3299404806269776169, 0.3333333333333333703, 0.3299404806269776169, 0.3333333333333333703, 0.3299404806269776169, 0.3333333333333333703, 0.3299404806269776169, 0.3333333333333333703, 0.3299404806269776169, 0.3333333333333333703, 0.3299404806269776169, 0.3333333333333333703, 0.3299404806269776169, 0.3333333333333333703, 0.3299404806269776169, 0.3333333333333333703, 0.3299404806269776169, 0.3333333333333333703, 0.3299404806269776169, 0.3333333333333333703, 0.3299404806269776169, 0.3333333333333333703, 0.3299404806269776169, 0.3333333333333333703, 0.3299404806269776169, 0.3333333333333333703, 0.3299404806269776169, 0.3333333333333333703, 0.3299404806269776169, 0.3333333333333333703, 0.3299404806269776169, 0.3333333333333333703, 0.3299404806269776169, 0.3333333333333333703, 0.3299404806269776169, 0.3333333333333333703, 0.3299404806269776169, 0.3333333333333333703, 0.3299404806269776169, 0.3333333333333333703, 0.3299404806269776169, 0.3333333333333333703, 0.3299404806269776169, 0.3333333333333333703, 0.3299404806269776169, 0.3333333333333333703, 0.3299404806269776169, 0.3333333333333333703, 0.3299404806269776169, 0.3333333333333333703, 0.3299404806269776169, 0.3333333333333333703, 0.3299404806269776169, 0.3333333333333333703, 0.3299404806269776169, 0.3333333333333333703, 0.3299404806269776169, 0.3333333333333333703, 0.3299404806269776169, 0.3333333333333333703, 0.3299404806269776169, 0.3333333333333333703, 0.3299404806269776169, 0.3333333333333333703, 0.3299404806269776169, 0.3333333333333333703, 0.3299404806269776169, 0.3333333333333333703, 0.3299404806269776169, 0.3333333333333333703, 0.3299404806269776169, 0.3333333333333333703, 0.3299404806269776169, 0.3333333333333333703, 0.3299404806269776169, 0.3333333333333333703, 0.3299404806269776169, 0.3333333333333333703, 0.3299404806269776169, 0.3333333333333333703, 0.3299404806269776169, 0.3333333333333333703, 0.3299404806269776169, 0.3333333333333333703, 0.3299404806269776169, 0.3333333333333333703, 0.3299404806269776169, 0.3333333333333333703, 0.3299404806269776169, 0.3333333333333333703, 0.3299404806269776169, 0.3333333333333333703, 0.3299404806269776169, 0.3333333333333333703, 0.3299404806269776169, 0.3333333333333333703, 0.3299404806269776169, 0.3333333333333333703, 0.3299404806269776169, 0.3333333333333333703, 0.3299404806269776169, 0.3333333333333333703, 0.3299404806269776169, 0.3333333333333333703, 0.3299404806269776169, 0.3333333333333333703, 0.3299404806269776169, 0.3333333333333333703, 0.3299404806269776169, 0.3333333333333333703, 0.3299404806269776169, 0.3333333333333333703, 0.3299404806269776169, 0.3333333333333333703, 0.3299404806269776169, 0.3333333333333333703, 0.3299404806269776169, 0.3333333333333333703, 0.3299404806269776169, 0.3333333333333333703, 0.3299404806269776169, 0.3333333333333333703, 0.3299404806269776169, 0.3333333333333333703, 0.3299404806269776169, 0.3333333333333333703, 0.3299404806269776169, 0.3333333333333333703, 0.3299404806269776169, 0.3333333333333333703, 0.3299404806269776169, 0.3333333333333333703, 0.3299404806269776169, 0.3333333333333333703, 0.3299404806269776169, 0.3333333333333333703, 0.3299404806269776169, 0.3333333333333333703, 0.3299404806269776169, 0.3333333333333333703, 0.3299404806269776169, 0.3333333333333333703, 0.3299404806269776169, 0.3333333333333333703, 0.3299404806269776169, 0.3333333333333333703, 0.3299404806269776169, 0.3333333333333333703, 0.3299404806269776169, 0.3333333333333333703, 0.3299404806269776169, 0.3333333333333333703, 0.3299404806269776169, 0.3333333333333333703, 0.3299404806269776169, 0.3333333333333333703, 0.3299404806269776169, 0.3333333333333333703, 0.3299404806269776169, 0.3333333333333333703, 0.3299404806269776169, 0.3333333333333333703, 0.3299404806269776169, 0.3333333333333333703, 0.3299404806269776169, 0.3333333333333333703, 0.3299404806269776169, 0.3333333333333333703, 0.3299404806269776169, 0.3333333333333333703, 0.3299404806269776169, 0.3333333333333333703, 0.3299404806269776169, 0.3333333333333333703, 0.3299404806269776169, 0.3333333333333333703, 0.3299404806269776169, 0.3333333333333333703, 0.3299404806269776169, 0.3333333333333333703, 0.3299404806269776169, 0.3333333333333333703, 0.3299404806269776169, 0.3333333333333333703, 0.3299404806269776169, 0.3333333333333333703, 0.3299404806269776169, 0.3333333333333333703, 0.3299404806269776169, 0.3333333333333333703, 0.3299404806269776169, 0.3333333333333333703, 0.3299404806269776169, 0.3333333333333333703, 0.3299404806269776169, 0.3333333333333333703, 0.3299404806269776169, 0.3333333333333333703, 0.3299404806269776169, 0.3333333333333333703, 0.3299404806269776169, 0.3333333333333333703, 0.3299404806269776169, 0.3333333333333333703, 0.3299404806269776169, 0.3333333333333333703, 0.3299404806269776169, 0.3333333333333333703, 0.3299404806269776169, 0.3333333333333333703, 0.3299404806269776169, 0.3333333333333333703, 0.3299404806269776169, 0.3333333333333333703, 0.3299404806269776169, 0.3333333333333333703, 0.3299404806269776169, 0.3333333333333333703, 0.3299404806269776169, 0.3333333333333333703, 0.3299404806269776169, 0.3333333333333333703, 0.3299404806269776169, 0.3333333333333333703, 0.3299404806269776169, 0.3333333333333333703, 0.3299404806269776169, 0.3333333333333333703, 0.3299404806269776169, 0.3333333333333333703, 0.3299404806269776169, 0.3333333333333333703, 0.3299404806269776169, 0.3333333333333333703, 0.3299404806269776169, 0.3333333333333333703, 0.3299404806269776169, 0.3333333333333333703, 0.3299404806269776169, 0.3333333333333333703, 0.3299404806269776169, 0.3333333333333333703, 0.3299404806269776169, 0.3333333333333333703, 0.3299404806269776169, 0.3333333333333333703, 0.3299404806269776169, 0.3333333333333333703, 0.3299404806269776169, 0.3333333333333333703, 0.3299404806269776169, 0.3333333333333333703, 0.3299404806269776169, 0.3333333333333333703, 0.3299404806269776169, 0.3333333333333333703, 0.3299404806269776169, 0.3333333333333333703, 0.3299404806269776169, 0.3333333333333333703, 0.3299404806269776169, 0.3333333333333333703, 0.3299404806269776169, 0.3333333333333333703, 0.3299404806269776169, 0.3333333333333333703, 0.3299404806269776169, 0.3333333333333333703, 0.3299404806269776169, 0.3333333333333333703, 0.3299404806269776169, 0.3333333333333333703, 0.3299404806269776169, 0.3333333333333333703, 0.3299404806269776169, 0.3333333333333333703, 0.3299404806269776169, 0.3333333333333333703, 0.3299404806269776169, 0.3333333333333333703, 0.3299404806269776169, 0.3333333333333333703, 0.3299404806269776169, 0.3333333333333333703, 0.3299404806269776169, 0.3333333333333333703, 0.3299404806269776169, 0.3333333333333333703, 0.3299404806269776169, 0.3333333333333333703, 0.3299404806269776169, 0.3333333333333333703, 0.3299404806269776169, 0.3333333333333333703, 0.3299404806269776169, 0.3333333333333333703, 0.3299404806269776169, 0.3333333333333333703, 0.3299404806269776169, 0.3333333333333333703, 0.3299404806269776169, 0.3333333333333333703, 0.3299404806269776169, 0.3333333333333333703, 0.3299404806269776169, 0.3333333333333333703, 0.3299404806269776169, 0.3333333333333333703, 0.3299404806269776169, 0.3333333333333333703, 0.3299404806269776169, 0.3333333333333333703, 0.3299404806269776169, 0.3333333333333333703, 0.3299404806269776169, 0.3333333333333333703, 0.3299404806269776169, 0.3333333333333333703, 0.3299404806269776169, 0.3333333333333333703, 0.3299404806269776169, 0.3333333333333333703, 0.3299404806269776169, 0.3333333333333333703, 0.3299404806269776169, 0.3333333333333333703, 0.3299404806269776169, 0.3333333333333333703, 0.3299404806269776169, 0.3333333333333333703, 0.3299404806269776169, 0.3333333333333333703, 0.3299404806269776169, 0.3333333333333333703, 0.3299404806269776169, 0.3333333333333333703, 0.3299404806269776169, 0.3333333333333333703, 0.3299404806269776169, 0.3333333333333333703, 0.3299404806269776169, 0.3333333333333333703, 0.3299404806269776169, 0.3333333333333333703, 0.3299404806269776169, 0.3333333333333333703, 0.3299404806269776169, 0.3333333333333333703, 0.3299404806269776169, 0.3333333333333333703, 0.3299404806269776169, 0.3333333333333333703, 0.3299404806269776169, 0.3333333333333333703, 0.3299404806269776169, 0.3333333333333333703, 0.3299404806269776169, 0.3333333333333333703, 0.3299404806269776169, 0.3333333333333333703, 0.3299404806269776169, 0.3333333333333333703, 0.3299404806269776169, 0.3333333333333333703, 0.3299404806269776169, 0.3333333333333333703, 0.3299404806269776169, 0.3333333333333333703, 0.3299404806269776169, 0.3333333333333333703, 0.3299404806269776169, 0.3333333333333333703, 0.3299404806269776169, 0.3333333333333333703, 0.3299404806269776169, 0.3333333333333333703, 0.3299404806269776169, 0.3333333333333333703, 0.3299404806269776169, 0.3333333333333333703, 0.3299404806269776169, 0.3333333333333333703, 0.3299404806269776169, 0.3333333333333333703, 0.3299404806269776169, 0.3333333333333333703, 0.3299404806269776169, 0.3333333333333333703, 0.3299404806269776169, 0.3333333333333333703, 0.3299404806269776169, 0.3333333333333333703, 0.3299404806269776169, 0.3333333333333333703, 0.3299404806269776169, 0.3333333333333333703, 0.3299404806269776169, 0.3333333333333333703, 0.3299404806269776169, 0.3333333333333333703, 0.3299404806269776169, 0.3333333333333333703, 0.3299404806269776169, 0.3333333333333333703, 0.3299404806269776169, 0.3333333333333333703, 0.3299404806269776169, 0.3333333333333333703, 0.3299404806269776169, 0.3333333333333333703, 0.3299404806269776169, 0.3333333333333333703, 0.3299404806269776169, 0.3333333333333333703, 0.3299404806269776169, 0.3333333333333333703, 0.3299404806269776169, 0.3333333333333333703, 0.3299404806269776169, 0.3333333333333333703, 0.3299404806269776169, 0.3333333333333333703, 0.3299404806269776169, 0.3333333333333333703, 0.3299404806269776169, 0.3333333333333333703, 0.3299404806269776169, 0.3333333333333333703, 0.3299404806269776169, 0.3333333333333333703, 0.3299404806269776169, 0.3333333333333333703, 0.3299404806269776169, 0.3333333333333333703, 0.3299404806269776169, 0.3333333333333333703, 0.3299404806269776169, 0.3333333333333333703, 0.3299404806269776169, 0.3333333333333333703, 0.3299404806269776169, 0.3333333333333333703, 0.3299404806269776169, 0.3333333333333333703, 0.3299404806269776169, 0.3333333333333333703, 0.3299404806269776169, 0.3333333333333333703, 0.3299404806269776169, 0.3333333333333333703, 0.3299404806269776169, 0.3333333333333333703, 0.3299404806269776169, 0.3333333333333333703, 0.3299404806269776169, 0.3333333333333333703, 0.3320603117974822438, 0.3317425830320511193),
 ( 1.000000000000000000, 0.9898214418809326842, 1.000000000000000000, 0.9898214418809326842, 1.000000000000000000, 0.9898214418809326842, 1.000000000000000000, 0.9898214418809326842, 1.000000000000000000, 0.9898214418809326842, 1.000000000000000000, 0.9898214418809326842, 1.000000000000000000, 0.9898214418809326842, 1.000000000000000000, 0.9898214418809326842, 1.000000000000000000, 0.9898214418809326842, 1.000000000000000000, 0.9898214418809326842, 1.000000000000000000, 0.9898214418809326842, 1.000000000000000000, 0.9898214418809326842, 1.000000000000000000, 0.9898214418809326842, 1.000000000000000000, 0.9898214418809326842, 1.000000000000000000, 0.9898214418809326842, 1.000000000000000000, 0.9898214418809326842, 1.000000000000000000, 0.9898214418809326842, 1.000000000000000000, 0.9898214418809326842, 1.000000000000000000, 0.9898214418809326842, 1.000000000000000000, 0.9898214418809326842, 1.000000000000000000, 0.9898214418809326842, 1.000000000000000000, 0.9898214418809326842, 1.000000000000000000, 0.9898214418809326842, 1.000000000000000000, 0.9898214418809326842, 1.000000000000000000, 0.9898214418809326842, 1.000000000000000000, 0.9898214418809326842, 1.000000000000000000, 0.9898214418809326842, 1.000000000000000000, 0.9898214418809326842, 1.000000000000000000, 0.9898214418809326842, 1.000000000000000000, 0.9898214418809326842, 1.000000000000000000, 0.9898214418809326842, 1.000000000000000000, 0.9898214418809326842, 1.000000000000000000, 0.9898214418809326842, 1.000000000000000000, 0.9898214418809326842, 1.000000000000000000, 0.9898214418809326842, 1.000000000000000000, 0.9898214418809326842, 1.000000000000000000, 0.9898214418809326842, 1.000000000000000000, 0.9898214418809326842, 1.000000000000000000, 0.9898214418809326842, 1.000000000000000000, 0.9898214418809326842, 1.000000000000000000, 0.9898214418809326842, 1.000000000000000000, 0.9898214418809326842, 1.000000000000000000, 0.9898214418809326842, 1.000000000000000000, 0.9898214418809326842, 1.000000000000000000, 0.9898214418809326842, 1.000000000000000000, 0.9898214418809326842, 1.000000000000000000, 0.9898214418809326842, 1.000000000000000000, 0.9898214418809326842, 1.000000000000000000, 0.9898214418809326842, 1.000000000000000000, 0.9898214418809326842, 1.000000000000000000, 0.9898214418809326842, 1.000000000000000000, 0.9898214418809326842, 1.000000000000000000, 0.9898214418809326842, 1.000000000000000000, 0.9898214418809326842, 1.000000000000000000, 0.9898214418809326842, 1.000000000000000000, 0.9898214418809326842, 1.000000000000000000, 0.9898214418809326842, 1.000000000000000000, 0.9898214418809326842, 1.000000000000000000, 0.9898214418809326842, 1.000000000000000000, 0.9898214418809326842, 1.000000000000000000, 0.9898214418809326842, 1.000000000000000000, 0.9898214418809326842, 1.000000000000000000, 0.9898214418809326842, 1.000000000000000000, 0.9898214418809326842, 1.000000000000000000, 0.9898214418809326842, 1.000000000000000000, 0.9898214418809326842, 1.000000000000000000, 0.9898214418809326842, 1.000000000000000000, 0.9898214418809326842, 1.000000000000000000, 0.9898214418809326842, 1.000000000000000000, 0.9898214418809326842, 1.000000000000000000, 0.9898214418809326842, 1.000000000000000000, 0.9898214418809326842, 1.000000000000000000, 0.9898214418809326842, 1.000000000000000000, 0.9898214418809326842, 1.000000000000000000, 0.9898214418809326842, 1.000000000000000000, 0.9898214418809326842, 1.000000000000000000, 0.9898214418809326842, 1.000000000000000000, 0.9898214418809326842, 1.000000000000000000, 0.9898214418809326842, 1.000000000000000000, 0.9898214418809326842, 1.000000000000000000, 0.9898214418809326842, 1.000000000000000000, 0.9898214418809326842, 1.000000000000000000, 0.9898214418809326842, 1.000000000000000000, 0.9898214418809326842, 1.000000000000000000, 0.9898214418809326842, 1.000000000000000000, 0.9898214418809326842, 1.000000000000000000, 0.9898214418809326842, 1.000000000000000000, 0.9898214418809326842, 1.000000000000000000, 0.9898214418809326842, 1.000000000000000000, 0.9898214418809326842, 1.000000000000000000, 0.9898214418809326842, 1.000000000000000000, 0.9898214418809326842, 1.000000000000000000, 0.9898214418809326842, 1.000000000000000000, 0.9898214418809326842, 1.000000000000000000, 0.9898214418809326842, 1.000000000000000000, 0.9898214418809326842, 1.000000000000000000, 0.9898214418809326842, 1.000000000000000000, 0.9898214418809326842, 1.000000000000000000, 0.9898214418809326842, 1.000000000000000000, 0.9898214418809326842, 1.000000000000000000, 0.9898214418809326842, 1.000000000000000000, 0.9898214418809326842, 1.000000000000000000, 0.9898214418809326842, 1.000000000000000000, 0.9898214418809326842, 1.000000000000000000, 0.9898214418809326842, 1.000000000000000000, 0.9898214418809326842, 1.000000000000000000, 0.9898214418809326842, 1.000000000000000000, 0.9898214418809326842, 1.000000000000000000, 0.9898214418809326842, 1.000000000000000000, 0.9898214418809326842, 1.000000000000000000, 0.9898214418809326842, 1.000000000000000000, 0.9898214418809326842, 1.000000000000000000, 0.9898214418809326842, 1.000000000000000000, 0.9898214418809326842, 1.000000000000000000, 0.9898214418809326842, 1.000000000000000000, 0.9898214418809326842, 1.000000000000000000, 0.9898214418809326842, 1.000000000000000000, 0.9898214418809326842, 1.000000000000000000, 0.9898214418809326842, 1.000000000000000000, 0.9898214418809326842, 1.000000000000000000, 0.9898214418809326842, 1.000000000000000000, 0.9898214418809326842, 1.000000000000000000, 0.9898214418809326842, 1.000000000000000000, 0.9898214418809326842, 1.000000000000000000, 0.9898214418809326842, 1.000000000000000000, 0.9898214418809326842, 1.000000000000000000, 0.9898214418809326842, 1.000000000000000000, 0.9898214418809326842, 1.000000000000000000, 0.9898214418809326842, 1.000000000000000000, 0.9898214418809326842, 1.000000000000000000, 0.9898214418809326842, 1.000000000000000000, 0.9898214418809326842, 1.000000000000000000, 0.9898214418809326842, 1.000000000000000000, 0.9898214418809326842, 1.000000000000000000, 0.9898214418809326842, 1.000000000000000000, 0.9898214418809326842, 1.000000000000000000, 0.9898214418809326842, 1.000000000000000000, 0.9898214418809326842, 1.000000000000000000, 0.9898214418809326842, 1.000000000000000000, 0.9898214418809326842, 1.000000000000000000, 0.9898214418809326842, 1.000000000000000000, 0.9898214418809326842, 1.000000000000000000, 0.9898214418809326842, 1.000000000000000000, 0.9898214418809326842, 1.000000000000000000, 0.9898214418809326842, 1.000000000000000000, 0.9898214418809326842, 1.000000000000000000, 0.9898214418809326842, 1.000000000000000000, 0.9898214418809326842, 1.000000000000000000, 0.9898214418809326842, 1.000000000000000000, 0.9898214418809326842, 1.000000000000000000, 0.9898214418809326842, 1.000000000000000000, 0.9898214418809326842, 1.000000000000000000, 0.9898214418809326842, 1.000000000000000000, 0.9898214418809326842, 1.000000000000000000, 0.9898214418809326842, 1.000000000000000000, 0.9898214418809326842, 1.000000000000000000, 0.9898214418809326842, 1.000000000000000000, 0.9898214418809326842, 1.000000000000000000, 0.9898214418809326842, 1.000000000000000000, 0.9898214418809326842, 1.000000000000000000, 0.9898214418809326842, 1.000000000000000000, 0.9898214418809326842, 1.000000000000000000, 0.9898214418809326842, 1.000000000000000000, 0.9898214418809326842, 1.000000000000000000, 0.9898214418809326842, 1.000000000000000000, 0.9898214418809326842, 1.000000000000000000, 0.9898214418809326842, 1.000000000000000000, 0.9898214418809326842, 1.000000000000000000, 0.9898214418809326842, 1.000000000000000000, 0.9898214418809326842, 1.000000000000000000, 0.9898214418809326842, 1.000000000000000000, 0.9898214418809326842, 1.000000000000000000, 0.9898214418809326842, 1.000000000000000000, 0.9898214418809326842, 1.000000000000000000, 0.9898214418809326842, 1.000000000000000000, 0.9898214418809326842, 1.000000000000000000, 0.9898214418809326842, 1.000000000000000000, 0.9898214418809326842, 1.000000000000000000, 0.9898214418809326842, 1.000000000000000000, 0.9898214418809326842, 1.000000000000000000, 0.9898214418809326842, 1.000000000000000000, 0.9898214418809326842, 1.000000000000000000, 0.9898214418809326842, 1.000000000000000000, 0.9898214418809326842, 1.000000000000000000, 0.9898214418809326842, 1.000000000000000000, 0.9898214418809326842, 1.000000000000000000, 0.9898214418809326842, 1.000000000000000000, 0.9898214418809326842, 1.000000000000000000, 0.9898214418809326842, 1.000000000000000000, 0.9898214418809326842, 1.000000000000000000, 0.9898214418809326842, 1.000000000000000000, 0.9898214418809326842, 1.000000000000000000, 0.9898214418809326842, 1.000000000000000000, 0.9898214418809326842, 1.000000000000000000, 0.9898214418809326842, 1.000000000000000000, 0.9898214418809326842, 1.000000000000000000, 0.9898214418809326842, 1.000000000000000000, 0.9898214418809326842, 1.000000000000000000, 0.9898214418809326842, 1.000000000000000000, 0.9898214418809326842, 1.000000000000000000, 0.9898214418809326842, 1.000000000000000000, 0.9898214418809326842, 1.000000000000000000, 0.9898214418809326842, 1.000000000000000000, 0.9898214418809326842, 1.000000000000000000, 0.9898214418809326842, 1.000000000000000000, 0.9898214418809326842, 1.000000000000000000, 0.9898214418809326842, 1.000000000000000000, 0.9898214418809326842, 1.000000000000000000, 0.9898214418809326842, 1.000000000000000000, 0.9898214418809326842, 1.000000000000000000, 0.9898214418809326842, 1.000000000000000000, 0.9898214418809326842, 1.000000000000000000, 0.9898214418809326842, 1.000000000000000000, 0.9898214418809326842, 1.000000000000000000, 0.9898214418809326842, 1.000000000000000000, 0.9898214418809326842, 1.000000000000000000, 0.9898214418809326842, 1.000000000000000000, 0.9898214418809326842, 1.000000000000000000, 0.9898214418809326842, 1.000000000000000000, 0.9898214418809326842, 1.000000000000000000, 0.9898214418809326842, 1.000000000000000000, 0.9898214418809326842, 1.000000000000000000, 0.9898214418809326842, 1.000000000000000000, 0.9898214418809326842, 1.000000000000000000, 0.9898214418809326842, 1.000000000000000000, 0.9898214418809326842, 1.000000000000000000, 0.9898214418809326842, 1.000000000000000000, 0.9898214418809326842, 1.000000000000000000, 0.9898214418809326842, 1.000000000000000000, 0.9898214418809326842, 1.000000000000000000, 0.9898214418809326842, 1.000000000000000000, 0.9898214418809326842, 1.000000000000000000, 0.9898214418809326842, 1.000000000000000000, 0.9898214418809326842, 1.000000000000000000, 0.9898214418809326842, 1.000000000000000000, 0.9898214418809326842, 1.000000000000000000, 0.9898214418809326842, 1.000000000000000000, 0.9898214418809326842, 1.000000000000000000, 0.9898214418809326842, 1.000000000000000000, 0.9898214418809326842, 1.000000000000000000, 0.9898214418809326842, 1.000000000000000000, 0.9898214418809326842, 1.000000000000000000, 0.9898214418809326842, 1.000000000000000000, 0.9898214418809326842, 1.000000000000000000, 0.9898214418809326842, 1.000000000000000000, 0.9898214418809326842, 1.000000000000000000, 0.9898214418809326842, 1.000000000000000000, 0.9898214418809326842, 1.000000000000000000, 0.9898214418809326842, 1.000000000000000000, 0.9898214418809326842, 1.000000000000000000, 0.9898214418809326842, 1.000000000000000000, 0.9898214418809326842, 1.000000000000000000, 0.9898214418809326842, 1.000000000000000000, 0.9898214418809326842, 1.000000000000000000, 0.9898214418809326842, 1.000000000000000000, 0.9898214418809326842, 1.000000000000000000, 0.9898214418809326842, 1.000000000000000000, 0.9898214418809326842, 1.000000000000000000, 0.9898214418809326842, 1.000000000000000000, 0.9898214418809326842, 1.000000000000000000, 0.9898214418809326842, 1.000000000000000000, 0.9898214418809326842, 1.000000000000000000, 0.9898214418809326842, 1.000000000000000000, 0.9898214418809326842, 1.000000000000000000, 0.9898214418809326842, 1.000000000000000000, 0.9898214418809326842, 1.000000000000000000, 0.9898214418809326842, 1.000000000000000000, 0.9898214418809326842, 1.000000000000000000, 0.9898214418809326842, 1.000000000000000000, 0.9898214418809326842, 1.000000000000000000, 0.9898214418809326842, 1.000000000000000000, 0.9898214418809326842, 1.000000000000000000, 0.9898214418809326842, 1.000000000000000000, 0.9898214418809326842, 1.000000000000000000, 0.9898214418809326842, 1.000000000000000000, 0.9898214418809326842, 1.000000000000000000, 0.9898214418809326842, 1.000000000000000000, 0.9898214418809326842, 1.000000000000000000, 0.9898214418809326842, 1.000000000000000000, 0.9898214418809326842, 1.000000000000000000, 0.9898214418809326842, 1.000000000000000000, 0.9898214418809326842, 1.000000000000000000, 0.9898214418809326842, 1.000000000000000000, 0.9898214418809326842, 1.000000000000000000, 0.9898214418809326842, 1.000000000000000000, 0.9898214418809326842, 1.000000000000000000, 0.9898214418809326842, 1.000000000000000000, 0.9898214418809326842, 1.000000000000000000, 0.9898214418809326842, 1.000000000000000000, 0.9898214418809326842, 1.000000000000000000, 0.9898214418809326842, 1.000000000000000000, 0.9898214418809326842, 1.000000000000000000, 0.9898214418809326842, 1.000000000000000000, 0.9898214418809326842, 1.000000000000000000, 0.9898214418809326842, 1.000000000000000000, 0.9898214418809326842, 1.000000000000000000, 0.9898214418809326842, 1.000000000000000000, 0.9898214418809326842, 1.000000000000000000, 0.9898214418809326842, 1.000000000000000000, 0.9898214418809326842, 1.000000000000000000, 0.9898214418809326842, 1.000000000000000000, 0.9898214418809326842, 1.000000000000000000, 0.9898214418809326842, 1.000000000000000000, 0.9898214418809326842, 1.000000000000000000, 0.9898214418809326842, 1.000000000000000000, 0.9898214418809326842, 1.000000000000000000, 0.9898214418809326842, 1.000000000000000000, 0.9898214418809326842, 1.000000000000000000, 0.9898214418809326842, 1.000000000000000000, 0.9898214418809326842, 1.000000000000000000, 0.9898214418809326842, 1.000000000000000000, 0.9898214418809326842, 1.000000000000000000, 0.9898214418809326842, 1.000000000000000000, 0.9898214418809326842, 1.000000000000000000, 0.9898214418809326842, 1.000000000000000000, 0.9898214418809326842, 1.000000000000000000, 0.9898214418809326842, 1.000000000000000000, 0.9898214418809326842, 1.000000000000000000, 0.9898214418809326842, 1.000000000000000000, 0.9898214418809326842, 1.000000000000000000, 0.9898214418809326842, 1.000000000000000000, 0.9898214418809326842, 1.000000000000000000, 0.9898214418809326842, 1.000000000000000000, 0.9898214418809326842, 1.000000000000000000, 0.9898214418809326842, 1.000000000000000000, 0.9898214418809326842, 1.000000000000000000, 0.9898214418809326842, 1.000000000000000000, 0.9898214418809326842, 1.000000000000000000, 0.9898214418809326842, 1.000000000000000000, 0.9898214418809326842, 1.000000000000000000, 0.9898214418809326842, 1.000000000000000000, 0.9898214418809326842, 1.000000000000000000, 0.9898214418809326842, 1.000000000000000000, 0.9898214418809326842, 1.000000000000000000, 0.9898214418809326842, 1.000000000000000000, 0.9898214418809326842, 1.000000000000000000, 0.9898214418809326842, 1.000000000000000000, 0.9898214418809326842, 1.000000000000000000, 0.9898214418809326842, 1.000000000000000000, 0.9898214418809326842, 1.000000000000000000, 0.9898214418809326842, 1.000000000000000000, 0.9898214418809326842, 1.000000000000000000, 0.9898214418809326842, 1.000000000000000000, 0.9898214418809326842, 1.000000000000000000, 0.9898214418809326842, 1.000000000000000000, 0.9898214418809326842, 1.000000000000000000, 0.9898214418809326842, 1.000000000000000000, 0.9898214418809326842, 1.000000000000000000, 0.9898214418809326842, 1.000000000000000000, 0.9898214418809326842, 1.000000000000000000, 0.9898214418809326842, 1.000000000000000000, 0.9898214418809326842, 1.000000000000000000, 0.9898214418809326842, 1.000000000000000000, 0.9898214418809326842, 1.000000000000000000, 0.9898214418809326842, 1.000000000000000000, 0.9898214418809326842, 1.000000000000000000, 0.9898214418809326842, 1.000000000000000000, 0.9898214418809326842, 1.000000000000000000, 0.9898214418809326842, 1.000000000000000000, 0.9898214418809326842, 1.000000000000000000, 0.9898214418809326842, 1.000000000000000000, 0.9898214418809326842, 1.000000000000000000, 0.9898214418809326842, 1.000000000000000000, 0.9898214418809326842, 1.000000000000000000, 0.9898214418809326842, 1.000000000000000000, 0.9898214418809326842, 1.000000000000000000, 0.9898214418809326842, 1.000000000000000000, 0.9898214418809326842, 1.000000000000000000, 0.9898214418809326842, 1.000000000000000000, 0.9898214418809326842, 1.000000000000000000, 0.9898214418809326842, 1.000000000000000000, 0.9898214418809326842, 1.000000000000000000, 0.9898214418809326842, 1.000000000000000000, 0.9898214418809326842, 1.000000000000000000, 0.9898214418809326842, 1.000000000000000000, 0.9898214418809326842, 1.000000000000000000, 0.9898214418809326842, 1.000000000000000000, 0.9898214418809326842, 1.000000000000000000, 0.9898214418809326842, 1.000000000000000000, 0.9898214418809326842, 1.000000000000000000, 0.9898214418809326842, 1.000000000000000000, 0.9898214418809326842, 1.000000000000000000, 0.9898214418809326842, 1.000000000000000000, 0.9898214418809326842, 1.000000000000000000, 0.9898214418809326842, 1.000000000000000000, 0.9898214418809326842, 1.000000000000000000, 0.9898214418809326842, 1.000000000000000000, 0.9898214418809326842, 1.000000000000000000, 0.9898214418809326842, 1.000000000000000000, 0.9898214418809326842, 1.000000000000000000, 0.9898214418809326842, 1.000000000000000000, 0.9898214418809326842, 1.000000000000000000, 0.9898214418809326842, 1.000000000000000000, 0.9898214418809326842, 1.000000000000000000, 0.9898214418809326842, 1.000000000000000000, 0.9898214418809326842, 1.000000000000000000, 0.9898214418809326842, 1.000000000000000000, 0.9898214418809326842, 1.000000000000000000, 0.9898214418809326842, 1.000000000000000000, 0.9898214418809326842, 1.000000000000000000, 0.9898214418809326842, 1.000000000000000000, 0.9898214418809326842, 1.000000000000000000, 0.9898214418809326842, 1.000000000000000000, 0.9898214418809326842, 1.000000000000000000, 0.9898214418809326842, 1.000000000000000000, 0.9898214418809326842, 1.000000000000000000, 0.9898214418809326842, 1.000000000000000000, 0.9898214418809326842, 1.000000000000000000, 0.9898214418809326842, 1.000000000000000000, 0.9898214418809326842, 1.000000000000000000, 0.9898214418809326842, 1.000000000000000000, 0.9898214418809326842, 1.000000000000000000, 0.9898214418809326842, 1.000000000000000000, 0.9898214418809326842, 1.000000000000000000, 0.9898214418809326842, 1.000000000000000000, 0.9898214418809326842, 1.000000000000000000, 0.9898214418809326842, 1.000000000000000000, 0.9898214418809326842, 1.000000000000000000, 0.9898214418809326842, 1.000000000000000000, 0.9898214418809326842, 1.000000000000000000, 0.9898214418809326842, 1.000000000000000000, 0.9898214418809326842, 1.000000000000000000, 0.9898214418809326842, 1.000000000000000000, 0.9898214418809326842, 1.000000000000000000, 0.9898214418809326842, 1.000000000000000000, 0.9898214418809326842, 1.000000000000000000, 0.9898214418809326842, 1.000000000000000000, 0.9898214418809326842, 1.000000000000000000, 0.9898214418809326842, 1.000000000000000000, 0.9898214418809326842, 1.000000000000000000, 0.9961809353924466759, 0.9952277490961531914) ) ) 
 REPRESENTATION_ITEM ( '' )  SURFACE ( )  );
#14456=CARTESIAN_POINT ( 'NONE',  ( 757.8323909638827445, -410.6346026584191122, 352.1044303154654358 ) ) ;
#14463=CARTESIAN_POINT ( 'NONE',  ( 759.0159684113467620, -448.9181544815156144, 325.8855110935213020 ) ) ;
#14464=CARTESIAN_POINT ( 'NONE',  ( 757.2208543904082489, -136.7146871989600072, 350.9844846989624330 ) ) ;
#14467=CARTESIAN_POINT ( 'NONE',  ( 748.3538107759620743, -376.7146871989592682, 355.8262568251490165 ) ) ;
#14472=CARTESIAN_POINT ( 'NONE',  ( 755.8990559732751535, -35.46360902697151829, 365.9055244015606831 ) ) ;
#14483=CARTESIAN_POINT ( 'NONE',  ( 755.8894580844503253, -351.8272453906068336, 332.3691319403863531 ) ) ;
#14484=CARTESIAN_POINT ( 'NONE',  ( 804.1009440267234822, -335.4636090269705733, 314.0944755984392600 ) ) ;
#14489=CARTESIAN_POINT ( 'NONE',  ( 749.5768839229115201, -156.5545181178802636, 358.0661480581553064 ) ) ;
#14491=CARTESIAN_POINT ( 'NONE',  ( 808.0189434323515343, -134.0891481129655745, 319.0252816721025511 ) ) ;
#14494=EDGE_CURVE ( 'NONE', #20178, #8526, #43311, .T. ) ;
#14498=CARTESIAN_POINT ( 'NONE',  ( 788.8264449731200330, -237.1800572038742985, 363.6646147819171233 ) ) ;
#14499=CARTESIAN_POINT ( 'NONE',  ( 762.1177392798416577, -450.5545181178793541, 309.8865473780659272 ) ) ;
#14503=CARTESIAN_POINT ( 'NONE',  ( 745.1769319972822814, 6.194403710130517382, 346.2694204179732083 ) ) ;
#14508=CARTESIAN_POINT ( 'NONE',  ( 781.2497674668890113, -300.3510508353230080, 375.3608509340180603 ) ) ;
#14509=CARTESIAN_POINT ( 'NONE',  ( 755.0636971347428243, -124.2709662947837899, 341.7834795799807353 ) ) ;
#14510=EDGE_LOOP ( 'NONE', ( #15423, #40472, #28932, #35008 ) ) ;
#14512=CARTESIAN_POINT ( 'NONE',  ( 765.0180583372156207, -288.9982390220559978, 360.0135310231089534 ) ) ;
#14515=CARTESIAN_POINT ( 'NONE',  ( 745.4481719005789273, -75.72551174932938522, 347.5162901302853697 ) ) ;
#14521=CARTESIAN_POINT ( 'NONE',  ( 759.7806653035534055, -30.99823902205680071, 324.8639956371180801 ) ) ;
#14524=CARTESIAN_POINT ( 'NONE',  ( 782.4968714119720516, -394.8164208402374697, 305.0891759886411023 ) ) ;
#14525=CARTESIAN_POINT ( 'NONE',  ( 803.8556311672234642, -297.6237781080502600, 365.6418435158340117 ) ) ;
#14526=CARTESIAN_POINT ( 'NONE',  ( 751.2241431872005251, -88.16923265350555994, 359.9636004259367610 ) ) ;
#14532=CARTESIAN_POINT ( 'NONE',  ( 808.3070685750230950, -402.9982390220555430, 361.1904061080339261 ) ) ;
#14533=CARTESIAN_POINT ( 'NONE',  ( 770.0084009877317612, 19.77989614203463375, 311.3857915150574627 ) ) ;
#14537=DIRECTION ( 'NONE',  ( 0.000000000000000000, 0.000000000000000000, -1.000000000000000000 ) ) ;
#14538=CARTESIAN_POINT ( 'NONE',  ( 754.7162404726377645, -254.7363362996981095, 339.4709603349214717 ) ) ;
#14539=CARTESIAN_POINT ( 'NONE',  ( 785.3141322388236176, -141.7255117493291721, 364.4286716492789537 ) ) ;
#14540=ORIENTED_EDGE ( 'NONE', *, *, #42688, .T. ) ;
#14543=CARTESIAN_POINT ( 'NONE',  ( 780.5290396650775619, -324.3510508353229511, 365.2837595273619513 ) ) ;
#14546=CARTESIAN_POINT ( 'NONE',  ( 760.0363995740630116, -34.91815448151697154, 368.7758568127991907 ) ) ;
#14550=CARTESIAN_POINT ( 'NONE',  ( 804.9363028652555840, -64.27096629478397460, 338.2165204200192079 ) ) ;
#14551=CARTESIAN_POINT ( 'NONE',  ( 759.9999999999992042, -462.9681489794448339, 370.0000000000000568 ) ) ;
#14553=AXIS2_PLACEMENT_3D ( 'NONE', #26378, #26146, #15755 ) ;
#14554=CARTESIAN_POINT ( 'NONE',  ( 768.9521613784389729, -441.8272453906066630, 373.2346286133773106 ) ) ;
#14557=CARTESIAN_POINT ( 'NONE',  ( 759.2295555964440155, -376.1692326535046504, 353.9708237608231229 ) ) ;
#14558=CARTESIAN_POINT ( 'NONE',  ( 777.4774526936600978, -34.27096629478407408, 304.7301800767028226 ) ) ;
#14563=CARTESIAN_POINT ( 'NONE',  ( 759.2295555964440155, -40.16923265350570915, 353.9708237608231229 ) ) ;
#14565=CARTESIAN_POINT ( 'NONE',  ( 810.1134526219336749, -200.5328690171415644, 357.8822607201570349 ) ) ;
#14566=CARTESIAN_POINT ( 'NONE',  ( 768.0187753319979720, -8.634602658420517329, 318.0580252608186242 ) ) ;
#14569=CARTESIAN_POINT ( 'NONE',  ( 756.5762568750052424, -195.1800572038744974, 348.7366044899774238 ) ) ;
#14571=CARTESIAN_POINT ( 'NONE',  ( 778.1981804954715471, -322.2709662947830793, 314.8072714833591021 ) ) ;
#14576=CARTESIAN_POINT ( 'NONE',  ( 800.7704444035546203, -52.16923265350567362, 326.0291762391768771 ) ) ;
#14580=CARTESIAN_POINT ( 'NONE',  ( 814.5518280994195948, -303.7255117493286889, 332.4837098697145166 ) ) ;
#14581=CARTESIAN_POINT ( 'NONE',  ( 771.2368401574024119, 10.55804007376686826, 374.2805881961240857 ) ) ;
#14588=CARTESIAN_POINT ( 'NONE',  ( 747.2067596250078623, -291.1800572038741848, 352.2312462859687230 ) ) ;
#14590=CARTESIAN_POINT ( 'NONE',  ( 784.1219089521767955, -213.2817908451527842, 315.0488828828318333 ) ) ;
#14591=CARTESIAN_POINT ( 'NONE',  ( 776.9566956441375396, -324.8965053807775121, 364.8461984189686405 ) ) ;
#14593=CARTESIAN_POINT ( 'NONE',  ( 755.8894580844503253, -159.8272453906075157, 332.3691319403863531 ) ) ;
#14594=CARTESIAN_POINT ( 'NONE',  ( 795.1360043628807261, -44.08914811296584446, 360.2193346964456282 ) ) ;
#14598=CARTESIAN_POINT ( 'NONE',  ( 746.4236121716829757, -255.8272453906072315, 328.8385539511384650 ) ) ;
#14599=CARTESIAN_POINT ( 'NONE',  ( 754.8983024940795303, -186.8965053807779668, 336.9254006560228163 ) ) ;
#14602=CARTESIAN_POINT ( 'NONE',  ( 797.6776695296629214, 4.456306432488530866, 357.6776695296636603 ) ) ;
#14606=CARTESIAN_POINT ( 'NONE',  ( 754.9967657858570647, -25.54369356751136877, 365.0032342141425374 ) ) ;
#14607=CARTESIAN_POINT ( 'NONE',  ( 745.4481719005789273, -99.72551174932928575, 347.5162901302853129 ) ) ;
#14611=CARTESIAN_POINT ( 'NONE',  ( 778.7629533639073998, -344.7363362996978253, 375.0009284576466371 ) ) ;
#14613=CARTESIAN_POINT ( 'NONE',  ( 751.9810565676468741, -314.0891481129650629, 360.9747183278973921 ) ) ;
#14618=CARTESIAN_POINT ( 'NONE',  ( 792.1044303154645831, -420.4527844766009252, 317.8323909638837677 ) ) ;
#14619=CARTESIAN_POINT ( 'NONE',  ( 763.8424801807145741, -186.0090635724255890, 320.5453621957614700 ) ) ;
#14622=CARTESIAN_POINT ( 'NONE',  ( 810.1134526219336749, -104.5328690171418913, 357.8822607201570349 ) ) ;
#14623=CARTESIAN_POINT ( 'NONE',  ( 762.1405469898973024, -409.5436935675101608, 357.8594530101016176 ) ) ;
#14624=VECTOR ( 'NONE', #42101, 1000.000000000000000 ) ;
#14626=VERTEX_POINT ( 'NONE', #22127 ) ;
#14629=CARTESIAN_POINT ( 'NONE',  ( 774.6312213355099630, -215.3618753856925423, 364.6798772138717482 ) ) ;
#14630=CARTESIAN_POINT ( 'NONE',  ( 771.1735550268780344, -225.1800572038743553, 316.3353852180828198 ) ) ;
#14634=CARTESIAN_POINT ( 'NONE',  ( 795.1360043628807261, -428.0891481129644944, 360.2193346964456282 ) ) ;
#14637=CARTESIAN_POINT ( 'NONE',  ( 767.6429770376291799, -201.1800572038744690, 306.8695393053162093 ) ) ;
#14638=CARTESIAN_POINT ( 'NONE',  ( 787.5531968255692163, -261.8272453906071746, 316.1348686366205811 ) ) ;
#14639=CARTESIAN_POINT ( 'NONE',  ( 755.0488828828309806, -377.8055962898682765, 344.1219089521771934 ) ) ;
#14646=CARTESIAN_POINT ( 'NONE',  ( 793.2243759319678702, -218.5328690171414792, 318.4439275373583200 ) ) ;
#14654=CARTESIAN_POINT ( 'NONE',  ( 750.9282345327678740, -184.9181544815165239, 319.8311093483690115 ) ) ;
#14659=CARTESIAN_POINT ( 'NONE',  ( 791.0478386215596629, -381.8272453906068336, 306.7653713866226326 ) ) ;
#14664=CARTESIAN_POINT ( 'NONE',  ( 794.9819416627830151, -12.99823902205686821, 319.9864689768909898 ) ) ;
#14665=CARTESIAN_POINT ( 'NONE',  ( 791.0478386215596629, -261.8272453906071746, 306.7653713866226326 ) ) ;
#14667=CARTESIAN_POINT ( 'NONE',  ( 801.1904061080336987, -212.0891481129652902, 368.3070685750235498 ) ) ;
#14670=CARTESIAN_POINT ( 'NONE',  ( 778.1981804954714335, -322.2709662947830225, 314.8072714833589885 ) ) ;
#14671=CARTESIAN_POINT ( 'NONE',  ( 759.0159684113467620, -88.91815448151682233, 325.8855110935213020 ) ) ;
#14672=CARTESIAN_POINT ( 'NONE',  ( 755.5913626894240451, -85.64542720878952764, 346.6156483768012890 ) ) ;
#14676=CARTESIAN_POINT ( 'NONE',  ( 769.1273215169530886, -166.7146871989598367, 317.4527132478988847 ) ) ;
#14677=CARTESIAN_POINT ( 'NONE',  ( 755.3201227861273992, -363.7255117493284047, 345.3687786644892981 ) ) ;
#14680=CARTESIAN_POINT ( 'NONE',  ( 762.3223304703356007, -127.5436935675110561, 322.3223304703362828 ) ) ;
#14683=CARTESIAN_POINT ( 'NONE',  ( 754.0944755984390895, -399.6237781080500326, 364.1009440267246760 ) ) ;
#14685=CARTESIAN_POINT ( 'NONE',  ( 800.2193346964447755, -330.9982390220558273, 355.1360043628815788 ) ) ;
#14690=CARTESIAN_POINT ( 'NONE',  ( 771.2633955100217236, -431.9073299311464211, 363.4237431249939618 ) ) ;
#14696=CARTESIAN_POINT ( 'NONE',  ( 767.8955696845333705, -0.4527844766023628176, 362.1676090361162323 ) ) ;
#14697=CARTESIAN_POINT ( 'NONE',  ( 811.0346526505616112, -230.6346026584197659, 323.0537975583477532 ) ) ;
#14698=CARTESIAN_POINT ( 'NONE',  ( 794.1144889064781864, -130.1692326535054463, 360.9840315886528401 ) ) ;
#14701=CARTESIAN_POINT ( 'NONE',  ( 813.2346286133761168, -389.2601417444136018, 328.9521613784389160 ) ) ;
#14706=CARTESIAN_POINT ( 'NONE',  ( 793.5525998758768083, -31.09997266333516919, 372.6845335610516941 ) ) ;
#14714=CARTESIAN_POINT ( 'NONE',  ( 775.8780910478218402, -369.2817908451523294, 364.9511171171680530 ) ) ;
#14715=CARTESIAN_POINT ( 'NONE',  ( 745.7194118038753459, -349.6454272087887603, 348.7631598425976449 ) ) ;
#14718=DIRECTION ( 'NONE',  ( 0.000000000000000000, 0.000000000000000000, -1.000000000000000000 ) ) ;
#14721=CARTESIAN_POINT ( 'NONE',  ( 771.3260364891663130, -139.6454272087893571, 306.0683387631859773 ) ) ;
#14723=CARTESIAN_POINT ( 'NONE',  ( 800.9747183278959710, -108.9982390220565804, 311.9810565676471583 ) ) ;
#14727=CARTESIAN_POINT ( 'NONE',  ( 778.1981804954714335, -226.2709662947834204, 314.8072714833589885 ) ) ;
#14728=CARTESIAN_POINT ( 'NONE',  ( 815.3608509340175488, -458.7363362996973706, 341.2497674668889545 ) ) ;
#14733=CARTESIAN_POINT ( 'NONE',  ( 758.0141637701419768, -39.07832356259662276, 367.2620300519063790 ) ) ;
#14735=CARTESIAN_POINT ( 'NONE',  ( 788.7366044899766848, -11.90732993114778182, 316.5762568750059813 ) ) ;
#14737=CARTESIAN_POINT ( 'NONE',  ( 815.1787889125755555, -318.8965053807775121, 343.7953271457877804 ) ) ;
#14738=CARTESIAN_POINT ( 'NONE',  ( 781.7834795799800531, -154.8164208402382371, 315.0636971347436202 ) ) ;
#14740=CARTESIAN_POINT ( 'NONE',  ( 794.9819416627830151, -300.9982390220559409, 319.9864689768909898 ) ) ;
#14742=CARTESIAN_POINT ( 'NONE',  ( 812.7932403749906598, -87.18005720387481006, 327.7687537140311633 ) ) ;
#14743=ORIENTED_EDGE ( 'NONE', *, *, #6040, .T. ) ;
#14748=CARTESIAN_POINT ( 'NONE',  ( 755.3201227861273992, -51.72551174932946338, 345.3687786644892981 ) ) ;
#14749=CARTESIAN_POINT ( 'NONE',  ( 766.0291762391763086, -322.9181544815161260, 360.7704444035551319 ) ) ;
#14751=CARTESIAN_POINT ( 'NONE',  ( 749.2812353651451076, -390.4527844766011526, 323.2262854647983090 ) ) ;
#14752=CARTESIAN_POINT ( 'NONE',  ( 808.7758568127978833, -292.1692326535048210, 320.0363995740631822 ) ) ;
#14760=CARTESIAN_POINT ( 'NONE',  ( 804.7487373415286811, -403.5436935675101608, 364.7487373415288516 ) ) ;
#14764=CARTESIAN_POINT ( 'NONE',  ( 769.9999999999992042, 178.9475563372491251, 320.0000000000000000 ) ) ;
#14767=CARTESIAN_POINT ( 'NONE',  ( 790.0220218866281812, -271.0999726633344267, 363.2186876482849129 ) ) ;
#14768=CARTESIAN_POINT ( 'NONE',  ( 795.1360043628807261, -164.0891481129655176, 360.2193346964456282 ) ) ;
#14773=CARTESIAN_POINT ( 'NONE',  ( 801.3366627262608972, -344.5328690171410813, 353.0897708529566899 ) ) ;
#14775=CARTESIAN_POINT ( 'NONE',  ( 805.6418435158337843, -53.46360902697146855, 363.8556311672236916 ) ) ;
#14777=CARTESIAN_POINT ( 'NONE',  ( 812.7932403749906598, -207.1800572038744406, 327.7687537140311633 ) ) ;
#14778=CARTESIAN_POINT ( 'NONE',  ( 774.6312213355099630, -119.3618753856928691, 364.6798772138717482 ) ) ;
#14780=CARTESIAN_POINT ( 'NONE',  ( 805.6418435158337843, -461.4636090269701754, 363.8556311672236916 ) ) ;
#14783=CARTESIAN_POINT ( 'NONE',  ( 793.2243759319678702, -362.5328690171410813, 318.4439275373583200 ) ) ;
#14784=CARTESIAN_POINT ( 'NONE',  ( 744.7301800767020268, -52.81642084023856398, 337.4774526936615189 ) ) ;
#14786=CARTESIAN_POINT ( 'NONE',  ( 786.6156483768007774, -49.44195992623295410, 315.5913626894246136 ) ) ;
#14788=CARTESIAN_POINT ( 'NONE',  ( 781.2497674668890113, -204.3510508353233774, 375.3608509340180603 ) ) ;
#14789=CARTESIAN_POINT ( 'NONE',  ( 795.1360043628808398, -68.08914811296577341, 360.2193346964456282 ) ) ;
#14792=CARTESIAN_POINT ( 'NONE',  ( 804.6798772138708955, -183.7255117493290015, 334.6312213355107019 ) ) ;
#14794=CARTESIAN_POINT ( 'NONE',  ( 794.9819416627830151, -324.9982390220559409, 319.9864689768909898 ) ) ;
#14798=CARTESIAN_POINT ( 'NONE',  ( 754.9735926884551418, -66.35105083532378956, 340.5236548041000333 ) ) ;
#14800=CARTESIAN_POINT ( 'NONE',  ( 808.3070685750232087, -282.9982390220559409, 361.1904061080339829 ) ) ;
#14802=CARTESIAN_POINT ( 'NONE',  ( 814.8230680027162407, 18.19440371013048008, 333.7305795820267917 ) ) ;
#14808=CARTESIAN_POINT ( 'NONE',  ( 792.3570229623688874, -285.1800572038740711, 373.1304606946836202 ) ) ;
#14810=CARTESIAN_POINT ( 'NONE',  ( 793.2243759319678702, -362.5328690171410813, 318.4439275373583200 ) ) ;
#14814=CARTESIAN_POINT ( 'NONE',  ( 793.0897708529556667, -174.5545181178801784, 361.3366627262616362 ) ) ;
#14815=CARTESIAN_POINT ( 'NONE',  ( 756.3353852180819104, -53.90732993114765037, 331.1735550268788302 ) ) ;
#14819=CARTESIAN_POINT ( 'NONE',  ( 744.6391490659812007, -278.7363362996980527, 338.7502325331110455 ) ) ;
#14820=CARTESIAN_POINT ( 'NONE',  ( 796.7845633553578182, -225.6237781080506011, 358.5707757039688204 ) ) ;
#14823=CARTESIAN_POINT ( 'NONE',  ( 804.6798772138708955, 8.274488250670337663, 334.6312213355107019 ) ) ;
#14826=CARTESIAN_POINT ( 'NONE',  ( 777.5031285880264704, 1.183579159761269040, 374.9108240113588408 ) ) ;
#14827=CARTESIAN_POINT ( 'NONE',  ( 745.0891759886404770, -100.2709662947838609, 342.4968714119734159 ) ) ;
#14832=CARTESIAN_POINT ( 'NONE',  ( 745.7194118038753459, -397.6454272087885329, 348.7631598425976449 ) ) ;
#14835=CARTESIAN_POINT ( 'NONE',  ( 755.2512626584698410, -343.5436935675103314, 315.2512626584710915 ) ) ;
#14839=CARTESIAN_POINT ( 'NONE',  ( 762.1405469898971887, -433.5436935675099903, 357.8594530101015607 ) ) ;
#14840=CARTESIAN_POINT ( 'NONE',  ( 793.9708237608222134, -190.9181544815164955, 319.2295555964448681 ) ) ;
#14843=CARTESIAN_POINT ( 'NONE',  ( 788.7631598425961101, -97.44195992623281199, 305.7194118038759143 ) ) ;
#14844=CARTESIAN_POINT ( 'NONE',  ( 757.8323909638828582, -410.6346026584191691, 352.1044303154654358 ) ) ;
#14845=CARTESIAN_POINT ( 'NONE',  ( 766.5853460496234675, -157.9874144716871456, 372.3518521366060554 ) ) ;
#14846=CARTESIAN_POINT ( 'NONE',  ( 791.9812246680005501, -452.6346026584191691, 361.9419747391813189 ) ) ;
#14847=ORIENTED_EDGE ( 'NONE', *, *, #17991, .T. ) ;
#14850=CARTESIAN_POINT ( 'NONE',  ( 785.3687786644884454, -275.3618753856923149, 315.3201227861279676 ) ) ;
#14851=CARTESIAN_POINT ( 'NONE',  ( 797.6776695296629214, -235.5436935675107293, 357.6776695296636603 ) ) ;
#14854=CARTESIAN_POINT ( 'NONE',  ( 756.3353852180819104, -437.9073299311463074, 331.1735550268788302 ) ) ;
#14857=( NAMED_UNIT ( * ) PLANE_ANGLE_UNIT ( ) SI_UNIT ( $, .RADIAN. ) );
#14858=CARTESIAN_POINT ( 'NONE',  ( 805.0032342141413437, -181.5436935675108430, 314.9967657858572352 ) ) ;
#14860=CARTESIAN_POINT ( 'NONE',  ( 793.0897708529556667, -270.5545181178798657, 361.3366627262616362 ) ) ;
#14863=CARTESIAN_POINT ( 'NONE',  ( 751.2241431872005251, -232.1692326535051620, 359.9636004259367610 ) ) ;
#14868=CARTESIAN_POINT ( 'NONE',  ( 755.0488828828309806, -281.8055962898686175, 344.1219089521771934 ) ) ;
#14876=CARTESIAN_POINT ( 'NONE',  ( 795.8262568251477660, -166.3726999360620198, 308.3538107759623585 ) ) ;
#14881=CARTESIAN_POINT ( 'NONE',  ( 751.9810565676468741, -26.08914811296592262, 360.9747183278973921 ) ) ;
#14885=CARTESIAN_POINT ( 'NONE',  ( 785.3687786644884454, -11.36187538569323863, 315.3201227861279676 ) ) ;
#14886=CARTESIAN_POINT ( 'NONE',  ( 771.3260364891663130, -283.6454272087889308, 306.0683387631859773 ) ) ;
#14888=CARTESIAN_POINT ( 'NONE',  ( 755.2512626584698410, -223.5436935675107577, 315.2512626584710915 ) ) ;
#14891=LINE ( 'NONE', #28969, #1798 ) ;
#14892=CARTESIAN_POINT ( 'NONE',  ( 774.6858677611749044, -321.7255117493286320, 315.5713283507209894 ) ) ;
#14893=CARTESIAN_POINT ( 'NONE',  ( 758.4439275373578084, -84.55451811788046257, 353.2243759319684386 ) ) ;
#14897=CARTESIAN_POINT ( 'NONE',  ( 773.3843516231979720, -157.4419599262326130, 364.4086373105754433 ) ) ;
#14898=CARTESIAN_POINT ( 'NONE',  ( 794.9819416627830151, -372.9982390220557704, 319.9864689768909898 ) ) ;
#14903=CARTESIAN_POINT ( 'NONE',  ( 801.1904061080336987, 3.910851887033985896, 368.3070685750235498 ) ) ;
#14905=CARTESIAN_POINT ( 'NONE',  ( 765.0180583372156207, -312.9982390220559409, 360.0135310231089534 ) ) ;
#14906=EDGE_CURVE ( 'NONE', #32527, #23783, #8736, .T. ) ;
#14910=EDGE_LOOP ( 'NONE', ( #41775, #36098, #11312, #42590 ) ) ;
#14915=CARTESIAN_POINT ( 'NONE',  ( 797.6776695296629214, 4.456306432488530866, 357.6776695296636603 ) ) ;
#14916=CARTESIAN_POINT ( 'NONE',  ( 756.7813123517142913, -139.9874144716872024, 329.9779781133712504 ) ) ;
#14919=CARTESIAN_POINT ( 'NONE',  ( 811.6461892240364477, -388.7146871989592114, 324.1737431748509835 ) ) ;
#14924=CARTESIAN_POINT ( 'NONE',  ( 814.4686193811664907, -51.28179084515328867, 346.2056067578752732 ) ) ;
#14932=CARTESIAN_POINT ( 'NONE',  ( 793.0897708529556667, -390.5545181178794678, 361.3366627262616362 ) ) ;
#14936=CARTESIAN_POINT ( 'NONE',  ( 764.1737431748507561, -130.3726999360621619, 371.6461892240376415 ) ) ;
#14938=CARTESIAN_POINT ( 'NONE',  ( 759.0252816721024374, -120.9982390220565378, 368.0189434323527280 ) ) ;
#14942=CARTESIAN_POINT ( 'NONE',  ( 802.1676090361156639, -206.6346026584198512, 327.8955696845344505 ) ) ;
#14944=CARTESIAN_POINT ( 'NONE',  ( 812.3518521366052028, -457.0999726633339151, 326.5853460496235243 ) ) ;
#14948=CARTESIAN_POINT ( 'NONE',  ( 745.1769319972822814, -17.80559628986940979, 346.2694204179732083 ) ) ;
#14951=CARTESIAN_POINT ( 'NONE',  ( 795.1360043628807261, -20.08914811296592973, 360.2193346964456282 ) ) ;
#14954=CARTESIAN_POINT ( 'NONE',  ( 783.7566961878529810, -336.8965053807774552, 305.1792804349288417 ) ) ;
#14955=CARTESIAN_POINT ( 'NONE',  ( 801.9419747391806368, -162.4527844766018632, 351.9812246680014027 ) ) ;
#14958=CARTESIAN_POINT ( 'NONE',  ( 759.7806653035534055, -342.9982390220557136, 324.8639956371180801 ) ) ;
#14960=CIRCLE ( 'NONE', #40758, 10.00000000000000888 ) ;
#14961=EDGE_CURVE ( 'NONE', #21828, #8827, #19479, .T. ) ;
#14966=CARTESIAN_POINT ( 'NONE',  ( 771.1735550268778070, -57.18005720387489532, 316.3353852180827630 ) ) ;
#14967=CARTESIAN_POINT ( 'NONE',  ( 769.9779781133707957, -379.0999726633341993, 316.7813123517150871 ) ) ;
#14969=CARTESIAN_POINT ( 'NONE',  ( 808.0189434323515343, -398.0891481129647218, 319.0252816721025511 ) ) ;
#14970=CARTESIAN_POINT ( 'NONE',  ( 814.8230680027162407, -293.8055962898685607, 333.7305795820267917 ) ) ;
#14971=CARTESIAN_POINT ( 'NONE',  ( 783.7566961878529810, -72.89650538077830788, 305.1792804349288417 ) ) ;
#14978=CARTESIAN_POINT ( 'NONE',  ( 767.6429770376289525, -441.1800572038735027, 306.8695393053162093 ) ) ;
#14979=CARTESIAN_POINT ( 'NONE',  ( 777.0937506421101943, 18.86692508245304367, 309.9999999999999432 ) ) ;
#14984=CARTESIAN_POINT ( 'NONE',  ( 805.2837595273609850, -266.7363362996981095, 340.5290396650784714 ) ) ;
#14985=CARTESIAN_POINT ( 'NONE',  ( 805.1927285166397041, -160.8164208402382371, 341.8018195045277707 ) ) ;
#14988=CARTESIAN_POINT ( 'NONE',  ( 764.0069404352550464, -327.0783235625956991, 359.2566176426627180 ) ) ;
#14989=LINE ( 'NONE', #24446, #41100 ) ;
#14990=CARTESIAN_POINT ( 'NONE',  ( 781.2370466360911223, -44.73633629969875614, 304.9990715423533629 ) ) ;
#14992=CARTESIAN_POINT ( 'NONE',  ( 778.1981804954714335, -106.2709662947838467, 314.8072714833589885 ) ) ;
#14996=CARTESIAN_POINT ( 'NONE',  ( 747.6481478633932056, -445.0999726633338582, 353.4146539503763620 ) ) ;
#14998=CARTESIAN_POINT ( 'NONE',  ( 799.9999999999993179, -462.9681489794448339, 370.0000000000000568 ) ) ;
#14999=CARTESIAN_POINT ( 'NONE',  ( 772.3691319403857278, -383.2601417444137155, 315.8894580844506663 ) ) ;
#15005=CARTESIAN_POINT ( 'NONE',  ( 744.8212110874229666, -210.8965053807778816, 336.2046728542121627 ) ) ;
#15006=CARTESIAN_POINT ( 'NONE',  ( 755.5713283507202505, -53.36187538569310362, 334.6858677611754729 ) ) ;
#15010=CARTESIAN_POINT ( 'NONE',  ( 765.0180583372156207, -216.9982390220562252, 360.0135310231089534 ) ) ;
#15012=CARTESIAN_POINT ( 'NONE',  ( 802.1676090361155502, -350.6346026584193396, 327.8955696845344505 ) ) ;
#15016=CARTESIAN_POINT ( 'NONE',  ( 805.0032342141413437, -277.5436935675105588, 314.9967657858572352 ) ) ;
#15017=CARTESIAN_POINT ( 'NONE',  ( 766.5853460496234675, 10.01258552831232329, 372.3518521366060554 ) ) ;
#15022=ORIENTED_EDGE ( 'NONE', *, *, #3156, .T. ) ;
#15025=EDGE_LOOP ( 'NONE', ( #19843, #22820, #43011, #42240 ) ) ;
#15026=CARTESIAN_POINT ( 'NONE',  ( 749.2812353651451076, -294.4527844766013800, 323.2262854647983090 ) ) ;
#15028=CARTESIAN_POINT ( 'NONE',  ( 759.0159684113467620, -208.9181544815164102, 325.8855110935213020 ) ) ;
#15030=CARTESIAN_POINT ( 'NONE',  ( 799.2566176426618085, -144.0090635724257027, 324.0069404352559559 ) ) ;
#15031=CARTESIAN_POINT ( 'NONE',  ( 781.8018195045266339, -46.27096629478404566, 365.1927285166406705 ) ) ;
#15035=CARTESIAN_POINT ( 'NONE',  ( 745.5313806188320314, -279.2817908451526137, 333.7943932421247268 ) ) ;
#15036=CARTESIAN_POINT ( 'NONE',  ( 754.9735926884551418, -210.3510508353233490, 340.5236548041000333 ) ) ;
#15040=CARTESIAN_POINT ( 'NONE',  ( 800.9840315886518738, -460.9181544815156713, 354.1144889064786412 ) ) ;
#15043=CARTESIAN_POINT ( 'NONE',  ( 810.7187646348534145, -42.45278447660223264, 356.7737145352016341 ) ) ;
#15044=CARTESIAN_POINT ( 'NONE',  ( 748.9653473494363425, -98.63460265842024910, 356.9462024416521331 ) ) ;
#15047=CARTESIAN_POINT ( 'NONE',  ( 746.4236121716829757, -375.8272453906069472, 328.8385539511384650 ) ) ;
#15049=CARTESIAN_POINT ( 'NONE',  ( 800.9747183278959710, -372.9982390220557704, 311.9810565676471583 ) ) ;
#15053=CARTESIAN_POINT ( 'NONE',  ( 800.2193346964447755, -426.9982390220554862, 355.1360043628815788 ) ) ;
#15054=CIRCLE ( 'NONE', #8391, 20.00000000000001776 ) ;
#15056=CARTESIAN_POINT ( 'NONE',  ( 760.7433823573367135, -180.0090635724255890, 355.9930595647440441 ) ) ;
#15059=CARTESIAN_POINT ( 'NONE',  ( 761.9338519418445230, -86.53286901714194812, 370.4231160770881957 ) ) ;
#15060=CARTESIAN_POINT ( 'NONE',  ( 774.6312213355098493, -431.3618753856918602, 364.6798772138717482 ) ) ;
#15067=CARTESIAN_POINT ( 'NONE',  ( 797.8594530101008786, -253.5436935675104735, 322.1405469898980982 ) ) ;
#15068=CARTESIAN_POINT ( 'NONE',  ( 767.8955696845334842, -264.4527844766016074, 362.1676090361161755 ) ) ;
#15071=CARTESIAN_POINT ( 'NONE',  ( 768.0187753319979720, -440.6346026584191122, 318.0580252608186242 ) ) ;
#15074=CARTESIAN_POINT ( 'NONE',  ( 751.9810565676468741, -194.0891481129654039, 360.9747183278973921 ) ) ;
#15075=CARTESIAN_POINT ( 'NONE',  ( 755.8894580844503253, -255.8272453906072315, 332.3691319403863531 ) ) ;
#15078=CARTESIAN_POINT ( 'NONE',  ( 791.1614460488616487, -227.2601417444141987, 373.5763878283158874 ) ) ;
#15085=CARTESIAN_POINT ( 'NONE',  ( 798.7617431975189675, -267.6237781080504305, 323.0428371773161871 ) ) ;
#15094=CARTESIAN_POINT ( 'NONE',  ( 815.3608509340175488, -170.7363362996983938, 341.2497674668889545 ) ) ;
#15103=CARTESIAN_POINT ( 'NONE',  ( 759.9864689768902508, -26.08914811296592262, 354.9819416627836404 ) ) ;
#15106=CARTESIAN_POINT ( 'NONE',  ( 797.8822607201568644, -294.5545181178797520, 370.1134526219340160 ) ) ;
#15108=CARTESIAN_POINT ( 'NONE',  ( 772.5602148656447525, -225.7255117493289163, 305.7998596910095443 ) ) ;
#15114=CARTESIAN_POINT ( 'NONE',  ( 778.2165204200184689, -334.8164208402376403, 364.9363028652563230 ) ) ;
#15115=CARTESIAN_POINT ( 'NONE',  ( 798.5707757039680246, -101.4636090269713264, 356.7845633553585003 ) ) ;
#15119=CARTESIAN_POINT ( 'NONE',  ( 796.7845633553578182, -153.6237781080508000, 358.5707757039688204 ) ) ;
#15120=CARTESIAN_POINT ( 'NONE',  ( 804.6798772138708955, -351.7255117493284047, 334.6312213355107019 ) ) ;
#15124=CARTESIAN_POINT ( 'NONE',  ( 785.3687786644884454, -155.3618753856927128, 315.3201227861279676 ) ) ;
#15128=CARTESIAN_POINT ( 'NONE',  ( 807.5423716828161105, -441.0783235625953580, 362.2119215644372048 ) ) ;
#15129=ORIENTED_EDGE ( 'NONE', *, *, #10566, .T. ) ;
#15130=CARTESIAN_POINT ( 'NONE',  ( 785.3141322388236176, -309.7255117493287457, 364.4286716492789537 ) ) ;
#15134=CARTESIAN_POINT ( 'NONE',  ( 795.1360043628807261, -428.0891481129644944, 360.2193346964456282 ) ) ;
#15142=CARTESIAN_POINT ( 'NONE',  ( 778.2165204200184689, 1.183579159761269040, 364.9363028652563230 ) ) ;
#15143=CARTESIAN_POINT ( 'NONE',  ( 748.9653473494363425, -218.6346026584197944, 356.9462024416521331 ) ) ;
#15144=CARTESIAN_POINT ( 'NONE',  ( 801.3366627262608972, -152.5328690171416781, 353.0897708529566899 ) ) ;
#15153=CARTESIAN_POINT ( 'NONE',  ( 804.1009440267234822, -71.46360902697141171, 314.0944755984392600 ) ) ;
#15161=CARTESIAN_POINT ( 'NONE',  ( 802.5472867521000353, -412.3726999360612808, 350.8726784830461156 ) ) ;
#15169=CARTESIAN_POINT ( 'NONE',  ( 788.6739635108323228, -175.6454272087892718, 373.9316612368139090 ) ) ;
#15171=CARTESIAN_POINT ( 'NONE',  ( 805.0032342141412300, -133.5436935675110135, 314.9967657858571783 ) ) ;
#15176=CARTESIAN_POINT ( 'NONE',  ( 804.6798772138708955, -231.7255117493288310, 334.6312213355107019 ) ) ;
#15177=CARTESIAN_POINT ( 'NONE',  ( 798.5707757039680246, -29.46360902697153250, 356.7845633553585003 ) ) ;
#15179=CIRCLE ( 'NONE', #40972, 30.00000000000008171 ) ;
#15181=DIRECTION ( 'NONE',  ( 0.000000000000000000, 0.000000000000000000, 1.000000000000000000 ) ) ;
#15182=CARTESIAN_POINT ( 'NONE',  ( 815.1787889125755555, -30.89650538077846065, 343.7953271457877804 ) ) ;
#15188=CARTESIAN_POINT ( 'NONE',  ( 755.3201227861273992, -27.72551174932954510, 345.3687786644892981 ) ) ;
#15191=CARTESIAN_POINT ( 'NONE',  ( 751.2241431872005251, -352.1692326535046504, 359.9636004259367610 ) ) ;
#15192=CARTESIAN_POINT ( 'NONE',  ( 778.2165204200184689, -166.8164208402382087, 364.9363028652563230 ) ) ;
#15195=CARTESIAN_POINT ( 'NONE',  ( 791.1614460488616487, -419.2601417444136587, 373.5763878283158874 ) ) ;
#15197=CARTESIAN_POINT ( 'NONE',  ( 804.6798772138708955, -351.7255117493284047, 334.6312213355107019 ) ) ;
#15204=CARTESIAN_POINT ( 'NONE',  ( 778.2165204200184689, -70.81642084023850714, 364.9363028652563230 ) ) ;
#15205=CARTESIAN_POINT ( 'NONE',  ( 786.5483106153019435, -367.6454272087886466, 364.1601925771022366 ) ) ;
#15208=CARTESIAN_POINT ( 'NONE',  ( 748.9653473494365699, -386.6346026584192828, 356.9462024416520762 ) ) ;
#15209=CARTESIAN_POINT ( 'NONE',  ( 800.1688906516307043, -274.1692326535049915, 369.0717654672308186 ) ) ;
#15210=CARTESIAN_POINT ( 'NONE',  ( 815.0009284576459549, -102.3510508353236901, 338.7629533639073429 ) ) ;
#15216=CARTESIAN_POINT ( 'NONE',  ( 745.4481719005789273, -411.7255117493282910, 347.5162901302853129 ) ) ;
#15217=AXIS2_PLACEMENT_3D ( 'NONE', #23605, #6296, #2838 ) ;
#15224=CARTESIAN_POINT ( 'NONE',  ( 757.0176451133909268, -301.0999726633342561, 349.9200121543848354 ) ) ;
#15225=CARTESIAN_POINT ( 'NONE',  ( 781.7834795799800531, -154.8164208402382371, 315.0636971347436202 ) ) ;
#15228=CARTESIAN_POINT ( 'NONE',  ( 779.4709603349208464, -312.3510508353230080, 314.7162404726379918 ) ) ;
#15230=CARTESIAN_POINT ( 'NONE',  ( 760.0363995740630116, -82.91815448151682233, 368.7758568127991907 ) ) ;
#15232=CARTESIAN_POINT ( 'NONE',  ( 804.4286716492782716, -113.3618753856929260, 345.3141322388244703 ) ) ;
#15236=CARTESIAN_POINT ( 'NONE',  ( 804.8461984189677878, -2.190881754244347945, 336.9566956441385628 ) ) ;
#15239=CARTESIAN_POINT ( 'NONE',  ( 804.1601925771018387, -391.4419599262317888, 346.5483106153029098 ) ) ;
#15246=CARTESIAN_POINT ( 'NONE',  ( 815.1787889125755555, -246.8965053807777679, 343.7953271457877804 ) ) ;
#15247=CARTESIAN_POINT ( 'NONE',  ( 804.9363028652555840, -64.27096629478397460, 338.2165204200192079 ) ) ;
#15249=CARTESIAN_POINT ( 'NONE',  ( 762.1405469898971887, -241.5436935675106156, 357.8594530101015607 ) ) ;
#15255=CARTESIAN_POINT ( 'NONE',  ( 772.5602148656447525, -297.7255117493286889, 305.7998596910095443 ) ) ;
#15256=CARTESIAN_POINT ( 'NONE',  ( 793.4146539503750546, -25.98741447168755769, 307.6481478633938877 ) ) ;
#15263=CARTESIAN_POINT ( 'NONE',  ( 746.8695393053150156, -317.9073299311468190, 327.6429770376306010 ) ) ;
#15265=CARTESIAN_POINT ( 'NONE',  ( 766.9102291470427417, -210.5545181178800647, 318.6633372737382501 ) ) ;
#15267=CARTESIAN_POINT ( 'NONE',  ( 801.3366627262608972, -368.5328690171409676, 353.0897708529566899 ) ) ;
#15270=CARTESIAN_POINT ( 'NONE',  ( 796.1575198192839480, -198.0090635724255606, 359.4546378042384163 ) ) ;
#15271=CARTESIAN_POINT ( 'NONE',  ( 764.8639956371174549, -56.08914811296580893, 319.7806653035542013 ) ) ;
#15276=CARTESIAN_POINT ( 'NONE',  ( 805.0264073115434940, -222.3510508353233206, 339.4763451958999099 ) ) ;
#15277=AXIS2_PLACEMENT_3D ( 'NONE', #29405, #36778, #19008 ) ;
#15280=CARTESIAN_POINT ( 'NONE',  ( 793.9708237608222134, -454.9181544815156713, 319.2295555964448681 ) ) ;
#15284=CARTESIAN_POINT ( 'NONE',  ( 796.9462024416508257, -36.45278447660223975, 308.9653473494370246 ) ) ;
#15285=CARTESIAN_POINT ( 'NONE',  ( 787.5162901302840055, -107.3618753856928976, 305.4481719005792684 ) ) ;
#15287=EDGE_CURVE ( 'NONE', #45297, #38829, #6157, .T. ) ;
#15289=CARTESIAN_POINT ( 'NONE',  ( 795.8262568251477660, -382.3726999360613945, 308.3538107759623585 ) ) ;
#15291=CARTESIAN_POINT ( 'NONE',  ( 804.7487373415286811, -379.5436935675102745, 364.7487373415288516 ) ) ;
#15293=CARTESIAN_POINT ( 'NONE',  ( 779.4709603349208464, -0.3510508353240099355, 314.7162404726379918 ) ) ;
#15294=CARTESIAN_POINT ( 'NONE',  ( 769.9779781133707957, -187.0999726633346825, 316.7813123517150871 ) ) ;
#15297=CARTESIAN_POINT ( 'NONE',  ( 803.8556311672234642, -129.6237781080508853, 365.6418435158340117 ) ) ;
#15298=CARTESIAN_POINT ( 'NONE',  ( 797.8594530101009923, -445.5436935675099335, 322.1405469898982119 ) ) ;
#15302=VECTOR ( 'NONE', #5929, 1000.000000000000000 ) ;
#15304=CARTESIAN_POINT ( 'NONE',  ( 774.6312213355099630, -263.3618753856924855, 364.6798772138717482 ) ) ;
#15305=CARTESIAN_POINT ( 'NONE',  ( 788.7366044899766848, -251.9073299311470748, 316.5762568750059813 ) ) ;
#15308=CARTESIAN_POINT ( 'NONE',  ( 759.2295555964440155, 7.830767346494148740, 353.9708237608231229 ) ) ;
#15312=CARTESIAN_POINT ( 'NONE',  ( 814.5518280994195948, -183.7255117493290300, 332.4837098697145166 ) ) ;
#15313=CARTESIAN_POINT ( 'NONE',  ( 755.5913626894240451, -277.6454272087889308, 346.6156483768012890 ) ) ;
#15316=CARTESIAN_POINT ( 'NONE',  ( 801.9858362298568863, -219.0783235625960401, 312.7379699480935642 ) ) ;
#15321=CARTESIAN_POINT ( 'NONE',  ( 755.0488828828309806, -257.8055962898686744, 344.1219089521771934 ) ) ;
#15328=CARTESIAN_POINT ( 'NONE',  ( 781.2370466360911223, -164.7363362996983938, 304.9990715423533629 ) ) ;
#15338=CARTESIAN_POINT ( 'NONE',  ( 758.0580252608178853, -54.45278447660219001, 328.0187753319985404 ) ) ;
#15340=CARTESIAN_POINT ( 'NONE',  ( 764.1737431748507561, -298.3726999360616787, 371.6461892240376415 ) ) ;
#15342=CARTESIAN_POINT ( 'NONE',  ( 767.6429770376289525, -249.1800572038742416, 306.8695393053162093 ) ) ;
#15346=CARTESIAN_POINT ( 'NONE',  ( 800.2193346964447755, -330.9982390220558273, 355.1360043628815788 ) ) ;
#15347=CARTESIAN_POINT ( 'NONE',  ( 779.4763451958990572, -80.73633629969864955, 365.0264073115438919 ) ) ;
#15351=CARTESIAN_POINT ( 'NONE',  ( 761.9338519418445230, -134.5328690171417350, 370.4231160770881957 ) ) ;
#15352=CARTESIAN_POINT ( 'NONE',  ( 786.6156483768007774, -169.4419599262325562, 315.5913626894246136 ) ) ;
#15353=CARTESIAN_POINT ( 'NONE',  ( 781.8018195045266339, -406.2709662947829088, 365.1927285166406705 ) ) ;
#15356=CARTESIAN_POINT ( 'NONE',  ( 791.9812246680005501, -164.6346026584200217, 361.9419747391813189 ) ) ;
#15360=CARTESIAN_POINT ( 'NONE',  ( 811.0346526505616112, 9.365397341579420498, 323.0537975583477532 ) ) ;
#15362=CARTESIAN_POINT ( 'NONE',  ( 788.7366044899766848, -371.9073299311465917, 316.5762568750059813 ) ) ;
#15364=CARTESIAN_POINT ( 'NONE',  ( 759.7806653035534055, -438.9982390220553157, 324.8639956371180801 ) ) ;
#15369=AXIS2_PLACEMENT_3D ( 'NONE', #20783, #45284, #5801 ) ;
#15371=CARTESIAN_POINT ( 'NONE',  ( 756.5762568750052424, -3.180057203875080063, 348.7366044899774238 ) ) ;
#15372=CARTESIAN_POINT ( 'NONE',  ( 745.7998596910086917, -221.3618753856925707, 332.5602148656461168 ) ) ;
#15373=CARTESIAN_POINT ( 'NONE',  ( 805.0264073115434940, -150.3510508353235480, 339.4763451958999099 ) ) ;
#15381=CARTESIAN_POINT ( 'NONE',  ( 814.8207195650702488, -74.19088175424410281, 336.2433038121456548 ) ) ;
#15390=EDGE_CURVE ( 'NONE', #8326, #35766, #2234, .T. ) ;
#15394=CARTESIAN_POINT ( 'NONE',  ( 745.1792804349281596, -182.1908817542437760, 343.7566961878542884 ) ) ;
#15396=CARTESIAN_POINT ( 'NONE',  ( 755.2512626584698410, -151.5436935675109851, 315.2512626584710915 ) ) ;
#15400=CARTESIAN_POINT ( 'NONE',  ( 778.2165204200184689, -214.8164208402380666, 364.9363028652563230 ) ) ;
#15401=CARTESIAN_POINT ( 'NONE',  ( 755.8894580844503253, -15.82724539060794200, 332.3691319403863531 ) ) ;
#15408=CARTESIAN_POINT ( 'NONE',  ( 752.4576283171824116, -21.07832356259667250, 317.7880784355627952 ) ) ;
#15412=CARTESIAN_POINT ( 'NONE',  ( 774.6858677611749044, -9.725511749329603717, 315.5713283507209894 ) ) ;
#15415=CARTESIAN_POINT ( 'NONE',  ( 798.0661480581538854, -362.5328690171410813, 309.5768839229118043 ) ) ;
#15418=CARTESIAN_POINT ( 'NONE',  ( 752.4576283171824116, -429.0783235625953580, 317.7880784355627952 ) ) ;
#15420=CARTESIAN_POINT ( 'NONE',  ( 754.8072714833581358, -340.8164208402376971, 338.1981804954720587 ) ) ;
#15423=ORIENTED_EDGE ( 'NONE', *, *, #19631, .T. ) ;
#15427=EDGE_CURVE ( 'NONE', #43717, #28582, #3396, .T. ) ;
#15428=CARTESIAN_POINT ( 'NONE',  ( 797.6776695296629214, -43.54369356751131903, 357.6776695296636603 ) ) ;
#15429=CARTESIAN_POINT ( 'NONE',  ( 804.8461984189677878, -362.1908817542432644, 336.9566956441385628 ) ) ;
#15431=CARTESIAN_POINT ( 'NONE',  ( 746.8695393053151292, -413.9073299311465348, 327.6429770376306578 ) ) ;
#15432=CARTESIAN_POINT ( 'NONE',  ( 752.4576283171824116, -309.0783235625957559, 317.7880784355627952 ) ) ;
#15440=CARTESIAN_POINT ( 'NONE',  ( 808.3070685750230950, -426.9982390220554862, 361.1904061080339261 ) ) ;
#15447=CARTESIAN_POINT ( 'NONE',  ( 763.8424801807145741, -306.0090635724252479, 320.5453621957614700 ) ) ;
#15448=CARTESIAN_POINT ( 'NONE',  ( 758.0580252608178853, -150.4527844766018916, 328.0187753319985404 ) ) ;
#15451=CARTESIAN_POINT ( 'NONE',  ( 755.0488828828309806, -329.8055962898683902, 344.1219089521771934 ) ) ;
#15454=CARTESIAN_POINT ( 'NONE',  ( 813.5763878283155464, -75.82724539060775726, 351.1614460488615350 ) ) ;
#15456=CARTESIAN_POINT ( 'NONE',  ( 768.0187753319979720, -128.6346026584201354, 318.0580252608186242 ) ) ;
#15459=CARTESIAN_POINT ( 'NONE',  ( 769.0155153010367712, -10.37269993606250473, 362.7791456095907279 ) ) ;
#15462=CARTESIAN_POINT ( 'NONE',  ( 764.0069404352550464, -399.0783235625955285, 359.2566176426627180 ) ) ;
#15464=CARTESIAN_POINT ( 'NONE',  ( 780.5290396650775619, -84.35105083532374692, 365.2837595273619513 ) ) ;
#15469=CARTESIAN_POINT ( 'NONE',  ( 805.9055244015594326, -243.6237781080504590, 315.8990559732753240 ) ) ;
#15470=CARTESIAN_POINT ( 'NONE',  ( 800.0135310231082713, -38.08914811296587999, 325.0180583372163028 ) ) ;
#15473=CARTESIAN_POINT ( 'NONE',  ( 797.6776695296629214, -235.5436935675107293, 357.6776695296636603 ) ) ;
#15476=FACE_OUTER_BOUND ( 'NONE', #22390, .T. ) ;
#15480=CARTESIAN_POINT ( 'NONE',  ( 787.4397851343537695, -285.7255117493286889, 374.2001403089903988 ) ) ;
#15481=CARTESIAN_POINT ( 'NONE',  ( 748.3538107759620743, -16.71468719896031985, 355.8262568251490165 ) ) ;
#15488=CARTESIAN_POINT ( 'NONE',  ( 813.1304606946830518, -329.9073299311467053, 352.3570229623690580 ) ) ;
#15489=LINE ( 'NONE', #923, #10061 ) ;
#15492=CARTESIAN_POINT ( 'NONE',  ( 793.9708237608222134, -190.9181544815164955, 319.2295555964448681 ) ) ;
#15493=CARTESIAN_POINT ( 'NONE',  ( 801.9419747391806368, -42.45278447660223264, 351.9812246680014027 ) ) ;
#15497=CARTESIAN_POINT ( 'NONE',  ( 769.1273215169530886, -238.7146871989596661, 317.4527132478988847 ) ) ;
#15500=CARTESIAN_POINT ( 'NONE',  ( 815.2698199232961542, -448.8164208402371855, 342.5225473063383106 ) ) ;
#15504=CARTESIAN_POINT ( 'NONE',  ( 744.7301800767019131, -52.81642084023856398, 337.4774526936615757 ) ) ;
#15505=CARTESIAN_POINT ( 'NONE',  ( 796.7737145352015204, -92.63460265842026331, 370.7187646348536987 ) ) ;
#15508=CARTESIAN_POINT ( 'NONE',  ( 781.2370466360911223, -380.7363362996977116, 304.9990715423533629 ) ) ;
#15510=CARTESIAN_POINT ( 'NONE',  ( 772.4837098697144029, -359.3618753856920875, 374.5518280994205611 ) ) ;
#15512=CARTESIAN_POINT ( 'NONE',  ( 790.8726784830453198, 13.28531280103958423, 362.5472867521010585 ) ) ;
#15515=CARTESIAN_POINT ( 'NONE',  ( 793.4146539503750546, -121.9874144716872593, 307.6481478633938877 ) ) ;
#15516=CARTESIAN_POINT ( 'NONE',  ( 791.0208441182601291, -452.8006503659887585, 362.4663821942984328 ) ) ;
#15520=CARTESIAN_POINT ( 'NONE',  ( 804.6798772138708955, -135.7255117493291152, 334.6312213355107019 ) ) ;
#15522=CARTESIAN_POINT ( 'NONE',  ( 756.5762568750052424, -267.1800572038742985, 348.7366044899774238 ) ) ;
#15523=CARTESIAN_POINT ( 'NONE',  ( 804.9363028652555840, -256.2709662947834204, 338.2165204200192079 ) ) ;
#15526=CARTESIAN_POINT ( 'NONE',  ( 772.3691319403857278, 24.73985825558500551, 315.8894580844506663 ) ) ;
#15528=CARTESIAN_POINT ( 'NONE',  ( 772.5602148656447525, -201.7255117493290015, 305.7998596910095443 ) ) ;
#15529=CARTESIAN_POINT ( 'NONE',  ( 787.5531968255692163, -285.8272453906071178, 316.1348686366205811 ) ) ;
#15530=CARTESIAN_POINT ( 'NONE',  ( 784.0799538623451781, -395.8055962898682765, 364.6971507214555572 ) ) ;
#15537=CARTESIAN_POINT ( 'NONE',  ( 754.8983024940795303, -258.8965053807777963, 336.9254006560228163 ) ) ;
#15544=CARTESIAN_POINT ( 'NONE',  ( 805.6418435158337843, -173.4636090269710849, 363.8556311672236916 ) ) ;
#15553=CARTESIAN_POINT ( 'NONE',  ( 778.2165204200184689, -46.81642084023858530, 364.9363028652563230 ) ) ;
#15554=CARTESIAN_POINT ( 'NONE',  ( 747.6481478633932056, -301.0999726633342561, 353.4146539503763620 ) ) ;
#15555=CARTESIAN_POINT ( 'NONE',  ( 772.4837098697144029, -263.3618753856924855, 374.5518280994205611 ) ) ;
#15559=CARTESIAN_POINT ( 'NONE',  ( 771.1735550268778070, -369.1800572038739574, 316.3353852180827630 ) ) ;
#15560=CARTESIAN_POINT ( 'NONE',  ( 779.4763451958990572, -128.7363362996984790, 365.0264073115438919 ) ) ;
#15564=CARTESIAN_POINT ( 'NONE',  ( 801.9419747391806368, -378.4527844766011526, 351.9812246680014027 ) ) ;
#15567=CARTESIAN_POINT ( 'NONE',  ( 801.9419747391806368, -162.4527844766018632, 351.9812246680014027 ) ) ;
#15572=CARTESIAN_POINT ( 'NONE',  ( 778.1981804954714335, -346.2709662947830793, 314.8072714833589885 ) ) ;
#15574=CARTESIAN_POINT ( 'NONE',  ( 788.7366044899766848, -443.9073299311464780, 316.5762568750059813 ) ) ;
#15577=CARTESIAN_POINT ( 'NONE',  ( 754.9967657858570647, -97.54369356751114140, 365.0032342141425943 ) ) ;
#15582=CARTESIAN_POINT ( 'NONE',  ( 762.3223304703356007, -7.543693567511430942, 322.3223304703362828 ) ) ;
#15583=CARTESIAN_POINT ( 'NONE',  ( 766.7756240680305382, -158.5328690171417065, 361.5560724626415663 ) ) ;
#15590=CARTESIAN_POINT ( 'NONE',  ( 776.2046728542105711, -68.19088175424413123, 304.8212110874238761 ) ) ;
#15591=LINE ( 'NONE', #33156, #4238 ) ;
#15597=CARTESIAN_POINT ( 'NONE',  ( 799.9999999999993179, 166.4563064324884465, 319.9999999999999432 ) ) ;
#15599=CARTESIAN_POINT ( 'NONE',  ( 796.1575198192839480, -414.0090635724249637, 359.4546378042384163 ) ) ;
#15603=CARTESIAN_POINT ( 'NONE',  ( 745.7194118038753459, -181.6454272087892434, 348.7631598425976449 ) ) ;
#15605=CARTESIAN_POINT ( 'NONE',  ( 748.9653473494363425, -146.6346026584200217, 356.9462024416521331 ) ) ;
#15608=CARTESIAN_POINT ( 'NONE',  ( 799.9999999999993179, 205.0000000000000568, 350.0000000000000000 ) ) ;
#15609=CARTESIAN_POINT ( 'NONE',  ( 788.7366044899766848, -251.9073299311470748, 316.5762568750059813 ) ) ;
#15610=CARTESIAN_POINT ( 'NONE',  ( 775.8780910478218402, -9.281790845153418346, 364.9511171171680530 ) ) ;
#15615=CARTESIAN_POINT ( 'NONE',  ( 754.9735926884551418, -66.35105083532378956, 340.5236548041000333 ) ) ;
#15616=CARTESIAN_POINT ( 'NONE',  ( 804.4286716492782716, -305.3618753856922581, 345.3141322388244703 ) ) ;
#15620=CARTESIAN_POINT ( 'NONE',  ( 785.3687786644884454, -11.36187538569323863, 315.3201227861279676 ) ) ;
#15623=CARTESIAN_POINT ( 'NONE',  ( 815.0009284576459549, -342.3510508353228943, 338.7629533639073429 ) ) ;
#15625=CARTESIAN_POINT ( 'NONE',  ( 755.3201227861273992, -339.7255117493285184, 345.3687786644892981 ) ) ;
#15634=CARTESIAN_POINT ( 'NONE',  ( 781.8018195045266339, -70.27096629478397460, 365.1927285166406705 ) ) ;
#15635=CARTESIAN_POINT ( 'NONE',  ( 766.9102291470427417, -354.5545181178796383, 318.6633372737382501 ) ) ;
#15636=CARTESIAN_POINT ( 'NONE',  ( 808.3070685750232087, -426.9982390220555430, 361.1904061080339829 ) ) ;
#15637=CARTESIAN_POINT ( 'NONE',  ( 789.5584187865343893, -452.9681489794450613, 363.1011989789364520 ) ) ;
#15638=CARTESIAN_POINT ( 'NONE',  ( 746.7653713866222915, -329.2601417444138860, 351.0478386215610271 ) ) ;
#15639=CARTESIAN_POINT ( 'NONE',  ( 807.5423716828161105, -105.0783235625964096, 362.2119215644372048 ) ) ;
#15644=CARTESIAN_POINT ( 'NONE',  ( 745.0891759886404770, -412.2709662947829088, 342.4968714119734159 ) ) ;
#15646=DIRECTION ( 'NONE',  ( -0.7071067811865697772, 0.000000000000000000, -0.7071067811865252573 ) ) ;
#15652=CARTESIAN_POINT ( 'NONE',  ( 755.3028492785439312, -303.2817908451525000, 335.9200461376539693 ) ) ;
#15653=CARTESIAN_POINT ( 'NONE',  ( 797.8594530101008786, -181.5436935675108145, 322.1405469898980982 ) ) ;
#15659=CARTESIAN_POINT ( 'NONE',  ( 754.3581564841646241, -89.46360902697134065, 316.1443688327762516 ) ) ;
#15662=CARTESIAN_POINT ( 'NONE',  ( 797.8594530101008786, -109.5436935675110988, 322.1405469898980982 ) ) ;
#15666=CARTESIAN_POINT ( 'NONE',  ( 800.9840315886518738, -28.91815448151699286, 354.1144889064786412 ) ) ;
#15669=CARTESIAN_POINT ( 'NONE',  ( 760.5453621957607311, -381.0783235625954717, 323.8424801807151425 ) ) ;
#15676=CARTESIAN_POINT ( 'NONE',  ( 771.2368401574024119, -253.4419599262323572, 374.2805881961240857 ) ) ;
#15677=CARTESIAN_POINT ( 'NONE',  ( 781.7834795799800531, -34.81642084023861372, 315.0636971347436202 ) ) ;
#15680=CARTESIAN_POINT ( 'NONE',  ( 762.3223304703356007, -223.5436935675107577, 322.3223304703362828 ) ) ;
#15684=CARTESIAN_POINT ( 'NONE',  ( 779.9999999999992042, 16.45630643248849267, 370.0000000000000568 ) ) ;
#15689=CARTESIAN_POINT ( 'NONE',  ( 751.9810565676468741, -314.0891481129650629, 360.9747183278973921 ) ) ;
#15690=CARTESIAN_POINT ( 'NONE',  ( 752.4576283171824116, -21.07832356259667250, 317.7880784355627952 ) ) ;
#15695=CARTESIAN_POINT ( 'NONE',  ( 794.9819416627830151, -204.9982390220562820, 319.9864689768909898 ) ) ;
#15698=CARTESIAN_POINT ( 'NONE',  ( 754.9967657858570647, -337.5436935675102177, 365.0032342141425374 ) ) ;
#15702=CARTESIAN_POINT ( 'NONE',  ( 766.0291762391763086, -178.9181544815165239, 360.7704444035551319 ) ) ;
#15703=CARTESIAN_POINT ( 'NONE',  ( 774.6312213355099630, -71.36187538569302546, 364.6798772138717482 ) ) ;
#15704=VERTEX_POINT ( 'NONE', #4077 ) ;
#15709=CARTESIAN_POINT ( 'NONE',  ( 799.4546378042377910, -225.0783235625959833, 356.1575198192848006 ) ) ;
#15712=CARTESIAN_POINT ( 'NONE',  ( 811.0346526505616112, -422.6346026584192259, 323.0537975583477532 ) ) ;
#15713=CARTESIAN_POINT ( 'NONE',  ( 779.9999999999992042, 16.45630643248849267, 339.9999999999999432 ) ) ;
#15716=CARTESIAN_POINT ( 'NONE',  ( 772.4837098697144029, -47.36187538569312494, 374.5518280994205611 ) ) ;
#15717=CARTESIAN_POINT ( 'NONE',  ( 758.8095938919642549, -128.0891481129655176, 311.6929314249763365 ) ) ;
#15721=CARTESIAN_POINT ( 'NONE',  ( 805.0032342141412300, -373.5436935675101040, 314.9967657858571783 ) ) ;
#15723=CARTESIAN_POINT ( 'NONE',  ( 754.9735926884551418, 5.648949164675971524, 340.5236548041000333 ) ) ;
#15726=CARTESIAN_POINT ( 'NONE',  ( 815.0009284576459549, -126.3510508353236048, 338.7629533639073429 ) ) ;
#15727=CARTESIAN_POINT ( 'NONE',  ( 797.6776695296629214, -451.5436935675099903, 357.6776695296636603 ) ) ;
#15731=CARTESIAN_POINT ( 'NONE',  ( 781.7834795799800531, -130.8164208402383224, 315.0636971347436202 ) ) ;
#15733=CARTESIAN_POINT ( 'NONE',  ( 755.0636971347428243, -268.2709662947833067, 341.7834795799807353 ) ) ;
#15734=CARTESIAN_POINT ( 'NONE',  ( 785.3687786644885591, -251.3618753856923718, 315.3201227861280813 ) ) ;
#15738=CARTESIAN_POINT ( 'NONE',  ( 804.9363028652555840, -448.2709662947827951, 338.2165204200192079 ) ) ;
#15743=CARTESIAN_POINT ( 'NONE',  ( 796.7737145352015204, -212.6346026584198796, 370.7187646348536987 ) ) ;
#15744=CARTESIAN_POINT ( 'NONE',  ( 804.6971507214547046, -291.2817908451525000, 344.0799538623459739 ) ) ;
#15745=CARTESIAN_POINT ( 'NONE',  ( 799.4546378042377910, -393.0783235625954717, 356.1575198192848006 ) ) ;
#15746=ORIENTED_EDGE ( 'NONE', *, *, #27251, .F. ) ;
#15753=CARTESIAN_POINT ( 'NONE',  ( 764.0069404352550464, -279.0783235625958127, 359.2566176426627180 ) ) ;
#15755=DIRECTION ( 'NONE',  ( 0.7071067811865753283, 0.000000000000000000, 0.7071067811865198172 ) ) ;
#15760=CARTESIAN_POINT ( 'NONE',  ( 748.6759233522253680, -208.3726999360619061, 324.3348316497537098 ) ) ;
#15765=CARTESIAN_POINT ( 'NONE',  ( 755.2512626584698410, -7.543693567511430942, 315.2512626584710915 ) ) ;
#15771=CARTESIAN_POINT ( 'NONE',  ( 757.8323909638827445, -50.63460265842036989, 352.1044303154654358 ) ) ;
#15772=CARTESIAN_POINT ( 'NONE',  ( 764.1737431748507561, -274.3726999360617356, 371.6461892240376415 ) ) ;
#15773=CARTESIAN_POINT ( 'NONE',  ( 782.5225473063381969, -262.2709662947831930, 375.2698199232970637 ) ) ;
#15777=CARTESIAN_POINT ( 'NONE',  ( 778.1981804954714335, -346.2709662947830793, 314.8072714833589885 ) ) ;
#15778=CARTESIAN_POINT ( 'NONE',  ( 776.9254006560222479, -116.1908817542440033, 314.8983024940802125 ) ) ;
#15783=CARTESIAN_POINT ( 'NONE',  ( 756.5762568750052424, -387.1800572038738437, 348.7366044899774238 ) ) ;
#15786=CARTESIAN_POINT ( 'NONE',  ( 768.0187753319979720, -152.6346026584200786, 318.0580252608186242 ) ) ;
#15789=DIRECTION ( 'NONE',  ( 0.000000000000000000, 0.000000000000000000, 1.000000000000000000 ) ) ;
#15791=CARTESIAN_POINT ( 'NONE',  ( 797.8594530101008786, -349.5436935675102745, 322.1405469898980982 ) ) ;
#15794=CARTESIAN_POINT ( 'NONE',  ( 805.0032342141413437, -85.54369356751118403, 314.9967657858572352 ) ) ;
#15800=CARTESIAN_POINT ( 'NONE',  ( 754.9967657858570647, -241.5436935675106156, 365.0032342141425374 ) ) ;
#15801=CARTESIAN_POINT ( 'NONE',  ( 757.2208543904082489, -160.7146871989598651, 350.9844846989624330 ) ) ;
#15804=CARTESIAN_POINT ( 'NONE',  ( 811.6461892240364477, -412.7146871989590409, 324.1737431748509835 ) ) ;
#15809=CARTESIAN_POINT ( 'NONE',  ( 778.7629533639073998, -56.73633629969872771, 375.0009284576466371 ) ) ;
#15814=LINE ( 'NONE', #35939, #44638 ) ;
#15816=CARTESIAN_POINT ( 'NONE',  ( 792.0613484971601110, -458.0032201311295807, 367.4685979341032294 ) ) ;
#15819=CARTESIAN_POINT ( 'NONE',  ( 755.5913626894240451, -397.6454272087885329, 346.6156483768012890 ) ) ;
#15823=DIRECTION ( 'NONE',  ( 0.000000000000000000, 0.000000000000000000, 1.000000000000000000 ) ) ;
#15825=CARTESIAN_POINT ( 'NONE',  ( 778.7629533639073998, -176.7363362996983369, 375.0009284576466371 ) ) ;
#15827=CARTESIAN_POINT ( 'NONE',  ( 800.9747183278959710, -156.9982390220564241, 311.9810565676471583 ) ) ;
#15830=CARTESIAN_POINT ( 'NONE',  ( 801.9419747391806368, -258.4527844766016074, 351.9812246680014027 ) ) ;
#15832=CARTESIAN_POINT ( 'NONE',  ( 773.4516893846965786, -19.64542720878974791, 315.8398074228977066 ) ) ;
#15838=CARTESIAN_POINT ( 'NONE',  ( 787.6308680596127942, -83.26014174441466764, 364.1105419155492768 ) ) ;
#15839=CARTESIAN_POINT ( 'NONE',  ( 800.2193346964447755, -306.9982390220558273, 355.1360043628815788 ) ) ;
#15842=CARTESIAN_POINT ( 'NONE',  ( 801.9419747391806368, -66.45278447660216159, 351.9812246680014027 ) ) ;
#15845=CARTESIAN_POINT ( 'NONE',  ( 766.5853460496234675, -349.9874144716865771, 372.3518521366060554 ) ) ;
#15848=CARTESIAN_POINT ( 'NONE',  ( 815.0009284576459549, -438.3510508353226669, 338.7629533639073429 ) ) ;
#15849=CARTESIAN_POINT ( 'NONE',  ( 756.5762568750052424, -363.1800572038739006, 348.7366044899774238 ) ) ;
#15859=CARTESIAN_POINT ( 'NONE',  ( 800.0135310231082713, -110.0891481129656597, 325.0180583372163028 ) ) ;
#15860=CARTESIAN_POINT ( 'NONE',  ( 754.7162404726377645, -374.7363362996978253, 339.4709603349214717 ) ) ;
#15861=CARTESIAN_POINT ( 'NONE',  ( 745.7998596910086917, -437.3618753856919170, 332.5602148656461168 ) ) ;
#15863=CARTESIAN_POINT ( 'NONE',  ( 745.1769319972822814, -329.8055962898683902, 346.2694204179732083 ) ) ;
#15865=CARTESIAN_POINT ( 'NONE',  ( 768.8385539511368734, -95.26014174441461080, 306.4236121716840557 ) ) ;
#15869=VECTOR ( 'NONE', #28630, 1000.000000000000000 ) ;
#15870=CARTESIAN_POINT ( 'NONE',  ( 746.8695393053150156, -437.9073299311463074, 327.6429770376306010 ) ) ;
#15878=CARTESIAN_POINT ( 'NONE',  ( 784.1219089521767955, -309.2817908451525568, 315.0488828828318333 ) ) ;
#15879=CARTESIAN_POINT ( 'NONE',  ( 802.1676090361156639, -182.6346026584199649, 327.8955696845344505 ) ) ;
#15881=CARTESIAN_POINT ( 'NONE',  ( 760.0363995740630116, -274.9181544815161828, 368.7758568127991907 ) ) ;
#15885=CARTESIAN_POINT ( 'NONE',  ( 766.4474001241216001, -67.09997266333506616, 307.3154664389482491 ) ) ;
#15890=CARTESIAN_POINT ( 'NONE',  ( 785.3687786644884454, -155.3618753856927128, 315.3201227861279676 ) ) ;
#15893=CARTESIAN_POINT ( 'NONE',  ( 755.1538015810308480, -14.19088175424431242, 343.0433043558613804 ) ) ;
#15896=CARTESIAN_POINT ( 'NONE',  ( 769.1273215169530886, -382.7146871989591546, 317.4527132478988847 ) ) ;
#15900=CARTESIAN_POINT ( 'NONE',  ( 786.2056067578752163, -227.8055962898687596, 374.4686193811670023 ) ) ;
#15901=CARTESIAN_POINT ( 'NONE',  ( 759.7806653035535192, -102.9982390220565662, 324.8639956371181370 ) ) ;
#15906=CARTESIAN_POINT ( 'NONE',  ( 791.9812246680005501, -236.6346026584198228, 361.9419747391813189 ) ) ;
#15912=VECTOR ( 'NONE', #8187, 1000.000000000000000 ) ;
#15916=CARTESIAN_POINT ( 'NONE',  ( 792.3570229623691148, -333.1800572038740142, 373.1304606946836770 ) ) ;
#15917=CARTESIAN_POINT ( 'NONE',  ( 759.8311093483677041, -46.16923265350568784, 310.9282345327691814 ) ) ;
#15922=CARTESIAN_POINT ( 'NONE',  ( 759.9864689768902508, -218.0891481129653187, 354.9819416627836404 ) ) ;
#15925=CARTESIAN_POINT ( 'NONE',  ( 787.5162901302840055, -323.3618753856923149, 305.4481719005792684 ) ) ;
#15929=CARTESIAN_POINT ( 'NONE',  ( 787.4999999999992042, -512.9681489794448908, 339.9999999999999432 ) ) ;
#15931=CARTESIAN_POINT ( 'NONE',  ( 801.5560724626406000, -192.5545181178801215, 326.7756240680316182 ) ) ;
#15932=CARTESIAN_POINT ( 'NONE',  ( 765.0180583372156207, -96.99823902205660886, 360.0135310231089534 ) ) ;
#15936=CARTESIAN_POINT ( 'NONE',  ( 787.6308680596127942, -251.2601417444141134, 364.1105419155492768 ) ) ;
#15940=CARTESIAN_POINT ( 'NONE',  ( 808.0189434323515343, -422.0891481129647218, 319.0252816721025511 ) ) ;
#15947=CARTESIAN_POINT ( 'NONE',  ( 792.2312462859673587, -59.90732993114762905, 307.2067596250082602 ) ) ;
#15948=CARTESIAN_POINT ( 'NONE',  ( 745.7998596910086917, -149.3618753856928265, 332.5602148656461168 ) ) ;
#15953=CARTESIAN_POINT ( 'NONE',  ( 745.0891759886404770, -364.2709662947830793, 342.4968714119734159 ) ) ;
#15955=CARTESIAN_POINT ( 'NONE',  ( 769.1273215169530886, 1.285312801039623753, 317.4527132478988847 ) ) ;
#15958=ADVANCED_FACE ( 'NONE', ( #43096 ), #11462, .F. ) ;
#15959=CARTESIAN_POINT ( 'NONE',  ( 811.6461892240364477, -148.7146871989598935, 324.1737431748509835 ) ) ;
#15960=CARTESIAN_POINT ( 'NONE',  ( 767.8955696845334842, -0.4527844766023629286, 362.1676090361161755 ) ) ;
#15962=CARTESIAN_POINT ( 'NONE',  ( 788.7631598425961101, -169.4419599262325562, 305.7194118038759143 ) ) ;
#15966=CARTESIAN_POINT ( 'NONE',  ( 801.9419747391806368, -138.4527844766019200, 351.9812246680014027 ) ) ;
#15968=CARTESIAN_POINT ( 'NONE',  ( 762.3223304703356007, -271.5436935675106156, 322.3223304703362828 ) ) ;
#15971=CARTESIAN_POINT ( 'NONE',  ( 763.2154366446407039, 2.376221891948710585, 321.4292242960311228 ) ) ;
#15976=CARTESIAN_POINT ( 'NONE',  ( 814.9108240113580450, -232.2709662947834488, 337.5031285880265273 ) ) ;
#15977=CARTESIAN_POINT ( 'NONE',  ( 799.2566176426618085, -312.0090635724251911, 324.0069404352559559 ) ) ;
#15978=CARTESIAN_POINT ( 'NONE',  ( 755.0488828828309806, -401.8055962898681059, 344.1219089521771934 ) ) ;
#15990=CARTESIAN_POINT ( 'NONE',  ( 780.5290396650775619, -300.3510508353230080, 365.2837595273619513 ) ) ;
#15997=CARTESIAN_POINT ( 'NONE',  ( 813.5763878283155464, -195.8272453906074304, 351.1614460488615350 ) ) ;
#16001=CARTESIAN_POINT ( 'NONE',  ( 755.2512626584698410, -31.54369356751135456, 315.2512626584710915 ) ) ;
#16005=CARTESIAN_POINT ( 'NONE',  ( 756.5762568750052424, -51.18005720387493085, 348.7366044899774238 ) ) ;
#16007=CARTESIAN_POINT ( 'NONE',  ( 766.4474001241216001, -307.0999726633343130, 307.3154664389482491 ) ) ;
#16008=CARTESIAN_POINT ( 'NONE',  ( 751.9810565676468741, -242.0891481129652618, 360.9747183278973921 ) ) ;
#16013=CARTESIAN_POINT ( 'NONE',  ( 759.9864689768902508, -362.0891481129648923, 354.9819416627836404 ) ) ;
#16014=CARTESIAN_POINT ( 'NONE',  ( 790.0220218866281812, -127.0999726633348672, 363.2186876482849129 ) ) ;
#16018=CARTESIAN_POINT ( 'NONE',  ( 776.2433038121456548, -132.8965053807781374, 374.8207195650711014 ) ) ;
#16019=CARTESIAN_POINT ( 'NONE',  ( 757.8323909638827445, -410.6346026584191122, 352.1044303154654358 ) ) ;
#16023=CARTESIAN_POINT ( 'NONE',  ( 755.0636971347428243, -172.2709662947836478, 341.7834795799807353 ) ) ;
#16024=CARTESIAN_POINT ( 'NONE',  ( 774.6858677611749044, -153.7255117493291721, 315.5713283507209894 ) ) ;
#16028=CARTESIAN_POINT ( 'NONE',  ( 803.6646147819161570, -353.9073299311467053, 348.8264449731210561 ) ) ;
#16029=ORIENTED_EDGE ( 'NONE', *, *, #6076, .F. ) ;
#16031=CARTESIAN_POINT ( 'NONE',  ( 749.2812353651451076, -102.4527844766020337, 323.2262854647983090 ) ) ;
#16036=CARTESIAN_POINT ( 'NONE',  ( 763.2262854647970016, -248.6346026584197659, 309.2812353651462445 ) ) ;
#16037=CARTESIAN_POINT ( 'NONE',  ( 801.3366627262608972, -176.5328690171416213, 353.0897708529566899 ) ) ;
#16040=VERTEX_POINT ( 'NONE', #22958 ) ;
#16045=CARTESIAN_POINT ( 'NONE',  ( 745.1792804349281596, -110.1908817542440033, 343.7566961878542884 ) ) ;
#16055=CARTESIAN_POINT ( 'NONE',  ( 763.0428371773158460, -443.4636090269702322, 358.7617431975195359 ) ) ;
#16057=CARTESIAN_POINT ( 'NONE',  ( 790.0220218866281812, -247.0999726633344835, 363.2186876482849129 ) ) ;
#16059=DIRECTION ( 'NONE',  ( 0.000000000000000000, 0.000000000000000000, 1.000000000000000000 ) ) ;
#16061=CARTESIAN_POINT ( 'NONE',  ( 781.2370466360911223, -164.7363362996983938, 304.9990715423533629 ) ) ;
#16063=CARTESIAN_POINT ( 'NONE',  ( 801.1904061080336987, -164.0891481129655176, 368.3070685750235498 ) ) ;
#16066=CARTESIAN_POINT ( 'NONE',  ( 781.8018195045266339, -238.2709662947833920, 365.1927285166406705 ) ) ;
#16067=CARTESIAN_POINT ( 'NONE',  ( 755.8894580844503253, -39.82724539060786384, 332.3691319403863531 ) ) ;
#16072=CARTESIAN_POINT ( 'NONE',  ( 786.6156483768007774, -73.44195992623286884, 315.5913626894246136 ) ) ;
#16075=CARTESIAN_POINT ( 'NONE',  ( 765.0180583372156207, -48.99823902205675807, 360.0135310231089534 ) ) ;
#16078=CARTESIAN_POINT ( 'NONE',  ( 813.2346286133761168, -389.2601417444136018, 328.9521613784389160 ) ) ;
#16081=CARTESIAN_POINT ( 'NONE',  ( 748.9653473494363425, -2.634602658420536869, 356.9462024416521331 ) ) ;
#16083=CARTESIAN_POINT ( 'NONE',  ( 797.6776695296629214, -379.5436935675102745, 357.6776695296636603 ) ) ;
#16090=CARTESIAN_POINT ( 'NONE',  ( 803.4237431249931660, -87.18005720387481006, 331.2633955100225194 ) ) ;
#16091=CARTESIAN_POINT ( 'NONE',  ( 757.0176451133909268, -397.0999726633340288, 349.9200121543848354 ) ) ;
#16092=CARTESIAN_POINT ( 'NONE',  ( 759.0252816721024374, -432.9982390220555999, 368.0189434323527280 ) ) ;
#16094=CARTESIAN_POINT ( 'NONE',  ( 766.5853460496234675, -325.9874144716865771, 372.3518521366060554 ) ) ;
#16095=CARTESIAN_POINT ( 'NONE',  ( 744.9990715423526808, -90.35105083532373271, 341.2370466360926002 ) ) ;
#16100=CARTESIAN_POINT ( 'NONE',  ( 745.5313806188320314, -15.28179084515340058, 333.7943932421247268 ) ) ;
#16102=FACE_OUTER_BOUND ( 'NONE', #40860, .T. ) ;
#16107=CARTESIAN_POINT ( 'NONE',  ( 755.3028492785439312, -327.2817908451525000, 335.9200461376539693 ) ) ;
#16108=CARTESIAN_POINT ( 'NONE',  ( 794.9819416627830151, -180.9982390220563389, 319.9864689768909898 ) ) ;
#16112=CARTESIAN_POINT ( 'NONE',  ( 762.1177392798416577, -90.55451811788041994, 309.8865473780659272 ) ) ;
#16115=CARTESIAN_POINT ( 'NONE',  ( 781.8018195045266339, -166.2709662947835909, 365.1927285166406705 ) ) ;
#16119=CARTESIAN_POINT ( 'NONE',  ( 802.5472867521000353, -28.37269993606244967, 350.8726784830461156 ) ) ;
#16122=CARTESIAN_POINT ( 'NONE',  ( 761.2382568024794409, -423.6237781080499190, 356.9571628226838129 ) ) ;
#16124=CARTESIAN_POINT ( 'NONE',  ( 769.1273215169530886, -70.71468719896014932, 317.4527132478988847 ) ) ;
#16127=CARTESIAN_POINT ( 'NONE',  ( 773.7943932421234194, -287.8055962898685038, 305.5313806188329409 ) ) ;
#16128=CARTESIAN_POINT ( 'NONE',  ( 781.8018195045267476, -70.27096629478397460, 365.1927285166407273 ) ) ;
#16129=ORIENTED_EDGE ( 'NONE', *, *, #24162, .T. ) ;
#16131=CARTESIAN_POINT ( 'NONE',  ( 795.1360043628807261, -260.0891481129650060, 360.2193346964456282 ) ) ;
#16133=CARTESIAN_POINT ( 'NONE',  ( 759.9999999999992042, 205.0000000000000568, 329.9999999999999432 ) ) ;
#16137=AXIS2_PLACEMENT_3D ( 'NONE', #24049, #28206, #9979 ) ;
#16140=CARTESIAN_POINT ( 'NONE',  ( 745.7998596910086917, -317.3618753856922581, 332.5602148656461168 ) ) ;
#16141=CARTESIAN_POINT ( 'NONE',  ( 761.9338519418445230, -206.5328690171415360, 370.4231160770881957 ) ) ;
#16142=CARTESIAN_POINT ( 'NONE',  ( 776.2433038121456548, -36.89650538077844288, 374.8207195650711014 ) ) ;
#16147=CARTESIAN_POINT ( 'NONE',  ( 797.6776695296629214, -211.5436935675107861, 357.6776695296636603 ) ) ;
#16150=CARTESIAN_POINT ( 'NONE',  ( 792.2312462859673587, -371.9073299311465917, 307.2067596250082602 ) ) ;
#16154=CARTESIAN_POINT ( 'NONE',  ( 760.7433823573367135, -180.0090635724255890, 355.9930595647440441 ) ) ;
#16155=CARTESIAN_POINT ( 'NONE',  ( 797.6776695296629214, -67.54369356751125508, 357.6776695296636603 ) ) ;
#16156=ORIENTED_EDGE ( 'NONE', *, *, #10295, .T. ) ;
#16159=CARTESIAN_POINT ( 'NONE',  ( 796.7845633553578182, -249.6237781080505158, 358.5707757039688204 ) ) ;
#16162=CARTESIAN_POINT ( 'NONE',  ( 755.2512626584698410, -439.5436935675101040, 315.2512626584710915 ) ) ;
#16166=CARTESIAN_POINT ( 'NONE',  ( 767.7687537140311633, -71.90732993114760063, 372.7932403749916830 ) ) ;
#16167=CARTESIAN_POINT ( 'NONE',  ( 787.4397851343537695, -141.7255117493291721, 374.2001403089903988 ) ) ;
#16173=CARTESIAN_POINT ( 'NONE',  ( 814.5518280994195948, -399.7255117493283478, 332.4837098697145734 ) ) ;
#16174=CARTESIAN_POINT ( 'NONE',  ( 810.7187646348534145, -18.45278447660230725, 356.7737145352016341 ) ) ;
#16176=CARTESIAN_POINT ( 'NONE',  ( 799.4546378042377910, 14.92167643740321381, 356.1575198192848006 ) ) ;
#16179=CARTESIAN_POINT ( 'NONE',  ( 791.1614460488616487, -131.2601417444144829, 373.5763878283158874 ) ) ;
#16184=CARTESIAN_POINT ( 'NONE',  ( 757.8323909638827445, -170.6346026584199649, 352.1044303154654358 ) ) ;
#16187=CARTESIAN_POINT ( 'NONE',  ( 804.4286716492782716, -305.3618753856922581, 345.3141322388244703 ) ) ;
#16188=FACE_OUTER_BOUND ( 'NONE', #41651, .T. ) ;
#16190=CARTESIAN_POINT ( 'NONE',  ( 801.3366627262608972, -32.53286901714208312, 353.0897708529566899 ) ) ;
#16192=ORIENTED_EDGE ( 'NONE', *, *, #30882, .T. ) ;
#16195=CARTESIAN_POINT ( 'NONE',  ( 808.0189434323515343, -230.0891481129652618, 319.0252816721025511 ) ) ;
#16196=CARTESIAN_POINT ( 'NONE',  ( 793.0897708529556667, -294.5545181178797520, 361.3366627262616362 ) ) ;
#16197=CARTESIAN_POINT ( 'NONE',  ( 756.7813123517142913, -403.9874144716863498, 329.9779781133712504 ) ) ;
#16205=CARTESIAN_POINT ( 'NONE',  ( 793.2243759319678702, -314.5328690171411949, 318.4439275373583200 ) ) ;
#16212=CARTESIAN_POINT ( 'NONE',  ( 745.5313806188320314, -207.2817908451527842, 333.7943932421247268 ) ) ;
#16217=EDGE_CURVE ( 'NONE', #34493, #44752, #35337, .T. ) ;
#16218=CARTESIAN_POINT ( 'NONE',  ( 814.5518280994195948, -39.72551174932951312, 332.4837098697145734 ) ) ;
#16222=CARTESIAN_POINT ( 'NONE',  ( 764.8639956371174549, -32.08914811296588709, 319.7806653035542013 ) ) ;
#16223=CARTESIAN_POINT ( 'NONE',  ( 771.3260364891663130, -331.6454272087888171, 306.0683387631859773 ) ) ;
#16224=CARTESIAN_POINT ( 'NONE',  ( 763.2262854647970016, -248.6346026584197659, 309.2812353651462445 ) ) ;
#16228=CARTESIAN_POINT ( 'NONE',  ( 794.9819416627830151, -372.9982390220557704, 319.9864689768909898 ) ) ;
#16229=CARTESIAN_POINT ( 'NONE',  ( 761.4292242960306112, -113.4636090269712554, 323.2154366446414429 ) ) ;
#16231=CARTESIAN_POINT ( 'NONE',  ( 811.6461892240364477, -28.71468719896028077, 324.1737431748509835 ) ) ;
#16232=CARTESIAN_POINT ( 'NONE',  ( 757.8323909638828582, -386.6346026584192828, 352.1044303154654358 ) ) ;
#16233=FACE_OUTER_BOUND ( 'NONE', #24305, .T. ) ;
#16236=CARTESIAN_POINT ( 'NONE',  ( 810.1134526219336749, -128.5328690171417634, 357.8822607201570349 ) ) ;
#16237=CARTESIAN_POINT ( 'NONE',  ( 804.9363028652555840, -400.2709662947828519, 338.2165204200192079 ) ) ;
#16238=ORIENTED_EDGE ( 'NONE', *, *, #14494, .T. ) ;
#16241=CARTESIAN_POINT ( 'NONE',  ( 762.1405469898971887, -193.5436935675108714, 357.8594530101015607 ) ) ;
#16242=CARTESIAN_POINT ( 'NONE',  ( 758.0580252608178853, -150.4527844766018916, 328.0187753319985404 ) ) ;
#16246=CARTESIAN_POINT ( 'NONE',  ( 792.1044303154645831, -372.4527844766010958, 317.8323909638837677 ) ) ;
#16248=ADVANCED_FACE ( 'NONE', ( #9580 ), #33367, .T. ) ;
#16251=CARTESIAN_POINT ( 'NONE',  ( 759.0252816721024374, -120.9982390220565378, 368.0189434323527280 ) ) ;
#16257=CARTESIAN_POINT ( 'NONE',  ( 751.6929314249748586, -246.9982390220560546, 318.8095938919659034 ) ) ;
#16258=CARTESIAN_POINT ( 'NONE',  ( 772.3691319403857278, -191.2601417444143976, 315.8894580844506663 ) ) ;
#16259=FACE_OUTER_BOUND ( 'NONE', #33588, .T. ) ;
#16269=CARTESIAN_POINT ( 'NONE',  ( 788.6739635108323228, -103.6454272087894850, 373.9316612368139090 ) ) ;
#16278=CARTESIAN_POINT ( 'NONE',  ( 755.5913626894240451, -445.6454272087883055, 346.6156483768012890 ) ) ;
#16285=CARTESIAN_POINT ( 'NONE',  ( 745.5313806188320314, -231.2817908451527558, 333.7943932421247268 ) ) ;
#16287=CARTESIAN_POINT ( 'NONE',  ( 792.3570229623688874, -165.1800572038745258, 373.1304606946836202 ) ) ;
#16290=CARTESIAN_POINT ( 'NONE',  ( 755.3201227861273992, -243.7255117493287742, 345.3687786644892981 ) ) ;
#16291=CARTESIAN_POINT ( 'NONE',  ( 763.8424801807145741, -42.00906357242603661, 320.5453621957614700 ) ) ;
#16296=CARTESIAN_POINT ( 'NONE',  ( 779.4709603349208464, -96.35105083532370429, 314.7162404726379918 ) ) ;
#16299=CARTESIAN_POINT ( 'NONE',  ( 762.3223304703356007, -55.54369356751127640, 322.3223304703362828 ) ) ;
#16302=CARTESIAN_POINT ( 'NONE',  ( 749.8865473780648472, -380.5328690171409676, 322.1177392798429082 ) ) ;
#16304=CARTESIAN_POINT ( 'NONE',  ( 759.7806653035534055, -270.9982390220561115, 324.8639956371180801 ) ) ;
#16305=CARTESIAN_POINT ( 'NONE',  ( 814.9108240113580450, 7.729033705215793582, 337.5031285880265273 ) ) ;
#16307=CARTESIAN_POINT ( 'NONE',  ( 795.1360043628807261, -380.0891481129646650, 360.2193346964456282 ) ) ;
#16315=CARTESIAN_POINT ( 'NONE',  ( 771.2633955100217236, -95.90732993114751537, 363.4237431249939618 ) ) ;
#16316=CARTESIAN_POINT ( 'NONE',  ( 802.5472867521000353, -388.3726999360613945, 350.8726784830461156 ) ) ;
#16317=CARTESIAN_POINT ( 'NONE',  ( 758.8095938919644823, -416.0891481129646650, 311.6929314249762797 ) ) ;
#16319=CARTESIAN_POINT ( 'NONE',  ( 798.0661480581538854, -314.5328690171411949, 309.5768839229118043 ) ) ;
#16320=CARTESIAN_POINT ( 'NONE',  ( 788.7631598425961101, -121.4419599262327267, 305.7194118038759143 ) ) ;
#16324=CARTESIAN_POINT ( 'NONE',  ( 808.3070685750230950, -450.9982390220554294, 361.1904061080339261 ) ) ;
#16331=CARTESIAN_POINT ( 'NONE',  ( 796.1575198192839480, -342.0090635724251342, 359.4546378042384163 ) ) ;
#16332=CARTESIAN_POINT ( 'NONE',  ( 774.6312213355099630, -191.3618753856925991, 364.6798772138717482 ) ) ;
#16333=ORIENTED_EDGE ( 'NONE', *, *, #17349, .F. ) ;
#16334=CARTESIAN_POINT ( 'NONE',  ( 815.3608509340175488, -290.7363362996980527, 341.2497674668889545 ) ) ;
#16337=CARTESIAN_POINT ( 'NONE',  ( 797.8822607201568644, -102.5545181178804057, 370.1134526219340160 ) ) ;
#16340=CARTESIAN_POINT ( 'NONE',  ( 774.6312213355099630, -167.3618753856927412, 364.6798772138717482 ) ) ;
#16343=CARTESIAN_POINT ( 'NONE',  ( 791.0478386215596629, -405.8272453906067199, 306.7653713866226326 ) ) ;
#16346=CARTESIAN_POINT ( 'NONE',  ( 754.7162404726377645, -38.73633629969877035, 339.4709603349214717 ) ) ;
#16348=CARTESIAN_POINT ( 'NONE',  ( 791.7608162188021197, 205.0000000000000568, 350.0000000000000000 ) ) ;
#16349=CARTESIAN_POINT ( 'NONE',  ( 803.8651313633788504, -437.2601417444135450, 332.4468031744301015 ) ) ;
#16351=CARTESIAN_POINT ( 'NONE',  ( 805.0264073115434940, -78.35105083532376113, 339.4763451958999099 ) ) ;
#16354=CYLINDRICAL_SURFACE ( 'NONE', #29959, 10.00000000000000888 ) ;
#16355=CARTESIAN_POINT ( 'NONE',  ( 776.2433038121456548, -276.8965053807776258, 374.8207195650711014 ) ) ;
#16356=CARTESIAN_POINT ( 'NONE',  ( 788.8264449731201466, -93.18005720387479585, 363.6646147819170665 ) ) ;
#16357=ORIENTED_EDGE ( 'NONE', *, *, #31257, .T. ) ;
#16358=CARTESIAN_POINT ( 'NONE',  ( 755.0636971347428243, -268.2709662947833067, 341.7834795799807353 ) ) ;
#16365=CARTESIAN_POINT ( 'NONE',  ( 754.9967657858570647, -337.5436935675102745, 365.0032342141425943 ) ) ;
#16366=CARTESIAN_POINT ( 'NONE',  ( 759.8311093483677041, -214.1692326535052189, 310.9282345327691814 ) ) ;
#16373=CARTESIAN_POINT ( 'NONE',  ( 785.3141322388236176, -213.7255117493289731, 364.4286716492789537 ) ) ;
#16376=CARTESIAN_POINT ( 'NONE',  ( 747.2067596250078623, -363.1800572038739006, 352.2312462859687230 ) ) ;
#16377=DIRECTION ( 'NONE',  ( -1.000000000000000000, -0.000000000000000000, 0.000000000000000000 ) ) ;
#16379=DIRECTION ( 'NONE',  ( 0.000000000000000000, 0.000000000000000000, -1.000000000000000000 ) ) ;
#16380=CARTESIAN_POINT ( 'NONE',  ( 793.0897708529556667, -222.5545181178800362, 361.3366627262616362 ) ) ;
#16381=CARTESIAN_POINT ( 'NONE',  ( 800.2193346964447755, -90.99823902205663728, 355.1360043628815788 ) ) ;
#16385=CARTESIAN_POINT ( 'NONE',  ( 756.1348686366196716, -257.2601417444141134, 347.5531968255698416 ) ) ;
#16388=CARTESIAN_POINT ( 'NONE',  ( 782.4968714119720516, -442.8164208402372992, 305.0891759886411023 ) ) ;
#16392=CARTESIAN_POINT ( 'NONE',  ( 744.7301800767019131, -76.81642084023845030, 337.4774526936615757 ) ) ;
#16393=CARTESIAN_POINT ( 'NONE',  ( 747.2067596250078623, -147.1800572038746395, 352.2312462859687230 ) ) ;
#16397=CARTESIAN_POINT ( 'NONE',  ( 745.7194118038753459, -421.6454272087885329, 348.7631598425976449 ) ) ;
#16400=CARTESIAN_POINT ( 'NONE',  ( 763.0537975583475827, -384.4527844766011526, 371.0346526505627480 ) ) ;
#16401=CARTESIAN_POINT ( 'NONE',  ( 745.7998596910086917, -5.361875385693257279, 332.5602148656461168 ) ) ;
#16403=CARTESIAN_POINT ( 'NONE',  ( 765.8855110935204493, -22.16923265350575889, 319.0159684113471599 ) ) ;
#16406=CARTESIAN_POINT ( 'NONE',  ( 811.6461892240364477, -172.7146871989598083, 324.1737431748509835 ) ) ;
#16407=CARTESIAN_POINT ( 'NONE',  ( 781.7834795799800531, 13.18357915976123174, 315.0636971347436202 ) ) ;
#16408=CARTESIAN_POINT ( 'NONE',  ( 810.1134526219336749, -176.5328690171416213, 357.8822607201570349 ) ) ;
#16411=CARTESIAN_POINT ( 'NONE',  ( 794.9819416627830151, -180.9982390220563389, 319.9864689768909898 ) ) ;
#16413=CARTESIAN_POINT ( 'NONE',  ( 757.8323909638827445, -290.6346026584195101, 352.1044303154654358 ) ) ;
#16414=CARTESIAN_POINT ( 'NONE',  ( 778.1981804954715471, -298.2709662947831930, 314.8072714833591021 ) ) ;
#16416=ORIENTED_EDGE ( 'NONE', *, *, #6076, .T. ) ;
#16417=CARTESIAN_POINT ( 'NONE',  ( 759.2295555964440155, -16.16923265350578021, 353.9708237608231229 ) ) ;
#16421=CARTESIAN_POINT ( 'NONE',  ( 787.4397851343537695, -237.7255117493289163, 374.2001403089903988 ) ) ;
#16422=CARTESIAN_POINT ( 'NONE',  ( 796.1575198192839480, -318.0090635724251911, 359.4546378042384163 ) ) ;
#16423=CARTESIAN_POINT ( 'NONE',  ( 804.9511171171677688, -413.8055962898681059, 335.8780910478229202 ) ) ;
#16432=CARTESIAN_POINT ( 'NONE',  ( 757.2208543904082489, -304.7146871989594388, 350.9844846989624330 ) ) ;
#16433=CARTESIAN_POINT ( 'NONE',  ( 793.4841229319055174, -454.6421165850785542, 372.0217908949762773 ) ) ;
#16435=CARTESIAN_POINT ( 'NONE',  ( 799.2566176426618085, -120.0090635724258021, 324.0069404352559559 ) ) ;
#16436=CARTESIAN_POINT ( 'NONE',  ( 785.3687786644884454, 12.63812461430668321, 315.3201227861279676 ) ) ;
#16439=CARTESIAN_POINT ( 'NONE',  ( 752.7379699480933368, -204.0090635724255606, 361.9858362298580232 ) ) ;
#16444=CARTESIAN_POINT ( 'NONE',  ( 782.4968714119720516, -58.81642084023854267, 305.0891759886411023 ) ) ;
#16447=DIRECTION ( 'NONE',  ( 0.000000000000000000, 0.000000000000000000, -1.000000000000000000 ) ) ;
#16448=CARTESIAN_POINT ( 'NONE',  ( 750.9282345327678740, -328.9181544815160692, 319.8311093483690115 ) ) ;
#16449=DIRECTION ( 'NONE',  ( 0.000000000000000000, 0.000000000000000000, 1.000000000000000000 ) ) ;
#16450=CARTESIAN_POINT ( 'NONE',  ( 801.1904061080336987, -284.0891481129650629, 368.3070685750235498 ) ) ;
#16455=CARTESIAN_POINT ( 'NONE',  ( 801.9419747391806368, -354.4527844766012095, 351.9812246680014027 ) ) ;
#16456=CARTESIAN_POINT ( 'NONE',  ( 783.0745993439762742, -104.1908817542440175, 365.1016975059196739 ) ) ;
#16458=CARTESIAN_POINT ( 'NONE',  ( 749.8865473780648472, -68.53286901714197654, 322.1177392798429082 ) ) ;
#16459=CARTESIAN_POINT ( 'NONE',  ( 755.0636971347428243, -364.2709662947830793, 341.7834795799807353 ) ) ;
#16463=CARTESIAN_POINT ( 'NONE',  ( 801.9858362298568863, -147.0783235625962959, 312.7379699480935642 ) ) ;
#16464=CARTESIAN_POINT ( 'NONE',  ( 765.0180583372156207, -432.9982390220555999, 360.0135310231089534 ) ) ;
#16467=CARTESIAN_POINT ( 'NONE',  ( 771.1735550268778070, -201.1800572038744690, 316.3353852180827630 ) ) ;
#16468=CARTESIAN_POINT ( 'NONE',  ( 797.8594530101009923, -181.5436935675108430, 322.1405469898982119 ) ) ;
#16473=CARTESIAN_POINT ( 'NONE',  ( 804.6798772138708955, -399.7255117493283478, 334.6312213355107019 ) ) ;
#16479=CARTESIAN_POINT ( 'NONE',  ( 772.4837098697145166, -119.3618753856928834, 374.5518280994205611 ) ) ;
#16485=CARTESIAN_POINT ( 'NONE',  ( 763.0537975583475827, -264.4527844766016074, 371.0346526505627480 ) ) ;
#16486=CARTESIAN_POINT ( 'NONE',  ( 787.6308680596127942, -179.2601417444143692, 364.1105419155492768 ) ) ;
#16489=CARTESIAN_POINT ( 'NONE',  ( 787.4999999999992042, -462.9681489794447202, 270.0000000000000568 ) ) ;
#16498=CARTESIAN_POINT ( 'NONE',  ( 791.0478386215596629, -93.82724539060770041, 306.7653713866226326 ) ) ;
#16507=CARTESIAN_POINT ( 'NONE',  ( 754.7162404726377645, -422.7363362996975980, 339.4709603349214717 ) ) ;
#16516=CARTESIAN_POINT ( 'NONE',  ( 813.5763878283155464, -219.8272453906073167, 351.1614460488615350 ) ) ;
#16518=CARTESIAN_POINT ( 'NONE',  ( 810.7187646348534145, -186.4527844766017779, 356.7737145352016341 ) ) ;
#16523=CARTESIAN_POINT ( 'NONE',  ( 759.7806653035534055, -270.9982390220561115, 324.8639956371180801 ) ) ;
#16524=CARTESIAN_POINT ( 'NONE',  ( 769.9779781133707957, -43.09997266333511590, 316.7813123517150871 ) ) ;
#16528=CARTESIAN_POINT ( 'NONE',  ( 800.7704444035546203, -76.16923265350557415, 326.0291762391768771 ) ) ;
#16529=CARTESIAN_POINT ( 'NONE',  ( 762.1405469898971887, -337.5436935675102177, 357.8594530101015607 ) ) ;
#16532=VECTOR ( 'NONE', #14718, 1000.000000000000000 ) ;
#16534=CARTESIAN_POINT ( 'NONE',  ( 781.8018195045266339, -70.27096629478397460, 365.1927285166406705 ) ) ;
#16537=CARTESIAN_POINT ( 'NONE',  ( 761.9338519418445230, -374.5328690171410813, 370.4231160770881957 ) ) ;
#16539=CARTESIAN_POINT ( 'NONE',  ( 755.5713283507202505, -293.3618753856923718, 334.6858677611754729 ) ) ;
#16540=CARTESIAN_POINT ( 'NONE',  ( 792.2269492836462632, -443.1233509495419298, 372.8191558162650949 ) ) ;
#16543=CARTESIAN_POINT ( 'NONE',  ( 755.5713283507202505, -389.3618753856919739, 334.6858677611754729 ) ) ;
#16546=EDGE_LOOP ( 'NONE', ( #38154, #31190, #37488, #26988, #45575, #31587 ) ) ;
#16550=CARTESIAN_POINT ( 'NONE',  ( 791.9812246680005501, -92.63460265842026331, 361.9419747391813189 ) ) ;
#16551=CARTESIAN_POINT ( 'NONE',  ( 766.0291762391763086, -418.9181544815157849, 360.7704444035551319 ) ) ;
#16552=CARTESIAN_POINT ( 'NONE',  ( 754.9735926884551418, -90.35105083532373271, 340.5236548041000333 ) ) ;
#16555=CARTESIAN_POINT ( 'NONE',  ( 776.2433038121456548, -348.8965053807774552, 374.8207195650711014 ) ) ;
#16561=CARTESIAN_POINT ( 'NONE',  ( 810.4231160770870019, -0.5545181178807169209, 321.9338519418446936 ) ) ;
#16569=CARTESIAN_POINT ( 'NONE',  ( 766.0291762391763086, -322.9181544815161260, 360.7704444035551319 ) ) ;
#16573=CARTESIAN_POINT ( 'NONE',  ( 797.8822607201568644, -294.5545181178797520, 370.1134526219340160 ) ) ;
#16577=CARTESIAN_POINT ( 'NONE',  ( 788.6739635108323228, -103.6454272087894850, 373.9316612368139090 ) ) ;
#16580=CARTESIAN_POINT ( 'NONE',  ( 779.9999999999992042, -452.9681489794448339, 329.9999999999999432 ) ) ;
#16582=CARTESIAN_POINT ( 'NONE',  ( 800.0135310231082713, -134.0891481129655745, 325.0180583372163028 ) ) ;
#16584=CARTESIAN_POINT ( 'NONE',  ( 776.2046728542105711, -428.1908817542430938, 304.8212110874238761 ) ) ;
#16588=CARTESIAN_POINT ( 'NONE',  ( 766.0291762391763086, -34.91815448151697154, 360.7704444035551319 ) ) ;
#16590=DIRECTION ( 'NONE',  ( -1.000000000000000000, -0.000000000000000000, -0.000000000000000000 ) ) ;
#16591=CARTESIAN_POINT ( 'NONE',  ( 783.7566961878529810, 23.10349461922137237, 305.1792804349288417 ) ) ;
#16596=CARTESIAN_POINT ( 'NONE',  ( 805.9055244015594326, -291.6237781080503169, 315.8990559732753240 ) ) ;
#16597=CARTESIAN_POINT ( 'NONE',  ( 765.0180583372156207, -96.99823902205660886, 360.0135310231089534 ) ) ;
#16599=CARTESIAN_POINT ( 'NONE',  ( 756.3353852180819104, -269.9073299311468190, 331.1735550268788302 ) ) ;
#16605=AXIS2_PLACEMENT_3D ( 'NONE', #39083, #32378, #25189 ) ;
#16606=CARTESIAN_POINT ( 'NONE',  ( 747.2067596250078623, -339.1800572038740142, 352.2312462859687230 ) ) ;
#16607=CARTESIAN_POINT ( 'NONE',  ( 813.2346286133761168, -269.2601417444139997, 328.9521613784389160 ) ) ;
#16611=CARTESIAN_POINT ( 'NONE',  ( 758.0580252608178853, -222.4527844766016642, 328.0187753319985404 ) ) ;
#16613=CARTESIAN_POINT ( 'NONE',  ( 812.7932403749906598, -351.1800572038740142, 327.7687537140311633 ) ) ;
#16614=CIRCLE ( 'NONE', #27684, 30.00000000000002842 ) ;
#16616=CARTESIAN_POINT ( 'NONE',  ( 794.4892657455289964, 16.45630643248850689, 314.6207049315058271 ) ) ;
#16619=CARTESIAN_POINT ( 'NONE',  ( 769.9779781133707957, -211.0999726633346540, 316.7813123517150871 ) ) ;
#16620=CARTESIAN_POINT ( 'NONE',  ( 788.7366044899766848, -83.90732993114754379, 316.5762568750059813 ) ) ;
#16624=CARTESIAN_POINT ( 'NONE',  ( 776.9566956441375396, -252.8965053807777394, 364.8461984189686405 ) ) ;
#16627=CARTESIAN_POINT ( 'NONE',  ( 786.2694204179717872, -21.28179084515337749, 305.1769319972829067 ) ) ;
#16631=CARTESIAN_POINT ( 'NONE',  ( 751.9810565676468741, -98.08914811296568814, 360.9747183278973921 ) ) ;
#16632=CARTESIAN_POINT ( 'NONE',  ( 782.4968714119720516, -154.8164208402382371, 305.0891759886411023 ) ) ;
#16637=CARTESIAN_POINT ( 'NONE',  ( 778.7629533639073998, -416.7363362996975980, 375.0009284576466371 ) ) ;
#16640=CARTESIAN_POINT ( 'NONE',  ( 772.4837098697144029, -383.3618753856921444, 374.5518280994205611 ) ) ;
#16641=CARTESIAN_POINT ( 'NONE',  ( 749.2812353651451076, -6.452784476602343666, 323.2262854647983090 ) ) ;
#16643=CARTESIAN_POINT ( 'NONE',  ( 800.7704444035546203, -28.16923265350574468, 326.0291762391768771 ) ) ;
#16647=CARTESIAN_POINT ( 'NONE',  ( 744.8212110874229666, -162.8965053807780521, 336.2046728542121627 ) ) ;
#16648=CARTESIAN_POINT ( 'NONE',  ( 797.6776695296629214, 4.456306432488530866, 357.6776695296636603 ) ) ;
#16653=CARTESIAN_POINT ( 'NONE',  ( 801.9419747391806368, -162.4527844766018632, 351.9812246680014027 ) ) ;
#16656=CARTESIAN_POINT ( 'NONE',  ( 800.2193346964447755, -282.9982390220558841, 355.1360043628815788 ) ) ;
#16657=CARTESIAN_POINT ( 'NONE',  ( 803.4237431249931660, -303.1800572038740711, 331.2633955100225194 ) ) ;
#16660=CARTESIAN_POINT ( 'NONE',  ( 766.7756240680305382, -14.53286901714214707, 361.5560724626415663 ) ) ;
#16663=CARTESIAN_POINT ( 'NONE',  ( 792.3570229623691148, -213.1800572038743837, 373.1304606946836770 ) ) ;
#16664=CARTESIAN_POINT ( 'NONE',  ( 783.0745993439762742, -320.1908817542434349, 365.1016975059196739 ) ) ;
#16665=CARTESIAN_POINT ( 'NONE',  ( 765.8855110935204493, -430.1692326535043094, 319.0159684113471599 ) ) ;
#16672=CIRCLE ( 'NONE', #38104, 4.999999999999982236 ) ;
#16673=CARTESIAN_POINT ( 'NONE',  ( 755.8398074228967971, -283.4419599262321867, 333.4516893846970333 ) ) ;
#16677=CARTESIAN_POINT ( 'NONE',  ( 796.9571628226829034, -119.4636090269712554, 321.2382568024804641 ) ) ;
#16683=LINE ( 'NONE', #41853, #31836 ) ;
#16686=CARTESIAN_POINT ( 'NONE',  ( 804.7487373415286811, -43.54369356751131903, 364.7487373415288516 ) ) ;
#16689=CARTESIAN_POINT ( 'NONE',  ( 779.9999999999992042, 166.4563064324884465, 339.9999999999999432 ) ) ;
#16690=CARTESIAN_POINT ( 'NONE',  ( 746.4236121716829757, -327.8272453906069472, 328.8385539511384650 ) ) ;
#16692=CARTESIAN_POINT ( 'NONE',  ( 767.7687537140311633, -287.9073299311468759, 372.7932403749916830 ) ) ;
#16697=CARTESIAN_POINT ( 'NONE',  ( 800.0135310231082713, -398.0891481129647218, 325.0180583372163028 ) ) ;
#16698=CARTESIAN_POINT ( 'NONE',  ( 805.2837595273609850, -170.7363362996983938, 340.5290396650784714 ) ) ;
#16700=CARTESIAN_POINT ( 'NONE',  ( 815.1787889125755555, -78.89650538077832209, 343.7953271457877804 ) ) ;
#16701=CARTESIAN_POINT ( 'NONE',  ( 800.0135310231082713, -374.0891481129647786, 325.0180583372163028 ) ) ;
#16703=CARTESIAN_POINT ( 'NONE',  ( 764.8639956371174549, -440.0891481129644944, 319.7806653035542013 ) ) ;
#16708=CARTESIAN_POINT ( 'NONE',  ( 756.3353852180819104, -197.9073299311472169, 331.1735550268788302 ) ) ;
#16709=CARTESIAN_POINT ( 'NONE',  ( 788.7366044899766848, -179.9073299311472454, 316.5762568750059813 ) ) ;
#16713=CARTESIAN_POINT ( 'NONE',  ( 759.7806653035534055, -390.9982390220557136, 324.8639956371180801 ) ) ;
#16716=CIRCLE ( 'NONE', #28523, 10.00000000000000888 ) ;
#16718=CARTESIAN_POINT ( 'NONE',  ( 747.2067596250078623, -123.1800572038747106, 352.2312462859687230 ) ) ;
#16719=ORIENTED_EDGE ( 'NONE', *, *, #6040, .F. ) ;
#16721=VERTEX_POINT ( 'NONE', #29415 ) ;
#16724=CARTESIAN_POINT ( 'NONE',  ( 755.0488828828309806, -185.8055962898689302, 344.1219089521771934 ) ) ;
#16725=CARTESIAN_POINT ( 'NONE',  ( 809.7763221938408833, -453.1000272243879863, 336.1997354883953903 ) ) ;
#16726=CARTESIAN_POINT ( 'NONE',  ( 767.9999999999992042, 205.0000000000000568, 350.0000000000000000 ) ) ;
#16728=DIRECTION ( 'NONE',  ( -0.000000000000000000, 1.000000000000000000, -0.000000000000000000 ) ) ;
#16735=CARTESIAN_POINT ( 'NONE',  ( 745.1792804349281596, -86.19088175424408860, 343.7566961878542884 ) ) ;
#16744=CARTESIAN_POINT ( 'NONE',  ( 769.9779781133707957, -427.0999726633338582, 316.7813123517150871 ) ) ;
#16746=FACE_OUTER_BOUND ( 'NONE', #44254, .T. ) ;
#16752=CARTESIAN_POINT ( 'NONE',  ( 752.7379699480933368, -204.0090635724255606, 361.9858362298580232 ) ) ;
#16754=CARTESIAN_POINT ( 'NONE',  ( 744.7301800767019131, -196.8164208402380950, 337.4774526936615757 ) ) ;
#16757=CARTESIAN_POINT ( 'NONE',  ( 799.9999999999993179, -462.9681489794448339, 370.0000000000000568 ) ) ;
#16758=CARTESIAN_POINT ( 'NONE',  ( 765.0180583372156207, -288.9982390220559978, 360.0135310231089534 ) ) ;
#16759=CARTESIAN_POINT ( 'NONE',  ( 783.0745993439762742, -56.19088175424417386, 365.1016975059196739 ) ) ;
#16763=CARTESIAN_POINT ( 'NONE',  ( 779.4709603349208464, -72.35105083532378956, 314.7162404726379918 ) ) ;
#16764=CARTESIAN_POINT ( 'NONE',  ( 762.1405469898971887, -313.5436935675102745, 357.8594530101015607 ) ) ;
#16768=CARTESIAN_POINT ( 'NONE',  ( 759.7806653035534055, -54.99823902205672255, 324.8639956371180801 ) ) ;
#16771=CARTESIAN_POINT ( 'NONE',  ( 746.7653713866222915, -377.2601417444137724, 351.0478386215610271 ) ) ;
#16774=CARTESIAN_POINT ( 'NONE',  ( 805.1927285166397041, -280.8164208402378677, 341.8018195045277707 ) ) ;
#16775=CARTESIAN_POINT ( 'NONE',  ( 772.4837098697144029, 0.6381246143067236254, 374.5518280994205611 ) ) ;
#16778=CARTESIAN_POINT ( 'NONE',  ( 762.1405469898971887, -385.5436935675102745, 357.8594530101015607 ) ) ;
#16786=CARTESIAN_POINT ( 'NONE',  ( 754.8072714833581358, -76.81642084023845030, 338.1981804954720587 ) ) ;
#16787=CARTESIAN_POINT ( 'NONE',  ( 799.2566176426618085, -408.0090635724249069, 324.0069404352559559 ) ) ;
#16788=CARTESIAN_POINT ( 'NONE',  ( 804.7487373415286811, -451.5436935675099903, 364.7487373415288516 ) ) ;
#16790=CARTESIAN_POINT ( 'NONE',  ( 793.4146539503750546, -361.9874144716864635, 307.6481478633938877 ) ) ;
#16792=CARTESIAN_POINT ( 'NONE',  ( 773.7943932421234194, -119.8055962898690865, 305.5313806188329409 ) ) ;
#16796=CARTESIAN_POINT ( 'NONE',  ( 755.8990559732751535, -11.46360902697159290, 365.9055244015606831 ) ) ;
#16802=CARTESIAN_POINT ( 'NONE',  ( 804.1105419155481968, -339.8272453906069472, 347.6308680596136469 ) ) ;
#16804=CARTESIAN_POINT ( 'NONE',  ( 812.3518521366052028, -313.0999726633342561, 326.5853460496235243 ) ) ;
#16807=DIRECTION ( 'NONE',  ( 1.000000000000000000, -0.000000000000000000, -0.000000000000000000 ) ) ;
#16808=CARTESIAN_POINT ( 'NONE',  ( 802.2119215644370342, -126.0090635724257737, 367.5423716828165084 ) ) ;
#16814=CARTESIAN_POINT ( 'NONE',  ( 804.6798772138708955, -135.7255117493291152, 334.6312213355107019 ) ) ;
#16816=CARTESIAN_POINT ( 'NONE',  ( 746.4236121716829757, -423.8272453906067199, 328.8385539511384650 ) ) ;
#16820=CARTESIAN_POINT ( 'NONE',  ( 757.0176451133909268, -61.09997266333506616, 349.9200121543848354 ) ) ;
#16823=CARTESIAN_POINT ( 'NONE',  ( 789.6640940660590786, -442.9180389616178672, 363.1300863558843162 ) ) ;
#16826=CARTESIAN_POINT ( 'NONE',  ( 799.9999999999993179, 205.0000000000000568, 339.9999999999999432 ) ) ;
#16827=CARTESIAN_POINT ( 'NONE',  ( 747.3154664389472828, -283.9874144716867477, 326.4474001241230781 ) ) ;
#16828=CARTESIAN_POINT ( 'NONE',  ( 755.5713283507202505, -77.36187538569302546, 334.6858677611754729 ) ) ;
#16832=CARTESIAN_POINT ( 'NONE',  ( 803.6646147819161570, -257.9073299311469896, 348.8264449731210561 ) ) ;
#16841=CARTESIAN_POINT ( 'NONE',  ( 745.0891759886404770, -364.2709662947830793, 342.4968714119734159 ) ) ;
#16842=CARTESIAN_POINT ( 'NONE',  ( 759.8311093483677041, -262.1692326535049347, 310.9282345327691814 ) ) ;
#16846=CARTESIAN_POINT ( 'NONE',  ( 759.9864689768902508, -242.0891481129652618, 354.9819416627836404 ) ) ;
#16849=CARTESIAN_POINT ( 'NONE',  ( 796.9462024416508257, -348.4527844766012663, 308.9653473494370246 ) ) ;
#16852=CARTESIAN_POINT ( 'NONE',  ( 789.5497161195852414, 16.45630643248838609, 314.2297168413928148 ) ) ;
#16854=CARTESIAN_POINT ( 'NONE',  ( 790.9844846989617508, -238.3726999360617640, 317.2208543904092721 ) ) ;
#16855=CARTESIAN_POINT ( 'NONE',  ( 785.3687786644884454, -131.3618753856928834, 315.3201227861279676 ) ) ;
#16859=CARTESIAN_POINT ( 'NONE',  ( 775.9200461376533440, -287.8055962898685038, 315.3028492785443291 ) ) ;
#16862=CARTESIAN_POINT ( 'NONE',  ( 801.1904061080336987, -452.0891481129646650, 368.3070685750235498 ) ) ;
#16864=CARTESIAN_POINT ( 'NONE',  ( 759.0252816721024374, -72.99823902205667991, 368.0189434323527280 ) ) ;
#16865=CARTESIAN_POINT ( 'NONE',  ( 796.7737145352015204, -188.6346026584199365, 370.7187646348536987 ) ) ;
#16869=CARTESIAN_POINT ( 'NONE',  ( 799.9636004259356241, -406.9181544815157849, 311.2241431872006956 ) ) ;
#16872=CARTESIAN_POINT ( 'NONE',  ( 787.4397851343537695, -381.7255117493284615, 374.2001403089903988 ) ) ;
#16873=CARTESIAN_POINT ( 'NONE',  ( 808.3070685750232087, -18.99823902205684689, 361.1904061080339829 ) ) ;
#16875=CARTESIAN_POINT ( 'NONE',  ( 804.1601925771018387, -31.44195992623299674, 346.5483106153029098 ) ) ;
#16878=CARTESIAN_POINT ( 'NONE',  ( 745.1769319972822814, -161.8055962898689870, 346.2694204179732083 ) ) ;
#16880=CARTESIAN_POINT ( 'NONE',  ( 754.0944755984390895, -183.6237781080507148, 364.1009440267246760 ) ) ;
#16884=CARTESIAN_POINT ( 'NONE',  ( 767.8955696845333705, -168.4527844766018347, 362.1676090361162323 ) ) ;
#16886=CARTESIAN_POINT ( 'NONE',  ( 764.8639956371174549, -296.0891481129650629, 319.7806653035542013 ) ) ;
#16887=CARTESIAN_POINT ( 'NONE',  ( 759.7806653035535192, -294.9982390220559978, 324.8639956371181370 ) ) ;
#16890=CARTESIAN_POINT ( 'NONE',  ( 796.7845633553578182, -9.623778108051251223, 358.5707757039688204 ) ) ;
#16892=CARTESIAN_POINT ( 'NONE',  ( 745.7998596910086917, -245.3618753856925139, 332.5602148656461168 ) ) ;
#16893=CARTESIAN_POINT ( 'NONE',  ( 769.9779781133707957, -331.0999726633342561, 316.7813123517150871 ) ) ;
#16894=CARTESIAN_POINT ( 'NONE',  ( 796.7845633553578182, -441.6237781080499190, 358.5707757039688204 ) ) ;
#16900=CARTESIAN_POINT ( 'NONE',  ( 754.8983024940795303, -306.8965053807775689, 336.9254006560228163 ) ) ;
#16903=CARTESIAN_POINT ( 'NONE',  ( 755.5913626894240451, -133.6454272087893571, 346.6156483768012890 ) ) ;
#16904=CARTESIAN_POINT ( 'NONE',  ( 801.9419747391806368, 5.547215523397618142, 351.9812246680014027 ) ) ;
#16907=CARTESIAN_POINT ( 'NONE',  ( 754.7162404726377645, -230.7363362996981664, 339.4709603349214717 ) ) ;
#16908=CARTESIAN_POINT ( 'NONE',  ( 795.8262568251477660, -238.3726999360617640, 308.3538107759623585 ) ) ;
#16913=CARTESIAN_POINT ( 'NONE',  ( 772.5602148656447525, -57.72551174932945628, 305.7998596910095443 ) ) ;
#16914=CARTESIAN_POINT ( 'NONE',  ( 809.4284809582966318, -452.9681489794448339, 335.2276976236387895 ) ) ;
#16916=DIRECTION ( 'NONE',  ( 0.000000000000000000, 0.000000000000000000, -1.000000000000000000 ) ) ;
#16917=CARTESIAN_POINT ( 'NONE',  ( 809.0717654672305343, -316.9181544815160692, 360.1688906516309885 ) ) ;
#16919=CARTESIAN_POINT ( 'NONE',  ( 808.0189434323515343, -278.0891481129651197, 319.0252816721025511 ) ) ;
#16923=CARTESIAN_POINT ( 'NONE',  ( 774.6858677611749044, -393.7255117493283478, 315.5713283507209894 ) ) ;
#16924=CARTESIAN_POINT ( 'NONE',  ( 775.8780910478218402, -153.2817908451529831, 364.9511171171680530 ) ) ;
#16927=CARTESIAN_POINT ( 'NONE',  ( 811.6461892240364477, -52.71468719896020616, 324.1737431748509835 ) ) ;
#16928=CARTESIAN_POINT ( 'NONE',  ( 771.1735550268780344, -369.1800572038739006, 316.3353852180828198 ) ) ;
#16931=CARTESIAN_POINT ( 'NONE',  ( 747.3154664389472828, -139.9874144716872024, 326.4474001241230781 ) ) ;
#16932=CARTESIAN_POINT ( 'NONE',  ( 756.3353852180819104, -413.9073299311465348, 331.1735550268788302 ) ) ;
#16936=CARTESIAN_POINT ( 'NONE',  ( 764.8639956371174549, -176.0891481129653755, 319.7806653035542013 ) ) ;
#16937=CARTESIAN_POINT ( 'NONE',  ( 800.2193346964446619, -186.9982390220563104, 355.1360043628816925 ) ) ;
#16941=CARTESIAN_POINT ( 'NONE',  ( 804.9363028652555840, -400.2709662947828519, 338.2165204200192079 ) ) ;
#16945=CARTESIAN_POINT ( 'NONE',  ( 746.8695393053151292, -125.9073299311474159, 327.6429770376306578 ) ) ;
#16951=CARTESIAN_POINT ( 'NONE',  ( 804.1601925771018387, -199.4419599262324709, 346.5483106153029098 ) ) ;
#16960=CARTESIAN_POINT ( 'NONE',  ( 781.2370466360911223, -140.7363362996984506, 304.9990715423533629 ) ) ;
#16961=CARTESIAN_POINT ( 'NONE',  ( 799.9999999999993179, -512.9681489794448908, 309.9999999999998863 ) ) ;
#16968=CARTESIAN_POINT ( 'NONE',  ( 804.6971507214547046, -435.2817908451521021, 344.0799538623459739 ) ) ;
#16969=CARTESIAN_POINT ( 'NONE',  ( 788.6739635108323228, -367.6454272087886466, 373.9316612368139090 ) ) ;
#16974=CARTESIAN_POINT ( 'NONE',  ( 788.7366044899766848, 12.09267006885214180, 316.5762568750059813 ) ) ;
#16976=CARTESIAN_POINT ( 'NONE',  ( 752.7379699480933368, -228.0090635724254753, 361.9858362298580232 ) ) ;
#16978=CARTESIAN_POINT ( 'NONE',  ( 754.9967657858570647, -193.5436935675108714, 365.0032342141425374 ) ) ;
#16981=CARTESIAN_POINT ( 'NONE',  ( 797.8594530101008786, -301.5436935675105588, 322.1405469898980982 ) ) ;
#16982=CARTESIAN_POINT ( 'NONE',  ( 758.4439275373578084, -60.55451811788051941, 353.2243759319684386 ) ) ;
#16986=CARTESIAN_POINT ( 'NONE',  ( 765.8855110935204493, -118.1692326535054463, 319.0159684113471599 ) ) ;
#16987=CARTESIAN_POINT ( 'NONE',  ( 800.2193346964447755, -330.9982390220558273, 355.1360043628815788 ) ) ;
#16991=CARTESIAN_POINT ( 'NONE',  ( 797.8594530101008786, -85.54369356751118403, 322.1405469898980982 ) ) ;
#16994=CARTESIAN_POINT ( 'NONE',  ( 800.1688906516307043, -370.1692326535045936, 369.0717654672308186 ) ) ;
#16996=CARTESIAN_POINT ( 'NONE',  ( 757.8323909638827445, -290.6346026584195101, 352.1044303154654358 ) ) ;
#16999=CARTESIAN_POINT ( 'NONE',  ( 804.6798772138708955, -423.7255117493281205, 334.6312213355107019 ) ) ;
#17005=CARTESIAN_POINT ( 'NONE',  ( 797.6776695296629214, -139.5436935675110135, 357.6776695296636603 ) ) ;
#17006=CARTESIAN_POINT ( 'NONE',  ( 755.3028492785439312, -423.2817908451521589, 335.9200461376539693 ) ) ;
#17009=CARTESIAN_POINT ( 'NONE',  ( 795.6651683502461765, -370.7146871989592114, 371.3240766477733814 ) ) ;
#17014=CARTESIAN_POINT ( 'NONE',  ( 792.2312462859673587, -443.9073299311464780, 307.2067596250082602 ) ) ;
#17021=CARTESIAN_POINT ( 'NONE',  ( 779.4763451958990572, -320.7363362996979390, 365.0264073115438919 ) ) ;
#17022=CARTESIAN_POINT ( 'NONE',  ( 814.2805881961230625, -289.6454272087889308, 331.2368401574024119 ) ) ;
#17025=CARTESIAN_POINT ( 'NONE',  ( 814.4686193811664907, -99.28179084515313946, 346.2056067578752732 ) ) ;
#17031=CARTESIAN_POINT ( 'NONE',  ( 755.0636971347428243, -196.2709662947835909, 341.7834795799807353 ) ) ;
#17033=CARTESIAN_POINT ( 'NONE',  ( 814.4686193811664907, -435.2817908451521021, 346.2056067578752732 ) ) ;
#17036=CARTESIAN_POINT ( 'NONE',  ( 786.5483106153019435, -55.64542720878963422, 364.1601925771022366 ) ) ;
#17039=CARTESIAN_POINT ( 'NONE',  ( 804.1601925771018387, -415.4419599262318457, 346.5483106153029098 ) ) ;
#17041=EDGE_CURVE ( 'NONE', #38829, #44752, #23676, .T. ) ;
#17043=CARTESIAN_POINT ( 'NONE',  ( 791.1614460488616487, -275.2601417444140566, 373.5763878283158874 ) ) ;
#17044=CARTESIAN_POINT ( 'NONE',  ( 804.6798772138710092, -111.7255117493292857, 334.6312213355106451 ) ) ;
#17046=CARTESIAN_POINT ( 'NONE',  ( 797.6776695296629214, -259.5436935675106156, 357.6776695296636603 ) ) ;
#17050=ORIENTED_EDGE ( 'NONE', *, *, #21115, .F. ) ;
#17055=CARTESIAN_POINT ( 'NONE',  ( 800.0135310231082713, -38.08914811296587999, 325.0180583372163028 ) ) ;
#17057=CARTESIAN_POINT ( 'NONE',  ( 782.4968714119720516, -370.8164208402375834, 305.0891759886411023 ) ) ;
#17058=CARTESIAN_POINT ( 'NONE',  ( 749.8865473780648472, -236.5328690171414792, 322.1177392798429082 ) ) ;
#17064=CARTESIAN_POINT ( 'NONE',  ( 804.9363028652555840, -232.2709662947834488, 338.2165204200192079 ) ) ;
#17066=CARTESIAN_POINT ( 'NONE',  ( 745.0891759886404770, -364.2709662947830793, 342.4968714119734159 ) ) ;
#17071=CARTESIAN_POINT ( 'NONE',  ( 802.9823548866075953, -241.0999726633345119, 330.0799878456151077 ) ) ;
#17072=CARTESIAN_POINT ( 'NONE',  ( 781.7834795799800531, -106.8164208402383935, 315.0636971347436202 ) ) ;
#17076=CARTESIAN_POINT ( 'NONE',  ( 757.2208543904082489, -280.7146871989594956, 350.9844846989624330 ) ) ;
#17080=CARTESIAN_POINT ( 'NONE',  ( 778.7629533639073998, -8.736336299698871599, 375.0009284576466371 ) ) ;
#17083=CARTESIAN_POINT ( 'NONE',  ( 745.4481719005789273, -171.7255117493291152, 347.5162901302853129 ) ) ;
#17084=CARTESIAN_POINT ( 'NONE',  ( 756.3353852180819104, -77.90732993114757221, 331.1735550268788302 ) ) ;
#17088=CARTESIAN_POINT ( 'NONE',  ( 804.1009440267234822, -431.4636090269702322, 314.0944755984392600 ) ) ;
#17091=CARTESIAN_POINT ( 'NONE',  ( 751.9810565676468741, -410.0891481129647218, 360.9747183278973921 ) ) ;
#17092=CARTESIAN_POINT ( 'NONE',  ( 815.2698199232962679, -16.81642084023867412, 342.5225473063383674 ) ) ;
#17096=CARTESIAN_POINT ( 'NONE',  ( 784.0799538623451781, -35.80559628986934229, 364.6971507214555572 ) ) ;
#17099=CARTESIAN_POINT ( 'NONE',  ( 813.2346286133761168, -173.2601417444143692, 328.9521613784389160 ) ) ;
#17100=CARTESIAN_POINT ( 'NONE',  ( 791.9812246680005501, -20.63460265842048003, 361.9419747391813189 ) ) ;
#17104=CARTESIAN_POINT ( 'NONE',  ( 781.7834795799800531, -154.8164208402382371, 315.0636971347436202 ) ) ;
#17109=CARTESIAN_POINT ( 'NONE',  ( 803.8651313633788504, -29.26014174441482751, 332.4468031744301015 ) ) ;
#17112=CARTESIAN_POINT ( 'NONE',  ( 792.3570229623691148, -261.1800572038742416, 373.1304606946836770 ) ) ;
#17113=CARTESIAN_POINT ( 'NONE',  ( 790.9844846989617508, -334.3726999360615082, 317.2208543904092721 ) ) ;
#17114=CARTESIAN_POINT ( 'NONE',  ( 798.0661480581538854, 21.46713098285774279, 309.5768839229118043 ) ) ;
#17119=CARTESIAN_POINT ( 'NONE',  ( 759.2295555964440155, -352.1692326535046504, 353.9708237608231229 ) ) ;
#17121=CARTESIAN_POINT ( 'NONE',  ( 804.6971507214547046, -123.2817908451530542, 344.0799538623459739 ) ) ;
#17122=CARTESIAN_POINT ( 'NONE',  ( 767.8955696845333705, -0.4527844766023628176, 362.1676090361162323 ) ) ;
#17126=CARTESIAN_POINT ( 'NONE',  ( 814.4686193811664907, -219.2817908451527558, 346.2056067578752732 ) ) ;
#17127=CARTESIAN_POINT ( 'NONE',  ( 802.7791456095903868, -172.7146871989598083, 329.0155153010375102 ) ) ;
#17132=EDGE_CURVE ( 'NONE', #26042, #34191, #44386, .T. ) ;
#17133=CARTESIAN_POINT ( 'NONE',  ( 815.2698199232961542, -64.81642084023852135, 342.5225473063383106 ) ) ;
#17135=CARTESIAN_POINT ( 'NONE',  ( 807.6521310549275086, -452.9681489794448339, 339.7933401739554711 ) ) ;
#17138=CARTESIAN_POINT ( 'NONE',  ( 809.0717654672305343, -340.9181544815160123, 360.1688906516309885 ) ) ;
#17143=CARTESIAN_POINT ( 'NONE',  ( 788.8264449731200330, -405.1800572038737300, 363.6646147819171233 ) ) ;
#17144=CARTESIAN_POINT ( 'NONE',  ( 796.9571628226829034, -143.4636090269711701, 321.2382568024804641 ) ) ;
#17147=CARTESIAN_POINT ( 'NONE',  ( 748.3538107759620743, -64.71468719896019195, 355.8262568251490165 ) ) ;
#17148=CARTESIAN_POINT ( 'NONE',  ( 758.0580252608178853, -366.4527844766012095, 328.0187753319985404 ) ) ;
#17150=CARTESIAN_POINT ( 'NONE',  ( 751.2241431872005251, -136.1692326535053894, 359.9636004259367610 ) ) ;
#17151=CARTESIAN_POINT ( 'NONE',  ( 755.3201227861273992, -435.7255117493282341, 345.3687786644892981 ) ) ;
#17155=CARTESIAN_POINT ( 'NONE',  ( 804.9363028652555840, -184.2709662947835909, 338.2165204200192079 ) ) ;
#17156=CARTESIAN_POINT ( 'NONE',  ( 754.8072714833583632, -196.8164208402380950, 338.1981804954721156 ) ) ;
#17161=CARTESIAN_POINT ( 'NONE',  ( 755.3201227861273992, -387.7255117493283478, 345.3687786644892981 ) ) ;
#17164=CARTESIAN_POINT ( 'NONE',  ( 810.7187646348534145, -138.4527844766019200, 356.7737145352016341 ) ) ;
#17167=CARTESIAN_POINT ( 'NONE',  ( 764.3348316497523456, -190.7146871989597798, 308.6759233522265617 ) ) ;
#17171=CARTESIAN_POINT ( 'NONE',  ( 789.9200121543843807, -241.9874144716869182, 317.0176451133914384 ) ) ;
#17179=CARTESIAN_POINT ( 'NONE',  ( 752.7379699480933368, -132.0090635724257595, 361.9858362298580232 ) ) ;
#17186=CARTESIAN_POINT ( 'NONE',  ( 815.3608509340175488, -386.7363362996977116, 341.2497674668889545 ) ) ;
#17193=CARTESIAN_POINT ( 'NONE',  ( 807.2620300519052989, -216.0090635724255037, 318.0141637701419768 ) ) ;
#17195=CARTESIAN_POINT ( 'NONE',  ( 746.8695393053150156, -197.9073299311472169, 327.6429770376306010 ) ) ;
#17198=CARTESIAN_POINT ( 'NONE',  ( 768.0187753319979720, -296.6346026584195670, 318.0580252608186242 ) ) ;
#17199=CARTESIAN_POINT ( 'NONE',  ( 779.4763451958990572, -56.73633629969872771, 365.0264073115438919 ) ) ;
#17204=CARTESIAN_POINT ( 'NONE',  ( 760.5453621957607311, -117.0783235625963528, 323.8424801807151425 ) ) ;
#17205=CARTESIAN_POINT ( 'NONE',  ( 778.2165204200184689, -310.8164208402377540, 364.9363028652563230 ) ) ;
#17208=CARTESIAN_POINT ( 'NONE',  ( 774.6858677611749044, -81.72551174932937101, 315.5713283507209894 ) ) ;
#17211=CARTESIAN_POINT ( 'NONE',  ( 805.9055244015594326, -411.6237781080499758, 315.8990559732753240 ) ) ;
#17213=CARTESIAN_POINT ( 'NONE',  ( 800.2193346964447755, -282.9982390220558841, 355.1360043628815788 ) ) ;
#17217=CARTESIAN_POINT ( 'NONE',  ( 804.4286716492782716, -425.3618753856919170, 345.3141322388244703 ) ) ;
#17225=CARTESIAN_POINT ( 'NONE',  ( 781.7834795799800531, -130.8164208402383224, 315.0636971347436202 ) ) ;
#17226=CARTESIAN_POINT ( 'NONE',  ( 772.4468031744293057, -441.8272453906066630, 363.8651313633793620 ) ) ;
#17227=CARTESIAN_POINT ( 'NONE',  ( 760.5453621957607311, -93.07832356259645223, 323.8424801807151425 ) ) ;
#17230=CARTESIAN_POINT ( 'NONE',  ( 812.6845335610512393, -343.9874144716865771, 353.5525998758768651 ) ) ;
#17235=CARTESIAN_POINT ( 'NONE',  ( 762.1177392798416577, -42.55451811788057626, 309.8865473780659272 ) ) ;
#17244=CARTESIAN_POINT ( 'NONE',  ( 787.5531968255692163, -381.8272453906068336, 316.1348686366205811 ) ) ;
#17245=CARTESIAN_POINT ( 'NONE',  ( 809.0717654672305343, -292.9181544815162397, 360.1688906516309885 ) ) ;
#17249=CARTESIAN_POINT ( 'NONE',  ( 778.7629533639073998, -104.7363362996985785, 375.0009284576466371 ) ) ;
#17253=CARTESIAN_POINT ( 'NONE',  ( 804.9363028652555840, -184.2709662947835909, 338.2165204200192079 ) ) ;
#17256=CARTESIAN_POINT ( 'NONE',  ( 791.0478386215596629, -429.8272453906067199, 306.7653713866226326 ) ) ;
#17261=CARTESIAN_POINT ( 'NONE',  ( 788.7631598425961101, -1.441959926233096656, 305.7194118038759143 ) ) ;
#17265=CARTESIAN_POINT ( 'NONE',  ( 798.0661480581538854, -314.5328690171411949, 309.5768839229118043 ) ) ;
#17266=CARTESIAN_POINT ( 'NONE',  ( 800.0135310231082713, -110.0891481129656597, 325.0180583372163028 ) ) ;
#17269=CARTESIAN_POINT ( 'NONE',  ( 792.1044303154645831, -300.4527844766012663, 317.8323909638837677 ) ) ;
#17271=CARTESIAN_POINT ( 'NONE',  ( 790.6613096012131336, -448.0786441114948389, 367.3906422790598185 ) ) ;
#17275=CARTESIAN_POINT ( 'NONE',  ( 771.1735550268778070, -33.18005720387498769, 316.3353852180827630 ) ) ;
#17277=CARTESIAN_POINT ( 'NONE',  ( 777.4774526936600978, -370.2709662947830793, 304.7301800767028226 ) ) ;
#17278=CARTESIAN_POINT ( 'NONE',  ( 813.9316612368132837, -247.4419599262323004, 348.6739635108323228 ) ) ;
#17286=CARTESIAN_POINT ( 'NONE',  ( 778.2165204200184689, -238.8164208402379813, 364.9363028652563230 ) ) ;
#17288=CARTESIAN_POINT ( 'NONE',  ( 748.9653473494363425, -386.6346026584191691, 356.9462024416521331 ) ) ;
#17294=CARTESIAN_POINT ( 'NONE',  ( 755.1538015810308480, -230.1908817542436338, 343.0433043558613804 ) ) ;
#17295=CARTESIAN_POINT ( 'NONE',  ( 804.6798772138708955, -111.7255117493293000, 334.6312213355107019 ) ) ;
#17299=CARTESIAN_POINT ( 'NONE',  ( 766.7756240680305382, -302.5328690171411949, 361.5560724626415663 ) ) ;
#17302=CARTESIAN_POINT ( 'NONE',  ( 762.1177392798416577, -18.55451811788065797, 309.8865473780659272 ) ) ;
#17305=CARTESIAN_POINT ( 'NONE',  ( 812.7932403749906598, -183.1800572038744974, 327.7687537140311633 ) ) ;
#17306=CARTESIAN_POINT ( 'NONE',  ( 785.3141322388236176, -93.72551174932934259, 364.4286716492789537 ) ) ;
#17310=CARTESIAN_POINT ( 'NONE',  ( 755.8990559732751535, -419.4636090269702891, 365.9055244015606831 ) ) ;
#17313=CARTESIAN_POINT ( 'NONE',  ( 769.1273215169530886, -358.7146871989592114, 317.4527132478988847 ) ) ;
#17314=CARTESIAN_POINT ( 'NONE',  ( 814.2001403089898304, -65.36187538569306810, 347.4397851343538264 ) ) ;
#17316=CARTESIAN_POINT ( 'NONE',  ( 793.2243759319678702, -2.532869017142183932, 318.4439275373583200 ) ) ;
#17320=CARTESIAN_POINT ( 'NONE',  ( 813.9316612368132837, -175.4419599262325562, 348.6739635108323228 ) ) ;
#17321=CARTESIAN_POINT ( 'NONE',  ( 756.3353852180820240, -5.907329931147799584, 331.1735550268787733 ) ) ;
#17327=CARTESIAN_POINT ( 'NONE',  ( 803.6646147819161570, -185.9073299311472454, 348.8264449731210561 ) ) ;
#17329=CARTESIAN_POINT ( 'NONE',  ( 778.1981804954715471, -346.2709662947830225, 314.8072714833591021 ) ) ;
#17332=CARTESIAN_POINT ( 'NONE',  ( 784.0799538623451781, -35.80559628986934229, 364.6971507214555572 ) ) ;
#17336=CARTESIAN_POINT ( 'NONE',  ( 755.2512626584698410, -271.5436935675106156, 315.2512626584710915 ) ) ;
#17338=CARTESIAN_POINT ( 'NONE',  ( 755.1538015810308480, -350.1908817542433212, 343.0433043558613804 ) ) ;
#17340=CARTESIAN_POINT ( 'NONE',  ( 783.0433043558608688, -432.8965053807771142, 315.1538015810313027 ) ) ;
#17345=CARTESIAN_POINT ( 'NONE',  ( 772.5602148656447525, -249.7255117493288594, 305.7998596910095443 ) ) ;
#17346=CARTESIAN_POINT ( 'NONE',  ( 802.7791456095903868, -340.7146871989592114, 329.0155153010375102 ) ) ;
#17349=EDGE_CURVE ( 'NONE', #22842, #23907, #20031, .T. ) ;
#17351=CARTESIAN_POINT ( 'NONE',  ( 754.7162404726377645, -134.7363362996984790, 339.4709603349214717 ) ) ;
#17352=CARTESIAN_POINT ( 'NONE',  ( 797.6776695296629214, -19.54369356751139364, 357.6776695296636603 ) ) ;
#17357=CARTESIAN_POINT ( 'NONE',  ( 766.0291762391763086, -226.9181544815163534, 360.7704444035551319 ) ) ;
#17358=CARTESIAN_POINT ( 'NONE',  ( 745.1792804349281596, -230.1908817542436338, 343.7566961878542884 ) ) ;
#17359=CARTESIAN_POINT ( 'NONE',  ( 759.2295555964440155, -184.1692326535052757, 353.9708237608231229 ) ) ;
#17363=CARTESIAN_POINT ( 'NONE',  ( 796.9462024416508257, -12.45278447660232146, 308.9653473494370246 ) ) ;
#17364=CARTESIAN_POINT ( 'NONE',  ( 749.2812353651451076, -78.45278447660211896, 323.2262854647983090 ) ) ;
#17365=CARTESIAN_POINT ( 'NONE',  ( 796.9142768083648889, -452.9681489794446634, 358.6301678913937963 ) ) ;
#17368=EDGE_CURVE ( 'NONE', #29782, #30209, #31214, .T. ) ;
#17370=CARTESIAN_POINT ( 'NONE',  ( 788.6739635108323228, -367.6454272087886466, 373.9316612368139090 ) ) ;
#17373=CARTESIAN_POINT ( 'NONE',  ( 813.1304606946830518, -281.9073299311468759, 352.3570229623690580 ) ) ;
#17378=CARTESIAN_POINT ( 'NONE',  ( 804.6798772138708955, -399.7255117493283478, 334.6312213355107019 ) ) ;
#17379=CARTESIAN_POINT ( 'NONE',  ( 801.5560724626406000, -144.5545181178802636, 326.7756240680316182 ) ) ;
#17382=CARTESIAN_POINT ( 'NONE',  ( 813.2346286133761168, -77.26014174441466764, 328.9521613784389160 ) ) ;
#17383=CARTESIAN_POINT ( 'NONE',  ( 755.3201227861273992, -411.7255117493282910, 345.3687786644892981 ) ) ;
#17384=CARTESIAN_POINT ( 'NONE',  ( 805.0032342141413437, 10.45630643248851044, 314.9967657858572352 ) ) ;
#17386=CARTESIAN_POINT ( 'NONE',  ( 778.7502325331095108, -144.3510508353235764, 304.6391490659818828 ) ) ;
#17387=CARTESIAN_POINT ( 'NONE',  ( 774.6312213355099630, -431.3618753856918033, 364.6798772138717482 ) ) ;
#17391=CARTESIAN_POINT ( 'NONE',  ( 759.9864689768902508, -242.0891481129652618, 354.9819416627836404 ) ) ;
#17392=CARTESIAN_POINT ( 'NONE',  ( 756.5762568750052424, -219.1800572038744122, 348.7366044899774238 ) ) ;
#17398=CARTESIAN_POINT ( 'NONE',  ( 755.0636971347428243, -388.2709662947829656, 341.7834795799807353 ) ) ;
#17400=EDGE_CURVE ( 'NONE', #13608, #19936, #16683, .T. ) ;
#17401=VERTEX_POINT ( 'NONE', #41393 ) ;
#17405=CARTESIAN_POINT ( 'NONE',  ( 756.1443688327750579, -189.6237781080507148, 314.3581564841659315 ) ) ;
#17413=CARTESIAN_POINT ( 'NONE',  ( 805.1016975059191054, -222.8965053807778531, 343.0745993439771837 ) ) ;
#17415=DIRECTION ( 'NONE',  ( 0.000000000000000000, 0.000000000000000000, 1.000000000000000000 ) ) ;
#17424=CARTESIAN_POINT ( 'NONE',  ( 744.6391490659812007, -134.7363362996984790, 338.7502325331110455 ) ) ;
#17431=CARTESIAN_POINT ( 'NONE',  ( 766.4474001241216001, -379.0999726633341993, 307.3154664389482491 ) ) ;
#17436=CARTESIAN_POINT ( 'NONE',  ( 794.9819416627830151, 11.00176097794305541, 319.9864689768909898 ) ) ;
#17438=CARTESIAN_POINT ( 'NONE',  ( 745.1792804349281596, -254.1908817542435770, 343.7566961878542884 ) ) ;
#17440=CARTESIAN_POINT ( 'NONE',  ( 792.3570229623688874, -189.1800572038744122, 373.1304606946836202 ) ) ;
#17444=CARTESIAN_POINT ( 'NONE',  ( 778.1981804954714335, -274.2709662947833067, 314.8072714833589885 ) ) ;
#17445=CARTESIAN_POINT ( 'NONE',  ( 761.4292242960306112, -89.46360902697134065, 323.2154366446414429 ) ) ;
#17448=DIRECTION ( 'NONE',  ( 0.000000000000000000, -1.000000000000000000, -1.056348263647623421E-15 ) ) ;
#17449=CARTESIAN_POINT ( 'NONE',  ( 759.2295555964440155, -112.1692326535054889, 353.9708237608231229 ) ) ;
#17450=CARTESIAN_POINT ( 'NONE',  ( 771.2633955100217236, -311.9073299311468759, 363.4237431249939618 ) ) ;
#17452=AXIS2_PLACEMENT_3D ( 'NONE', #18952, #29114, #43426 ) ;
#17454=CARTESIAN_POINT ( 'NONE',  ( 778.1981804954714335, -82.27096629478388934, 314.8072714833589885 ) ) ;
#17457=CARTESIAN_POINT ( 'NONE',  ( 751.2241431872005251, -400.1692326535045936, 359.9636004259367610 ) ) ;
#17458=EDGE_LOOP ( 'NONE', ( #2330, #4045 ) ) ;
#17459=CARTESIAN_POINT ( 'NONE',  ( 778.1981804954714335, -298.2709662947830793, 314.8072714833589885 ) ) ;
#17463=CARTESIAN_POINT ( 'NONE',  ( 781.7834795799800531, -394.8164208402374697, 315.0636971347436202 ) ) ;
#17470=CARTESIAN_POINT ( 'NONE',  ( 794.9819416627830151, -132.9982390220564810, 319.9864689768909898 ) ) ;
#17471=CARTESIAN_POINT ( 'NONE',  ( 804.1105419155481968, -435.8272453906066062, 347.6308680596136469 ) ) ;
#17472=CARTESIAN_POINT ( 'NONE',  ( 790.8726784830453198, -130.7146871989599504, 362.5472867521010585 ) ) ;
#17476=CARTESIAN_POINT ( 'NONE',  ( 744.8212110874229666, -402.8965053807773415, 336.2046728542121627 ) ) ;
#17482=CARTESIAN_POINT ( 'NONE',  ( 788.6739635108323228, -31.64542720878970883, 373.9316612368139090 ) ) ;
#17492=CARTESIAN_POINT ( 'NONE',  ( 796.9571628226829034, -383.4636090269704596, 321.2382568024804641 ) ) ;
#17493=CARTESIAN_POINT ( 'NONE',  ( 799.9636004259356241, -334.9181544815160692, 311.2241431872006956 ) ) ;
#17496=CARTESIAN_POINT ( 'NONE',  ( 745.5313806188320314, -135.2817908451530116, 333.7943932421247268 ) ) ;
#17500=CARTESIAN_POINT ( 'NONE',  ( 778.2165204200184689, -190.8164208402381234, 364.9363028652563230 ) ) ;
#17502=CARTESIAN_POINT ( 'NONE',  ( 811.3240766477731540, -412.3726999360612808, 355.6651683502462902 ) ) ;
#17508=CARTESIAN_POINT ( 'NONE',  ( 781.2497674668890113, 11.64894916467595642, 375.3608509340180603 ) ) ;
#17512=CARTESIAN_POINT ( 'NONE',  ( 747.3154664389472828, -307.9874144716866340, 326.4474001241230781 ) ) ;
#17513=CARTESIAN_POINT ( 'NONE',  ( 788.8264449731201466, -117.1800572038747106, 363.6646147819170665 ) ) ;
#17517=CARTESIAN_POINT ( 'NONE',  ( 797.8594530101008786, -301.5436935675105588, 322.1405469898980982 ) ) ;
#17521=CARTESIAN_POINT ( 'NONE',  ( 789.8509095638472672, -449.0441647919901698, 365.1129080010174448 ) ) ;
#17526=CARTESIAN_POINT ( 'NONE',  ( 804.6798772138708955, -15.72551174932958951, 334.6312213355107019 ) ) ;
#17528=CARTESIAN_POINT ( 'NONE',  ( 804.7487373415286811, -355.5436935675103882, 364.7487373415288516 ) ) ;
#17529=CARTESIAN_POINT ( 'NONE',  ( 813.2346286133761168, -245.2601417444141987, 328.9521613784389160 ) ) ;
#17530=CARTESIAN_POINT ( 'NONE',  ( 752.4576283171824116, -69.07832356259653750, 317.7880784355627952 ) ) ;
#17535=CARTESIAN_POINT ( 'NONE',  ( 792.1044303154645831, -252.4527844766015789, 317.8323909638837677 ) ) ;
#17536=CARTESIAN_POINT ( 'NONE',  ( 763.0537975583475827, -384.4527844766011526, 371.0346526505627480 ) ) ;
#17541=CARTESIAN_POINT ( 'NONE',  ( 796.1575198192839480, -246.0090635724253900, 359.4546378042384163 ) ) ;
#17542=APPLICATION_CONTEXT ( 'automotive_design' ) ;
#17543=CARTESIAN_POINT ( 'NONE',  ( 771.1735550268778070, -105.1800572038747248, 316.3353852180827630 ) ) ;
#17547=CARTESIAN_POINT ( 'NONE',  ( 756.1348686366196716, -305.2601417444139429, 347.5531968255698416 ) ) ;
#17549=CARTESIAN_POINT ( 'NONE',  ( 764.1737431748507561, -34.37269993606243901, 371.6461892240376415 ) ) ;
#17551=CARTESIAN_POINT ( 'NONE',  ( 767.7687537140311633, -191.9073299311471885, 372.7932403749916830 ) ) ;
#17552=CARTESIAN_POINT ( 'NONE',  ( 768.0187753319979720, -80.63460265842029173, 318.0580252608186242 ) ) ;
#17555=CARTESIAN_POINT ( 'NONE',  ( 780.5236548040995785, 3.263663700301089765, 314.9735926884559944 ) ) ;
#17558=CARTESIAN_POINT ( 'NONE',  ( 756.1348686366196716, -353.2601417444137724, 347.5531968255698416 ) ) ;
#17559=CARTESIAN_POINT ( 'NONE',  ( 814.9108240113580450, -40.27096629478405987, 337.5031285880265273 ) ) ;
#17561=CARTESIAN_POINT ( 'NONE',  ( 755.8398074228967971, -67.44195992623289726, 333.4516893846970333 ) ) ;
#17564=CARTESIAN_POINT ( 'NONE',  ( 758.0141637701419768, -207.0783235625960685, 367.2620300519063790 ) ) ;
#17565=CARTESIAN_POINT ( 'NONE',  ( 755.5713283507202505, -5.361875385693257279, 334.6858677611754729 ) ) ;
#17568=CARTESIAN_POINT ( 'NONE',  ( 805.1927285166397041, -208.8164208402380666, 341.8018195045277707 ) ) ;
#17571=CARTESIAN_POINT ( 'NONE',  ( 764.8639956371174549, -344.0891481129648355, 319.7806653035542581 ) ) ;
#17574=CARTESIAN_POINT ( 'NONE',  ( 796.7845633553578182, -57.62377810805111267, 358.5707757039688204 ) ) ;
#17577=CARTESIAN_POINT ( 'NONE',  ( 814.5518280994195948, -255.7255117493287742, 332.4837098697145166 ) ) ;
#17578=CARTESIAN_POINT ( 'NONE',  ( 776.2433038121456548, -12.89650538077851216, 374.8207195650711014 ) ) ;
#17583=CARTESIAN_POINT ( 'NONE',  ( 813.1304606946830518, -305.9073299311467622, 352.3570229623690580 ) ) ;
#17585=CARTESIAN_POINT ( 'NONE',  ( 790.8726784830453198, -322.7146871989593819, 362.5472867521010585 ) ) ;
#17587=CARTESIAN_POINT ( 'NONE',  ( 804.8461984189677878, -146.1908817542438896, 336.9566956441385628 ) ) ;
#17588=CARTESIAN_POINT ( 'NONE',  ( 762.1405469898971887, -25.54369356751136877, 357.8594530101015607 ) ) ;
#17592=CARTESIAN_POINT ( 'NONE',  ( 755.8990559732751535, -251.4636090269709143, 365.9055244015606831 ) ) ;
#17593=CARTESIAN_POINT ( 'NONE',  ( 800.7704444035546203, -172.1692326535052757, 326.0291762391768771 ) ) ;
#17597=CARTESIAN_POINT ( 'NONE',  ( 755.2512626584698410, -31.54369356751135456, 315.2512626584710915 ) ) ;
#17598=CARTESIAN_POINT ( 'NONE',  ( 777.5031285880264704, -70.81642084023850714, 374.9108240113588408 ) ) ;
#17599=CARTESIAN_POINT ( 'NONE',  ( 808.1998602359702772, -452.9681489794448908, 337.6500903519150825 ) ) ;
#17603=CARTESIAN_POINT ( 'NONE',  ( 747.6481478633932056, -349.0999726633342561, 353.4146539503763620 ) ) ;
#17605=CARTESIAN_POINT ( 'NONE',  ( 800.9747183278959710, -324.9982390220559409, 311.9810565676471583 ) ) ;
#17609=FACE_OUTER_BOUND ( 'NONE', #1267, .T. ) ;
#17610=CARTESIAN_POINT ( 'NONE',  ( 781.8018195045266339, -382.2709662947828519, 365.1927285166406705 ) ) ;
#17611=CARTESIAN_POINT ( 'NONE',  ( 796.9571628226829034, -167.4636090269711133, 321.2382568024804641 ) ) ;
#17614=CARTESIAN_POINT ( 'NONE',  ( 758.0141637701419768, -87.07832356259646645, 367.2620300519063790 ) ) ;
#17615=CARTESIAN_POINT ( 'NONE',  ( 774.6858677611749044, -393.7255117493283478, 315.5713283507209894 ) ) ;
#17616=CARTESIAN_POINT ( 'NONE',  ( 813.1304606946831655, 6.092670068852160448, 352.3570229623691716 ) ) ;
#17618=CARTESIAN_POINT ( 'NONE',  ( 808.7758568127978833, -148.1692326535053610, 320.0363995740631822 ) ) ;
#17626=CARTESIAN_POINT ( 'NONE',  ( 794.9819416627830151, -228.9982390220561683, 319.9864689768909898 ) ) ;
#17627=CARTESIAN_POINT ( 'NONE',  ( 801.9419747391806368, -210.4527844766016926, 351.9812246680014027 ) ) ;
#17630=CARTESIAN_POINT ( 'NONE',  ( 787.4397851343537695, 2.274488250670355871, 374.2001403089903988 ) ) ;
#17632=EDGE_LOOP ( 'NONE', ( #21999, #40693, #29995, #38908 ) ) ;
#17633=CARTESIAN_POINT ( 'NONE',  ( 762.1405469898971887, -433.5436935675099903, 357.8594530101015607 ) ) ;
#17637=CARTESIAN_POINT ( 'NONE',  ( 801.1904061080338124, -140.0891481129655176, 368.3070685750236066 ) ) ;
#17639=CARTESIAN_POINT ( 'NONE',  ( 746.0683387631852383, -187.4419599262325278, 331.3260364891676204 ) ) ;
#17647=CARTESIAN_POINT ( 'NONE',  ( 803.8651313633788504, -221.2601417444142271, 332.4468031744301015 ) ) ;
#17656=CARTESIAN_POINT ( 'NONE',  ( 805.6418435158337843, -149.4636090269711417, 363.8556311672236916 ) ) ;
#17666=CARTESIAN_POINT ( 'NONE',  ( 765.0180583372156207, -0.9982390220569063999, 360.0135310231089534 ) ) ;
#17669=CARTESIAN_POINT ( 'NONE',  ( 776.2046728542105711, -260.1908817542435486, 304.8212110874238761 ) ) ;
#17671=CARTESIAN_POINT ( 'NONE',  ( 787.5162901302840055, -227.3618753856925707, 305.4481719005792684 ) ) ;
#17675=CARTESIAN_POINT ( 'NONE',  ( 767.8955696845333705, -288.4527844766014937, 362.1676090361162323 ) ) ;
#17676=CARTESIAN_POINT ( 'NONE',  ( 798.5707757039680246, -77.46360902697138329, 356.7845633553585003 ) ) ;
#17678=CIRCLE ( 'NONE', #19151, 30.00000000000008171 ) ;
#17681=CARTESIAN_POINT ( 'NONE',  ( 804.1601925771018387, -127.4419599262326983, 346.5483106153029098 ) ) ;
#17682=CARTESIAN_POINT ( 'NONE',  ( 764.8639956371174549, -344.0891481129647786, 319.7806653035542013 ) ) ;
#17683=ORIENTED_EDGE ( 'NONE', *, *, #17041, .F. ) ;
#17686=CARTESIAN_POINT ( 'NONE',  ( 800.2193346964447755, -90.99823902205663728, 355.1360043628815788 ) ) ;
#17689=CARTESIAN_POINT ( 'NONE',  ( 814.8230680027162407, -413.8055962898681059, 333.7305795820267917 ) ) ;
#17691=CARTESIAN_POINT ( 'NONE',  ( 794.9819416627830151, -324.9982390220559409, 319.9864689768909898 ) ) ;
#17695=CARTESIAN_POINT ( 'NONE',  ( 768.0187753319979720, -416.6346026584192259, 318.0580252608186242 ) ) ;
#17701=CARTESIAN_POINT ( 'NONE',  ( 767.8955696845333705, -120.4527844766019484, 362.1676090361162323 ) ) ;
#17702=CARTESIAN_POINT ( 'NONE',  ( 802.9823548866075953, -433.0999726633339151, 330.0799878456151077 ) ) ;
#17703=CARTESIAN_POINT ( 'NONE',  ( 789.9200121543843807, -121.9874144716872593, 317.0176451133914384 ) ) ;
#17704=CARTESIAN_POINT ( 'NONE',  ( 791.7608162188021197, 205.0000000000000568, 329.9999999999999432 ) ) ;
#17705=DIRECTION ( 'NONE',  ( 0.000000000000000000, 0.000000000000000000, -1.000000000000000000 ) ) ;
#17706=CARTESIAN_POINT ( 'NONE',  ( 746.0683387631852383, -379.4419599262318457, 331.3260364891676204 ) ) ;
#17711=CARTESIAN_POINT ( 'NONE',  ( 802.2119215644370342, -30.00906357242607925, 367.5423716828165084 ) ) ;
#17718=CARTESIAN_POINT ( 'NONE',  ( 761.4292242960306112, -353.4636090269705733, 323.2154366446414429 ) ) ;
#17719=CARTESIAN_POINT ( 'NONE',  ( 760.0363995740630116, -322.9181544815161260, 368.7758568127991907 ) ) ;
#17722=DIRECTION ( 'NONE',  ( 0.000000000000000000, 0.000000000000000000, 1.000000000000000000 ) ) ;
#17724=CARTESIAN_POINT ( 'NONE',  ( 745.1792804349281596, -158.1908817542438612, 343.7566961878542884 ) ) ;
#17726=CARTESIAN_POINT ( 'NONE',  ( 808.0189434323515343, -86.08914811296573077, 319.0252816721025511 ) ) ;
#17730=CARTESIAN_POINT ( 'NONE',  ( 767.8955696845333705, -192.4527844766016926, 362.1676090361162323 ) ) ;
#17731=CARTESIAN_POINT ( 'NONE',  ( 814.4686193811664907, -459.2817908451519884, 346.2056067578752732 ) ) ;
#17736=CARTESIAN_POINT ( 'NONE',  ( 807.5423716828161105, 14.92167643740321381, 362.2119215644372048 ) ) ;
#17741=CARTESIAN_POINT ( 'NONE',  ( 812.6845335610512393, -319.9874144716866340, 353.5525998758768651 ) ) ;
#17742=CARTESIAN_POINT ( 'NONE',  ( 764.8639956371174549, -128.0891481129655745, 319.7806653035542581 ) ) ;
#17744=CARTESIAN_POINT ( 'NONE',  ( 803.6646147819161570, -305.9073299311467622, 348.8264449731210561 ) ) ;
#17746=CARTESIAN_POINT ( 'NONE',  ( 792.3570229623691148, -93.18005720387479585, 373.1304606946836770 ) ) ;
#17751=CARTESIAN_POINT ( 'NONE',  ( 756.3353852180819104, -29.90732993114771787, 331.1735550268788302 ) ) ;
#17753=CARTESIAN_POINT ( 'NONE',  ( 792.2312462859673587, -371.9073299311465917, 307.2067596250082602 ) ) ;
#17754=CARTESIAN_POINT ( 'NONE',  ( 813.9316612368132837, -271.4419599262321867, 348.6739635108323228 ) ) ;
#17755=CARTESIAN_POINT ( 'NONE',  ( 803.8556311672234642, -57.62377810805111267, 365.6418435158340117 ) ) ;
#17761=CARTESIAN_POINT ( 'NONE',  ( 815.2698199232961542, -376.8164208402375834, 342.5225473063383106 ) ) ;
#17762=CARTESIAN_POINT ( 'NONE',  ( 759.9999999999992042, 205.0000000000000568, 319.9999999999999432 ) ) ;
#17767=CARTESIAN_POINT ( 'NONE',  ( 755.5913626894240451, -253.6454272087889876, 346.6156483768012890 ) ) ;
#17768=CARTESIAN_POINT ( 'NONE',  ( 756.3353852180819104, -101.9073299311474727, 331.1735550268788302 ) ) ;
#17772=CARTESIAN_POINT ( 'NONE',  ( 764.0069404352550464, -279.0783235625958127, 359.2566176426627180 ) ) ;
#17774=CARTESIAN_POINT ( 'NONE',  ( 810.4231160770870019, -48.55451811788057626, 321.9338519418446936 ) ) ;
#17776=CARTESIAN_POINT ( 'NONE',  ( 805.0032342141412300, -181.5436935675108145, 314.9967657858571783 ) ) ;
#17777=CARTESIAN_POINT ( 'NONE',  ( 762.1405469898971887, -73.54369356751118403, 357.8594530101015607 ) ) ;
#17780=CARTESIAN_POINT ( 'NONE',  ( 814.4686193811664907, -435.2817908451521021, 346.2056067578752732 ) ) ;
#17783=CARTESIAN_POINT ( 'NONE',  ( 804.9511171171677688, -365.8055962898682765, 335.8780910478229202 ) ) ;
#17784=CARTESIAN_POINT ( 'NONE',  ( 745.0891759886404770, -52.27096629478401724, 342.4968714119734159 ) ) ;
#17786=CARTESIAN_POINT ( 'NONE',  ( 793.2243759319678702, -50.53286901714203339, 318.4439275373583200 ) ) ;
#17789=CARTESIAN_POINT ( 'NONE',  ( 771.2368401574024119, -205.4419599262324425, 374.2805881961240857 ) ) ;
#17790=CARTESIAN_POINT ( 'NONE',  ( 771.2633955100217236, -23.90732993114773919, 363.4237431249939618 ) ) ;
#17793=CARTESIAN_POINT ( 'NONE',  ( 797.6776695296629214, -211.5436935675107861, 357.6776695296636603 ) ) ;
#17796=CARTESIAN_POINT ( 'NONE',  ( 781.8018195045267476, -334.2709662947830793, 365.1927285166407273 ) ) ;
#17797=DIRECTION ( 'NONE',  ( 0.000000000000000000, 0.000000000000000000, 1.000000000000000000 ) ) ;
#17798=ORIENTED_EDGE ( 'NONE', *, *, #35606, .F. ) ;
#17799=CARTESIAN_POINT ( 'NONE',  ( 776.9566956441375396, -36.89650538077844288, 364.8461984189686405 ) ) ;
#17801=CARTESIAN_POINT ( 'NONE',  ( 767.7687537140311633, -263.9073299311469327, 372.7932403749916830 ) ) ;
#17802=CARTESIAN_POINT ( 'NONE',  ( 758.0141637701419768, -15.07832356259669560, 367.2620300519063790 ) ) ;
#17807=CARTESIAN_POINT ( 'NONE',  ( 787.4397851343537695, -285.7255117493286889, 374.2001403089903988 ) ) ;
#17809=CARTESIAN_POINT ( 'NONE',  ( 804.8461984189677878, -218.1908817542437191, 336.9566956441385628 ) ) ;
#17810=CARTESIAN_POINT ( 'NONE',  ( 764.0069404352550464, -327.0783235625956991, 359.2566176426627180 ) ) ;
#17812=CARTESIAN_POINT ( 'NONE',  ( 773.4516893846965786, -163.6454272087893003, 315.8398074228977066 ) ) ;
#17813=CARTESIAN_POINT ( 'NONE',  ( 804.4286716492782716, -17.36187538569322086, 345.3141322388244703 ) ) ;
#17817=CARTESIAN_POINT ( 'NONE',  ( 749.5768839229115201, -228.5545181178799794, 358.0661480581553064 ) ) ;
#17818=CARTESIAN_POINT ( 'NONE',  ( 793.2243759319678702, -194.5328690171415644, 318.4439275373583200 ) ) ;
#17820=CARTESIAN_POINT ( 'NONE',  ( 805.2837595273609850, -458.7363362996973706, 340.5290396650784714 ) ) ;
#17823=CARTESIAN_POINT ( 'NONE',  ( 814.2001403089898304, -17.36187538569322086, 347.4397851343538264 ) ) ;
#17824=CARTESIAN_POINT ( 'NONE',  ( 744.7301800767019131, -76.81642084023845030, 337.4774526936615757 ) ) ;
#17828=CARTESIAN_POINT ( 'NONE',  ( 807.2620300519052989, -360.0090635724250774, 318.0141637701419768 ) ) ;
#17830=CARTESIAN_POINT ( 'NONE',  ( 792.3570229623688874, -333.1800572038740142, 373.1304606946836202 ) ) ;
#17834=CARTESIAN_POINT ( 'NONE',  ( 771.2633955100217236, -431.9073299311464211, 363.4237431249939618 ) ) ;
#17836=CARTESIAN_POINT ( 'NONE',  ( 800.9840315886518738, -196.9181544815164386, 354.1144889064786412 ) ) ;
#17839=CARTESIAN_POINT ( 'NONE',  ( 813.2346286133761168, -101.2601417444146250, 328.9521613784389160 ) ) ;
#17840=CARTESIAN_POINT ( 'NONE',  ( 804.6798772138710092, -399.7255117493283478, 334.6312213355106451 ) ) ;
#17841=CARTESIAN_POINT ( 'NONE',  ( 786.2056067578752163, -155.8055962898689586, 374.4686193811670023 ) ) ;
#17843=ORIENTED_EDGE ( 'NONE', *, *, #3514, .T. ) ;
#17847=CARTESIAN_POINT ( 'NONE',  ( 797.6776695296629214, -211.5436935675107861, 357.6776695296636603 ) ) ;
#17848=CARTESIAN_POINT ( 'NONE',  ( 755.5713283507202505, -221.3618753856925707, 334.6858677611754729 ) ) ;
#17852=CARTESIAN_POINT ( 'NONE',  ( 804.4286716492782716, -425.3618753856919170, 345.3141322388244703 ) ) ;
#17856=CARTESIAN_POINT ( 'NONE',  ( 815.2698199232962679, -160.8164208402382371, 342.5225473063383674 ) ) ;
#17857=CARTESIAN_POINT ( 'NONE',  ( 783.0745993439762742, -272.1908817542434917, 365.1016975059196739 ) ) ;
#17863=CARTESIAN_POINT ( 'NONE',  ( 779.4709603349208464, -216.3510508353233490, 314.7162404726379918 ) ) ;
#17874=CARTESIAN_POINT ( 'NONE',  ( 773.7305795820266212, -153.2817908451529831, 374.8230680027170365 ) ) ;
#17885=CARTESIAN_POINT ( 'NONE',  ( 785.3141322388236176, -21.72551174932956641, 364.4286716492789537 ) ) ;
#17886=CARTESIAN_POINT ( 'NONE',  ( 746.4236121716829757, -255.8272453906072315, 328.8385539511384650 ) ) ;
#17888=CARTESIAN_POINT ( 'NONE',  ( 814.5518280994195948, -231.7255117493288310, 332.4837098697145734 ) ) ;
#17891=CARTESIAN_POINT ( 'NONE',  ( 754.8072714833581358, -316.8164208402377540, 338.1981804954720587 ) ) ;
#17893=CARTESIAN_POINT ( 'NONE',  ( 793.0897708529556667, -102.5545181178804057, 361.3366627262616362 ) ) ;
#17894=CARTESIAN_POINT ( 'NONE',  ( 766.9102291470427417, -66.55451811788050520, 318.6633372737382501 ) ) ;
#17899=CARTESIAN_POINT ( 'NONE',  ( 780.5290396650775619, -108.3510508353236759, 365.2837595273619513 ) ) ;
#17900=CARTESIAN_POINT ( 'NONE',  ( 756.3353852180819104, -365.9073299311465917, 331.1735550268788302 ) ) ;
#17903=CARTESIAN_POINT ( 'NONE',  ( 800.0135310231082713, -110.0891481129656597, 325.0180583372163028 ) ) ;
#17906=CARTESIAN_POINT ( 'NONE',  ( 744.9990715423526808, -426.3510508353226669, 341.2370466360926002 ) ) ;
#17907=VERTEX_POINT ( 'NONE', #5305 ) ;
#17908=CARTESIAN_POINT ( 'NONE',  ( 781.7834795799800531, -322.8164208402377540, 315.0636971347436202 ) ) ;
#17912=CARTESIAN_POINT ( 'NONE',  ( 759.7806653035534055, -414.9982390220555430, 324.8639956371180801 ) ) ;
#17916=ORIENTED_EDGE ( 'NONE', *, *, #11193, .F. ) ;
#17919=CARTESIAN_POINT ( 'NONE',  ( 755.3028492785439312, -447.2817908451521021, 335.9200461376539693 ) ) ;
#17920=CARTESIAN_POINT ( 'NONE',  ( 766.7756240680305382, -134.5328690171417350, 361.5560724626415663 ) ) ;
#17923=CARTESIAN_POINT ( 'NONE',  ( 746.7653713866222915, -377.2601417444137724, 351.0478386215610271 ) ) ;
#17931=CARTESIAN_POINT ( 'NONE',  ( 804.1009440267234822, -47.46360902697148987, 314.0944755984392600 ) ) ;
#17940=CARTESIAN_POINT ( 'NONE',  ( 754.7162404726377645, -374.7363362996978253, 339.4709603349214717 ) ) ;
#17941=CARTESIAN_POINT ( 'NONE',  ( 754.3581564841646241, -329.4636090269706870, 316.1443688327762516 ) ) ;
#17945=CARTESIAN_POINT ( 'NONE',  ( 768.9521613784389729, -153.8272453906075157, 373.2346286133773106 ) ) ;
#17947=CARTESIAN_POINT ( 'NONE',  ( 751.6929314249748586, -126.9982390220565094, 318.8095938919659034 ) ) ;
#17951=CARTESIAN_POINT ( 'NONE',  ( 774.6858677611749044, -177.7255117493290868, 315.5713283507209894 ) ) ;
#17952=CARTESIAN_POINT ( 'NONE',  ( 805.2837595273609850, -2.736336299698892027, 340.5290396650784714 ) ) ;
#17958=CARTESIAN_POINT ( 'NONE',  ( 781.2497674668890113, -12.35105083532396897, 375.3608509340180603 ) ) ;
#17963=CARTESIAN_POINT ( 'NONE',  ( 761.9338519418445230, -326.5328690171411381, 370.4231160770881957 ) ) ;
#17964=CARTESIAN_POINT ( 'NONE',  ( 801.9419747391806368, -138.4527844766019200, 351.9812246680014027 ) ) ;
#17967=CARTESIAN_POINT ( 'NONE',  ( 764.8639956371174549, -320.0891481129648355, 319.7806653035542013 ) ) ;
#17969=CARTESIAN_POINT ( 'NONE',  ( 745.4481719005789273, -99.72551174932931417, 347.5162901302853697 ) ) ;
#17977=CARTESIAN_POINT ( 'NONE',  ( 814.9108240113580450, -400.2709662947828519, 337.5031285880265273 ) ) ;
#17978=CARTESIAN_POINT ( 'NONE',  ( 764.3348316497523456, -286.7146871989594388, 308.6759233522265617 ) ) ;
#17980=CARTESIAN_POINT ( 'NONE',  ( 758.0141637701419768, -63.07832356259653750, 367.2620300519063790 ) ) ;
#17983=CARTESIAN_POINT ( 'NONE',  ( 799.9999999999993179, -462.9681489794448339, 309.9999999999998863 ) ) ;
#17985=CARTESIAN_POINT ( 'NONE',  ( 796.7737145352015204, -404.6346026584193396, 370.7187646348536987 ) ) ;
#17987=CARTESIAN_POINT ( 'NONE',  ( 792.9530673105016376, -457.3789191291447196, 369.8291253130404357 ) ) ;
#17991=EDGE_CURVE ( 'NONE', #17401, #18157, #26163, .T. ) ;
#17992=CARTESIAN_POINT ( 'NONE',  ( 802.5472867521000353, -268.3726999360616787, 350.8726784830461156 ) ) ;
#17993=CARTESIAN_POINT ( 'NONE',  ( 781.8018195045266339, -142.2709662947837330, 365.1927285166406705 ) ) ;
#17999=CARTESIAN_POINT ( 'NONE',  ( 805.0264073115434940, -342.3510508353228943, 339.4763451958999099 ) ) ;
#18001=CARTESIAN_POINT ( 'NONE',  ( 813.5763878283155464, -51.82724539060782121, 351.1614460488615350 ) ) ;
#18003=CARTESIAN_POINT ( 'NONE',  ( 782.5225473063381969, -214.2709662947834488, 375.2698199232970637 ) ) ;
#18004=CARTESIAN_POINT ( 'NONE',  ( 785.3141322388236176, -69.72551174932942786, 364.4286716492789537 ) ) ;
#18008=CARTESIAN_POINT ( 'NONE',  ( 791.0478386215596629, -453.8272453906066630, 306.7653713866226326 ) ) ;
#18011=CARTESIAN_POINT ( 'NONE',  ( 787.6308680596127942, -371.2601417444136587, 364.1105419155492768 ) ) ;
#18012=CARTESIAN_POINT ( 'NONE',  ( 787.5162901302840055, -59.36187538569307520, 305.4481719005793252 ) ) ;
#18014=CARTESIAN_POINT ( 'NONE',  ( 765.8855110935204493, -70.16923265350563099, 319.0159684113471599 ) ) ;
#18017=CARTESIAN_POINT ( 'NONE',  ( 814.8230680027162407, -221.8055962898687881, 333.7305795820267917 ) ) ;
#18018=CARTESIAN_POINT ( 'NONE',  ( 774.6858677611749044, -33.72551174932952733, 315.5713283507209894 ) ) ;
#18021=CARTESIAN_POINT ( 'NONE',  ( 771.2633955100217236, -215.9073299311471317, 363.4237431249939618 ) ) ;
#18023=CARTESIAN_POINT ( 'NONE',  ( 795.1360043628808398, -332.0891481129649492, 360.2193346964456282 ) ) ;
#18027=CARTESIAN_POINT ( 'NONE',  ( 765.8855110935204493, -46.16923265350568784, 319.0159684113471599 ) ) ;
#18029=CARTESIAN_POINT ( 'NONE',  ( 800.9747183278959710, -300.9982390220559409, 311.9810565676471583 ) ) ;
#18030=CARTESIAN_POINT ( 'NONE',  ( 795.6651683502461765, -10.71468719896033761, 371.3240766477733814 ) ) ;
#18035=CARTESIAN_POINT ( 'NONE',  ( 748.9653473494363425, -290.6346026584195101, 356.9462024416521331 ) ) ;
#18038=CARTESIAN_POINT ( 'NONE',  ( 776.9566956441375396, -348.8965053807774552, 364.8461984189686405 ) ) ;
#18041=CARTESIAN_POINT ( 'NONE',  ( 804.6971507214547046, -171.2817908451529263, 344.0799538623459739 ) ) ;
#18042=CARTESIAN_POINT ( 'NONE',  ( 755.5713283507202505, -29.36187538569318178, 334.6858677611754729 ) ) ;
#18046=CARTESIAN_POINT ( 'NONE',  ( 814.8207195650702488, -266.1908817542435486, 336.2433038121456548 ) ) ;
#18047=CARTESIAN_POINT ( 'NONE',  ( 805.0264073115434940, -198.3510508353234059, 339.4763451958999099 ) ) ;
#18049=CARTESIAN_POINT ( 'NONE',  ( 781.8018195045266339, 1.729033705215812011, 365.1927285166406705 ) ) ;
#18052=CARTESIAN_POINT ( 'NONE',  ( 758.8095938919642549, -8.089148112965974136, 311.6929314249763365 ) ) ;
#18053=CARTESIAN_POINT ( 'NONE',  ( 814.9108240113580450, -88.27096629478390355, 337.5031285880265273 ) ) ;
#18059=CARTESIAN_POINT ( 'NONE',  ( 809.0717654672305343, -364.9181544815158986, 360.1688906516309885 ) ) ;
#18061=CARTESIAN_POINT ( 'NONE',  ( 814.2001403089898304, -329.3618753856922581, 347.4397851343538264 ) ) ;
#18065=CARTESIAN_POINT ( 'NONE',  ( 759.7806653035534055, -438.9982390220553157, 324.8639956371180801 ) ) ;
#18066=CARTESIAN_POINT ( 'NONE',  ( 760.7433823573367135, -204.0090635724255606, 355.9930595647440441 ) ) ;
#18069=CARTESIAN_POINT ( 'NONE',  ( 764.3348316497523456, -94.71468719896007826, 308.6759233522265617 ) ) ;
#18070=CARTESIAN_POINT ( 'NONE',  ( 805.1927285166399315, -400.8164208402374697, 341.8018195045277707 ) ) ;
#18072=CARTESIAN_POINT ( 'NONE',  ( 803.6646147819161570, -449.9073299311463643, 348.8264449731210561 ) ) ;
#18078=CARTESIAN_POINT ( 'NONE',  ( 771.2633955100217236, -215.9073299311471317, 363.4237431249939618 ) ) ;
#18079=CARTESIAN_POINT ( 'NONE',  ( 795.1360043628808398, -236.0891481129652334, 360.2193346964456282 ) ) ;
#18083=CARTESIAN_POINT ( 'NONE',  ( 801.9419747391806368, -426.4527844766010389, 351.9812246680014027 ) ) ;
#18087=CARTESIAN_POINT ( 'NONE',  ( 763.0537975583476964, -168.4527844766018347, 371.0346526505628617 ) ) ;
#18089=CARTESIAN_POINT ( 'NONE',  ( 769.0155153010367712, -250.3726999360618208, 362.7791456095907279 ) ) ;
#18099=CARTESIAN_POINT ( 'NONE',  ( 756.7813123517142913, -235.9874144716868898, 329.9779781133712504 ) ) ;
#18109=CARTESIAN_POINT ( 'NONE',  ( 744.6391490659812007, -182.7363362996983369, 338.7502325331110455 ) ) ;
#18121=CARTESIAN_POINT ( 'NONE',  ( 771.2633955100217236, -23.90732993114773919, 363.4237431249939618 ) ) ;
#18122=CARTESIAN_POINT ( 'NONE',  ( 748.6759233522253680, -256.3726999360617924, 324.3348316497537098 ) ) ;
#18124=CARTESIAN_POINT ( 'NONE',  ( 796.7737145352015204, -236.6346026584198228, 370.7187646348536987 ) ) ;
#18127=CARTESIAN_POINT ( 'NONE',  ( 800.0135310231082713, -326.0891481129649492, 325.0180583372163028 ) ) ;
#18129=CARTESIAN_POINT ( 'NONE',  ( 779.4763451958990572, -104.7363362996985785, 365.0264073115438919 ) ) ;
#18130=CARTESIAN_POINT ( 'NONE',  ( 799.2566176426618085, -72.00906357242594424, 324.0069404352559559 ) ) ;
#18135=CARTESIAN_POINT ( 'NONE',  ( 783.0433043558608688, -144.8965053807781089, 315.1538015810313027 ) ) ;
#18136=CARTESIAN_POINT ( 'NONE',  ( 801.9419747391806368, -354.4527844766012095, 351.9812246680014027 ) ) ;
#18139=CARTESIAN_POINT ( 'NONE',  ( 755.0636971347428243, -124.2709662947837899, 341.7834795799807353 ) ) ;
#18142=CARTESIAN_POINT ( 'NONE',  ( 746.7653713866222915, -401.2601417444137155, 351.0478386215610271 ) ) ;
#18145=CARTESIAN_POINT ( 'NONE',  ( 764.8639956371174549, -320.0891481129648355, 319.7806653035542013 ) ) ;
#18149=CARTESIAN_POINT ( 'NONE',  ( 795.1360043628807261, -452.0891481129646650, 360.2193346964456282 ) ) ;
#18157=VERTEX_POINT ( 'NONE', #30025 ) ;
#18159=CARTESIAN_POINT ( 'NONE',  ( 781.7834795799800531, 13.18357915976123174, 315.0636971347436202 ) ) ;
#18160=CARTESIAN_POINT ( 'NONE',  ( 745.4481719005789273, -219.7255117493289447, 347.5162901302853129 ) ) ;
#18161=CARTESIAN_POINT ( 'NONE',  ( 769.1273215169530886, -118.7146871989600072, 317.4527132478988847 ) ) ;
#18164=CARTESIAN_POINT ( 'NONE',  ( 754.0944755984390895, -399.6237781080500326, 364.1009440267246760 ) ) ;
#18169=CARTESIAN_POINT ( 'NONE',  ( 771.3260364891663130, -43.64542720878966975, 306.0683387631859773 ) ) ;
#18179=CARTESIAN_POINT ( 'NONE',  ( 755.5913626894240451, -373.6454272087887034, 346.6156483768012890 ) ) ;
#18180=CARTESIAN_POINT ( 'NONE',  ( 793.5525998758768083, -343.0999726633342561, 372.6845335610516941 ) ) ;
#18182=CARTESIAN_POINT ( 'NONE',  ( 759.9999999999992042, -462.9681489794448339, 309.9999999999998863 ) ) ;
#18185=CARTESIAN_POINT ( 'NONE',  ( 752.7379699480933368, -132.0090635724257595, 361.9858362298580232 ) ) ;
#18187=CARTESIAN_POINT ( 'NONE',  ( 787.5162901302840055, -107.3618753856928976, 305.4481719005792684 ) ) ;
#18192=CARTESIAN_POINT ( 'NONE',  ( 756.5762568750052424, -219.1800572038744122, 348.7366044899774238 ) ) ;
#18193=CARTESIAN_POINT ( 'NONE',  ( 755.8990559732751535, -443.4636090269702322, 365.9055244015606831 ) ) ;
#18197=CARTESIAN_POINT ( 'NONE',  ( 754.0944755984390895, 8.376221891948691933, 364.1009440267246760 ) ) ;
#18200=CARTESIAN_POINT ( 'NONE',  ( 804.4286716492782716, -17.36187538569322086, 345.3141322388244703 ) ) ;
#18203=CARTESIAN_POINT ( 'NONE',  ( 766.5853460496234675, -301.9874144716867477, 372.3518521366060554 ) ) ;
#18204=CARTESIAN_POINT ( 'NONE',  ( 756.5762568750052424, -171.1800572038745543, 348.7366044899774238 ) ) ;
#18206=CARTESIAN_POINT ( 'NONE',  ( 762.1405469898971887, -289.5436935675103882, 357.8594530101015607 ) ) ;
#18211=CARTESIAN_POINT ( 'NONE',  ( 811.0346526505617248, -86.63460265842024910, 323.0537975583478101 ) ) ;
#18216=CARTESIAN_POINT ( 'NONE',  ( 801.9419747391806368, -66.45278447660216159, 351.9812246680014027 ) ) ;
#18217=CARTESIAN_POINT ( 'NONE',  ( 793.9708237608222134, -334.9181544815160692, 319.2295555964448681 ) ) ;
#18219=CARTESIAN_POINT ( 'NONE',  ( 787.5162901302840055, -395.3618753856919739, 305.4481719005793252 ) ) ;
#18220=CARTESIAN_POINT ( 'NONE',  ( 773.7943932421234194, -287.8055962898685038, 305.5313806188329409 ) ) ;
#18221=CARTESIAN_POINT ( 'NONE',  ( 807.5423716828161105, -81.07832356259649487, 362.2119215644372048 ) ) ;
#18224=FACE_OUTER_BOUND ( 'NONE', #23678, .T. ) ;
#18228=CARTESIAN_POINT ( 'NONE',  ( 777.5031285880264704, -382.8164208402374697, 374.9108240113588408 ) ) ;
#18235=CARTESIAN_POINT ( 'NONE',  ( 804.4086373105744769, -265.6454272087889876, 333.3843516231986541 ) ) ;
#18236=CARTESIAN_POINT ( 'NONE',  ( 791.9812246680005501, -140.6346026584201070, 361.9419747391813189 ) ) ;
#18241=CARTESIAN_POINT ( 'NONE',  ( 803.2186876482843445, -343.9874144716865771, 350.0220218866286928 ) ) ;
#18244=CARTESIAN_POINT ( 'NONE',  ( 793.5525998758768083, -55.09997266333508747, 372.6845335610516941 ) ) ;
#18247=CARTESIAN_POINT ( 'NONE',  ( 797.6776695296629214, -115.5436935675110988, 357.6776695296636603 ) ) ;
#18252=CARTESIAN_POINT ( 'NONE',  ( 811.3240766477731540, -460.3726999360611103, 355.6651683502462902 ) ) ;
#18255=CARTESIAN_POINT ( 'NONE',  ( 755.8398074228967971, -379.4419599262318457, 333.4516893846970333 ) ) ;
#18256=CARTESIAN_POINT ( 'NONE',  ( 796.9462024416508257, -36.45278447660224685, 308.9653473494370246 ) ) ;
#18260=CARTESIAN_POINT ( 'NONE',  ( 770.0799878456142551, -37.98741447168752927, 362.9823548866085616 ) ) ;
#18262=CARTESIAN_POINT ( 'NONE',  ( 746.0683387631852383, -211.4419599262324709, 331.3260364891676204 ) ) ;
#18263=CARTESIAN_POINT ( 'NONE',  ( 764.8639956371174549, -56.08914811296581604, 319.7806653035542581 ) ) ;
#18266=EDGE_CURVE ( 'NONE', #7675, #10697, #40225, .T. ) ;
#18267=CARTESIAN_POINT ( 'NONE',  ( 801.9419747391806368, -186.4527844766017779, 351.9812246680014027 ) ) ;
#18270=CARTESIAN_POINT ( 'NONE',  ( 803.6646147819162707, -329.9073299311467622, 348.8264449731211130 ) ) ;
#18274=CARTESIAN_POINT ( 'NONE',  ( 759.2295555964440155, -40.16923265350570915, 353.9708237608231229 ) ) ;
#18276=CARTESIAN_POINT ( 'NONE',  ( 808.3070685750232087, -306.9982390220558841, 361.1904061080339829 ) ) ;
#18277=CARTESIAN_POINT ( 'NONE',  ( 744.9990715423526808, 5.648949164675971524, 341.2370466360926002 ) ) ;
#18283=CARTESIAN_POINT ( 'NONE',  ( 814.5518280994195948, -279.7255117493288026, 332.4837098697145734 ) ) ;
#18286=CARTESIAN_POINT ( 'NONE',  ( 796.1575198192839480, -174.0090635724256742, 359.4546378042384163 ) ) ;
#18287=CARTESIAN_POINT ( 'NONE',  ( 794.9819416627830151, -36.99823902205679360, 319.9864689768909898 ) ) ;
#18291=CARTESIAN_POINT ( 'NONE',  ( 810.4231160770870019, -264.5545181178798657, 321.9338519418446936 ) ) ;
#18292=CARTESIAN_POINT ( 'NONE',  ( 755.0488828828309806, -209.8055962898687881, 344.1219089521771934 ) ) ;
#18295=CARTESIAN_POINT ( 'NONE',  ( 788.8264449731200330, 2.819942796124898177, 363.6646147819171233 ) ) ;
#18298=CARTESIAN_POINT ( 'NONE',  ( 792.3570229623688874, 2.819942796124898177, 373.1304606946836202 ) ) ;
#18299=CARTESIAN_POINT ( 'NONE',  ( 800.9747183278959710, -108.9982390220565804, 311.9810565676471583 ) ) ;
#18300=PLANE ( 'NONE',  #16605 ) ;
#18303=CARTESIAN_POINT ( 'NONE',  ( 788.6739635108323228, -391.6454272087885897, 373.9316612368139090 ) ) ;
#18306=CARTESIAN_POINT ( 'NONE',  ( 744.7301800767019131, -316.8164208402377540, 337.4774526936615757 ) ) ;
#18310=CARTESIAN_POINT ( 'NONE',  ( 755.5713283507202505, -413.3618753856920307, 334.6858677611754729 ) ) ;
#18311=CARTESIAN_POINT ( 'NONE',  ( 784.1219089521767955, -189.2817908451528979, 315.0488828828318333 ) ) ;
#18314=CARTESIAN_POINT ( 'NONE',  ( 807.5423716828161105, -105.0783235625964096, 362.2119215644372048 ) ) ;
#18315=CARTESIAN_POINT ( 'NONE',  ( 778.1981804954715471, -418.2709662947828519, 314.8072714833591021 ) ) ;
#18317=CARTESIAN_POINT ( 'NONE',  ( 804.4286716492782716, -449.3618753856918602, 345.3141322388244703 ) ) ;
#18322=CARTESIAN_POINT ( 'NONE',  ( 804.4286716492782716, -233.3618753856925423, 345.3141322388244703 ) ) ;
#18323=CARTESIAN_POINT ( 'NONE',  ( 802.1676090361155502, -230.6346026584197944, 327.8955696845344505 ) ) ;
#18327=CARTESIAN_POINT ( 'NONE',  ( 755.0636971347428243, -436.2709662947827951, 341.7834795799807353 ) ) ;
#18329=CARTESIAN_POINT ( 'NONE',  ( 754.9967657858570647, -193.5436935675108714, 365.0032342141425943 ) ) ;
#18330=CARTESIAN_POINT ( 'NONE',  ( 776.9254006560222479, -260.1908817542435486, 314.8983024940802125 ) ) ;
#18333=CARTESIAN_POINT ( 'NONE',  ( 766.5853460496234675, -229.9874144716869466, 372.3518521366060554 ) ) ;
#18338=CARTESIAN_POINT ( 'NONE',  ( 780.5290396650775619, -252.3510508353232353, 365.2837595273619513 ) ) ;
#18346=CARTESIAN_POINT ( 'NONE',  ( 745.7194118038753459, -181.6454272087892434, 348.7631598425976449 ) ) ;
#18352=CARTESIAN_POINT ( 'NONE',  ( 782.5225473063381969, -22.27096629478410250, 375.2698199232970637 ) ) ;
#18356=CARTESIAN_POINT ( 'NONE',  ( 788.8264449731200330, 2.819942796124898177, 363.6646147819171233 ) ) ;
#18357=CARTESIAN_POINT ( 'NONE',  ( 745.1792804349281596, -278.1908817542434917, 343.7566961878542884 ) ) ;
#18359=CARTESIAN_POINT ( 'NONE',  ( 804.7487373415286811, -211.5436935675107861, 364.7487373415288516 ) ) ;
#18363=CARTESIAN_POINT ( 'NONE',  ( 795.1360043628807261, -332.0891481129649492, 360.2193346964456282 ) ) ;
#18365=CARTESIAN_POINT ( 'NONE',  ( 759.0159684113467620, -88.91815448151682233, 325.8855110935213020 ) ) ;
#18369=CARTESIAN_POINT ( 'NONE',  ( 805.0264073115434940, -150.3510508353235480, 339.4763451958999099 ) ) ;
#18370=CARTESIAN_POINT ( 'NONE',  ( 781.7834795799800531, -370.8164208402375834, 315.0636971347436202 ) ) ;
#18375=CARTESIAN_POINT ( 'NONE',  ( 803.8556311672234642, -441.6237781080499190, 365.6418435158340117 ) ) ;
#18377=CARTESIAN_POINT ( 'NONE',  ( 765.0180583372156207, -336.9982390220558273, 360.0135310231089534 ) ) ;
#18385=CARTESIAN_POINT ( 'NONE',  ( 798.5707757039680246, -461.4636090269701754, 356.7845633553585003 ) ) ;
#18386=CARTESIAN_POINT ( 'NONE',  ( 759.0252816721024374, -216.9982390220562252, 368.0189434323527280 ) ) ;
#18387=CARTESIAN_POINT ( 'NONE',  ( 772.3691319403857278, -119.2601417444145397, 315.8894580844506663 ) ) ;
#18390=CARTESIAN_POINT ( 'NONE',  ( 766.5853460496234675, -397.9874144716864066, 372.3518521366060554 ) ) ;
#18395=CARTESIAN_POINT ( 'NONE',  ( 773.7305795820266212, -81.28179084515319630, 374.8230680027170365 ) ) ;
#18403=CARTESIAN_POINT ( 'NONE',  ( 772.4468031744293057, -417.8272453906067199, 363.8651313633793620 ) ) ;
#18405=LINE ( 'NONE', #18182, #16532 ) ;
#18408=CARTESIAN_POINT ( 'NONE',  ( 760.0363995740630116, -130.9181544815166660, 368.7758568127991907 ) ) ;
#18410=CARTESIAN_POINT ( 'NONE',  ( 796.7737145352015204, -116.6346026584201780, 370.7187646348536987 ) ) ;
#18414=CARTESIAN_POINT ( 'NONE',  ( 774.6858677611749044, -225.7255117493289163, 315.5713283507209894 ) ) ;
#18415=CARTESIAN_POINT ( 'NONE',  ( 799.2566176426618085, -0.009063572426172561425, 324.0069404352559559 ) ) ;
#18419=CARTESIAN_POINT ( 'NONE',  ( 773.7943932421234194, -47.80559628986931386, 305.5313806188329409 ) ) ;
#18422=CARTESIAN_POINT ( 'NONE',  ( 797.8594530101008786, -37.54369356751132614, 322.1405469898980982 ) ) ;
#18425=CARTESIAN_POINT ( 'NONE',  ( 752.4576283171824116, -357.0783235625956422, 317.7880784355627952 ) ) ;
#18426=CARTESIAN_POINT ( 'NONE',  ( 757.8323909638828582, -146.6346026584200786, 352.1044303154654358 ) ) ;
#18429=CARTESIAN_POINT ( 'NONE',  ( 765.0180583372156207, -336.9982390220558273, 360.0135310231089534 ) ) ;
#18437=CARTESIAN_POINT ( 'NONE',  ( 756.3353852180819104, -53.90732993114765037, 331.1735550268788302 ) ) ;
#18438=CARTESIAN_POINT ( 'NONE',  ( 804.1105419155481968, -387.8272453906067767, 347.6308680596136469 ) ) ;
#18440=CARTESIAN_POINT ( 'NONE',  ( 810.7187646348534145, -378.4527844766011526, 356.7737145352016341 ) ) ;
#18441=CARTESIAN_POINT ( 'NONE',  ( 761.9338519418445230, -302.5328690171411949, 370.4231160770881957 ) ) ;
#18442=CARTESIAN_POINT ( 'NONE',  ( 764.3348316497523456, -70.71468719896014932, 308.6759233522265617 ) ) ;
#18449=CARTESIAN_POINT ( 'NONE',  ( 796.7737145352015204, -428.6346026584192259, 370.7187646348536987 ) ) ;
#18454=DIRECTION ( 'NONE',  ( -1.000000000000000000, -0.000000000000000000, -0.000000000000000000 ) ) ;
#18455=EDGE_CURVE ( 'NONE', #6, #16721, #35016, .T. ) ;
#18456=CARTESIAN_POINT ( 'NONE',  ( 766.9102291470427417, -258.5545181178799226, 318.6633372737382501 ) ) ;
#18457=CARTESIAN_POINT ( 'NONE',  ( 756.3353852180819104, -149.9073299311473875, 331.1735550268788302 ) ) ;
#18459=CARTESIAN_POINT ( 'NONE',  ( 789.9200121543843807, -313.9874144716866908, 317.0176451133914384 ) ) ;
#18461=CARTESIAN_POINT ( 'NONE',  ( 773.7305795820266212, -57.28179084515326736, 374.8230680027170365 ) ) ;
#18464=CARTESIAN_POINT ( 'NONE',  ( 755.2512626584698410, -199.5436935675108430, 315.2512626584710915 ) ) ;
#18465=CARTESIAN_POINT ( 'NONE',  ( 785.3687786644884454, -107.3618753856928976, 315.3201227861279676 ) ) ;
#18468=CARTESIAN_POINT ( 'NONE',  ( 794.5607502887775127, -462.9631818684622999, 371.8524697363486666 ) ) ;
#18471=CARTESIAN_POINT ( 'NONE',  ( 755.8398074228967971, -403.4419599262317888, 333.4516893846970333 ) ) ;
#18475=CARTESIAN_POINT ( 'NONE',  ( 760.5453621957607311, -69.07832356259653750, 323.8424801807151425 ) ) ;
#18480=CARTESIAN_POINT ( 'NONE',  ( 776.2433038121456548, -204.8965053807779100, 374.8207195650711014 ) ) ;
#18481=CARTESIAN_POINT ( 'NONE',  ( 759.9864689768902508, -50.08914811296584446, 354.9819416627836404 ) ) ;
#18485=CARTESIAN_POINT ( 'NONE',  ( 800.2193346964447755, -234.9982390220561683, 355.1360043628815788 ) ) ;
#18487=CARTESIAN_POINT ( 'NONE',  ( 800.0135310231082713, -350.0891481129648923, 325.0180583372163028 ) ) ;
#18492=CARTESIAN_POINT ( 'NONE',  ( 812.7932403749906598, -279.1800572038741848, 327.7687537140311633 ) ) ;
#18493=CARTESIAN_POINT ( 'NONE',  ( 781.2497674668890113, -12.35105083532396897, 375.3608509340180603 ) ) ;
#18499=CARTESIAN_POINT ( 'NONE',  ( 777.5031285880264704, -286.8164208402378677, 374.9108240113588408 ) ) ;
#18502=CARTESIAN_POINT ( 'NONE',  ( 804.4086373105744769, -217.6454272087891582, 333.3843516231986541 ) ) ;
#18505=CARTESIAN_POINT ( 'NONE',  ( 801.5560724626406000, -144.5545181178802636, 326.7756240680316182 ) ) ;
#18506=CARTESIAN_POINT ( 'NONE',  ( 759.9864689768902508, -50.08914811296584446, 354.9819416627836404 ) ) ;
#18509=CARTESIAN_POINT ( 'NONE',  ( 805.6418435158337843, -269.4636090269708006, 363.8556311672236916 ) ) ;
#18510=CARTESIAN_POINT ( 'NONE',  ( 800.7704444035546203, -220.1692326535051052, 326.0291762391768771 ) ) ;
#18513=CARTESIAN_POINT ( 'NONE',  ( 754.8072714833581358, -4.816420840238714085, 338.1981804954720587 ) ) ;
#18517=CARTESIAN_POINT ( 'NONE',  ( 782.4968714119720516, -34.81642084023861372, 305.0891759886411023 ) ) ;
#18518=CARTESIAN_POINT ( 'NONE',  ( 747.2067596250078623, -99.18005720387478164, 352.2312462859687230 ) ) ;
#18519=CYLINDRICAL_SURFACE ( 'NONE', #18825, 10.00000000000000888 ) ;
#18521=CARTESIAN_POINT ( 'NONE',  ( 754.3581564841646241, -377.4636090269704596, 316.1443688327762516 ) ) ;
#18523=CARTESIAN_POINT ( 'NONE',  ( 777.5031285880264704, -310.8164208402377540, 374.9108240113588408 ) ) ;
#18526=CARTESIAN_POINT ( 'NONE',  ( 778.1981804954714335, -442.2709662947826814, 314.8072714833589885 ) ) ;
#18527=CARTESIAN_POINT ( 'NONE',  ( 775.8780910478218402, -201.2817908451528126, 364.9511171171680530 ) ) ;
#18530=CARTESIAN_POINT ( 'NONE',  ( 756.1443688327750579, -117.6237781080509279, 314.3581564841659315 ) ) ;
#18531=CARTESIAN_POINT ( 'NONE',  ( 765.0180583372156207, -432.9982390220555999, 360.0135310231089534 ) ) ;
#18533=CARTESIAN_POINT ( 'NONE',  ( 776.2433038121456548, -156.8965053807780805, 374.8207195650711014 ) ) ;
#18539=CARTESIAN_POINT ( 'NONE',  ( 788.8264449731200330, -261.1800572038741848, 363.6646147819171233 ) ) ;
#18540=CARTESIAN_POINT ( 'NONE',  ( 794.9819416627830151, -276.9982390220559978, 319.9864689768909898 ) ) ;
#18544=CARTESIAN_POINT ( 'NONE',  ( 804.9363028652555840, -424.2709662947829088, 338.2165204200192079 ) ) ;
#18546=CARTESIAN_POINT ( 'NONE',  ( 751.6929314249750860, -198.9982390220562536, 318.8095938919659034 ) ) ;
#18547=CARTESIAN_POINT ( 'NONE',  ( 775.8780910478218402, -273.2817908451526137, 364.9511171171680530 ) ) ;
#18550=CARTESIAN_POINT ( 'NONE',  ( 807.5423716828161105, -201.0783235625961254, 362.2119215644372048 ) ) ;
#18556=CARTESIAN_POINT ( 'NONE',  ( 779.4709603349208464, -264.3510508353232353, 314.7162404726379918 ) ) ;
#18564=CARTESIAN_POINT ( 'NONE',  ( 746.4236121716829757, -159.8272453906075157, 328.8385539511384650 ) ) ;
#18569=CARTESIAN_POINT ( 'NONE',  ( 745.0891759886404770, -28.27096629478409540, 342.4968714119734159 ) ) ;
#18575=CARTESIAN_POINT ( 'NONE',  ( 767.8955696845333705, -24.45278447660229304, 362.1676090361162323 ) ) ;
#18576=CARTESIAN_POINT ( 'NONE',  ( 812.3518521366052028, -289.0999726633343698, 326.5853460496235243 ) ) ;
#18578=CARTESIAN_POINT ( 'NONE',  ( 759.0252816721024374, -240.9982390220561683, 368.0189434323527280 ) ) ;
#18582=CARTESIAN_POINT ( 'NONE',  ( 797.6776695296629214, -331.5436935675104451, 357.6776695296636603 ) ) ;
#18583=CARTESIAN_POINT ( 'NONE',  ( 800.9840315886518738, -100.9181544815167513, 354.1144889064786412 ) ) ;
#18587=CARTESIAN_POINT ( 'NONE',  ( 802.7791456095903868, -148.7146871989598935, 329.0155153010375102 ) ) ;
#18588=CARTESIAN_POINT ( 'NONE',  ( 804.4286716492782716, -353.3618753856922012, 345.3141322388244703 ) ) ;
#18591=CARTESIAN_POINT ( 'NONE',  ( 803.4237431249931660, -159.1800572038746111, 331.2633955100225194 ) ) ;
#18594=CARTESIAN_POINT ( 'NONE',  ( 812.6845335610512393, -439.9874144716862929, 353.5525998758768651 ) ) ;
#18596=CARTESIAN_POINT ( 'NONE',  ( 785.3687786644884454, -323.3618753856923149, 315.3201227861279676 ) ) ;
#18598=CARTESIAN_POINT ( 'NONE',  ( 785.3687786644884454, -443.3618753856917465, 315.3201227861279676 ) ) ;
#18605=CARTESIAN_POINT ( 'NONE',  ( 788.7366044899766848, 12.09267006885214180, 316.5762568750059813 ) ) ;
#18606=CARTESIAN_POINT ( 'NONE',  ( 801.1904061080336987, -236.0891481129651766, 368.3070685750235498 ) ) ;
#18607=CARTESIAN_POINT ( 'NONE',  ( 796.7845633553578182, -177.6237781080507148, 358.5707757039688204 ) ) ;
#18614=CARTESIAN_POINT ( 'NONE',  ( 749.5768839229115201, -60.55451811788051941, 358.0661480581553064 ) ) ;
#18618=DIRECTION ( 'NONE',  ( 0.000000000000000000, -1.000000000000000000, 0.000000000000000000 ) ) ;
#18622=CARTESIAN_POINT ( 'NONE',  ( 801.5560724626406000, -384.5545181178795247, 326.7756240680316182 ) ) ;
#18627=CARTESIAN_POINT ( 'NONE',  ( 755.8990559732751535, -179.4636090269710849, 365.9055244015606831 ) ) ;
#18629=CARTESIAN_POINT ( 'NONE',  ( 804.7487373415286811, -115.5436935675110988, 364.7487373415288516 ) ) ;
#18633=CARTESIAN_POINT ( 'NONE',  ( 800.0135310231082713, -230.0891481129652618, 325.0180583372163028 ) ) ;
#18635=CARTESIAN_POINT ( 'NONE',  ( 802.2119215644370342, -462.0090635724247932, 367.5423716828165084 ) ) ;
#18639=CARTESIAN_POINT ( 'NONE',  ( 766.5853460496234675, -13.98741447168760033, 372.3518521366060554 ) ) ;
#18641=CARTESIAN_POINT ( 'NONE',  ( 797.6776695296629214, -19.54369356751139364, 357.6776695296636603 ) ) ;
#18643=CARTESIAN_POINT ( 'NONE',  ( 805.9055244015594326, -339.6237781080502600, 315.8990559732753240 ) ) ;
#18644=CARTESIAN_POINT ( 'NONE',  ( 791.9812246680005501, -164.6346026584200217, 361.9419747391813189 ) ) ;
#18646=CARTESIAN_POINT ( 'NONE',  ( 746.0683387631852383, -427.4419599262317888, 331.3260364891676204 ) ) ;
#18648=CARTESIAN_POINT ( 'NONE',  ( 757.8323909638827445, -338.6346026584195101, 352.1044303154654358 ) ) ;
#18655=CARTESIAN_POINT ( 'NONE',  ( 805.1927285166397041, -64.81642084023852135, 341.8018195045277707 ) ) ;
#18656=CARTESIAN_POINT ( 'NONE',  ( 780.5236548040995785, -380.7363362996977116, 314.9735926884559944 ) ) ;
#18658=CARTESIAN_POINT ( 'NONE',  ( 754.9967657858570647, -385.5436935675102745, 365.0032342141425943 ) ) ;
#18659=CARTESIAN_POINT ( 'NONE',  ( 798.0661480581538854, -290.5328690171412518, 309.5768839229118043 ) ) ;
#18667=CARTESIAN_POINT ( 'NONE',  ( 777.4774526936600978, -418.2709662947827383, 304.7301800767027657 ) ) ;
#18673=CARTESIAN_POINT ( 'NONE',  ( 775.8780910478218402, -297.2817908451526137, 364.9511171171680530 ) ) ;
#18674=CARTESIAN_POINT ( 'NONE',  ( 778.1981804954714335, -154.2709662947836478, 314.8072714833589885 ) ) ;
#18677=CARTESIAN_POINT ( 'NONE',  ( 772.3691319403857278, -335.2601417444137724, 315.8894580844506663 ) ) ;
#18679=CARTESIAN_POINT ( 'NONE',  ( 778.7629533639073998, -80.73633629969864955, 375.0009284576466371 ) ) ;
#18682=CARTESIAN_POINT ( 'NONE',  ( 755.3201227861273992, -99.72551174932928575, 345.3687786644892981 ) ) ;
#18687=CARTESIAN_POINT ( 'NONE',  ( 804.8461984189677878, -26.19088175424427334, 336.9566956441385628 ) ) ;
#18690=CARTESIAN_POINT ( 'NONE',  ( 783.0433043558608688, -408.8965053807772847, 315.1538015810313027 ) ) ;
#18695=CARTESIAN_POINT ( 'NONE',  ( 746.0683387631852383, -235.4419599262323857, 331.3260364891676204 ) ) ;
#18696=CARTESIAN_POINT ( 'NONE',  ( 756.5762568750052424, -51.18005720387493085, 348.7366044899774238 ) ) ;
#18699=CARTESIAN_POINT ( 'NONE',  ( 802.1676090361156639, -230.6346026584197659, 327.8955696845344505 ) ) ;
#18703=CARTESIAN_POINT ( 'NONE',  ( 760.5453621957607311, -69.07832356259653750, 323.8424801807151425 ) ) ;
#18705=EDGE_CURVE ( 'NONE', #23565, #29447, #25450, .T. ) ;
#18706=CARTESIAN_POINT ( 'NONE',  ( 810.7187646348534145, -282.4527844766014937, 356.7737145352016341 ) ) ;
#18707=CARTESIAN_POINT ( 'NONE',  ( 768.8385539511368734, -23.26014174441484883, 306.4236121716840557 ) ) ;
#18717=CARTESIAN_POINT ( 'NONE',  ( 808.3070685750230950, -306.9982390220558273, 361.1904061080339261 ) ) ;
#18719=CARTESIAN_POINT ( 'NONE',  ( 802.5472867521000353, -220.3726999360618208, 350.8726784830461156 ) ) ;
#18720=CARTESIAN_POINT ( 'NONE',  ( 804.9511171171677688, -365.8055962898682765, 335.8780910478229202 ) ) ;
#18722=CARTESIAN_POINT ( 'NONE',  ( 769.0155153010367712, -178.3726999360619629, 362.7791456095907279 ) ) ;
#18723=CARTESIAN_POINT ( 'NONE',  ( 804.9363028652555840, -64.27096629478397460, 338.2165204200192079 ) ) ;
#18727=CARTESIAN_POINT ( 'NONE',  ( 744.6391490659812007, -254.7363362996981095, 338.7502325331110455 ) ) ;
#18728=CARTESIAN_POINT ( 'NONE',  ( 766.7756240680305382, -206.5328690171415360, 361.5560724626415663 ) ) ;
#18733=CARTESIAN_POINT ( 'NONE',  ( 768.0187753319979720, 15.36539734157940629, 318.0580252608186242 ) ) ;
#18736=CARTESIAN_POINT ( 'NONE',  ( 772.5602148656447525, -57.72551174932945628, 305.7998596910095443 ) ) ;
#18737=CARTESIAN_POINT ( 'NONE',  ( 772.5602148656447525, -105.7255117493293000, 305.7998596910095443 ) ) ;
#18740=CARTESIAN_POINT ( 'NONE',  ( 748.6759233522253680, -400.3726999360612808, 324.3348316497537098 ) ) ;
#18742=CARTESIAN_POINT ( 'NONE',  ( 810.7187646348534145, -378.4527844766011526, 356.7737145352016341 ) ) ;
#18744=CARTESIAN_POINT ( 'NONE',  ( 788.8264449731200330, -429.1800572038737869, 363.6646147819171233 ) ) ;
#18747=CARTESIAN_POINT ( 'NONE',  ( 766.0291762391763086, -178.9181544815165239, 360.7704444035551319 ) ) ;
#18750=CARTESIAN_POINT ( 'NONE',  ( 813.9316612368132837, -127.4419599262326983, 348.6739635108323228 ) ) ;
#18751=CARTESIAN_POINT ( 'NONE',  ( 792.1044303154646968, -444.4527844766009821, 317.8323909638837677 ) ) ;
#18758=CARTESIAN_POINT ( 'NONE',  ( 788.7366044899766848, -251.9073299311470748, 316.5762568750059813 ) ) ;
#18759=CARTESIAN_POINT ( 'NONE',  ( 755.0636971347428243, -244.2709662947834204, 341.7834795799807353 ) ) ;
#18762=CARTESIAN_POINT ( 'NONE',  ( 801.9419747391806368, -450.4527844766009821, 351.9812246680014027 ) ) ;
#18768=CARTESIAN_POINT ( 'NONE',  ( 814.9108240113580450, -184.2709662947835909, 337.5031285880265273 ) ) ;
#18769=CARTESIAN_POINT ( 'NONE',  ( 802.9823548866075953, -265.0999726633344267, 330.0799878456151077 ) ) ;
#18772=CARTESIAN_POINT ( 'NONE',  ( 751.2241431872005251, -208.1692326535051905, 359.9636004259367610 ) ) ;
#18777=CARTESIAN_POINT ( 'NONE',  ( 775.9200461376533440, -263.8055962898686175, 315.3028492785443291 ) ) ;
#18781=PLANE ( 'NONE',  #5576 ) ;
#18782=EDGE_LOOP ( 'NONE', ( #16333, #39535 ) ) ;
#18784=AXIS2_PLACEMENT_3D ( 'NONE', #9300, #33995, #12748 ) ;
#18786=CARTESIAN_POINT ( 'NONE',  ( 791.0478386215596629, -165.8272453906074873, 306.7653713866226326 ) ) ;
#18792=CARTESIAN_POINT ( 'NONE',  ( 782.4968714119720516, -10.81642084023869543, 305.0891759886411023 ) ) ;
#18797=CARTESIAN_POINT ( 'NONE',  ( 802.1676090361156639, -62.63460265842031305, 327.8955696845344505 ) ) ;
#18799=CARTESIAN_POINT ( 'NONE',  ( 802.2119215644370342, -294.0090635724253048, 367.5423716828165084 ) ) ;
#18801=CARTESIAN_POINT ( 'NONE',  ( 812.7932403749906598, -255.1800572038742700, 327.7687537140311633 ) ) ;
#18804=AXIS2_PLACEMENT_3D ( 'NONE', #35654, #7040, #38682 ) ;
#18806=CARTESIAN_POINT ( 'NONE',  ( 804.4286716492782716, -329.3618753856922581, 345.3141322388244703 ) ) ;
#18808=CARTESIAN_POINT ( 'NONE',  ( 784.1219089521767955, -93.28179084515315367, 315.0488828828318333 ) ) ;
#18811=EDGE_CURVE ( 'NONE', #15704, #32527, #15814, .T. ) ;
#18813=CARTESIAN_POINT ( 'NONE',  ( 787.6308680596127942, -155.2601417444144261, 364.1105419155492768 ) ) ;
#18814=CARTESIAN_POINT ( 'NONE',  ( 771.2633955100217236, -383.9073299311466485, 363.4237431249939618 ) ) ;
#18818=CARTESIAN_POINT ( 'NONE',  ( 804.4286716492782716, -161.3618753856927697, 345.3141322388244703 ) ) ;
#18822=CARTESIAN_POINT ( 'NONE',  ( 772.5602148656447525, 14.27448825067031812, 305.7998596910095443 ) ) ;
#18824=CARTESIAN_POINT ( 'NONE',  ( 802.1676090361156639, -350.6346026584192828, 327.8955696845344505 ) ) ;
#18825=AXIS2_PLACEMENT_3D ( 'NONE', #942, #29371, #28441 ) ;
#18828=CARTESIAN_POINT ( 'NONE',  ( 804.9363028652555840, -448.2709662947827951, 338.2165204200192079 ) ) ;
#18834=CIRCLE ( 'NONE', #3368, 10.00000000000000888 ) ;
#18835=CARTESIAN_POINT ( 'NONE',  ( 802.5472867521000353, -460.3726999360611103, 350.8726784830461156 ) ) ;
#18836=CARTESIAN_POINT ( 'NONE',  ( 795.9930595647434757, -147.0783235625962959, 320.7433823573372820 ) ) ;
#18839=CARTESIAN_POINT ( 'NONE',  ( 812.6845335610512393, -415.9874144716862361, 353.5525998758768651 ) ) ;
#18841=VECTOR ( 'NONE', #31210, 1000.000000000000000 ) ;
#18846=CARTESIAN_POINT ( 'NONE',  ( 812.3518521366052028, -73.09997266333502353, 326.5853460496235243 ) ) ;
#18854=CARTESIAN_POINT ( 'NONE',  ( 757.0176451133909268, -397.0999726633340288, 349.9200121543848354 ) ) ;
#18859=AXIS2_PLACEMENT_3D ( 'NONE', #31315, #20473, #9844 ) ;
#18860=CARTESIAN_POINT ( 'NONE',  ( 815.3608509340175488, -170.7363362996983938, 341.2497674668889545 ) ) ;
#18862=CARTESIAN_POINT ( 'NONE',  ( 777.5031285880264704, -118.8164208402383508, 374.9108240113588408 ) ) ;
#18866=CARTESIAN_POINT ( 'NONE',  ( 795.1360043628807261, -236.0891481129651766, 360.2193346964456282 ) ) ;
#18867=CARTESIAN_POINT ( 'NONE',  ( 757.0176451133909268, -37.09997266333514432, 349.9200121543848354 ) ) ;
#18872=CARTESIAN_POINT ( 'NONE',  ( 761.9338519418445230, -38.53286901714206891, 370.4231160770881957 ) ) ;
#18876=CARTESIAN_POINT ( 'NONE',  ( 801.9419747391806368, -18.45278447660230725, 351.9812246680014027 ) ) ;
#18879=CARTESIAN_POINT ( 'NONE',  ( 773.7943932421234194, -359.8055962898683333, 305.5313806188329409 ) ) ;
#18881=CARTESIAN_POINT ( 'NONE',  ( 807.5423716828161105, -417.0783235625954148, 362.2119215644372048 ) ) ;
#18882=CARTESIAN_POINT ( 'NONE',  ( 800.2193346964447755, -354.9982390220557704, 355.1360043628815788 ) ) ;
#18890=CARTESIAN_POINT ( 'NONE',  ( 756.5762568750052424, -51.18005720387493085, 348.7366044899774238 ) ) ;
#18891=CARTESIAN_POINT ( 'NONE',  ( 775.8780910478218402, -369.2817908451523294, 364.9511171171680530 ) ) ;
#18894=CARTESIAN_POINT ( 'NONE',  ( 759.0252816721024374, -408.9982390220556567, 368.0189434323527280 ) ) ;
#18895=CARTESIAN_POINT ( 'NONE',  ( 768.8385539511368734, -335.2601417444137724, 306.4236121716840557 ) ) ;
#18901=CARTESIAN_POINT ( 'NONE',  ( 804.7487373415286811, -427.5436935675101040, 364.7487373415288516 ) ) ;
#18910=CARTESIAN_POINT ( 'NONE',  ( 755.8894580844503253, -279.8272453906071746, 332.3691319403863531 ) ) ;
#18911=CARTESIAN_POINT ( 'NONE',  ( 762.3223304703356007, -151.5436935675109851, 322.3223304703362828 ) ) ;
#18914=CARTESIAN_POINT ( 'NONE',  ( 765.8855110935204493, -334.1692326535047073, 319.0159684113471599 ) ) ;
#18916=CARTESIAN_POINT ( 'NONE',  ( 746.4236121716829757, -63.82724539060779279, 328.8385539511384650 ) ) ;
#18918=CARTESIAN_POINT ( 'NONE',  ( 782.4968714119720516, -202.8164208402380950, 305.0891759886411023 ) ) ;
#18919=CARTESIAN_POINT ( 'NONE',  ( 794.9819416627830151, -108.9982390220565804, 319.9864689768909898 ) ) ;
#18923=CARTESIAN_POINT ( 'NONE',  ( 804.1105419155481968, -3.827245390607979303, 347.6308680596136469 ) ) ;
#18926=CARTESIAN_POINT ( 'NONE',  ( 805.1016975059191054, -390.8965053807772279, 343.0745993439771837 ) ) ;
#18933=CARTESIAN_POINT ( 'NONE',  ( 744.9990715423526808, -234.3510508353232638, 341.2370466360926002 ) ) ;
#18934=CARTESIAN_POINT ( 'NONE',  ( 794.9819416627830151, -60.99823902205671544, 319.9864689768909898 ) ) ;
#18936=CARTESIAN_POINT ( 'NONE',  ( 771.1735550268778070, -249.1800572038742416, 316.3353852180827630 ) ) ;
#18943=CARTESIAN_POINT ( 'NONE',  ( 792.2312462859673587, -275.9073299311469896, 307.2067596250082602 ) ) ;
#18944=CARTESIAN_POINT ( 'NONE',  ( 747.3154664389472828, -19.98741447168758256, 326.4474001241230781 ) ) ;
#18948=EDGE_LOOP ( 'NONE', ( #38962, #31483 ) ) ;
#18951=CARTESIAN_POINT ( 'NONE',  ( 815.2698199232961542, -328.8164208402375834, 342.5225473063383106 ) ) ;
#18952=CARTESIAN_POINT ( 'NONE',  ( 799.9999999999993179, -462.9681489794448339, 309.9999999999998863 ) ) ;
#18953=CIRCLE ( 'NONE', #10844, 30.00000000000008171 ) ;
#18955=CARTESIAN_POINT ( 'NONE',  ( 766.0291762391763086, -202.9181544815164386, 360.7704444035551319 ) ) ;
#18956=CARTESIAN_POINT ( 'NONE',  ( 759.7806653035534055, -54.99823902205672255, 324.8639956371180801 ) ) ;
#18957=VERTEX_POINT ( 'NONE', #26882 ) ;
#18961=CARTESIAN_POINT ( 'NONE',  ( 755.0488828828309806, -233.8055962898687028, 344.1219089521771934 ) ) ;
#18965=CARTESIAN_POINT ( 'NONE',  ( 812.7932403749906598, -447.1800572038736732, 327.7687537140311633 ) ) ;
#18970=CARTESIAN_POINT ( 'NONE',  ( 751.9810565676468741, -50.08914811296584446, 360.9747183278973921 ) ) ;
#18971=CARTESIAN_POINT ( 'NONE',  ( 772.4837098697144029, -119.3618753856928691, 374.5518280994205611 ) ) ;
#18975=CARTESIAN_POINT ( 'NONE',  ( 797.8822607201568644, -390.5545181178794678, 370.1134526219340160 ) ) ;
#18977=CARTESIAN_POINT ( 'NONE',  ( 767.6429770376289525, -345.1800572038739006, 306.8695393053162093 ) ) ;
#18980=CARTESIAN_POINT ( 'NONE',  ( 805.0264073115434940, 17.64894916467593688, 339.4763451958999099 ) ) ;
#18983=CARTESIAN_POINT ( 'NONE',  ( 810.1134526219336749, -128.5328690171417634, 357.8822607201570349 ) ) ;
#18984=CARTESIAN_POINT ( 'NONE',  ( 785.3687786644885591, -443.3618753856917465, 315.3201227861280813 ) ) ;
#18988=CARTESIAN_POINT ( 'NONE',  ( 755.3201227861273992, -123.7255117493292147, 345.3687786644892981 ) ) ;
#18990=CARTESIAN_POINT ( 'NONE',  ( 771.1735550268778070, -273.1800572038742985, 316.3353852180827630 ) ) ;
#18991=CARTESIAN_POINT ( 'NONE',  ( 758.0580252608178853, -246.4527844766016074, 328.0187753319985404 ) ) ;
#18994=CARTESIAN_POINT ( 'NONE',  ( 803.6646147819161570, -449.9073299311463643, 348.8264449731210561 ) ) ;
#18997=CARTESIAN_POINT ( 'NONE',  ( 751.9810565676468741, -170.0891481129654608, 360.9747183278973921 ) ) ;
#18998=CARTESIAN_POINT ( 'NONE',  ( 758.4439275373578084, -300.5545181178797520, 353.2243759319684386 ) ) ;
#18999=CARTESIAN_POINT ( 'NONE',  ( 801.3366627262608972, -416.5328690171409107, 353.0897708529566899 ) ) ;
#19006=CARTESIAN_POINT ( 'NONE',  ( 776.9566956441375396, -252.8965053807777394, 364.8461984189686405 ) ) ;
#19008=DIRECTION ( 'NONE',  ( 0.000000000000000000, 0.000000000000000000, 1.000000000000000000 ) ) ;
#19013=CARTESIAN_POINT ( 'NONE',  ( 799.9636004259356241, -166.9181544815165523, 311.2241431872006956 ) ) ;
#19024=CARTESIAN_POINT ( 'NONE',  ( 774.6312213355099630, -47.36187538569312494, 364.6798772138717482 ) ) ;
#19025=CARTESIAN_POINT ( 'NONE',  ( 752.7379699480933368, -300.0090635724252479, 361.9858362298580232 ) ) ;
#19027=CARTESIAN_POINT ( 'NONE',  ( 801.1904061080336987, -260.0891481129650060, 368.3070685750235498 ) ) ;
#19032=CARTESIAN_POINT ( 'NONE',  ( 791.9812246680005501, -356.6346026584193964, 361.9419747391813189 ) ) ;
#19033=CARTESIAN_POINT ( 'NONE',  ( 786.5483106153019435, -127.6454272087894140, 364.1601925771022366 ) ) ;
#19037=CARTESIAN_POINT ( 'NONE',  ( 785.3141322388236176, -405.7255117493283478, 364.4286716492789537 ) ) ;
#19040=CARTESIAN_POINT ( 'NONE',  ( 765.0180583372156207, -168.9982390220563673, 360.0135310231089534 ) ) ;
#19045=CARTESIAN_POINT ( 'NONE',  ( 774.6312213355099630, -359.3618753856920875, 364.6798772138717482 ) ) ;
#19048=CARTESIAN_POINT ( 'NONE',  ( 797.6776695296629214, -451.5436935675099903, 357.6776695296636603 ) ) ;
#19050=CARTESIAN_POINT ( 'NONE',  ( 777.4774526936600978, -82.27096629478390355, 304.7301800767028226 ) ) ;
#19056=CARTESIAN_POINT ( 'NONE',  ( 803.4237431249931660, 8.819942796124882634, 331.2633955100225194 ) ) ;
#19057=CARTESIAN_POINT ( 'NONE',  ( 755.2512626584698410, -223.5436935675107577, 315.2512626584710915 ) ) ;
#19058=CARTESIAN_POINT ( 'NONE',  ( 765.8855110935204493, -166.1692326535053041, 319.0159684113471599 ) ) ;
#19061=CARTESIAN_POINT ( 'NONE',  ( 801.9858362298568863, -411.0783235625954717, 312.7379699480935642 ) ) ;
#19066=CARTESIAN_POINT ( 'NONE',  ( 744.6391490659812007, -62.73633629969871350, 338.7502325331110455 ) ) ;
#19073=CARTESIAN_POINT ( 'NONE',  ( 799.9999999999993179, 205.0000000000000568, 319.9999999999999432 ) ) ;
#19076=CARTESIAN_POINT ( 'NONE',  ( 763.8424801807145741, -402.0090635724250205, 320.5453621957614700 ) ) ;
#19081=CARTESIAN_POINT ( 'NONE',  ( 766.4474001241216001, -187.0999726633346825, 307.3154664389482491 ) ) ;
#19083=CARTESIAN_POINT ( 'NONE',  ( 782.5225473063381969, -142.2709662947837330, 375.2698199232970637 ) ) ;
#19085=EDGE_CURVE ( 'NONE', #25624, #27436, #6956, .T. ) ;
#19088=FACE_OUTER_BOUND ( 'NONE', #40190, .T. ) ;
#19089=CARTESIAN_POINT ( 'NONE',  ( 785.3141322388236176, -237.7255117493289163, 364.4286716492789537 ) ) ;
#19090=CARTESIAN_POINT ( 'NONE',  ( 793.0897708529556667, -6.554518117880697048, 361.3366627262616362 ) ) ;
#19092=CIRCLE ( 'NONE', #44159, 10.00000000000000888 ) ;
#19095=CARTESIAN_POINT ( 'NONE',  ( 746.7653713866222915, -17.26014174441486659, 351.0478386215610271 ) ) ;
#19098=CARTESIAN_POINT ( 'NONE',  ( 781.8018195045266339, -22.27096629478410250, 365.1927285166406705 ) ) ;
#19101=CARTESIAN_POINT ( 'NONE',  ( 758.0141637701419768, -351.0783235625955854, 367.2620300519063790 ) ) ;
#19103=CARTESIAN_POINT ( 'NONE',  ( 758.0580252608178853, -270.4527844766014937, 328.0187753319985404 ) ) ;
#19104=CARTESIAN_POINT ( 'NONE',  ( 798.0661480581538854, -434.5328690171407970, 309.5768839229118043 ) ) ;
#19106=CARTESIAN_POINT ( 'NONE',  ( 781.7834795799800531, -322.8164208402377540, 315.0636971347436202 ) ) ;
#19113=CARTESIAN_POINT ( 'NONE',  ( 803.6646147819161570, -41.90732993114767169, 348.8264449731210561 ) ) ;
#19114=CARTESIAN_POINT ( 'NONE',  ( 804.6971507214547046, -363.2817908451523294, 344.0799538623459739 ) ) ;
#19115=CARTESIAN_POINT ( 'NONE',  ( 800.9747183278959710, -420.9982390220555999, 311.9810565676471583 ) ) ;
#19117=CARTESIAN_POINT ( 'NONE',  ( 815.0009284576459549, -318.3510508353230080, 338.7629533639073429 ) ) ;
#19118=CARTESIAN_POINT ( 'NONE',  ( 746.7653713866222915, -89.26014174441463922, 351.0478386215610271 ) ) ;
#19123=CARTESIAN_POINT ( 'NONE',  ( 782.5225473063381969, -430.2709662947827383, 375.2698199232970637 ) ) ;
#19124=FACE_OUTER_BOUND ( 'NONE', #26747, .T. ) ;
#19130=CARTESIAN_POINT ( 'NONE',  ( 802.9823548866075953, -289.0999726633343698, 330.0799878456151077 ) ) ;
#19134=CARTESIAN_POINT ( 'NONE',  ( 745.5313806188320314, -87.28179084515316788, 333.7943932421247268 ) ) ;
#19137=CARTESIAN_POINT ( 'NONE',  ( 754.8072714833581358, -100.8164208402383792, 338.1981804954720587 ) ) ;
#19141=CARTESIAN_POINT ( 'NONE',  ( 798.5707757039680246, -5.463609026971610660, 356.7845633553585003 ) ) ;
#19144=CARTESIAN_POINT ( 'NONE',  ( 804.9511171171677688, -389.8055962898682765, 335.8780910478229202 ) ) ;
#19146=CARTESIAN_POINT ( 'NONE',  ( 795.9930595647434757, -75.07832356259649487, 320.7433823573372820 ) ) ;
#19149=CARTESIAN_POINT ( 'NONE',  ( 771.2368401574024119, -229.4419599262323572, 374.2805881961240857 ) ) ;
#19150=CARTESIAN_POINT ( 'NONE',  ( 771.2633955100217236, -47.90732993114767169, 363.4237431249939618 ) ) ;
#19151=AXIS2_PLACEMENT_3D ( 'NONE', #41435, #16728, #17415 ) ;
#19153=CARTESIAN_POINT ( 'NONE',  ( 756.5762568750052424, -219.1800572038744122, 348.7366044899774238 ) ) ;
#19161=CARTESIAN_POINT ( 'NONE',  ( 777.4774526936600978, -322.2709662947830793, 304.7301800767028226 ) ) ;
#19162=CARTESIAN_POINT ( 'NONE',  ( 771.2368401574024119, -37.44195992623299674, 374.2805881961240857 ) ) ;
#19167=CARTESIAN_POINT ( 'NONE',  ( 781.7834795799800531, -226.8164208402380098, 315.0636971347436202 ) ) ;
#19170=CARTESIAN_POINT ( 'NONE',  ( 782.5225473063381969, -334.2709662947829656, 375.2698199232970637 ) ) ;
#19174=CARTESIAN_POINT ( 'NONE',  ( 757.4527132478984868, -208.3726999360619061, 329.1273215169538844 ) ) ;
#19175=CARTESIAN_POINT ( 'NONE',  ( 785.3141322388236176, -93.72551174932934259, 364.4286716492789537 ) ) ;
#19179=CARTESIAN_POINT ( 'NONE',  ( 754.9735926884551418, -234.3510508353232638, 340.5236548041000333 ) ) ;
#19185=CARTESIAN_POINT ( 'NONE',  ( 808.0189434323515343, -38.08914811296587999, 319.0252816721025511 ) ) ;
#19186=CARTESIAN_POINT ( 'NONE',  ( 805.0032342141412300, -133.5436935675110135, 314.9967657858571783 ) ) ;
#19190=CARTESIAN_POINT ( 'NONE',  ( 814.5518280994195948, -351.7255117493284047, 332.4837098697145734 ) ) ;
#19192=CARTESIAN_POINT ( 'NONE',  ( 804.4286716492782716, -449.3618753856918602, 345.3141322388244703 ) ) ;
#19195=CARTESIAN_POINT ( 'NONE',  ( 761.9338519418445230, -134.5328690171417350, 370.4231160770881957 ) ) ;
#19196=CARTESIAN_POINT ( 'NONE',  ( 804.6798772138710092, -447.7255117493281205, 334.6312213355106451 ) ) ;
#19200=CARTESIAN_POINT ( 'NONE',  ( 771.2633955100217236, -119.9073299311474443, 363.4237431249939618 ) ) ;
#19202=CARTESIAN_POINT ( 'NONE',  ( 755.5713283507202505, -269.3618753856924286, 334.6858677611754729 ) ) ;
#19203=CARTESIAN_POINT ( 'NONE',  ( 801.9419747391806368, -258.4527844766016074, 351.9812246680014027 ) ) ;
#19206=CARTESIAN_POINT ( 'NONE',  ( 779.4709603349208464, 23.64894916467591912, 314.7162404726379918 ) ) ;
#19210=CARTESIAN_POINT ( 'NONE',  ( 754.9967657858570647, -169.5436935675108998, 365.0032342141425943 ) ) ;
#19211=CARTESIAN_POINT ( 'NONE',  ( 799.2566176426618085, -288.0090635724252479, 324.0069404352559559 ) ) ;
#19212=CARTESIAN_POINT ( 'NONE',  ( 805.0264073115434940, -390.3510508353227237, 339.4763451958999099 ) ) ;
#19219=CARTESIAN_POINT ( 'NONE',  ( 773.3843516231979720, -277.4419599262322436, 364.4086373105754433 ) ) ;
#19226=CARTESIAN_POINT ( 'NONE',  ( 815.3608509340175488, -194.7363362996982517, 341.2497674668889545 ) ) ;
#19227=CARTESIAN_POINT ( 'NONE',  ( 799.9999999999993179, 205.0000000000000568, 350.0000000000000000 ) ) ;
#19231=CARTESIAN_POINT ( 'NONE',  ( 812.7932403749906598, -15.18005720387504631, 327.7687537140311633 ) ) ;
#19234=CARTESIAN_POINT ( 'NONE',  ( 767.9999999999992042, 205.0000000000000568, 339.9999999999999432 ) ) ;
#19235=CARTESIAN_POINT ( 'NONE',  ( 754.8072714833581358, -52.81642084023856398, 338.1981804954720587 ) ) ;
#19236=CARTESIAN_POINT ( 'NONE',  ( 749.5768839229115201, -300.5545181178797520, 358.0661480581553064 ) ) ;
#19237=CARTESIAN_POINT ( 'NONE',  ( 745.7998596910086917, -245.3618753856925139, 332.5602148656461168 ) ) ;
#19239=FACE_OUTER_BOUND ( 'NONE', #20391, .T. ) ;
#19241=CARTESIAN_POINT ( 'NONE',  ( 781.7834795799800531, -346.8164208402376971, 315.0636971347436202 ) ) ;
#19242=CARTESIAN_POINT ( 'NONE',  ( 758.4439275373578084, -108.5545181178803915, 353.2243759319684386 ) ) ;
#19246=CARTESIAN_POINT ( 'NONE',  ( 805.9055244015594326, -123.6237781080508569, 315.8990559732753240 ) ) ;
#19247=CARTESIAN_POINT ( 'NONE',  ( 768.0187753319979720, -392.6346026584193396, 318.0580252608186242 ) ) ;
#19250=CARTESIAN_POINT ( 'NONE',  ( 788.8264449731200330, -141.1800572038746395, 363.6646147819171233 ) ) ;
#19252=CARTESIAN_POINT ( 'NONE',  ( 792.0613484971601110, -458.0032201311295807, 367.4685979341032294 ) ) ;
#19254=CARTESIAN_POINT ( 'NONE',  ( 800.2193346964447755, -354.9982390220557704, 355.1360043628815788 ) ) ;
#19257=EDGE_CURVE ( 'NONE', #10891, #32443, #13665, .T. ) ;
#19259=CARTESIAN_POINT ( 'NONE',  ( 754.9967657858570647, -73.54369356751121245, 365.0032342141425943 ) ) ;
#19264=CARTESIAN_POINT ( 'NONE',  ( 782.5225473063381969, -262.2709662947831930, 375.2698199232970637 ) ) ;
#19265=CARTESIAN_POINT ( 'NONE',  ( 790.8726784830453198, -154.7146871989598935, 362.5472867521010585 ) ) ;
#19274=CARTESIAN_POINT ( 'NONE',  ( 757.7880784355613741, -66.00906357242595845, 312.4576283171834916 ) ) ;
#19283=CARTESIAN_POINT ( 'NONE',  ( 784.1219089521767955, -405.2817908451522158, 315.0488828828318333 ) ) ;
#19284=CARTESIAN_POINT ( 'NONE',  ( 776.2046728542105711, -356.1908817542432075, 304.8212110874238761 ) ) ;
#19286=CARTESIAN_POINT ( 'NONE',  ( 759.0159684113467620, -232.9181544815163249, 325.8855110935213020 ) ) ;
#19287=LINE ( 'NONE', #33373, #30530 ) ;
#19288=CARTESIAN_POINT ( 'NONE',  ( 799.9999999999993179, 205.0000000000000568, 339.9999999999999432 ) ) ;
#19290=CARTESIAN_POINT ( 'NONE',  ( 814.4686193811664907, -195.2817908451528410, 346.2056067578752732 ) ) ;
#19293=CARTESIAN_POINT ( 'NONE',  ( 749.2812353651451076, -150.4527844766018916, 323.2262854647983090 ) ) ;
#19297=CARTESIAN_POINT ( 'NONE',  ( 756.5762568750052424, -243.1800572038743269, 348.7366044899774238 ) ) ;
#19298=CARTESIAN_POINT ( 'NONE',  ( 758.4439275373578084, -36.55451811788061178, 353.2243759319684386 ) ) ;
#19303=CARTESIAN_POINT ( 'NONE',  ( 756.1348686366196716, -89.26014174441463922, 347.5531968255698416 ) ) ;
#19304=CARTESIAN_POINT ( 'NONE',  ( 803.6646147819161570, -305.9073299311467622, 348.8264449731210561 ) ) ;
#19307=CARTESIAN_POINT ( 'NONE',  ( 756.5762568750052424, -51.18005720387493085, 348.7366044899774238 ) ) ;
#19311=CARTESIAN_POINT ( 'NONE',  ( 759.8311093483677041, -358.1692326535047641, 310.9282345327691814 ) ) ;
#19313=CARTESIAN_POINT ( 'NONE',  ( 805.9055244015594326, -435.6237781080499190, 315.8990559732753240 ) ) ;
#19316=CARTESIAN_POINT ( 'NONE',  ( 805.1927285166397041, -328.8164208402375834, 341.8018195045277707 ) ) ;
#19323=CARTESIAN_POINT ( 'NONE',  ( 792.1044303154645831, -108.4527844766019911, 317.8323909638837677 ) ) ;
#19324=CARTESIAN_POINT ( 'NONE',  ( 793.9708237608222134, -358.9181544815160123, 319.2295555964448681 ) ) ;
#19326=CARTESIAN_POINT ( 'NONE',  ( 745.7998596910086917, -413.3618753856920307, 332.5602148656461168 ) ) ;
#19328=CARTESIAN_POINT ( 'NONE',  ( 791.1614460488616487, -323.2601417444138860, 373.5763878283158874 ) ) ;
#19329=ADVANCED_FACE ( 'NONE', ( #23026, #12645 ), #37119, .T. ) ;
#19330=CARTESIAN_POINT ( 'NONE',  ( 776.2433038121456548, -108.8965053807782084, 374.8207195650711014 ) ) ;
#19334=CARTESIAN_POINT ( 'NONE',  ( 805.0032342141412300, -421.5436935675101040, 314.9967657858571783 ) ) ;
#19340=CARTESIAN_POINT ( 'NONE',  ( 804.8461984189677878, -290.1908817542434349, 336.9566956441385628 ) ) ;
#19345=DIRECTION ( 'NONE',  ( -1.000000000000000000, -0.000000000000000000, 0.000000000000000000 ) ) ;
#19346=CARTESIAN_POINT ( 'NONE',  ( 804.1009440267234822, -71.46360902697141171, 314.0944755984392600 ) ) ;
#19350=CARTESIAN_POINT ( 'NONE',  ( 778.2165204200184689, -142.8164208402382656, 364.9363028652563230 ) ) ;
#19354=CARTESIAN_POINT ( 'NONE',  ( 790.9844846989617508, -22.37269993606246743, 317.2208543904092721 ) ) ;
#19356=CARTESIAN_POINT ( 'NONE',  ( 791.7608162188021197, 240.0000000000000853, 320.0000000000000000 ) ) ;
#19357=CARTESIAN_POINT ( 'NONE',  ( 796.7845633553578182, -393.6237781080500326, 358.5707757039688204 ) ) ;
#19359=CARTESIAN_POINT ( 'NONE',  ( 800.7704444035546203, -76.16923265350557415, 326.0291762391768771 ) ) ;
#19364=CARTESIAN_POINT ( 'NONE',  ( 811.6461892240364477, -244.7146871989596093, 324.1737431748509835 ) ) ;
#19365=CARTESIAN_POINT ( 'NONE',  ( 771.2633955100217236, -95.90732993114751537, 363.4237431249939618 ) ) ;
#19369=CARTESIAN_POINT ( 'NONE',  ( 757.8323909638827445, -242.6346026584197659, 352.1044303154654358 ) ) ;
#19377=CARTESIAN_POINT ( 'NONE',  ( 782.5225473063383106, -334.2709662947830793, 375.2698199232970637 ) ) ;
#19378=CARTESIAN_POINT ( 'NONE',  ( 798.0661480581538854, -26.53286901714210799, 309.5768839229118043 ) ) ;
#19383=CARTESIAN_POINT ( 'NONE',  ( 788.7366044899766848, -203.9073299311471885, 316.5762568750059813 ) ) ;
#19386=CARTESIAN_POINT ( 'NONE',  ( 749.2812353651451076, -318.4527844766014368, 323.2262854647983090 ) ) ;
#19390=CARTESIAN_POINT ( 'NONE',  ( 790.0220218866281812, -175.0999726633346825, 363.2186876482849129 ) ) ;
#19391=CARTESIAN_POINT ( 'NONE',  ( 767.8955696845333705, -72.45278447660213317, 362.1676090361162323 ) ) ;
#19397=CARTESIAN_POINT ( 'NONE',  ( 786.6156483768007774, -241.4419599262322720, 315.5913626894246136 ) ) ;
#19400=CARTESIAN_POINT ( 'NONE',  ( 814.2001403089898304, -425.3618753856919170, 347.4397851343538264 ) ) ;
#19404=CARTESIAN_POINT ( 'NONE',  ( 747.2067596250078623, -51.18005720387493085, 352.2312462859687230 ) ) ;
#19405=CARTESIAN_POINT ( 'NONE',  ( 782.5225473063381969, -142.2709662947837330, 375.2698199232970637 ) ) ;
#19409=CARTESIAN_POINT ( 'NONE',  ( 808.0189434323515343, -374.0891481129647786, 319.0252816721025511 ) ) ;
#19411=CARTESIAN_POINT ( 'NONE',  ( 803.2186876482843445, 16.01258552831230375, 350.0220218866286928 ) ) ;
#19414=CARTESIAN_POINT ( 'NONE',  ( 747.3154664389472828, -139.9874144716872024, 326.4474001241230781 ) ) ;
#19415=CARTESIAN_POINT ( 'NONE',  ( 791.9812246680005501, -428.6346026584192259, 361.9419747391813189 ) ) ;
#19419=CARTESIAN_POINT ( 'NONE',  ( 759.7806653035534055, -126.9982390220565094, 324.8639956371180801 ) ) ;
#19421=CARTESIAN_POINT ( 'NONE',  ( 774.6858677611749044, -273.7255117493288026, 315.5713283507209894 ) ) ;
#19424=ORIENTED_EDGE ( 'NONE', *, *, #20676, .F. ) ;
#19425=CARTESIAN_POINT ( 'NONE',  ( 756.1348686366196716, 6.739858255585061464, 347.5531968255698416 ) ) ;
#19429=CARTESIAN_POINT ( 'NONE',  ( 800.9747183278959710, -204.9982390220562820, 311.9810565676471583 ) ) ;
#19430=CARTESIAN_POINT ( 'NONE',  ( 776.9254006560222479, -308.1908817542434349, 314.8983024940802125 ) ) ;
#19431=CARTESIAN_POINT ( 'NONE',  ( 772.3691319403857278, -407.2601417444137155, 315.8894580844506663 ) ) ;
#19438=CARTESIAN_POINT ( 'NONE',  ( 804.1601925771018387, -295.4419599262320730, 346.5483106153029098 ) ) ;
#19441=CARTESIAN_POINT ( 'NONE',  ( 768.0187753319979720, 15.36539734157940629, 318.0580252608186242 ) ) ;
#19444=CARTESIAN_POINT ( 'NONE',  ( 799.9636004259356241, -214.9181544815164386, 311.2241431872006956 ) ) ;
#19449=CARTESIAN_POINT ( 'NONE',  ( 755.2512626584698410, -55.54369356751127640, 315.2512626584710915 ) ) ;
#19455=CARTESIAN_POINT ( 'NONE',  ( 792.1044303154645831, -36.45278447660223975, 317.8323909638837677 ) ) ;
#19456=CARTESIAN_POINT ( 'NONE',  ( 754.3581564841646241, -305.4636090269706870, 316.1443688327762516 ) ) ;
#19457=CARTESIAN_POINT ( 'NONE',  ( 796.7737145352015204, -260.6346026584197375, 370.7187646348536987 ) ) ;
#19459=CYLINDRICAL_SURFACE ( 'NONE', #4065, 10.00000000000000888 ) ;
#19461=CARTESIAN_POINT ( 'NONE',  ( 788.7366044899766848, -371.9073299311465917, 316.5762568750059813 ) ) ;
#19462=CARTESIAN_POINT ( 'NONE',  ( 798.5707757039680246, -125.4636090269712412, 356.7845633553585003 ) ) ;
#19467=CARTESIAN_POINT ( 'NONE',  ( 765.0180583372156207, -408.9982390220556567, 360.0135310231089534 ) ) ;
#19470=CARTESIAN_POINT ( 'NONE',  ( 756.5762568750052424, -171.1800572038745543, 348.7366044899774238 ) ) ;
#19471=CARTESIAN_POINT ( 'NONE',  ( 785.3687786644885591, -155.3618753856927697, 315.3201227861280813 ) ) ;
#19475=ORIENTED_EDGE ( 'NONE', *, *, #35991, .T. ) ;
#19476=CARTESIAN_POINT ( 'NONE',  ( 804.9363028652555840, -352.2709662947830225, 338.2165204200192079 ) ) ;
#19479=B_SPLINE_CURVE_WITH_KNOTS ( 'NONE', 3,
 ( #5467, #41048, #30189, #37109 ),
 .UNSPECIFIED., .F., .F.,
 ( 4, 4 ),
 ( 0.03659475354221209537, 0.03709560045499031566 ),
 .UNSPECIFIED. ) ;
#19480=CARTESIAN_POINT ( 'NONE',  ( 745.0891759886404770, -124.2709662947837899, 342.4968714119734159 ) ) ;
#19486=CARTESIAN_POINT ( 'NONE',  ( 811.0346526505616112, -254.6346026584196238, 323.0537975583477532 ) ) ;
#19487=CARTESIAN_POINT ( 'NONE',  ( 786.6156483768007774, -145.4419599262326699, 315.5913626894246136 ) ) ;
#19495=CARTESIAN_POINT ( 'NONE',  ( 807.2620300519052989, -96.00906357242585898, 318.0141637701419768 ) ) ;
#19502=CARTESIAN_POINT ( 'NONE',  ( 791.4716058693660443, -452.9681489794448339, 367.7200696026887954 ) ) ;
#19505=CARTESIAN_POINT ( 'NONE',  ( 760.7433823573367135, -420.0090635724249069, 355.9930595647440441 ) ) ;
#19506=CARTESIAN_POINT ( 'NONE',  ( 809.0717654672305343, -364.9181544815158986, 360.1688906516309885 ) ) ;
#19511=CARTESIAN_POINT ( 'NONE',  ( 793.5525998758768083, -175.0999726633346825, 372.6845335610516941 ) ) ;
#19513=CARTESIAN_POINT ( 'NONE',  ( 811.0346526505616112, -158.6346026584199933, 323.0537975583477532 ) ) ;
#19517=CARTESIAN_POINT ( 'NONE',  ( 804.9363028652555840, -256.2709662947834204, 338.2165204200192079 ) ) ;
#19519=CARTESIAN_POINT ( 'NONE',  ( 772.4468031744293057, -33.82724539060788516, 363.8651313633793620 ) ) ;
#19524=CARTESIAN_POINT ( 'NONE',  ( 763.2154366446407039, -93.62377810805098477, 321.4292242960311228 ) ) ;
#19528=CARTESIAN_POINT ( 'NONE',  ( 755.0636971347428243, -76.27096629478394618, 341.7834795799807353 ) ) ;
#19531=CARTESIAN_POINT ( 'NONE',  ( 808.7758568127978833, -364.1692326535046504, 320.0363995740631822 ) ) ;
#19534=CARTESIAN_POINT ( 'NONE',  ( 771.2368401574024119, -421.4419599262317888, 374.2805881961240857 ) ) ;
#19537=CARTESIAN_POINT ( 'NONE',  ( 800.0135310231082713, -374.0891481129647786, 325.0180583372163028 ) ) ;
#19545=CARTESIAN_POINT ( 'NONE',  ( 800.2193346964447755, -90.99823902205663728, 355.1360043628815788 ) ) ;
#19546=CARTESIAN_POINT ( 'NONE',  ( 786.5483106153019435, -391.6454272087885897, 364.1601925771022366 ) ) ;
#19547=CARTESIAN_POINT ( 'NONE',  ( 751.6929314249750860, -438.9982390220554294, 318.8095938919659034 ) ) ;
#19548=PLANE ( 'NONE',  #24733 ) ;
#19549=CARTESIAN_POINT ( 'NONE',  ( 810.1134526219336749, -320.5328690171411949, 357.8822607201570349 ) ) ;
#19551=CARTESIAN_POINT ( 'NONE',  ( 751.2241431872005251, -112.1692326535054889, 359.9636004259367610 ) ) ;
#19556=CARTESIAN_POINT ( 'NONE',  ( 745.7194118038753459, -13.64542720878976390, 348.7631598425976449 ) ) ;
#19564=CARTESIAN_POINT ( 'NONE',  ( 780.5236548040995785, -284.7363362996979390, 314.9735926884559944 ) ) ;
#19566=CARTESIAN_POINT ( 'NONE',  ( 762.1177392798416577, -282.5545181178798657, 309.8865473780659272 ) ) ;
#19571=CARTESIAN_POINT ( 'NONE',  ( 807.2620300519052989, -72.00906357242594424, 318.0141637701419768 ) ) ;
#19576=CARTESIAN_POINT ( 'NONE',  ( 791.9812246680005501, -164.6346026584200217, 361.9419747391813189 ) ) ;
#19580=CARTESIAN_POINT ( 'NONE',  ( 793.9708237608222134, -22.91815448151701062, 319.2295555964448681 ) ) ;
#19583=CARTESIAN_POINT ( 'NONE',  ( 805.1016975059191054, -414.8965053807771710, 343.0745993439771837 ) ) ;
#19588=CARTESIAN_POINT ( 'NONE',  ( 803.8556311672234642, -225.6237781080506011, 365.6418435158340117 ) ) ;
#19589=CARTESIAN_POINT ( 'NONE',  ( 800.0135310231082713, -86.08914811296573077, 325.0180583372163028 ) ) ;
#19592=CARTESIAN_POINT ( 'NONE',  ( 765.0180583372156207, -264.9982390220561115, 360.0135310231089534 ) ) ;
#19603=CARTESIAN_POINT ( 'NONE',  ( 805.0032342141413437, -325.5436935675104451, 314.9967657858572352 ) ) ;
#19604=CARTESIAN_POINT ( 'NONE',  ( 795.6651683502461765, -226.7146871989596661, 371.3240766477733814 ) ) ;
#19605=CARTESIAN_POINT ( 'NONE',  ( 798.0661480581538854, -50.53286901714203339, 309.5768839229118043 ) ) ;
#19610=CARTESIAN_POINT ( 'NONE',  ( 802.1676090361156639, -206.6346026584198512, 327.8955696845344505 ) ) ;
#19613=CARTESIAN_POINT ( 'NONE',  ( 814.5518280994195948, -327.7255117493285184, 332.4837098697145734 ) ) ;
#19617=CARTESIAN_POINT ( 'NONE',  ( 790.9844846989617508, -190.3726999360619629, 317.2208543904092721 ) ) ;
#19618=CARTESIAN_POINT ( 'NONE',  ( 795.1360043628807261, -68.08914811296575920, 360.2193346964456282 ) ) ;
#19622=CARTESIAN_POINT ( 'NONE',  ( 805.0264073115434940, -246.3510508353232638, 339.4763451958999099 ) ) ;
#19623=CIRCLE ( 'NONE', #38073, 30.00000000000008171 ) ;
#19627=CARTESIAN_POINT ( 'NONE',  ( 772.5602148656447525, -441.7255117493282910, 305.7998596910095443 ) ) ;
#19631=EDGE_CURVE ( 'NONE', #22578, #25515, #23485, .T. ) ;
#19632=CARTESIAN_POINT ( 'NONE',  ( 814.2001403089898304, -89.36187538569299704, 347.4397851343538264 ) ) ;
#19633=CARTESIAN_POINT ( 'NONE',  ( 814.5518280994195948, -135.7255117493291152, 332.4837098697145734 ) ) ;
#19637=DIRECTION ( 'NONE',  ( 0.000000000000000000, 0.000000000000000000, 1.000000000000000000 ) ) ;
#19638=CARTESIAN_POINT ( 'NONE',  ( 745.4481719005789273, -363.7255117493284047, 347.5162901302853129 ) ) ;
#19639=CARTESIAN_POINT ( 'NONE',  ( 796.7737145352015204, 3.365397341579444479, 370.7187646348536987 ) ) ;
#19643=CARTESIAN_POINT ( 'NONE',  ( 791.9812246680005501, -452.6346026584191691, 361.9419747391813189 ) ) ;
#19646=CARTESIAN_POINT ( 'NONE',  ( 815.1787889125755555, -150.8965053807781089, 343.7953271457877804 ) ) ;
#19647=CARTESIAN_POINT ( 'NONE',  ( 791.9812246680005501, 3.365397341579444479, 361.9419747391813189 ) ) ;
#19648=CARTESIAN_POINT ( 'NONE',  ( 798.0661480581538854, -170.5328690171416781, 309.5768839229118043 ) ) ;
#19651=CARTESIAN_POINT ( 'NONE',  ( 762.1405469898971887, -145.5436935675109851, 357.8594530101015607 ) ) ;
#19653=CARTESIAN_POINT ( 'NONE',  ( 797.6776695296629214, -283.5436935675105019, 357.6776695296636603 ) ) ;
#19654=CARTESIAN_POINT ( 'NONE',  ( 801.9419747391806368, -282.4527844766014937, 351.9812246680014027 ) ) ;
#19657=CARTESIAN_POINT ( 'NONE',  ( 789.5670355615794733, -453.0432664090020012, 363.0970091259334822 ) ) ;
#19661=CARTESIAN_POINT ( 'NONE',  ( 751.6929314249750860, -222.9982390220561683, 318.8095938919659034 ) ) ;
#19662=CARTESIAN_POINT ( 'NONE',  ( 802.5472867521000353, -316.3726999360615082, 350.8726784830461156 ) ) ;
#19663=CARTESIAN_POINT ( 'NONE',  ( 770.0799878456142551, -397.9874144716864066, 362.9823548866085616 ) ) ;
#19672=CARTESIAN_POINT ( 'NONE',  ( 756.1348686366196716, -305.2601417444139429, 347.5531968255698416 ) ) ;
#19674=DIRECTION ( 'NONE',  ( -0.000000000000000000, -1.110223024625155554E-15, 1.000000000000000000 ) ) ;
#19679=CARTESIAN_POINT ( 'NONE',  ( 771.3260364891663130, -211.6454272087891582, 306.0683387631859773 ) ) ;
#19685=CARTESIAN_POINT ( 'NONE',  ( 767.6429770376289525, -33.18005720387498769, 306.8695393053162093 ) ) ;
#19689=CARTESIAN_POINT ( 'NONE',  ( 785.3687786644884454, -35.36187538569316047, 315.3201227861279676 ) ) ;
#19691=CARTESIAN_POINT ( 'NONE',  ( 744.6391490659812007, -326.7363362996979390, 338.7502325331110455 ) ) ;
#19692=CARTESIAN_POINT ( 'NONE',  ( 754.9967657858570647, -241.5436935675106156, 365.0032342141425374 ) ) ;
#19698=CARTESIAN_POINT ( 'NONE',  ( 754.8072714833581358, -364.8164208402374697, 338.1981804954720587 ) ) ;
#19699=CARTESIAN_POINT ( 'NONE',  ( 759.0159684113467620, -136.9181544815166376, 325.8855110935213020 ) ) ;
#19701=CARTESIAN_POINT ( 'NONE',  ( 759.9864689768902508, -386.0891481129647786, 354.9819416627836404 ) ) ;
#19705=CARTESIAN_POINT ( 'NONE',  ( 813.2346286133761168, -125.2601417444145255, 328.9521613784389160 ) ) ;
#19706=CARTESIAN_POINT ( 'NONE',  ( 800.0135310231082713, -398.0891481129647218, 325.0180583372163028 ) ) ;
#19711=CARTESIAN_POINT ( 'NONE',  ( 797.8594530101008786, -181.5436935675108145, 322.1405469898980982 ) ) ;
#19712=CARTESIAN_POINT ( 'NONE',  ( 767.8955696845334842, -144.4527844766018632, 362.1676090361161755 ) ) ;
#19716=CARTESIAN_POINT ( 'NONE',  ( 797.6776695296629214, -355.5436935675103882, 357.6776695296636603 ) ) ;
#19719=CARTESIAN_POINT ( 'NONE',  ( 814.2001403089898304, -113.3618753856929260, 347.4397851343538264 ) ) ;
#19725=CARTESIAN_POINT ( 'NONE',  ( 808.3070685750230950, -258.9982390220561115, 361.1904061080339261 ) ) ;
#19726=CARTESIAN_POINT ( 'NONE',  ( 763.2154366446407039, -189.6237781080507148, 321.4292242960311228 ) ) ;
#19736=CARTESIAN_POINT ( 'NONE',  ( 804.1009440267234822, -95.46360902697132644, 314.0944755984392600 ) ) ;
#19746=CARTESIAN_POINT ( 'NONE',  ( 773.4516893846965786, -427.6454272087885897, 315.8398074228977066 ) ) ;
#19753=CARTESIAN_POINT ( 'NONE',  ( 815.3608509340175488, -218.7363362996982232, 341.2497674668889545 ) ) ;
#19755=CARTESIAN_POINT ( 'NONE',  ( 767.7687537140311633, -167.9073299311473022, 372.7932403749916830 ) ) ;
#19757=DIRECTION ( 'NONE',  ( -0.000000000000000000, 1.000000000000000000, -0.000000000000000000 ) ) ;
#19758=CARTESIAN_POINT ( 'NONE',  ( 758.0580252608178853, -246.4527844766016074, 328.0187753319985404 ) ) ;
#19759=CARTESIAN_POINT ( 'NONE',  ( 804.4086373105744769, -73.64542720878957027, 333.3843516231986541 ) ) ;
#19764=CARTESIAN_POINT ( 'NONE',  ( 789.9200121543843807, -73.98741447168741558, 317.0176451133914384 ) ) ;
#19768=CARTESIAN_POINT ( 'NONE',  ( 785.3687786644884454, -59.36187538569306810, 315.3201227861279676 ) ) ;
#19771=CARTESIAN_POINT ( 'NONE',  ( 778.7502325331095108, -384.3510508353227806, 304.6391490659818828 ) ) ;
#19774=CARTESIAN_POINT ( 'NONE',  ( 810.1134526219336749, -440.5328690171407970, 357.8822607201570349 ) ) ;
#19777=CARTESIAN_POINT ( 'NONE',  ( 781.7834795799800531, -370.8164208402375834, 315.0636971347436202 ) ) ;
#19781=VERTEX_POINT ( 'NONE', #16580 ) ;
#19783=CARTESIAN_POINT ( 'NONE',  ( 771.1735550268778070, -81.18005720387481006, 316.3353852180827630 ) ) ;
#19784=CARTESIAN_POINT ( 'NONE',  ( 796.9571628226829034, -407.4636090269703459, 321.2382568024804641 ) ) ;
#19785=CARTESIAN_POINT ( 'NONE',  ( 755.8398074228967971, -91.44195992623282621, 333.4516893846970333 ) ) ;
#19786=CARTESIAN_POINT ( 'NONE',  ( 815.2698199232962679, -424.8164208402373561, 342.5225473063383674 ) ) ;
#19788=CARTESIAN_POINT ( 'NONE',  ( 786.2056067578752163, -323.8055962898684470, 374.4686193811670023 ) ) ;
#19789=CARTESIAN_POINT ( 'NONE',  ( 778.7502325331095108, -120.3510508353236048, 304.6391490659818828 ) ) ;
#19793=CARTESIAN_POINT ( 'NONE',  ( 804.1009440267234822, 0.5363909730283709099, 314.0944755984392600 ) ) ;
#19799=CARTESIAN_POINT ( 'NONE',  ( 787.5531968255692163, -333.8272453906070041, 316.1348686366205811 ) ) ;
#19800=CARTESIAN_POINT ( 'NONE',  ( 791.9812246680005501, -188.6346026584199365, 361.9419747391813189 ) ) ;
#19802=CARTESIAN_POINT ( 'NONE',  ( 783.7953271457878373, -320.1908817542434349, 375.1787889125761239 ) ) ;
#19804=CARTESIAN_POINT ( 'NONE',  ( 799.9999999999993179, -462.9681489794448339, 370.0000000000000568 ) ) ;
#19806=CARTESIAN_POINT ( 'NONE',  ( 760.0363995740630116, -106.9181544815167371, 368.7758568127991907 ) ) ;
#19809=CARTESIAN_POINT ( 'NONE',  ( 778.2165204200184689, -166.8164208402382087, 364.9363028652563230 ) ) ;
#19811=CARTESIAN_POINT ( 'NONE',  ( 781.2370466360911223, -404.7363362996975980, 304.9990715423533629 ) ) ;
#19814=CARTESIAN_POINT ( 'NONE',  ( 766.0291762391763086, -58.91815448151690759, 360.7704444035551319 ) ) ;
#19817=CARTESIAN_POINT ( 'NONE',  ( 763.2154366446407039, -429.6237781080499190, 321.4292242960311228 ) ) ;
#19819=CARTESIAN_POINT ( 'NONE',  ( 803.8651313633788504, -77.26014174441466764, 332.4468031744301015 ) ) ;
#19822=CARTESIAN_POINT ( 'NONE',  ( 786.2056067578752163, -275.8055962898685038, 374.4686193811670023 ) ) ;
#19823=CARTESIAN_POINT ( 'NONE',  ( 778.1981804954715471, -82.27096629478390355, 314.8072714833591021 ) ) ;
#19826=CARTESIAN_POINT ( 'NONE',  ( 785.3141322388236176, -285.7255117493286889, 364.4286716492789537 ) ) ;
#19834=CARTESIAN_POINT ( 'NONE',  ( 747.2067596250078623, -315.1800572038740711, 352.2312462859687230 ) ) ;
#19835=CARTESIAN_POINT ( 'NONE',  ( 814.8230680027162407, -221.8055962898687881, 333.7305795820267917 ) ) ;
#19841=CARTESIAN_POINT ( 'NONE',  ( 756.5762568750052424, -195.1800572038744974, 348.7366044899774238 ) ) ;
#19843=ORIENTED_EDGE ( 'NONE', *, *, #11308, .F. ) ;
#19844=CARTESIAN_POINT ( 'NONE',  ( 815.2698199232961542, -352.8164208402374129, 342.5225473063383106 ) ) ;
#19849=CARTESIAN_POINT ( 'NONE',  ( 790.0220218866281812, -223.0999726633346256, 363.2186876482849129 ) ) ;
#19851=CARTESIAN_POINT ( 'NONE',  ( 804.4286716492782716, -89.36187538569299704, 345.3141322388244703 ) ) ;
#19855=CARTESIAN_POINT ( 'NONE',  ( 784.0799538623451781, -251.8055962898686744, 364.6971507214555572 ) ) ;
#19858=CARTESIAN_POINT ( 'NONE',  ( 748.9653473494363425, -434.6346026584190554, 356.9462024416521331 ) ) ;
#19862=CARTESIAN_POINT ( 'NONE',  ( 808.3070685750230950, -66.99823902205672255, 361.1904061080339261 ) ) ;
#19863=CARTESIAN_POINT ( 'NONE',  ( 751.6929314249748586, -150.9982390220563957, 318.8095938919659034 ) ) ;
#19869=CARTESIAN_POINT ( 'NONE',  ( 807.2620300519052989, -408.0090635724249069, 318.0141637701419768 ) ) ;
#19872=CARTESIAN_POINT ( 'NONE',  ( 772.4837098697144029, -407.3618753856920307, 374.5518280994205611 ) ) ;
#19873=CARTESIAN_POINT ( 'NONE',  ( 751.9810565676468741, -2.089148112965993231, 360.9747183278973921 ) ) ;
#19875=CARTESIAN_POINT ( 'NONE',  ( 803.8651313633788504, -29.26014174441482751, 332.4468031744301015 ) ) ;
#19879=CARTESIAN_POINT ( 'NONE',  ( 807.5423716828161105, -177.0783235625961538, 362.2119215644372048 ) ) ;
#19880=CARTESIAN_POINT ( 'NONE',  ( 771.1735550268780344, 14.81994279612486309, 316.3353852180828198 ) ) ;
#19883=CARTESIAN_POINT ( 'NONE',  ( 778.1981804954714335, -178.2709662947835625, 314.8072714833589885 ) ) ;
#19886=CARTESIAN_POINT ( 'NONE',  ( 781.7834795799800531, -298.8164208402377540, 315.0636971347436202 ) ) ;
#19889=CARTESIAN_POINT ( 'NONE',  ( 795.9930595647434757, -3.078323562596726681, 320.7433823573372820 ) ) ;
#19894=CARTESIAN_POINT ( 'NONE',  ( 782.4968714119720516, -226.8164208402380098, 305.0891759886411023 ) ) ;
#19896=CARTESIAN_POINT ( 'NONE',  ( 790.9844846989617508, -310.3726999360616219, 317.2208543904092721 ) ) ;
#19897=CARTESIAN_POINT ( 'NONE',  ( 802.7791456095903868, -388.7146871989592114, 329.0155153010375102 ) ) ;
#19902=ORIENTED_EDGE ( 'NONE', *, *, #34603, .T. ) ;
#19904=CARTESIAN_POINT ( 'NONE',  ( 796.7845633553578182, -297.6237781080502600, 358.5707757039688204 ) ) ;
#19908=CARTESIAN_POINT ( 'NONE',  ( 771.1735550268778070, 14.81994279612486309, 316.3353852180827630 ) ) ;
#19911=CARTESIAN_POINT ( 'NONE',  ( 814.8207195650702488, -194.1908817542437475, 336.2433038121456548 ) ) ;
#19915=CARTESIAN_POINT ( 'NONE',  ( 782.4968714119720516, -34.81642084023861372, 305.0891759886411023 ) ) ;
#19919=CARTESIAN_POINT ( 'NONE',  ( 803.4237431249931660, -63.18005720387488822, 331.2633955100225194 ) ) ;
#19920=CARTESIAN_POINT ( 'NONE',  ( 799.9636004259356241, -310.9181544815160123, 311.2241431872006956 ) ) ;
#19923=CARTESIAN_POINT ( 'NONE',  ( 814.9108240113580450, -280.2709662947833067, 337.5031285880265273 ) ) ;
#19926=DIRECTION ( 'NONE',  ( 0.000000000000000000, 0.000000000000000000, 1.000000000000000000 ) ) ;
#19927=CARTESIAN_POINT ( 'NONE',  ( 804.9363028652555840, -376.2709662947829656, 338.2165204200192079 ) ) ;
#19928=CARTESIAN_POINT ( 'NONE',  ( 804.4086373105744769, -121.6454272087894282, 333.3843516231986541 ) ) ;
#19930=CARTESIAN_POINT ( 'NONE',  ( 747.3154664389472828, -43.98741447168752217, 326.4474001241230781 ) ) ;
#19931=CARTESIAN_POINT ( 'NONE',  ( 762.3223304703356007, -367.5436935675102745, 322.3223304703362828 ) ) ;
#19934=CARTESIAN_POINT ( 'NONE',  ( 788.7631598425961101, -145.4419599262326699, 305.7194118038759143 ) ) ;
#19935=CARTESIAN_POINT ( 'NONE',  ( 778.1981804954714335, -442.2709662947826814, 314.8072714833589885 ) ) ;
#19936=VERTEX_POINT ( 'NONE', #32265 ) ;
#19938=CARTESIAN_POINT ( 'NONE',  ( 767.8955696845333705, -192.4527844766016926, 362.1676090361162323 ) ) ;
#19939=CARTESIAN_POINT ( 'NONE',  ( 788.8264449731201466, -189.1800572038744690, 363.6646147819170665 ) ) ;
#19943=CARTESIAN_POINT ( 'NONE',  ( 788.7366044899766848, -395.9073299311465348, 316.5762568750059813 ) ) ;
#19947=CARTESIAN_POINT ( 'NONE',  ( 808.0189434323515343, -134.0891481129655745, 319.0252816721025511 ) ) ;
#19954=CARTESIAN_POINT ( 'NONE',  ( 808.0189434323515343, -254.0891481129652334, 319.0252816721025511 ) ) ;
#19955=CARTESIAN_POINT ( 'NONE',  ( 805.1016975059191054, -198.8965053807779384, 343.0745993439771837 ) ) ;
#19966=CARTESIAN_POINT ( 'NONE',  ( 762.1177392798416577, -114.5545181178803631, 309.8865473780659272 ) ) ;
#19973=CARTESIAN_POINT ( 'NONE',  ( 802.9823548866075953, -433.0999726633339151, 330.0799878456151077 ) ) ;
#19978=DIRECTION ( 'NONE',  ( 0.000000000000000000, -1.000000000000000000, 0.000000000000000000 ) ) ;
#19980=CARTESIAN_POINT ( 'NONE',  ( 793.5525998758768083, -199.0999726633346825, 372.6845335610516941 ) ) ;
#19982=CARTESIAN_POINT ( 'NONE',  ( 758.8095938919642549, -200.0891481129653187, 311.6929314249763365 ) ) ;
#19985=CARTESIAN_POINT ( 'NONE',  ( 800.0135310231082713, -254.0891481129652334, 325.0180583372163028 ) ) ;
#19986=CARTESIAN_POINT ( 'NONE',  ( 763.0428371773158460, -59.46360902697142592, 358.7617431975195359 ) ) ;
#19990=CARTESIAN_POINT ( 'NONE',  ( 769.1273215169530886, -94.71468719896007826, 317.4527132478988847 ) ) ;
#19993=CARTESIAN_POINT ( 'NONE',  ( 759.9864689768902508, -50.08914811296584446, 354.9819416627836404 ) ) ;
#19996=CARTESIAN_POINT ( 'NONE',  ( 812.6845335610512393, -367.9874144716865203, 353.5525998758768651 ) ) ;
#19998=CARTESIAN_POINT ( 'NONE',  ( 755.2512626584698410, 16.45630643248849267, 315.2512626584710915 ) ) ;
#20000=CARTESIAN_POINT ( 'NONE',  ( 767.8955696845333705, -384.4527844766011526, 362.1676090361162323 ) ) ;
#20007=CARTESIAN_POINT ( 'NONE',  ( 778.1981804954714335, -82.27096629478388934, 314.8072714833589885 ) ) ;
#20008=CARTESIAN_POINT ( 'NONE',  ( 779.4763451958990572, -416.7363362996975980, 365.0264073115438919 ) ) ;
#20009=CARTESIAN_POINT ( 'NONE',  ( 814.9108240113580450, -424.2709662947829088, 337.5031285880265273 ) ) ;
#20010=LINE ( 'NONE', #41036, #34330 ) ;
#20011=CARTESIAN_POINT ( 'NONE',  ( 761.9338519418445230, -350.5328690171411381, 370.4231160770881957 ) ) ;
#20015=CARTESIAN_POINT ( 'NONE',  ( 814.2805881961230625, -1.645427208789804308, 331.2368401574024119 ) ) ;
#20016=CARTESIAN_POINT ( 'NONE',  ( 781.3877698825695006, 18.31902617013176027, 309.9999999999999432 ) ) ;
#20022=CARTESIAN_POINT ( 'NONE',  ( 804.6971507214547046, -339.2817908451524431, 344.0799538623459739 ) ) ;
#20024=CARTESIAN_POINT ( 'NONE',  ( 748.6759233522253680, -304.3726999360615082, 324.3348316497537098 ) ) ;
#20027=CARTESIAN_POINT ( 'NONE',  ( 762.1177392798416577, -114.5545181178803631, 309.8865473780659272 ) ) ;
#20030=CARTESIAN_POINT ( 'NONE',  ( 804.4286716492782716, -161.3618753856927697, 345.3141322388244703 ) ) ;
#20031=CIRCLE ( 'NONE', #28912, 10.00000000000000888 ) ;
#20033=CARTESIAN_POINT ( 'NONE',  ( 788.6739635108323228, -415.6454272087885897, 373.9316612368139090 ) ) ;
#20036=CARTESIAN_POINT ( 'NONE',  ( 804.6971507214547046, -51.28179084515328867, 344.0799538623459739 ) ) ;
#20039=CARTESIAN_POINT ( 'NONE',  ( 773.7943932421234194, 24.19440371013046231, 305.5313806188329409 ) ) ;
#20043=CARTESIAN_POINT ( 'NONE',  ( 759.8311093483677041, -286.1692326535048778, 310.9282345327691814 ) ) ;
#20044=CARTESIAN_POINT ( 'NONE',  ( 803.4237431249931660, -87.18005720387481006, 331.2633955100225194 ) ) ;
#20046=CARTESIAN_POINT ( 'NONE',  ( 755.3201227861273992, -267.7255117493286320, 345.3687786644892981 ) ) ;
#20049=CARTESIAN_POINT ( 'NONE',  ( 793.1929000023510525, -451.7523979515906944, 372.2801657505705180 ) ) ;
#20053=CARTESIAN_POINT ( 'NONE',  ( 759.0252816721024374, -312.9982390220559409, 368.0189434323527280 ) ) ;
#20054=CARTESIAN_POINT ( 'NONE',  ( 798.0661480581538854, -242.5328690171414507, 309.5768839229118043 ) ) ;
#20059=CARTESIAN_POINT ( 'NONE',  ( 778.1981804954714335, -202.2709662947834772, 314.8072714833589885 ) ) ;
#20062=CARTESIAN_POINT ( 'NONE',  ( 751.6929314249748586, -366.9982390220556567, 318.8095938919659034 ) ) ;
#20065=CARTESIAN_POINT ( 'NONE',  ( 795.1616405723528942, 16.45630643248848912, 314.3282859078202591 ) ) ;
#20067=CARTESIAN_POINT ( 'NONE',  ( 787.5531968255692163, -237.8272453906072599, 316.1348686366205811 ) ) ;
#20068=CARTESIAN_POINT ( 'NONE',  ( 755.3201227861273992, -99.72551174932928575, 345.3687786644892981 ) ) ;
#20073=CARTESIAN_POINT ( 'NONE',  ( 801.3366627262608972, -248.5328690171414223, 353.0897708529566899 ) ) ;
#20076=CARTESIAN_POINT ( 'NONE',  ( 754.3581564841646241, -17.46360902697157513, 316.1443688327762516 ) ) ;
#20080=CARTESIAN_POINT ( 'NONE',  ( 749.2812353651451076, -78.45278447660211896, 323.2262854647983090 ) ) ;
#20081=CARTESIAN_POINT ( 'NONE',  ( 814.5518280994195948, -159.7255117493291436, 332.4837098697145734 ) ) ;
#20086=CARTESIAN_POINT ( 'NONE',  ( 797.8822607201568644, -414.5545181178795247, 370.1134526219340160 ) ) ;
#20089=CARTESIAN_POINT ( 'NONE',  ( 814.9108240113580450, -400.2709662947828519, 337.5031285880265273 ) ) ;
#20090=CARTESIAN_POINT ( 'NONE',  ( 787.4397851343537695, 2.274488250670355871, 374.2001403089903988 ) ) ;
#20092=CARTESIAN_POINT ( 'NONE',  ( 761.2382568024794409, -15.62377810805123524, 356.9571628226838129 ) ) ;
#20095=CARTESIAN_POINT ( 'NONE',  ( 793.4146539503750546, -169.9874144716871172, 307.6481478633938877 ) ) ;
#20097=CARTESIAN_POINT ( 'NONE',  ( 795.6651683502461765, -178.7146871989598083, 371.3240766477733814 ) ) ;
#20098=EDGE_LOOP ( 'NONE', ( #45171, #13951, #39803, #25945 ) ) ;
#20101=CARTESIAN_POINT ( 'NONE',  ( 805.1927285166397041, -160.8164208402382371, 341.8018195045277707 ) ) ;
#20104=CARTESIAN_POINT ( 'NONE',  ( 764.8639956371174549, -296.0891481129650629, 319.7806653035542581 ) ) ;
#20106=VERTEX_POINT ( 'NONE', #841 ) ;
#20107=CARTESIAN_POINT ( 'NONE',  ( 775.9200461376533440, -23.80559628986938847, 315.3028492785443291 ) ) ;
#20112=CARTESIAN_POINT ( 'NONE',  ( 792.2312462859673587, -203.9073299311471885, 307.2067596250082602 ) ) ;
#20113=CARTESIAN_POINT ( 'NONE',  ( 763.0428371773158460, -347.4636090269705733, 358.7617431975195359 ) ) ;
#20114=CARTESIAN_POINT ( 'NONE',  ( 794.1144889064781864, -418.1692326535044799, 360.9840315886528401 ) ) ;
#20122=CARTESIAN_POINT ( 'NONE',  ( 755.8398074228967971, -307.4419599262320730, 333.4516893846970333 ) ) ;
#20125=CARTESIAN_POINT ( 'NONE',  ( 758.4439275373578084, -108.5545181178803915, 353.2243759319684386 ) ) ;
#20129=CARTESIAN_POINT ( 'NONE',  ( 795.8262568251477660, -190.3726999360619629, 308.3538107759623585 ) ) ;
#20133=CARTESIAN_POINT ( 'NONE',  ( 745.4481719005789273, -51.72551174932946338, 347.5162901302853129 ) ) ;
#20137=CARTESIAN_POINT ( 'NONE',  ( 755.8990559732751535, -323.4636090269706301, 365.9055244015606831 ) ) ;
#20138=PLANE ( 'NONE',  #10987 ) ;
#20139=CARTESIAN_POINT ( 'NONE',  ( 814.5518280994195948, -279.7255117493288026, 332.4837098697145734 ) ) ;
#20144=CARTESIAN_POINT ( 'NONE',  ( 762.1405469898971887, -385.5436935675102745, 357.8594530101015607 ) ) ;
#20145=AXIS2_PLACEMENT_3D ( 'NONE', #3634, #6163, #20252 ) ;
#20146=CARTESIAN_POINT ( 'NONE',  ( 804.4086373105744769, -169.6454272087892718, 333.3843516231986541 ) ) ;
#20148=CARTESIAN_POINT ( 'NONE',  ( 801.9858362298568863, -75.07832356259649487, 312.7379699480935642 ) ) ;
#20149=CARTESIAN_POINT ( 'NONE',  ( 781.8018195045267476, -358.2709662947830225, 365.1927285166407273 ) ) ;
#20151=CARTESIAN_POINT ( 'NONE',  ( 794.9819416627830151, -420.9982390220555999, 319.9864689768909898 ) ) ;
#20157=CARTESIAN_POINT ( 'NONE',  ( 755.3201227861273992, -195.7255117493289731, 345.3687786644892981 ) ) ;
#20158=CARTESIAN_POINT ( 'NONE',  ( 791.9812246680005501, -188.6346026584199365, 361.9419747391813189 ) ) ;
#20160=LINE ( 'NONE', #30796, #14624 ) ;
#20161=VERTEX_POINT ( 'NONE', #33615 ) ;
#20162=CARTESIAN_POINT ( 'NONE',  ( 801.9419747391806368, -378.4527844766011526, 351.9812246680014027 ) ) ;
#20166=CARTESIAN_POINT ( 'NONE',  ( 748.9653473494365699, -122.6346026584201496, 356.9462024416520762 ) ) ;
#20173=CARTESIAN_POINT ( 'NONE',  ( 755.2512626584698410, -271.5436935675106156, 315.2512626584710915 ) ) ;
#20174=CARTESIAN_POINT ( 'NONE',  ( 776.9566956441375396, -204.8965053807779100, 364.8461984189686405 ) ) ;
#20178=VERTEX_POINT ( 'NONE', #40344 ) ;
#20185=CARTESIAN_POINT ( 'NONE',  ( 814.4686193811664907, -99.28179084515313946, 346.2056067578752732 ) ) ;
#20193=CARTESIAN_POINT ( 'NONE',  ( 755.8894580844503253, -447.8272453906067199, 332.3691319403863531 ) ) ;
#20194=CARTESIAN_POINT ( 'NONE',  ( 805.6418435158337843, -365.4636090269705164, 363.8556311672236916 ) ) ;
#20201=CARTESIAN_POINT ( 'NONE',  ( 797.8822607201568644, -198.5545181178800647, 370.1134526219340160 ) ) ;
#20203=CARTESIAN_POINT ( 'NONE',  ( 751.6929314249748586, -174.9982390220563673, 318.8095938919659034 ) ) ;
#20207=CARTESIAN_POINT ( 'NONE',  ( 755.5713283507202505, -293.3618753856923718, 334.6858677611754729 ) ) ;
#20208=CARTESIAN_POINT ( 'NONE',  ( 790.9844846989617508, -70.37269993606230400, 317.2208543904092721 ) ) ;
#20211=LINE ( 'NONE', #6805, #32840 ) ;
#20212=CARTESIAN_POINT ( 'NONE',  ( 783.0433043558608688, -72.89650538077830788, 315.1538015810313027 ) ) ;
#20213=CARTESIAN_POINT ( 'NONE',  ( 765.0180583372156207, -336.9982390220558273, 360.0135310231089534 ) ) ;
#20216=CARTESIAN_POINT ( 'NONE',  ( 800.2193346964447755, -42.99823902205675807, 355.1360043628815788 ) ) ;
#20220=CARTESIAN_POINT ( 'NONE',  ( 811.6461892240364477, -388.7146871989592114, 324.1737431748509835 ) ) ;
#20222=CARTESIAN_POINT ( 'NONE',  ( 785.3687786644884454, -275.3618753856923149, 315.3201227861279676 ) ) ;
#20223=CARTESIAN_POINT ( 'NONE',  ( 782.5225473063381969, 1.729033705215812011, 375.2698199232970637 ) ) ;
#20225=CARTESIAN_POINT ( 'NONE',  ( 803.4237431249931660, -375.1800572038739574, 331.2633955100225194 ) ) ;
#20232=CARTESIAN_POINT ( 'NONE',  ( 785.3687786644884454, -107.3618753856928976, 315.3201227861279676 ) ) ;
#20233=CARTESIAN_POINT ( 'NONE',  ( 800.9840315886518738, -388.9181544815158986, 354.1144889064786412 ) ) ;
#20234=CARTESIAN_POINT ( 'NONE',  ( 793.3938497862117174, -453.0432664090020580, 372.3358127763067955 ) ) ;
#20236=CARTESIAN_POINT ( 'NONE',  ( 798.0661480581538854, -362.5328690171410813, 309.5768839229118043 ) ) ;
#20241=CARTESIAN_POINT ( 'NONE',  ( 814.9108240113580450, -448.2709662947827951, 337.5031285880265273 ) ) ;
#20247=CARTESIAN_POINT ( 'NONE',  ( 793.9708237608222134, -334.9181544815160692, 319.2295555964448681 ) ) ;
#20249=CARTESIAN_POINT ( 'NONE',  ( 799.9636004259356241, -286.9181544815161828, 311.2241431872006956 ) ) ;
#20250=VECTOR ( 'NONE', #5359, 1000.000000000000000 ) ;
#20252=DIRECTION ( 'NONE',  ( 0.000000000000000000, 0.000000000000000000, 1.000000000000000000 ) ) ;
#20254=CARTESIAN_POINT ( 'NONE',  ( 814.4686193811664907, -123.2817908451530542, 346.2056067578752732 ) ) ;
#20258=CARTESIAN_POINT ( 'NONE',  ( 757.8323909638827445, -146.6346026584200217, 352.1044303154654358 ) ) ;
#20260=CARTESIAN_POINT ( 'NONE',  ( 745.1792804349281596, -422.1908817542430370, 343.7566961878542884 ) ) ;
#20264=CARTESIAN_POINT ( 'NONE',  ( 790.9844846989617508, -46.37269993606239638, 317.2208543904092721 ) ) ;
#20267=CARTESIAN_POINT ( 'NONE',  ( 770.0799878456142551, -421.9874144716863498, 362.9823548866085616 ) ) ;
#20269=CARTESIAN_POINT ( 'NONE',  ( 767.8955696845333705, -264.4527844766016074, 362.1676090361162323 ) ) ;
#20272=CARTESIAN_POINT ( 'NONE',  ( 783.7566961878529810, -288.8965053807775121, 305.1792804349288417 ) ) ;
#20273=CARTESIAN_POINT ( 'NONE',  ( 756.5762568750052424, -99.18005720387478164, 348.7366044899774238 ) ) ;
#20276=CARTESIAN_POINT ( 'NONE',  ( 794.9819416627830151, -252.9982390220560831, 319.9864689768909898 ) ) ;
#20284=CARTESIAN_POINT ( 'NONE',  ( 748.9653473494365699, -362.6346026584193964, 356.9462024416520762 ) ) ;
#20285=CARTESIAN_POINT ( 'NONE',  ( 768.8385539511368734, -239.2601417444141987, 306.4236121716840557 ) ) ;
#20289=CARTESIAN_POINT ( 'NONE',  ( 757.8323909638827445, -242.6346026584197659, 352.1044303154654358 ) ) ;
#20291=CARTESIAN_POINT ( 'NONE',  ( 805.0032342141412300, -349.5436935675102745, 314.9967657858571783 ) ) ;
#20295=CARTESIAN_POINT ( 'NONE',  ( 794.1255485493337574, 16.45630643248849978, 314.6638991903497526 ) ) ;
#20298=CARTESIAN_POINT ( 'NONE',  ( 805.2837595273609850, -242.7363362996980811, 340.5290396650784714 ) ) ;
#20299=CARTESIAN_POINT ( 'NONE',  ( 778.1981804954714335, -130.2709662947837899, 314.8072714833589885 ) ) ;
#20303=CARTESIAN_POINT ( 'NONE',  ( 758.6633372737375112, -260.5328690171413086, 326.9102291470432533 ) ) ;
#20306=CARTESIAN_POINT ( 'NONE',  ( 807.2620300519052989, -0.009063572426172561425, 318.0141637701419768 ) ) ;
#20309=CARTESIAN_POINT ( 'NONE',  ( 745.0891759886404770, -76.27096629478394618, 342.4968714119734159 ) ) ;
#20315=CARTESIAN_POINT ( 'NONE',  ( 745.1792804349281596, -422.1908817542430370, 343.7566961878542884 ) ) ;
#20318=CARTESIAN_POINT ( 'NONE',  ( 763.0537975583475827, -408.4527844766009252, 371.0346526505627480 ) ) ;
#20319=CARTESIAN_POINT ( 'NONE',  ( 792.2312462859673587, -11.90732993114778182, 307.2067596250082602 ) ) ;
#20321=CARTESIAN_POINT ( 'NONE',  ( 804.9511171171677688, -29.80559628986937781, 335.8780910478229202 ) ) ;
#20324=CARTESIAN_POINT ( 'NONE',  ( 754.0944755984390895, -183.6237781080507148, 364.1009440267246760 ) ) ;
#20325=CARTESIAN_POINT ( 'NONE',  ( 762.3223304703356007, 16.45630643248849267, 322.3223304703362828 ) ) ;
#20330=CARTESIAN_POINT ( 'NONE',  ( 774.6312213355099630, -167.3618753856927412, 364.6798772138717482 ) ) ;
#20334=CARTESIAN_POINT ( 'NONE',  ( 758.0580252608178853, -294.4527844766013800, 328.0187753319985404 ) ) ;
#20335=CARTESIAN_POINT ( 'NONE',  ( 759.9864689768902508, -290.0891481129650629, 354.9819416627836404 ) ) ;
#20338=CARTESIAN_POINT ( 'NONE',  ( 800.7704444035546203, -28.16923265350574468, 326.0291762391768771 ) ) ;
#20341=CARTESIAN_POINT ( 'NONE',  ( 777.4774526936600978, -226.2709662947834488, 304.7301800767028226 ) ) ;
#20342=CARTESIAN_POINT ( 'NONE',  ( 772.4468031744293057, -345.8272453906069472, 363.8651313633793620 ) ) ;
#20343=CARTESIAN_POINT ( 'NONE',  ( 799.4546378042377910, -441.0783235625953580, 356.1575198192848006 ) ) ;
#20349=CARTESIAN_POINT ( 'NONE',  ( 804.9511171171677688, -293.8055962898685607, 335.8780910478229202 ) ) ;
#20353=CARTESIAN_POINT ( 'NONE',  ( 766.0291762391763086, -130.9181544815166660, 360.7704444035551319 ) ) ;
#20354=CARTESIAN_POINT ( 'NONE',  ( 774.6858677611749044, 14.27448825067031812, 315.5713283507209894 ) ) ;
#20357=CARTESIAN_POINT ( 'NONE',  ( 786.2694204179717872, -237.2817908451526421, 305.1769319972829067 ) ) ;
#20365=CARTESIAN_POINT ( 'NONE',  ( 745.0891759886404770, -52.27096629478401724, 342.4968714119734159 ) ) ;
#20369=CARTESIAN_POINT ( 'NONE',  ( 805.6418435158337843, -317.4636090269706301, 363.8556311672236916 ) ) ;
#20371=CARTESIAN_POINT ( 'NONE',  ( 777.5031285880264704, -286.8164208402378677, 374.9108240113588408 ) ) ;
#20375=CARTESIAN_POINT ( 'NONE',  ( 764.8639956371174549, -392.0891481129648355, 319.7806653035542013 ) ) ;
#20376=CARTESIAN_POINT ( 'NONE',  ( 796.1575198192839480, -150.0090635724257027, 359.4546378042384163 ) ) ;
#20378=CARTESIAN_POINT ( 'NONE',  ( 801.9858362298568863, -51.07832356259657303, 312.7379699480935642 ) ) ;
#20379=CARTESIAN_POINT ( 'NONE',  ( 774.6312213355098493, -359.3618753856921444, 364.6798772138717482 ) ) ;
#20381=CARTESIAN_POINT ( 'NONE',  ( 803.6646147819161570, -425.9073299311463074, 348.8264449731210561 ) ) ;
#20382=EDGE_LOOP ( 'NONE', ( #7304, #3868, #5039, #26637, #22272, #3880 ) ) ;
#20386=CARTESIAN_POINT ( 'NONE',  ( 804.9363028652555840, -208.2709662947835341, 338.2165204200192079 ) ) ;
#20387=CARTESIAN_POINT ( 'NONE',  ( 768.0187753319979720, -200.6346026584199365, 318.0580252608186242 ) ) ;
#20391=EDGE_LOOP ( 'NONE', ( #34246, #30979, #44511, #4969 ) ) ;
#20392=CARTESIAN_POINT ( 'NONE',  ( 778.1981804954714335, -394.2709662947827951, 314.8072714833589885 ) ) ;
#20397=CARTESIAN_POINT ( 'NONE',  ( 772.5602148656447525, -129.7255117493292289, 305.7998596910095443 ) ) ;
#20403=CARTESIAN_POINT ( 'NONE',  ( 754.8983024940795303, -186.8965053807779668, 336.9254006560228163 ) ) ;
#20406=CARTESIAN_POINT ( 'NONE',  ( 799.9999999999993179, 205.0000000000000568, 339.9999999999999432 ) ) ;
#20414=CARTESIAN_POINT ( 'NONE',  ( 802.2119215644370342, -102.0090635724258448, 367.5423716828165084 ) ) ;
#20425=CARTESIAN_POINT ( 'NONE',  ( 766.9102291470427417, -450.5545181178793541, 318.6633372737382501 ) ) ;
#20426=CARTESIAN_POINT ( 'NONE',  ( 793.5525998758768083, -367.0999726633342561, 372.6845335610516941 ) ) ;
#20434=CARTESIAN_POINT ( 'NONE',  ( 799.9636004259356241, -214.9181544815164386, 311.2241431872006956 ) ) ;
#20436=CARTESIAN_POINT ( 'NONE',  ( 787.5162901302840055, -203.3618753856925991, 305.4481719005792684 ) ) ;
#20440=CARTESIAN_POINT ( 'NONE',  ( 802.1676090361156639, -302.6346026584196238, 327.8955696845344505 ) ) ;
#20441=CARTESIAN_POINT ( 'NONE',  ( 761.4292242960306112, -65.46360902697142592, 323.2154366446414429 ) ) ;
#20447=CARTESIAN_POINT ( 'NONE',  ( 754.9735926884551418, -114.3510508353236617, 340.5236548041000333 ) ) ;
#20448=CARTESIAN_POINT ( 'NONE',  ( 797.8594530101008786, -325.5436935675105019, 322.1405469898980982 ) ) ;
#20452=CARTESIAN_POINT ( 'NONE',  ( 759.7806653035534055, -78.99823902205662307, 324.8639956371180801 ) ) ;
#20455=CARTESIAN_POINT ( 'NONE',  ( 771.2368401574024119, -397.4419599262317320, 374.2805881961240857 ) ) ;
#20458=CARTESIAN_POINT ( 'NONE',  ( 771.1735550268778070, -273.1800572038742985, 316.3353852180827630 ) ) ;
#20461=CARTESIAN_POINT ( 'NONE',  ( 785.3141322388236176, -357.7255117493285184, 364.4286716492789537 ) ) ;
#20469=CARTESIAN_POINT ( 'NONE',  ( 803.6646147819161570, -137.9073299311473875, 348.8264449731210561 ) ) ;
#20470=CARTESIAN_POINT ( 'NONE',  ( 802.5472867521000353, -412.3726999360612808, 350.8726784830461156 ) ) ;
#20471=CARTESIAN_POINT ( 'NONE',  ( 754.8983024940795303, -90.89650538077827946, 336.9254006560228163 ) ) ;
#20472=CARTESIAN_POINT ( 'NONE',  ( 796.7737145352015204, -452.6346026584191691, 370.7187646348536987 ) ) ;
#20473=DIRECTION ( 'NONE',  ( 0.000000000000000000, -1.000000000000000000, 0.000000000000000000 ) ) ;
#20474=CARTESIAN_POINT ( 'NONE',  ( 783.7566961878529810, -360.8965053807773984, 305.1792804349288417 ) ) ;
#20476=CARTESIAN_POINT ( 'NONE',  ( 752.4576283171824116, -117.0783235625963528, 317.7880784355627952 ) ) ;
#20480=CARTESIAN_POINT ( 'NONE',  ( 781.2370466360911223, 3.263663700301089765, 304.9990715423533629 ) ) ;
#20488=CARTESIAN_POINT ( 'NONE',  ( 755.1538015810308480, -326.1908817542433781, 343.0433043558613804 ) ) ;
#20489=CARTESIAN_POINT ( 'NONE',  ( 795.8262568251477660, -286.3726999360617356, 308.3538107759623585 ) ) ;
#20492=CARTESIAN_POINT ( 'NONE',  ( 793.5525998758768083, -127.0999726633348672, 372.6845335610516941 ) ) ;
#20496=CARTESIAN_POINT ( 'NONE',  ( 757.8323909638827445, -194.6346026584198796, 352.1044303154654358 ) ) ;
#20498=CARTESIAN_POINT ( 'NONE',  ( 814.8207195650702488, -410.1908817542430370, 336.2433038121456548 ) ) ;
#20502=CARTESIAN_POINT ( 'NONE',  ( 755.3028492785439312, -39.28179084515331709, 335.9200461376539693 ) ) ;
#20506=CARTESIAN_POINT ( 'NONE',  ( 769.1273215169530886, -430.7146871989590409, 317.4527132478988847 ) ) ;
#20510=CARTESIAN_POINT ( 'NONE',  ( 744.9990715423526808, -258.3510508353231785, 341.2370466360926002 ) ) ;
#20511=CARTESIAN_POINT ( 'NONE',  ( 759.9864689768902508, -122.0891481129656171, 354.9819416627836404 ) ) ;
#20513=CARTESIAN_POINT ( 'NONE',  ( 758.0580252608178853, -270.4527844766014937, 328.0187753319985404 ) ) ;
#20520=CARTESIAN_POINT ( 'NONE',  ( 813.1304606946831655, -353.9073299311467053, 352.3570229623691716 ) ) ;
#20521=CARTESIAN_POINT ( 'NONE',  ( 815.0009284576459549, -270.3510508353231216, 338.7629533639073429 ) ) ;
#20526=CARTESIAN_POINT ( 'NONE',  ( 768.0187753319979720, -248.6346026584197659, 318.0580252608186242 ) ) ;
#20528=CARTESIAN_POINT ( 'NONE',  ( 792.2312462859673587, -347.9073299311467053, 307.2067596250082602 ) ) ;
#20533=CARTESIAN_POINT ( 'NONE',  ( 776.9254006560222479, -236.1908817542436338, 314.8983024940802125 ) ) ;
#20534=CARTESIAN_POINT ( 'NONE',  ( 794.9819416627830151, -108.9982390220565804, 319.9864689768909898 ) ) ;
#20538=CARTESIAN_POINT ( 'NONE',  ( 761.2382568024794409, -279.6237781080503737, 356.9571628226838129 ) ) ;
#20541=CARTESIAN_POINT ( 'NONE',  ( 797.8822607201568644, -6.554518117880697048, 370.1134526219340160 ) ) ;
#20546=CARTESIAN_POINT ( 'NONE',  ( 791.0478386215596629, -429.8272453906067199, 306.7653713866226326 ) ) ;
#20549=CARTESIAN_POINT ( 'NONE',  ( 745.7998596910086917, -413.3618753856920307, 332.5602148656461168 ) ) ;
#20550=CARTESIAN_POINT ( 'NONE',  ( 744.7301800767020268, -28.81642084023863504, 337.4774526936615189 ) ) ;
#20553=CARTESIAN_POINT ( 'NONE',  ( 805.0264073115434940, -30.35105083532391390, 339.4763451958999099 ) ) ;
#20556=CARTESIAN_POINT ( 'NONE',  ( 746.7653713866222915, -161.2601417444143976, 351.0478386215610271 ) ) ;
#20557=CARTESIAN_POINT ( 'NONE',  ( 771.2633955100217236, 0.09267006885218045942, 363.4237431249939618 ) ) ;
#20559=CARTESIAN_POINT ( 'NONE',  ( 811.6461892240364477, -172.7146871989598083, 324.1737431748509835 ) ) ;
#20564=CARTESIAN_POINT ( 'NONE',  ( 765.0180583372156207, -168.9982390220563673, 360.0135310231089534 ) ) ;
#20568=CARTESIAN_POINT ( 'NONE',  ( 776.9566956441375396, -12.89650538077851216, 364.8461984189686405 ) ) ;
#20570=CARTESIAN_POINT ( 'NONE',  ( 745.0891759886404770, -244.2709662947834204, 342.4968714119734159 ) ) ;
#20571=CARTESIAN_POINT ( 'NONE',  ( 796.9571628226829034, -335.4636090269705733, 321.2382568024804641 ) ) ;
#20572=CARTESIAN_POINT ( 'NONE',  ( 783.7566961878529810, 23.10349461922137237, 305.1792804349288417 ) ) ;
#20577=B_SPLINE_CURVE_WITH_KNOTS ( 'NONE', 3,
 ( #38763, #35050, #20049, #10123, #38522, #34370, #24198, #38305, #13141, #17271, #27218, #2740, #17521, #31127, #20727, #10568, #24417, #31595 ),
 .UNSPECIFIED., .F., .F.,
 ( 4, 2, 2, 2, 2, 2, 2, 2, 4 ),
 ( 0.5000000000000000000, 0.5621992937191080397, 0.6243985874382160794, 0.6865978811573241192, 0.7487971748764321589, 0.8109964685955401986, 0.8731957623146482383, 0.9353950560337562781, 0.9975943497528643178 ),
 .UNSPECIFIED. ) ;
#20578=CARTESIAN_POINT ( 'NONE',  ( 784.0799538623451781, -323.8055962898684470, 364.6971507214555572 ) ) ;
#20580=CARTESIAN_POINT ( 'NONE',  ( 761.4292242960306112, -113.4636090269712554, 323.2154366446414429 ) ) ;
#20581=CARTESIAN_POINT ( 'NONE',  ( 791.9812246680005501, -20.63460265842048003, 361.9419747391813189 ) ) ;
#20585=CARTESIAN_POINT ( 'NONE',  ( 783.7953271457878373, -248.1908817542435202, 375.1787889125761239 ) ) ;
#20587=CARTESIAN_POINT ( 'NONE',  ( 760.5453621957607311, -189.0783235625961822, 323.8424801807151425 ) ) ;
#20590=CARTESIAN_POINT ( 'NONE',  ( 810.7187646348534145, -90.45278447660209054, 356.7737145352016341 ) ) ;
#20591=CARTESIAN_POINT ( 'NONE',  ( 808.9106007788763009, -452.9681489794446065, 335.7521713694408731 ) ) ;
#20594=CARTESIAN_POINT ( 'NONE',  ( 814.8207195650702488, -362.1908817542432644, 336.2433038121456548 ) ) ;
#20596=CARTESIAN_POINT ( 'NONE',  ( 792.3570229623688874, -309.1800572038740711, 373.1304606946836202 ) ) ;
#20600=CARTESIAN_POINT ( 'NONE',  ( 795.1360043628807261, -380.0891481129646650, 360.2193346964456282 ) ) ;
#20601=CARTESIAN_POINT ( 'NONE',  ( 758.4439275373578084, -156.5545181178802636, 353.2243759319684386 ) ) ;
#20604=CARTESIAN_POINT ( 'NONE',  ( 781.2497674668890113, -60.35105083532383219, 375.3608509340180603 ) ) ;
#20605=CARTESIAN_POINT ( 'NONE',  ( 785.3141322388236176, -381.7255117493284615, 364.4286716492789537 ) ) ;
#20608=CARTESIAN_POINT ( 'NONE',  ( 785.3687786644884454, -419.3618753856918033, 315.3201227861279676 ) ) ;
#20612=CARTESIAN_POINT ( 'NONE',  ( 755.0636971347428243, -196.2709662947835909, 341.7834795799807353 ) ) ;
#20613=CARTESIAN_POINT ( 'NONE',  ( 804.4286716492782716, -185.3618753856926844, 345.3141322388244703 ) ) ;
#20616=ORIENTED_EDGE ( 'NONE', *, *, #15287, .T. ) ;
#20617=CARTESIAN_POINT ( 'NONE',  ( 801.9419747391806368, -402.4527844766010389, 351.9812246680014027 ) ) ;
#20621=CARTESIAN_POINT ( 'NONE',  ( 745.7998596910086917, -149.3618753856928265, 332.5602148656461168 ) ) ;
#20628=CARTESIAN_POINT ( 'NONE',  ( 759.2295555964440155, -208.1692326535051905, 353.9708237608231229 ) ) ;
#20636=CARTESIAN_POINT ( 'NONE',  ( 812.3518521366052028, -145.0999726633347677, 326.5853460496235243 ) ) ;
#20644=CARTESIAN_POINT ( 'NONE',  ( 811.3240766477731540, -388.3726999360613945, 355.6651683502462902 ) ) ;
#20645=CARTESIAN_POINT ( 'NONE',  ( 772.4999999999993179, -512.9681489794448908, 309.9999999999998863 ) ) ;
#20651=CARTESIAN_POINT ( 'NONE',  ( 746.4236121716829757, -207.8272453906073451, 328.8385539511384650 ) ) ;
#20653=CARTESIAN_POINT ( 'NONE',  ( 787.4397851343537695, -189.7255117493290300, 374.2001403089903988 ) ) ;
#20656=CARTESIAN_POINT ( 'NONE',  ( 800.0135310231082713, -278.0891481129651197, 325.0180583372163028 ) ) ;
#20657=CARTESIAN_POINT ( 'NONE',  ( 763.8424801807145741, -66.00906357242595845, 320.5453621957614700 ) ) ;
#20661=CARTESIAN_POINT ( 'NONE',  ( 794.1144889064781864, -106.1692326535054889, 360.9840315886528401 ) ) ;
#20662=CARTESIAN_POINT ( 'NONE',  ( 788.8264449731200330, -309.1800572038740711, 363.6646147819171233 ) ) ;
#20666=CARTESIAN_POINT ( 'NONE',  ( 804.6798772138708955, -87.72551174932937101, 334.6312213355107019 ) ) ;
#20669=CARTESIAN_POINT ( 'NONE',  ( 766.5853460496234675, -397.9874144716864066, 372.3518521366060554 ) ) ;
#20671=CARTESIAN_POINT ( 'NONE',  ( 788.7366044899766848, -299.9073299311468759, 316.5762568750059813 ) ) ;
#20675=CARTESIAN_POINT ( 'NONE',  ( 804.9363028652555840, -424.2709662947829088, 338.2165204200192079 ) ) ;
#20676=EDGE_CURVE ( 'NONE', #32443, #11154, #2420, .T. ) ;
#20682=CARTESIAN_POINT ( 'NONE',  ( 803.4237431249931660, -135.1800572038746679, 331.2633955100225194 ) ) ;
#20683=CARTESIAN_POINT ( 'NONE',  ( 761.4292242960306112, -425.4636090269703459, 323.2154366446414429 ) ) ;
#20685=CARTESIAN_POINT ( 'NONE',  ( 759.9999999999992042, -512.9681489794448908, 309.9999999999998863 ) ) ;
#20686=CARTESIAN_POINT ( 'NONE',  ( 815.1787889125755555, -342.8965053807773984, 343.7953271457877804 ) ) ;
#20691=CARTESIAN_POINT ( 'NONE',  ( 786.2694204179717872, -45.28179084515329578, 305.1769319972829067 ) ) ;
#20699=CARTESIAN_POINT ( 'NONE',  ( 763.8424801807145741, -330.0090635724251342, 320.5453621957614700 ) ) ;
#20700=CARTESIAN_POINT ( 'NONE',  ( 754.3581564841646241, -305.4636090269706870, 316.1443688327762516 ) ) ;
#20703=CARTESIAN_POINT ( 'NONE',  ( 773.7305795820266212, -105.2817908451530968, 374.8230680027170365 ) ) ;
#20707=CARTESIAN_POINT ( 'NONE',  ( 757.8323909638827445, -170.6346026584199649, 352.1044303154654358 ) ) ;
#20709=CARTESIAN_POINT ( 'NONE',  ( 812.3518521366052028, -433.0999726633339151, 326.5853460496235243 ) ) ;
#20715=CARTESIAN_POINT ( 'NONE',  ( 756.1443688327750579, 2.376221891948710585, 314.3581564841659315 ) ) ;
#20720=CARTESIAN_POINT ( 'NONE',  ( 744.9990715423526808, -282.3510508353230080, 341.2370466360926002 ) ) ;
#20721=CARTESIAN_POINT ( 'NONE',  ( 771.1735550268780344, -129.1800572038746679, 316.3353852180828198 ) ) ;
#20724=CARTESIAN_POINT ( 'NONE',  ( 755.3201227861273992, -291.7255117493285752, 345.3687786644892981 ) ) ;
#20727=CARTESIAN_POINT ( 'NONE',  ( 789.5207239089294262, -450.4903526743926250, 363.8345956117046285 ) ) ;
#20730=CARTESIAN_POINT ( 'NONE',  ( 771.2633955100217236, -23.90732993114773919, 363.4237431249939618 ) ) ;
#20732=CARTESIAN_POINT ( 'NONE',  ( 787.5162901302840055, -371.3618753856920307, 305.4481719005793252 ) ) ;
#20733=CARTESIAN_POINT ( 'NONE',  ( 808.7758568127978833, -244.1692326535050768, 320.0363995740631822 ) ) ;
#20734=CARTESIAN_POINT ( 'NONE',  ( 815.0009284576459549, -54.35105083532383219, 338.7629533639073429 ) ) ;
#20740=CARTESIAN_POINT ( 'NONE',  ( 774.6858677611749044, -249.7255117493288594, 315.5713283507209894 ) ) ;
#20741=CARTESIAN_POINT ( 'NONE',  ( 782.4968714119720516, -370.8164208402375834, 305.0891759886411023 ) ) ;
#20747=CARTESIAN_POINT ( 'NONE',  ( 759.0159684113467620, -232.9181544815163249, 325.8855110935213020 ) ) ;
#20749=CARTESIAN_POINT ( 'NONE',  ( 758.0580252608178853, -126.4527844766019626, 328.0187753319985404 ) ) ;
#20754=CARTESIAN_POINT ( 'NONE',  ( 799.4546378042377910, -297.0783235625957559, 356.1575198192848006 ) ) ;
#20756=CARTESIAN_POINT ( 'NONE',  ( 750.9282345327678740, -16.91815448151702839, 319.8311093483690115 ) ) ;
#20758=CARTESIAN_POINT ( 'NONE',  ( 755.2512626584698410, -175.5436935675108998, 315.2512626584710915 ) ) ;
#20759=CARTESIAN_POINT ( 'NONE',  ( 755.5713283507202505, -77.36187538569302546, 334.6858677611754729 ) ) ;
#20761=DIRECTION ( 'NONE',  ( 0.000000000000000000, 0.000000000000000000, 1.000000000000000000 ) ) ;
#20765=CARTESIAN_POINT ( 'NONE',  ( 747.6481478633932056, -421.0999726633340288, 353.4146539503763620 ) ) ;
#20768=CARTESIAN_POINT ( 'NONE',  ( 770.0799878456142551, -349.9874144716865771, 362.9823548866085616 ) ) ;
#20769=CARTESIAN_POINT ( 'NONE',  ( 747.2067596250078623, -51.18005720387493085, 352.2312462859687230 ) ) ;
#20772=CARTESIAN_POINT ( 'NONE',  ( 786.6156483768007774, -25.44195992623301450, 315.5913626894246136 ) ) ;
#20775=CARTESIAN_POINT ( 'NONE',  ( 747.3154664389472828, -187.9874144716870603, 326.4474001241230781 ) ) ;
#20776=CARTESIAN_POINT ( 'NONE',  ( 788.7366044899766848, -11.90732993114778182, 316.5762568750059813 ) ) ;
#20777=ORIENTED_EDGE ( 'NONE', *, *, #30930, .F. ) ;
#20780=CARTESIAN_POINT ( 'NONE',  ( 778.1981804954714335, -154.2709662947836478, 314.8072714833589885 ) ) ;
#20782=CARTESIAN_POINT ( 'NONE',  ( 803.4237431249931660, -327.1800572038741279, 331.2633955100225194 ) ) ;
#20783=CARTESIAN_POINT ( 'NONE',  ( 799.9999999999993179, 205.0000000000000568, 339.9999999999999432 ) ) ;
#20785=CARTESIAN_POINT ( 'NONE',  ( 803.2186876482843445, -31.98741447168754348, 350.0220218866286928 ) ) ;
#20787=CARTESIAN_POINT ( 'NONE',  ( 749.2812353651451076, -270.4527844766014937, 323.2262854647983090 ) ) ;
#20788=CARTESIAN_POINT ( 'NONE',  ( 766.0291762391763086, -346.9181544815160123, 360.7704444035551319 ) ) ;
#20789=CARTESIAN_POINT ( 'NONE',  ( 756.7813123517142913, -427.9874144716862929, 329.9779781133712504 ) ) ;
#20794=CARTESIAN_POINT ( 'NONE',  ( 803.2186876482843445, -319.9874144716866340, 350.0220218866286928 ) ) ;
#20796=CARTESIAN_POINT ( 'NONE',  ( 760.7433823573367135, -132.0090635724257595, 355.9930595647440441 ) ) ;
#20797=CARTESIAN_POINT ( 'NONE',  ( 794.9819416627830151, -12.99823902205686821, 319.9864689768909898 ) ) ;
#20800=CARTESIAN_POINT ( 'NONE',  ( 772.4999999999993179, -462.9681489794447202, 270.0000000000000568 ) ) ;
#20801=CARTESIAN_POINT ( 'NONE',  ( 809.0717654672305343, -220.9181544815164102, 360.1688906516309885 ) ) ;
#20802=CARTESIAN_POINT ( 'NONE',  ( 763.2154366446407039, -189.6237781080507148, 321.4292242960311228 ) ) ;
#20806=CARTESIAN_POINT ( 'NONE',  ( 787.4397851343537695, 2.274488250670355871, 374.2001403089903988 ) ) ;
#20807=CARTESIAN_POINT ( 'NONE',  ( 745.7998596910086917, -77.36187538569302546, 332.5602148656461168 ) ) ;
#20809=CARTESIAN_POINT ( 'NONE',  ( 807.4745771775690173, -452.9681489794449476, 340.5093320845589346 ) ) ;
#20812=CARTESIAN_POINT ( 'NONE',  ( 811.3240766477731540, -340.3726999360615082, 355.6651683502462902 ) ) ;
#20814=CARTESIAN_POINT ( 'NONE',  ( 787.5162901302840055, -299.3618753856922581, 305.4481719005792684 ) ) ;
#20818=CARTESIAN_POINT ( 'NONE',  ( 800.2193346964447755, -402.9982390220555430, 355.1360043628815788 ) ) ;
#20819=CARTESIAN_POINT ( 'NONE',  ( 804.8461984189677878, -146.1908817542438896, 336.9566956441385628 ) ) ;
#20822=CARTESIAN_POINT ( 'NONE',  ( 791.1614460488616487, -59.26014174441473870, 373.5763878283158874 ) ) ;
#20823=CARTESIAN_POINT ( 'NONE',  ( 802.1676090361155502, -398.6346026584193396, 327.8955696845344505 ) ) ;
#20824=CARTESIAN_POINT ( 'NONE',  ( 800.9747183278959710, 11.00176097794305541, 311.9810565676471583 ) ) ;
#20826=CARTESIAN_POINT ( 'NONE',  ( 805.1927285166397041, -424.8164208402372992, 341.8018195045277707 ) ) ;
#20828=ORIENTED_EDGE ( 'NONE', *, *, #10242, .F. ) ;
#20831=CARTESIAN_POINT ( 'NONE',  ( 765.0180583372156207, -240.9982390220561683, 360.0135310231089534 ) ) ;
#20832=CARTESIAN_POINT ( 'NONE',  ( 755.0636971347428243, -196.2709662947835909, 341.7834795799807353 ) ) ;
#20838=CARTESIAN_POINT ( 'NONE',  ( 765.0180583372156207, -408.9982390220556567, 360.0135310231089534 ) ) ;
#20842=CARTESIAN_POINT ( 'NONE',  ( 744.7301800767020268, -148.8164208402382656, 337.4774526936615189 ) ) ;
#20849=CARTESIAN_POINT ( 'NONE',  ( 803.2186876482843445, -223.9874144716869182, 350.0220218866286928 ) ) ;
#20850=CARTESIAN_POINT ( 'NONE',  ( 787.4999999999992042, -462.9681489794447202, 270.0000000000000568 ) ) ;
#20851=CYLINDRICAL_SURFACE ( 'NONE', #11044, 10.00000000000000888 ) ;
#20858=CARTESIAN_POINT ( 'NONE',  ( 810.4231160770870019, -144.5545181178802636, 321.9338519418446936 ) ) ;
#20865=CARTESIAN_POINT ( 'NONE',  ( 755.8990559732751535, -371.4636090269705164, 365.9055244015606831 ) ) ;
#20867=PLANE ( 'NONE',  #27638 ) ;
#20874=CARTESIAN_POINT ( 'NONE',  ( 797.8822607201568644, -246.5545181178799510, 370.1134526219340160 ) ) ;
#20876=CARTESIAN_POINT ( 'NONE',  ( 808.3070685750230950, -186.9982390220563104, 361.1904061080339261 ) ) ;
#20879=CARTESIAN_POINT ( 'NONE',  ( 762.1405469898971887, -289.5436935675103882, 357.8594530101015607 ) ) ;
#20880=CARTESIAN_POINT ( 'NONE',  ( 755.8894580844503253, -87.82724539060770041, 332.3691319403863531 ) ) ;
#20885=CARTESIAN_POINT ( 'NONE',  ( 783.0433043558608688, -120.8965053807781800, 315.1538015810313027 ) ) ;
#20886=CARTESIAN_POINT ( 'NONE',  ( 767.8955696845333705, -312.4527844766012663, 362.1676090361162323 ) ) ;
#20889=CARTESIAN_POINT ( 'NONE',  ( 755.0636971347428243, -100.2709662947838609, 341.7834795799807353 ) ) ;
#20892=CARTESIAN_POINT ( 'NONE',  ( 807.5423716828161105, -417.0783235625954148, 362.2119215644372048 ) ) ;
#20894=CARTESIAN_POINT ( 'NONE',  ( 758.0580252608178853, -294.4527844766013800, 328.0187753319985404 ) ) ;
#20898=CARTESIAN_POINT ( 'NONE',  ( 778.1981804954714335, -394.2709662947827951, 314.8072714833589885 ) ) ;
#20900=CIRCLE ( 'NONE', #995, 30.00000000000008171 ) ;
#20905=CARTESIAN_POINT ( 'NONE',  ( 792.1044303154645831, -132.4527844766018916, 317.8323909638837677 ) ) ;
#20906=CARTESIAN_POINT ( 'NONE',  ( 755.1538015810308480, -446.1908817542429802, 343.0433043558613804 ) ) ;
#20907=CARTESIAN_POINT ( 'NONE',  ( 805.1016975059191054, -126.8965053807781516, 343.0745993439771837 ) ) ;
#20908=DIRECTION ( 'NONE',  ( -0.000000000000000000, -1.110223024625155554E-15, 1.000000000000000000 ) ) ;
#20909=DIRECTION ( 'NONE',  ( 0.000000000000000000, 0.000000000000000000, -1.000000000000000000 ) ) ;
#20910=CARTESIAN_POINT ( 'NONE',  ( 814.8230680027162407, -365.8055962898682765, 333.7305795820267917 ) ) ;
#20915=CARTESIAN_POINT ( 'NONE',  ( 771.3260364891663130, -19.64542720878974791, 306.0683387631859773 ) ) ;
#20922=CARTESIAN_POINT ( 'NONE',  ( 799.9999999999993179, -512.9681489794448908, 370.0000000000000000 ) ) ;
#20924=CARTESIAN_POINT ( 'NONE',  ( 790.9844846989617508, -382.3726999360613945, 317.2208543904092721 ) ) ;
#20925=CARTESIAN_POINT ( 'NONE',  ( 786.2694204179717872, -333.2817908451523863, 305.1769319972829067 ) ) ;
#20928=CARTESIAN_POINT ( 'NONE',  ( 768.9521613784389729, -129.8272453906075725, 373.2346286133773106 ) ) ;
#20933=CARTESIAN_POINT ( 'NONE',  ( 797.6776695296629214, -187.5436935675108430, 357.6776695296636603 ) ) ;
#20937=CARTESIAN_POINT ( 'NONE',  ( 764.1737431748507561, -418.3726999360612808, 371.6461892240376415 ) ) ;
#20942=CARTESIAN_POINT ( 'NONE',  ( 771.2368401574024119, 10.55804007376686826, 374.2805881961240857 ) ) ;
#20946=CARTESIAN_POINT ( 'NONE',  ( 754.0944755984390895, -303.6237781080503169, 364.1009440267246760 ) ) ;
#20947=CARTESIAN_POINT ( 'NONE',  ( 803.6646147819162707, -113.9073299311474585, 348.8264449731211130 ) ) ;
#20950=CARTESIAN_POINT ( 'NONE',  ( 755.5713283507202505, -317.3618753856922581, 334.6858677611754729 ) ) ;
#20953=EDGE_CURVE ( 'NONE', #38419, #9771, #26132, .T. ) ;
#20958=CARTESIAN_POINT ( 'NONE',  ( 745.7998596910086917, -365.3618753856920875, 332.5602148656461168 ) ) ;
#20959=CARTESIAN_POINT ( 'NONE',  ( 814.8230680027162407, -245.8055962898686460, 333.7305795820267917 ) ) ;
#20961=CARTESIAN_POINT ( 'NONE',  ( 813.9316612368132837, -79.44195992623286884, 348.6739635108323228 ) ) ;
#20967=CIRCLE ( 'NONE', #27601, 30.00000000000008171 ) ;
#20968=CARTESIAN_POINT ( 'NONE',  ( 771.2633955100217236, -239.9073299311470748, 363.4237431249939618 ) ) ;
#20970=CARTESIAN_POINT ( 'NONE',  ( 804.7487373415286811, -379.5436935675102745, 364.7487373415288516 ) ) ;
#20974=CARTESIAN_POINT ( 'NONE',  ( 799.9999999999993179, 205.0000000000000568, 339.9999999999999432 ) ) ;
#20976=CARTESIAN_POINT ( 'NONE',  ( 783.0745993439762742, -272.1908817542434917, 365.1016975059196739 ) ) ;
#20977=CARTESIAN_POINT ( 'NONE',  ( 778.1981804954714335, -106.2709662947838467, 314.8072714833589885 ) ) ;
#20982=CARTESIAN_POINT ( 'NONE',  ( 787.6308680596127942, -299.2601417444139997, 364.1105419155492768 ) ) ;
#20985=CARTESIAN_POINT ( 'NONE',  ( 752.7379699480933368, -12.00906357242613609, 361.9858362298580232 ) ) ;
#20990=CARTESIAN_POINT ( 'NONE',  ( 792.3570229623688874, -165.1800572038745258, 373.1304606946836202 ) ) ;
#20991=CARTESIAN_POINT ( 'NONE',  ( 778.2165204200184689, -70.81642084023850714, 364.9363028652563230 ) ) ;
#20992=CARTESIAN_POINT ( 'NONE',  ( 755.2512626584698410, 16.45630643248848912, 315.2512626584710915 ) ) ;
#20994=CARTESIAN_POINT ( 'NONE',  ( 773.4516893846965786, 4.354572791210176597, 315.8398074228977066 ) ) ;
#20997=CARTESIAN_POINT ( 'NONE',  ( 790.8726784830453198, -370.7146871989592114, 362.5472867521010585 ) ) ;
#20998=CARTESIAN_POINT ( 'NONE',  ( 777.4774526936600978, -58.27096629478398881, 304.7301800767028226 ) ) ;
#21000=CARTESIAN_POINT ( 'NONE',  ( 773.3843516231979720, -37.44195992623299674, 364.4086373105754433 ) ) ;
#21006=CARTESIAN_POINT ( 'NONE',  ( 811.6461892240364477, -196.7146871989598083, 324.1737431748509835 ) ) ;
#21007=CARTESIAN_POINT ( 'NONE',  ( 788.8264449731201466, -21.18005720387502322, 363.6646147819170665 ) ) ;
#21013=CARTESIAN_POINT ( 'NONE',  ( 754.8072714833581358, -196.8164208402380950, 338.1981804954720587 ) ) ;
#21015=CARTESIAN_POINT ( 'NONE',  ( 755.5713283507202505, -317.3618753856922581, 334.6858677611754729 ) ) ;
#21018=CARTESIAN_POINT ( 'NONE',  ( 790.8726784830453198, -34.71468719896025590, 362.5472867521010585 ) ) ;
#21022=CARTESIAN_POINT ( 'NONE',  ( 804.7487373415286811, -259.5436935675106156, 364.7487373415288516 ) ) ;
#21023=CARTESIAN_POINT ( 'NONE',  ( 759.0159684113467620, -328.9181544815160692, 325.8855110935213020 ) ) ;
#21025=CARTESIAN_POINT ( 'NONE',  ( 803.8651313633788504, -437.2601417444135450, 332.4468031744301015 ) ) ;
#21030=CARTESIAN_POINT ( 'NONE',  ( 815.2698199232961542, -304.8164208402376403, 342.5225473063383106 ) ) ;
#21032=CARTESIAN_POINT ( 'NONE',  ( 805.1016975059191054, -318.8965053807775121, 343.0745993439771837 ) ) ;
#21036=CARTESIAN_POINT ( 'NONE',  ( 766.9102291470427417, -114.5545181178803631, 318.6633372737382501 ) ) ;
#21037=CARTESIAN_POINT ( 'NONE',  ( 764.8639956371174549, -8.089148112965974136, 319.7806653035542013 ) ) ;
#21042=CARTESIAN_POINT ( 'NONE',  ( 788.6739635108323228, -247.6454272087890160, 373.9316612368139090 ) ) ;
#21043=CARTESIAN_POINT ( 'NONE',  ( 803.8651313633788504, -197.2601417444143124, 332.4468031744301015 ) ) ;
#21051=CARTESIAN_POINT ( 'NONE',  ( 792.2312462859673587, -11.90732993114778182, 307.2067596250082602 ) ) ;
#21052=CARTESIAN_POINT ( 'NONE',  ( 792.2312462859673587, -83.90732993114754379, 307.2067596250082602 ) ) ;
#21053=CARTESIAN_POINT ( 'NONE',  ( 801.0087853405226497, -452.9681489794447202, 354.4092604580203556 ) ) ;
#21057=CARTESIAN_POINT ( 'NONE',  ( 768.9521613784389729, -345.8272453906069472, 373.2346286133773106 ) ) ;
#21059=CARTESIAN_POINT ( 'NONE',  ( 748.9653473494363425, -314.6346026584194533, 356.9462024416521331 ) ) ;
#21064=CARTESIAN_POINT ( 'NONE',  ( 755.0636971347428243, -388.2709662947829656, 341.7834795799807353 ) ) ;
#21065=CARTESIAN_POINT ( 'NONE',  ( 793.9708237608222134, -166.9181544815165523, 319.2295555964448681 ) ) ;
#21068=CARTESIAN_POINT ( 'NONE',  ( 761.9338519418445230, -62.53286901714199786, 370.4231160770881957 ) ) ;
#21069=CARTESIAN_POINT ( 'NONE',  ( 804.9363028652555840, -400.2709662947828519, 338.2165204200192079 ) ) ;
#21070=CARTESIAN_POINT ( 'NONE',  ( 815.2698199232962679, 7.183579159761249500, 342.5225473063383674 ) ) ;
#21072=CARTESIAN_POINT ( 'NONE',  ( 813.2346286133761168, -149.2601417444144261, 328.9521613784389160 ) ) ;
#21077=CARTESIAN_POINT ( 'NONE',  ( 771.2633955100217236, -239.9073299311470748, 363.4237431249939618 ) ) ;
#21078=CARTESIAN_POINT ( 'NONE',  ( 797.6776695296629214, -211.5436935675107861, 357.6776695296636603 ) ) ;
#21082=CARTESIAN_POINT ( 'NONE',  ( 800.9747183278959710, 11.00176097794305541, 311.9810565676471583 ) ) ;
#21085=CARTESIAN_POINT ( 'NONE',  ( 759.9864689768902508, -434.0891481129646081, 354.9819416627836404 ) ) ;
#21091=CARTESIAN_POINT ( 'NONE',  ( 745.4481719005789273, -147.7255117493291721, 347.5162901302853697 ) ) ;
#21099=CARTESIAN_POINT ( 'NONE',  ( 759.2295555964440155, -232.1692326535051620, 353.9708237608231229 ) ) ;
#21109=CARTESIAN_POINT ( 'NONE',  ( 811.3240766477731540, -148.3726999360620198, 355.6651683502462902 ) ) ;
#21115=EDGE_CURVE ( 'NONE', #27436, #43717, #28377, .T. ) ;
#21122=CARTESIAN_POINT ( 'NONE',  ( 773.7305795820266212, -249.2817908451526421, 374.8230680027170365 ) ) ;
#21124=CARTESIAN_POINT ( 'NONE',  ( 767.6429770376289525, -225.1800572038743269, 306.8695393053162093 ) ) ;
#21128=CARTESIAN_POINT ( 'NONE',  ( 800.0135310231082713, -302.0891481129650629, 325.0180583372163028 ) ) ;
#21129=CARTESIAN_POINT ( 'NONE',  ( 804.4086373105744769, -97.64542720878949922, 333.3843516231986541 ) ) ;
#21133=CARTESIAN_POINT ( 'NONE',  ( 784.0799538623451781, -107.8055962898691433, 364.6971507214555572 ) ) ;
#21134=CARTESIAN_POINT ( 'NONE',  ( 791.9812246680005501, -332.6346026584195101, 361.9419747391813189 ) ) ;
#21138=CARTESIAN_POINT ( 'NONE',  ( 768.0187753319979720, -104.6346026584202207, 318.0580252608186242 ) ) ;
#21141=CARTESIAN_POINT ( 'NONE',  ( 776.2433038121456548, -420.8965053807772279, 374.8207195650711014 ) ) ;
#21143=CARTESIAN_POINT ( 'NONE',  ( 804.9363028652555840, -304.2709662947832499, 338.2165204200192079 ) ) ;
#21147=CARTESIAN_POINT ( 'NONE',  ( 774.6858677611749044, -393.7255117493283478, 315.5713283507209894 ) ) ;
#21152=CARTESIAN_POINT ( 'NONE',  ( 804.8461984189677878, -434.1908817542430370, 336.9566956441385628 ) ) ;
#21153=CARTESIAN_POINT ( 'NONE',  ( 773.3843516231979720, -109.4419599262327836, 364.4086373105754433 ) ) ;
#21157=CARTESIAN_POINT ( 'NONE',  ( 748.3538107759620743, -400.7146871989590977, 355.8262568251490165 ) ) ;
#21163=CARTESIAN_POINT ( 'NONE',  ( 810.4231160770870019, -24.55451811788064020, 321.9338519418446936 ) ) ;
#21171=DIRECTION ( 'NONE',  ( 0.000000000000000000, 0.000000000000000000, 1.000000000000000000 ) ) ;
#21173=CARTESIAN_POINT ( 'NONE',  ( 759.0159684113467620, -352.9181544815159555, 325.8855110935213020 ) ) ;
#21174=CARTESIAN_POINT ( 'NONE',  ( 797.8822607201568644, -342.5545181178796952, 370.1134526219340160 ) ) ;
#21177=CARTESIAN_POINT ( 'NONE',  ( 779.9999999999992042, -462.9681489794448339, 339.9999999999999432 ) ) ;
#21178=CARTESIAN_POINT ( 'NONE',  ( 813.5763878283155464, -147.8272453906075157, 351.1614460488615350 ) ) ;
#21180=CARTESIAN_POINT ( 'NONE',  ( 772.4837098697144029, -71.36187538569302546, 374.5518280994205611 ) ) ;
#21184=CARTESIAN_POINT ( 'NONE',  ( 756.3353852180819104, -197.9073299311472169, 331.1735550268788302 ) ) ;
#21186=CARTESIAN_POINT ( 'NONE',  ( 781.2370466360911223, -452.7363362996975411, 304.9990715423533629 ) ) ;
#21191=CARTESIAN_POINT ( 'NONE',  ( 814.8230680027162407, 18.19440371013048008, 333.7305795820267917 ) ) ;
#21195=CARTESIAN_POINT ( 'NONE',  ( 751.2241431872005251, -304.1692326535048210, 359.9636004259367610 ) ) ;
#21196=CARTESIAN_POINT ( 'NONE',  ( 797.8594530101009923, -109.5436935675110988, 322.1405469898982119 ) ) ;
#21198=CARTESIAN_POINT ( 'NONE',  ( 771.2633955100217236, -287.9073299311468759, 363.4237431249939618 ) ) ;
#21200=CARTESIAN_POINT ( 'NONE',  ( 782.5225473063383106, -70.27096629478397460, 375.2698199232970637 ) ) ;
#21205=CARTESIAN_POINT ( 'NONE',  ( 755.5713283507202505, -29.36187538569318178, 334.6858677611754729 ) ) ;
#21207=CARTESIAN_POINT ( 'NONE',  ( 777.5031285880264704, -358.8164208402375834, 374.9108240113588408 ) ) ;
#21208=CARTESIAN_POINT ( 'NONE',  ( 791.1614460488616487, -299.2601417444139997, 373.5763878283158874 ) ) ;
#21209=CARTESIAN_POINT ( 'NONE',  ( 745.1769319972822814, -65.80559628986925702, 346.2694204179732083 ) ) ;
#21214=CARTESIAN_POINT ( 'NONE',  ( 797.6776695296629214, -259.5436935675106156, 357.6776695296636603 ) ) ;
#21216=CARTESIAN_POINT ( 'NONE',  ( 772.4837098697144029, -383.3618753856921444, 374.5518280994205611 ) ) ;
#21221=CYLINDRICAL_SURFACE ( 'NONE', #10493, 20.00000000000001776 ) ;
#21222=CARTESIAN_POINT ( 'NONE',  ( 755.1538015810308480, -278.1908817542434917, 343.0433043558613804 ) ) ;
#21223=CARTESIAN_POINT ( 'NONE',  ( 785.3687786644884454, -107.3618753856928976, 315.3201227861279676 ) ) ;
#21227=CARTESIAN_POINT ( 'NONE',  ( 776.9566956441375396, -276.8965053807776258, 364.8461984189686405 ) ) ;
#21230=CARTESIAN_POINT ( 'NONE',  ( 749.5768839229115201, -36.55451811788061178, 358.0661480581553064 ) ) ;
#21232=CARTESIAN_POINT ( 'NONE',  ( 782.4968714119720516, -178.8164208402381519, 305.0891759886411023 ) ) ;
#21233=CARTESIAN_POINT ( 'NONE',  ( 762.1405469898971887, -97.54369356751112718, 357.8594530101015607 ) ) ;
#21235=CARTESIAN_POINT ( 'NONE',  ( 799.9636004259356241, -454.9181544815156713, 311.2241431872006956 ) ) ;
#21238=CARTESIAN_POINT ( 'NONE',  ( 803.2186876482843445, -367.9874144716865203, 350.0220218866286928 ) ) ;
#21239=CARTESIAN_POINT ( 'NONE',  ( 808.3070685750232087, -42.99823902205676518, 361.1904061080339829 ) ) ;
#21241=CARTESIAN_POINT ( 'NONE',  ( 783.0433043558608688, -48.89650538077840025, 315.1538015810313027 ) ) ;
#21244=CARTESIAN_POINT ( 'NONE',  ( 814.8230680027162407, -197.8055962898688733, 333.7305795820267917 ) ) ;
#21245=CARTESIAN_POINT ( 'NONE',  ( 756.3353852180820240, -29.90732993114772142, 331.1735550268787733 ) ) ;
#21246=CARTESIAN_POINT ( 'NONE',  ( 770.0799878456142551, -373.9874144716864066, 362.9823548866085616 ) ) ;
#21249=CARTESIAN_POINT ( 'NONE',  ( 755.3201227861273992, -195.7255117493289731, 345.3687786644892981 ) ) ;
#21252=CARTESIAN_POINT ( 'NONE',  ( 762.3223304703356007, -319.5436935675104451, 322.3223304703362828 ) ) ;
#21255=CARTESIAN_POINT ( 'NONE',  ( 775.9200461376533440, -47.80559628986931386, 315.3028492785443291 ) ) ;
#21259=CARTESIAN_POINT ( 'NONE',  ( 800.9747183278959710, -252.9982390220560831, 311.9810565676471583 ) ) ;
#21260=CARTESIAN_POINT ( 'NONE',  ( 786.2056067578752163, 12.19440371013049784, 374.4686193811670023 ) ) ;
#21265=CARTESIAN_POINT ( 'NONE',  ( 805.0032342141412300, -301.5436935675105588, 314.9967657858571783 ) ) ;
#21267=CARTESIAN_POINT ( 'NONE',  ( 801.3366627262608972, -320.5328690171411949, 353.0897708529566899 ) ) ;
#21269=CARTESIAN_POINT ( 'NONE',  ( 755.5913626894240451, -157.6454272087893287, 346.6156483768012890 ) ) ;
#21270=CARTESIAN_POINT ( 'NONE',  ( 765.0180583372156207, -0.9982390220569063999, 360.0135310231089534 ) ) ;
#21275=CARTESIAN_POINT ( 'NONE',  ( 764.1737431748507561, -226.3726999360617924, 371.6461892240376415 ) ) ;
#21276=CARTESIAN_POINT ( 'NONE',  ( 795.9930595647434757, -171.0783235625962106, 320.7433823573372820 ) ) ;
#21279=CARTESIAN_POINT ( 'NONE',  ( 802.9823548866075953, -457.0999726633339151, 330.0799878456151077 ) ) ;
#21282=CARTESIAN_POINT ( 'NONE',  ( 745.7998596910086917, -5.361875385693257279, 332.5602148656461168 ) ) ;
#21283=CARTESIAN_POINT ( 'NONE',  ( 808.3070685750230950, -66.99823902205672255, 361.1904061080339261 ) ) ;
#21288=CARTESIAN_POINT ( 'NONE',  ( 783.7953271457878373, -344.1908817542433212, 375.1787889125761239 ) ) ;
#21290=CARTESIAN_POINT ( 'NONE',  ( 767.6429770376289525, -321.1800572038740142, 306.8695393053162093 ) ) ;
#21294=CARTESIAN_POINT ( 'NONE',  ( 802.1676090361156639, -422.6346026584192259, 327.8955696845344505 ) ) ;
#21295=CARTESIAN_POINT ( 'NONE',  ( 793.0897708529556667, -198.5545181178800647, 361.3366627262616362 ) ) ;
#21298=CARTESIAN_POINT ( 'NONE',  ( 746.0683387631852383, -115.4419599262327409, 331.3260364891676204 ) ) ;
#21299=CARTESIAN_POINT ( 'NONE',  ( 768.0187753319979720, -416.6346026584192259, 318.0580252608186242 ) ) ;
#21307=CARTESIAN_POINT ( 'NONE',  ( 802.1676090361156639, -230.6346026584197659, 327.8955696845344505 ) ) ;
#21308=CARTESIAN_POINT ( 'NONE',  ( 758.0580252608178853, -222.4527844766016642, 328.0187753319985404 ) ) ;
#21313=CARTESIAN_POINT ( 'NONE',  ( 767.8955696845333705, -432.4527844766008684, 362.1676090361162323 ) ) ;
#21316=ADVANCED_FACE ( 'NONE', ( #19239 ), #19459, .T. ) ;
#21318=CARTESIAN_POINT ( 'NONE',  ( 813.1304606946831655, -161.9073299311472738, 352.3570229623691716 ) ) ;
#21325=CARTESIAN_POINT ( 'NONE',  ( 779.4709603349208464, -240.3510508353232069, 314.7162404726379918 ) ) ;
#21334=CARTESIAN_POINT ( 'NONE',  ( 788.6739635108323228, -127.6454272087894140, 373.9316612368139090 ) ) ;
#21341=CARTESIAN_POINT ( 'NONE',  ( 797.8822607201568644, -390.5545181178794678, 370.1134526219340160 ) ) ;
#21346=CARTESIAN_POINT ( 'NONE',  ( 797.6776695296629214, -19.54369356751139364, 357.6776695296636603 ) ) ;
#21347=CARTESIAN_POINT ( 'NONE',  ( 795.8262568251477660, -238.3726999360617640, 308.3538107759623585 ) ) ;
#21349=CARTESIAN_POINT ( 'NONE',  ( 763.2262854647970016, -224.6346026584198228, 309.2812353651462445 ) ) ;
#21352=CARTESIAN_POINT ( 'NONE',  ( 764.8639956371174549, -320.0891481129648355, 319.7806653035542013 ) ) ;
#21353=CARTESIAN_POINT ( 'NONE',  ( 783.0745993439762742, -80.19088175424411702, 365.1016975059196739 ) ) ;
#21354=CARTESIAN_POINT ( 'NONE',  ( 755.3028492785439312, -63.28179084515324604, 335.9200461376539693 ) ) ;
#21359=CARTESIAN_POINT ( 'NONE',  ( 779.9999999999992042, 126.4563064324884465, 339.9999999999999432 ) ) ;
#21360=CARTESIAN_POINT ( 'NONE',  ( 758.6633372737375112, -116.5328690171418202, 326.9102291470432533 ) ) ;
#21361=CARTESIAN_POINT ( 'NONE',  ( 765.0180583372156207, -360.9982390220557704, 360.0135310231089534 ) ) ;
#21366=CARTESIAN_POINT ( 'NONE',  ( 768.0187753319979720, -80.63460265842029173, 318.0580252608186242 ) ) ;
#21369=CARTESIAN_POINT ( 'NONE',  ( 771.2368401574024119, -421.4419599262317888, 374.2805881961240857 ) ) ;
#21371=CARTESIAN_POINT ( 'NONE',  ( 757.8323909638827445, -314.6346026584194533, 352.1044303154654358 ) ) ;
#21375=CARTESIAN_POINT ( 'NONE',  ( 781.7834795799800531, -418.8164208402374129, 315.0636971347436202 ) ) ;
#21381=ORIENTED_EDGE ( 'NONE', *, *, #31752, .T. ) ;
#21383=CARTESIAN_POINT ( 'NONE',  ( 765.0180583372156207, -120.9982390220565378, 360.0135310231089534 ) ) ;
#21384=CARTESIAN_POINT ( 'NONE',  ( 801.5560724626406000, -432.5545181178793541, 326.7756240680316182 ) ) ;
#21385=CARTESIAN_POINT ( 'NONE',  ( 796.7845633553578182, -129.6237781080508853, 358.5707757039688204 ) ) ;
#21388=CARTESIAN_POINT ( 'NONE',  ( 745.1769319972822814, -401.8055962898681059, 346.2694204179732083 ) ) ;
#21393=CARTESIAN_POINT ( 'NONE',  ( 757.7880784355613741, -18.00906357242611477, 312.4576283171834916 ) ) ;
#21394=CARTESIAN_POINT ( 'NONE',  ( 779.9999999999992042, 16.45630643248849267, 329.9999999999999432 ) ) ;
#21400=CARTESIAN_POINT ( 'NONE',  ( 757.4527132478984868, -352.3726999360614514, 329.1273215169538844 ) ) ;
#21401=CARTESIAN_POINT ( 'NONE',  ( 811.3240766477731540, -340.3726999360615082, 355.6651683502462902 ) ) ;
#21405=CARTESIAN_POINT ( 'NONE',  ( 747.6481478633932056, -133.0999726633348246, 353.4146539503763620 ) ) ;
#21407=CARTESIAN_POINT ( 'NONE',  ( 754.9967657858570647, -121.5436935675110419, 365.0032342141425374 ) ) ;
#21411=CARTESIAN_POINT ( 'NONE',  ( 762.1405469898971887, -169.5436935675108430, 357.8594530101015607 ) ) ;
#21412=CARTESIAN_POINT ( 'NONE',  ( 748.6759233522253680, -448.3726999360611103, 324.3348316497537098 ) ) ;
#21416=CARTESIAN_POINT ( 'NONE',  ( 758.0141637701419768, 8.921676437403235127, 367.2620300519063790 ) ) ;
#21421=CARTESIAN_POINT ( 'NONE',  ( 783.7566961878529810, -312.8965053807775689, 305.1792804349288417 ) ) ;
#21422=CARTESIAN_POINT ( 'NONE',  ( 762.1405469898973024, -121.5436935675110561, 357.8594530101016176 ) ) ;
#21424=CARTESIAN_POINT ( 'NONE',  ( 781.7834795799800531, -298.8164208402377540, 315.0636971347436202 ) ) ;
#21426=CARTESIAN_POINT ( 'NONE',  ( 787.4397851343537695, -69.72551174932942786, 374.2001403089903988 ) ) ;
#21431=CARTESIAN_POINT ( 'NONE',  ( 774.6858677611749044, -33.72551174932952733, 315.5713283507209894 ) ) ;
#21433=CARTESIAN_POINT ( 'NONE',  ( 808.3070685750232087, -402.9982390220555999, 361.1904061080339829 ) ) ;
#21434=CARTESIAN_POINT ( 'NONE',  ( 813.9316612368132837, -295.4419599262320730, 348.6739635108323228 ) ) ;
#21435=CARTESIAN_POINT ( 'NONE',  ( 758.0141637701419768, -87.07832356259646645, 367.2620300519063790 ) ) ;
#21441=CARTESIAN_POINT ( 'NONE',  ( 810.7187646348534145, -402.4527844766010389, 356.7737145352016341 ) ) ;
#21443=LINE ( 'NONE', #3895, #35163 ) ;
#21447=CARTESIAN_POINT ( 'NONE',  ( 775.8780910478218402, -273.2817908451526137, 364.9511171171680530 ) ) ;
#21448=CARTESIAN_POINT ( 'NONE',  ( 804.9363028652555840, -160.2709662947836762, 338.2165204200192079 ) ) ;
#21452=CARTESIAN_POINT ( 'NONE',  ( 793.2243759319678702, -290.5328690171412518, 318.4439275373583200 ) ) ;
#21454=CARTESIAN_POINT ( 'NONE',  ( 752.7379699480933368, -36.00906357242605793, 361.9858362298580232 ) ) ;
#21456=CARTESIAN_POINT ( 'NONE',  ( 747.2067596250078623, -195.1800572038744974, 352.2312462859687230 ) ) ;
#21457=CARTESIAN_POINT ( 'NONE',  ( 764.8639956371174549, -80.08914811296574499, 319.7806653035542013 ) ) ;
#21458=LINE ( 'NONE', #42708, #29167 ) ;
#21460=CARTESIAN_POINT ( 'NONE',  ( 750.9282345327678740, -448.9181544815156144, 319.8311093483690115 ) ) ;
#21463=CARTESIAN_POINT ( 'NONE',  ( 794.1144889064781864, -346.1692326535047641, 360.9840315886528401 ) ) ;
#21464=CARTESIAN_POINT ( 'NONE',  ( 796.7737145352015204, -44.63460265842040542, 370.7187646348536987 ) ) ;
#21466=CARTESIAN_POINT ( 'NONE',  ( 756.1348686366196716, -65.26014174441471027, 347.5531968255698416 ) ) ;
#21468=CARTESIAN_POINT ( 'NONE',  ( 764.3348316497523456, -214.7146871989597230, 308.6759233522265617 ) ) ;
#21469=CARTESIAN_POINT ( 'NONE',  ( 785.3141322388236176, -21.72551174932956641, 364.4286716492789537 ) ) ;
#21472=CARTESIAN_POINT ( 'NONE',  ( 785.3687786644884454, -203.3618753856925991, 315.3201227861279676 ) ) ;
#21475=CARTESIAN_POINT ( 'NONE',  ( 805.1927285166399315, -328.8164208402375834, 341.8018195045277707 ) ) ;
#21479=CARTESIAN_POINT ( 'NONE',  ( 801.3366627262608972, -56.53286901714201917, 353.0897708529566899 ) ) ;
#21481=CARTESIAN_POINT ( 'NONE',  ( 759.0252816721024374, -288.9982390220559978, 368.0189434323527280 ) ) ;
#21482=CARTESIAN_POINT ( 'NONE',  ( 764.3348316497523456, 1.285312801039623753, 308.6759233522265617 ) ) ;
#21488=CARTESIAN_POINT ( 'NONE',  ( 759.0252816721024374, -288.9982390220559978, 368.0189434323527280 ) ) ;
#21489=CARTESIAN_POINT ( 'NONE',  ( 806.6271908675616942, -455.4127378225107350, 353.8200110890837777 ) ) ;
#21490=CARTESIAN_POINT ( 'NONE',  ( 757.2208543904082489, -328.7146871989592682, 350.9844846989624330 ) ) ;
#21492=CARTESIAN_POINT ( 'NONE',  ( 804.8461984189677878, -170.1908817542438328, 336.9566956441385628 ) ) ;
#21493=CARTESIAN_POINT ( 'NONE',  ( 765.0180583372156207, -24.99823902205683268, 360.0135310231089534 ) ) ;
#21497=CARTESIAN_POINT ( 'NONE',  ( 786.2694204179717872, -285.2817908451526137, 305.1769319972829067 ) ) ;
#21498=CARTESIAN_POINT ( 'NONE',  ( 758.6633372737375112, -188.5328690171416497, 326.9102291470432533 ) ) ;
#21500=CARTESIAN_POINT ( 'NONE',  ( 792.1044303154645831, 11.54721552339760038, 317.8323909638837677 ) ) ;
#21503=CARTESIAN_POINT ( 'NONE',  ( 814.5518280994195948, -15.72551174932958951, 332.4837098697145734 ) ) ;
#21504=CARTESIAN_POINT ( 'NONE',  ( 811.0346526505616112, -86.63460265842023489, 323.0537975583477532 ) ) ;
#21507=CARTESIAN_POINT ( 'NONE',  ( 779.9999999999992042, -452.9681489794448339, 350.0000000000000000 ) ) ;
#21508=CARTESIAN_POINT ( 'NONE',  ( 755.8990559732751535, -371.4636090269705164, 365.9055244015606831 ) ) ;
#21510=CARTESIAN_POINT ( 'NONE',  ( 777.5031285880264704, -334.8164208402376403, 374.9108240113588408 ) ) ;
#21515=CARTESIAN_POINT ( 'NONE',  ( 778.1981804954714335, -418.2709662947827383, 314.8072714833589885 ) ) ;
#21518=CARTESIAN_POINT ( 'NONE',  ( 799.2566176426618085, -192.0090635724255606, 324.0069404352559559 ) ) ;
#21521=CARTESIAN_POINT ( 'NONE',  ( 747.3154664389472828, -91.98741447168737295, 326.4474001241230781 ) ) ;
#21522=CARTESIAN_POINT ( 'NONE',  ( 754.8072714833583632, -412.8164208402373561, 338.1981804954721156 ) ) ;
#21523=CARTESIAN_POINT ( 'NONE',  ( 812.6845335610512393, -151.9874144716871740, 353.5525998758768651 ) ) ;
#21528=CARTESIAN_POINT ( 'NONE',  ( 768.0187753319979720, -224.6346026584198228, 318.0580252608186242 ) ) ;
#21529=CARTESIAN_POINT ( 'NONE',  ( 788.8264449731201466, -237.1800572038742985, 363.6646147819170665 ) ) ;
#21533=CARTESIAN_POINT ( 'NONE',  ( 788.7366044899766848, -419.9073299311465348, 316.5762568750059813 ) ) ;
#21536=CARTESIAN_POINT ( 'NONE',  ( 767.7687537140311633, -167.9073299311473022, 372.7932403749916830 ) ) ;
#21537=CARTESIAN_POINT ( 'NONE',  ( 804.6971507214547046, -267.2817908451526137, 344.0799538623459739 ) ) ;
#21538=ORIENTED_EDGE ( 'NONE', *, *, #33417, .T. ) ;
#21544=CARTESIAN_POINT ( 'NONE',  ( 798.7617431975189675, -219.6237781080506295, 323.0428371773161871 ) ) ;
#21554=CARTESIAN_POINT ( 'NONE',  ( 746.4236121716829757, -135.8272453906076009, 328.8385539511384650 ) ) ;
#21560=CARTESIAN_POINT ( 'NONE',  ( 757.7880784355613741, -378.0090635724250774, 312.4576283171834916 ) ) ;
#21565=CARTESIAN_POINT ( 'NONE',  ( 791.9812246680005501, 3.365397341579444479, 361.9419747391813189 ) ) ;
#21566=CARTESIAN_POINT ( 'NONE',  ( 804.1009440267234822, -239.4636090269709143, 314.0944755984392600 ) ) ;
#21568=CARTESIAN_POINT ( 'NONE',  ( 810.7187646348534145, -234.4527844766016358, 356.7737145352016341 ) ) ;
#21573=CARTESIAN_POINT ( 'NONE',  ( 756.5762568750052424, -315.1800572038740711, 348.7366044899774238 ) ) ;
#21574=CARTESIAN_POINT ( 'NONE',  ( 799.2566176426618085, -96.00906357242585898, 324.0069404352559559 ) ) ;
#21575=CARTESIAN_POINT ( 'NONE',  ( 757.0176451133909268, -85.09997266333499510, 349.9200121543848354 ) ) ;
#21578=CARTESIAN_POINT ( 'NONE',  ( 779.9999999999992042, -452.9681489794448339, 329.9999999999999432 ) ) ;
#21579=CARTESIAN_POINT ( 'NONE',  ( 757.2208543904082489, -160.7146871989598651, 350.9844846989624330 ) ) ;
#21580=CARTESIAN_POINT ( 'NONE',  ( 792.1044303154645831, -348.4527844766012663, 317.8323909638837677 ) ) ;
#21583=CARTESIAN_POINT ( 'NONE',  ( 756.5762568750052424, -123.1800572038747106, 348.7366044899774238 ) ) ;
#21587=CARTESIAN_POINT ( 'NONE',  ( 744.9990715423526808, -402.3510508353228374, 341.2370466360926002 ) ) ;
#21590=CARTESIAN_POINT ( 'NONE',  ( 804.9363028652555840, -328.2709662947831362, 338.2165204200192079 ) ) ;
#21595=CARTESIAN_POINT ( 'NONE',  ( 758.0580252608178853, -414.4527844766010389, 328.0187753319985404 ) ) ;
#21602=CARTESIAN_POINT ( 'NONE',  ( 776.9254006560222479, -452.1908817542428665, 314.8983024940802125 ) ) ;
#21603=CARTESIAN_POINT ( 'NONE',  ( 769.1273215169530886, -142.7146871989599219, 317.4527132478988847 ) ) ;
#21606=CARTESIAN_POINT ( 'NONE',  ( 808.7758568127978833, -388.1692326535045936, 320.0363995740631822 ) ) ;
#21612=CARTESIAN_POINT ( 'NONE',  ( 752.7379699480933368, -36.00906357242605793, 361.9858362298580232 ) ) ;
#21620=CARTESIAN_POINT ( 'NONE',  ( 779.9999999999992042, -462.9681489794448339, 339.9999999999999432 ) ) ;
#21621=CARTESIAN_POINT ( 'NONE',  ( 761.4292242960306112, -377.4636090269704596, 323.2154366446414429 ) ) ;
#21623=CARTESIAN_POINT ( 'NONE',  ( 762.1177392798416577, -330.5545181178796952, 309.8865473780659272 ) ) ;
#21627=CARTESIAN_POINT ( 'NONE',  ( 754.3581564841646241, -137.4636090269711985, 316.1443688327762516 ) ) ;
#21629=CARTESIAN_POINT ( 'NONE',  ( 758.8095938919642549, -104.0891481129656881, 311.6929314249763365 ) ) ;
#21634=CARTESIAN_POINT ( 'NONE',  ( 804.9363028652555840, -208.2709662947835341, 338.2165204200192079 ) ) ;
#21635=CARTESIAN_POINT ( 'NONE',  ( 805.6418435158337843, -461.4636090269701754, 363.8556311672236916 ) ) ;
#21638=CARTESIAN_POINT ( 'NONE',  ( 815.1787889125755555, 17.10349461922139369, 343.7953271457877804 ) ) ;
#21641=CARTESIAN_POINT ( 'NONE',  ( 785.3687786644884454, -35.36187538569316047, 315.3201227861279676 ) ) ;
#21644=CARTESIAN_POINT ( 'NONE',  ( 764.3348316497523456, -310.7146871989593251, 308.6759233522265617 ) ) ;
#21645=CARTESIAN_POINT ( 'NONE',  ( 797.6776695296629214, -163.5436935675109567, 357.6776695296636603 ) ) ;
#21648=CARTESIAN_POINT ( 'NONE',  ( 804.6798772138708955, -303.7255117493287457, 334.6312213355107019 ) ) ;
#21650=CARTESIAN_POINT ( 'NONE',  ( 767.6429770376291799, -81.18005720387482427, 306.8695393053162093 ) ) ;
#21651=ORIENTED_EDGE ( 'NONE', *, *, #14268, .F. ) ;
#21656=CARTESIAN_POINT ( 'NONE',  ( 804.4286716492782716, -65.36187538569306810, 345.3141322388244703 ) ) ;
#21658=CARTESIAN_POINT ( 'NONE',  ( 772.4837098697145166, -383.3618753856920875, 374.5518280994205611 ) ) ;
#21659=CARTESIAN_POINT ( 'NONE',  ( 786.2056067578752163, -299.8055962898685038, 374.4686193811670023 ) ) ;
#21660=CARTESIAN_POINT ( 'NONE',  ( 812.6845335610512393, -55.98741447168748664, 353.5525998758768651 ) ) ;
#21663=CARTESIAN_POINT ( 'NONE',  ( 799.9999999999993179, -512.9681489794448908, 370.0000000000000000 ) ) ;
#21665=CARTESIAN_POINT ( 'NONE',  ( 810.7187646348534145, -378.4527844766011526, 356.7737145352016341 ) ) ;
#21671=CARTESIAN_POINT ( 'NONE',  ( 769.9779781133707957, -259.0999726633343698, 316.7813123517150871 ) ) ;
#21672=CARTESIAN_POINT ( 'NONE',  ( 762.1405469898971887, -169.5436935675108430, 357.8594530101015607 ) ) ;
#21678=CARTESIAN_POINT ( 'NONE',  ( 805.1016975059191054, -342.8965053807773984, 343.0745993439771837 ) ) ;
#21680=CARTESIAN_POINT ( 'NONE',  ( 783.7953271457878373, -32.19088175424425913, 375.1787889125761239 ) ) ;
#21682=CARTESIAN_POINT ( 'NONE',  ( 758.8095938919642549, -200.0891481129653187, 311.6929314249763365 ) ) ;
#21683=CARTESIAN_POINT ( 'NONE',  ( 756.5762568750052424, -99.18005720387478164, 348.7366044899774238 ) ) ;
#21686=CARTESIAN_POINT ( 'NONE',  ( 755.8990559732751535, -443.4636090269702322, 365.9055244015606831 ) ) ;
#21689=CARTESIAN_POINT ( 'NONE',  ( 754.8983024940795303, -378.8965053807772847, 336.9254006560228163 ) ) ;
#21690=CARTESIAN_POINT ( 'NONE',  ( 755.2512626584698410, -55.54369356751127640, 315.2512626584710915 ) ) ;
#21692=CARTESIAN_POINT ( 'NONE',  ( 801.3366627262608972, -56.53286901714201917, 353.0897708529566899 ) ) ;
#21694=CARTESIAN_POINT ( 'NONE',  ( 788.7631598425961101, -193.4419599262325278, 305.7194118038759143 ) ) ;
#21695=CARTESIAN_POINT ( 'NONE',  ( 797.6776695296629214, -19.54369356751139364, 357.6776695296636603 ) ) ;
#21698=CARTESIAN_POINT ( 'NONE',  ( 759.7806653035534055, -198.9982390220562252, 324.8639956371180801 ) ) ;
#21700=CARTESIAN_POINT ( 'NONE',  ( 801.9419747391806368, -330.4527844766013231, 351.9812246680014027 ) ) ;
#21705=VERTEX_POINT ( 'NONE', #12601 ) ;
#21706=CARTESIAN_POINT ( 'NONE',  ( 794.1144889064781864, -34.16923265350572336, 360.9840315886528401 ) ) ;
#21708=CARTESIAN_POINT ( 'NONE',  ( 745.7998596910086917, -293.3618753856923718, 332.5602148656461168 ) ) ;
#21709=CARTESIAN_POINT ( 'NONE',  ( 803.8556311672234642, -9.623778108051251223, 365.6418435158340117 ) ) ;
#21715=CARTESIAN_POINT ( 'NONE',  ( 782.4968714119720516, -298.8164208402377540, 305.0891759886411023 ) ) ;
#21718=CARTESIAN_POINT ( 'NONE',  ( 780.5236548040995785, -212.7363362996982232, 314.9735926884559944 ) ) ;
#21721=CARTESIAN_POINT ( 'NONE',  ( 805.2837595273609850, -146.7363362996984506, 340.5290396650784714 ) ) ;
#21722=CARTESIAN_POINT ( 'NONE',  ( 778.2165204200184689, -46.81642084023858530, 364.9363028652563230 ) ) ;
#21726=CARTESIAN_POINT ( 'NONE',  ( 747.6481478633932056, -253.0999726633345119, 353.4146539503763620 ) ) ;
#21727=CARTESIAN_POINT ( 'NONE',  ( 757.2208543904082489, -232.7146871989596377, 350.9844846989624330 ) ) ;
#21730=CARTESIAN_POINT ( 'NONE',  ( 755.0636971347428243, -4.270966294784170003, 341.7834795799807353 ) ) ;
#21732=CARTESIAN_POINT ( 'NONE',  ( 759.0252816721024374, -24.99823902205683268, 368.0189434323527280 ) ) ;
#21733=CARTESIAN_POINT ( 'NONE',  ( 805.0032342141412300, -109.5436935675110988, 314.9967657858571783 ) ) ;
#21738=CARTESIAN_POINT ( 'NONE',  ( 814.4686193811664907, -387.2817908451522726, 346.2056067578752732 ) ) ;
#21740=CARTESIAN_POINT ( 'NONE',  ( 749.2812353651451076, -342.4527844766013231, 323.2262854647983090 ) ) ;
#21744=CARTESIAN_POINT ( 'NONE',  ( 781.7834795799800531, -442.8164208402372992, 315.0636971347436202 ) ) ;
#21746=CARTESIAN_POINT ( 'NONE',  ( 754.7162404726377645, -182.7363362996983369, 339.4709603349214717 ) ) ;
#21749=CARTESIAN_POINT ( 'NONE',  ( 781.2497674668890113, -108.3510508353236759, 375.3608509340180603 ) ) ;
#21750=CARTESIAN_POINT ( 'NONE',  ( 788.8264449731201466, -405.1800572038737869, 363.6646147819170665 ) ) ;
#21752=CARTESIAN_POINT ( 'NONE',  ( 811.6461892240364477, -148.7146871989598935, 324.1737431748509835 ) ) ;
#21759=CARTESIAN_POINT ( 'NONE',  ( 800.2193346964447755, -210.9982390220561967, 355.1360043628815788 ) ) ;
#21760=CARTESIAN_POINT ( 'NONE',  ( 800.0135310231082713, -230.0891481129652618, 325.0180583372163028 ) ) ;
#21764=CARTESIAN_POINT ( 'NONE',  ( 755.3201227861273992, -411.7255117493282910, 345.3687786644892981 ) ) ;
#21767=CARTESIAN_POINT ( 'NONE',  ( 792.3570229623691148, -189.1800572038744690, 373.1304606946836770 ) ) ;
#21769=CARTESIAN_POINT ( 'NONE',  ( 779.4763451958990572, -248.7363362996981380, 365.0264073115438919 ) ) ;
#21778=CARTESIAN_POINT ( 'NONE',  ( 805.0264073115434940, -246.3510508353232638, 339.4763451958999099 ) ) ;
#21786=CARTESIAN_POINT ( 'NONE',  ( 749.5768839229115201, -156.5545181178802636, 358.0661480581553064 ) ) ;
#21797=CARTESIAN_POINT ( 'NONE',  ( 792.1044303154645831, -12.45278447660232146, 317.8323909638837677 ) ) ;
#21798=CARTESIAN_POINT ( 'NONE',  ( 755.8990559732751535, -251.4636090269709143, 365.9055244015606831 ) ) ;
#21800=CARTESIAN_POINT ( 'NONE',  ( 767.7687537140311633, -215.9073299311471317, 372.7932403749916830 ) ) ;
#21803=CARTESIAN_POINT ( 'NONE',  ( 802.1676090361156639, -326.6346026584193396, 327.8955696845344505 ) ) ;
#21804=CARTESIAN_POINT ( 'NONE',  ( 763.0428371773158460, -83.46360902697136908, 358.7617431975195359 ) ) ;
#21809=CARTESIAN_POINT ( 'NONE',  ( 804.9511171171677688, -149.8055962898689870, 335.8780910478229202 ) ) ;
#21810=CARTESIAN_POINT ( 'NONE',  ( 774.6858677611749044, -369.7255117493284615, 315.5713283507209894 ) ) ;
#21815=CARTESIAN_POINT ( 'NONE',  ( 778.2165204200184689, -142.8164208402382656, 364.9363028652563230 ) ) ;
#21818=CARTESIAN_POINT ( 'NONE',  ( 763.2262854647970016, 15.36539734157940629, 309.2812353651462445 ) ) ;
#21820=CARTESIAN_POINT ( 'NONE',  ( 759.9864689768902508, -338.0891481129649492, 354.9819416627836404 ) ) ;
#21822=CARTESIAN_POINT ( 'NONE',  ( 805.1927285166397041, -448.8164208402371855, 341.8018195045277707 ) ) ;
#21828=VERTEX_POINT ( 'NONE', #41012 ) ;
#21830=CARTESIAN_POINT ( 'NONE',  ( 802.9823548866075953, -457.0999726633339151, 330.0799878456151077 ) ) ;
#21831=CARTESIAN_POINT ( 'NONE',  ( 815.2698199232961542, -232.8164208402379245, 342.5225473063383106 ) ) ;
#21832=CARTESIAN_POINT ( 'NONE',  ( 755.8398074228967971, -139.4419599262326699, 333.4516893846970333 ) ) ;
#21835=CARTESIAN_POINT ( 'NONE',  ( 749.8865473780648472, -380.5328690171409676, 322.1177392798429082 ) ) ;
#21841=CARTESIAN_POINT ( 'NONE',  ( 793.5525998758768083, -55.09997266333508747, 372.6845335610516941 ) ) ;
#21842=VECTOR ( 'NONE', #34501, 1000.000000000000000 ) ;
#21852=CARTESIAN_POINT ( 'NONE',  ( 757.0176451133909268, -373.0999726633340856, 349.9200121543848354 ) ) ;
#21853=CARTESIAN_POINT ( 'NONE',  ( 754.3581564841646241, -353.4636090269705733, 316.1443688327762516 ) ) ;
#21859=CARTESIAN_POINT ( 'NONE',  ( 745.7194118038753459, -133.6454272087893571, 348.7631598425976449 ) ) ;
#21862=CARTESIAN_POINT ( 'NONE',  ( 811.0346526505616112, -110.6346026584201638, 323.0537975583477532 ) ) ;
#21868=CARTESIAN_POINT ( 'NONE',  ( 785.3141322388236176, -213.7255117493289731, 364.4286716492789537 ) ) ;
#21869=CARTESIAN_POINT ( 'NONE',  ( 795.8262568251477660, -454.3726999360611103, 308.3538107759623585 ) ) ;
#21873=CARTESIAN_POINT ( 'NONE',  ( 815.0009284576459549, -30.35105083532391390, 338.7629533639073429 ) ) ;
#21876=CARTESIAN_POINT ( 'NONE',  ( 803.6646147819161570, -41.90732993114767169, 348.8264449731210561 ) ) ;
#21879=CARTESIAN_POINT ( 'NONE',  ( 813.2346286133761168, -317.2601417444139429, 328.9521613784389160 ) ) ;
#21880=CARTESIAN_POINT ( 'NONE',  ( 778.1981804954715471, -154.2709662947836762, 314.8072714833591021 ) ) ;
#21884=CARTESIAN_POINT ( 'NONE',  ( 804.9363028652555840, -328.2709662947831362, 338.2165204200192079 ) ) ;
#21889=CARTESIAN_POINT ( 'NONE',  ( 777.5031285880264704, -94.81642084023843609, 374.9108240113588408 ) ) ;
#21895=CARTESIAN_POINT ( 'NONE',  ( 781.8018195045266339, -46.27096629478404566, 365.1927285166406705 ) ) ;
#21896=CARTESIAN_POINT ( 'NONE',  ( 805.2837595273609850, -386.7363362996977116, 340.5290396650784714 ) ) ;
#21899=CARTESIAN_POINT ( 'NONE',  ( 814.5518280994195948, -399.7255117493283478, 332.4837098697145166 ) ) ;
#21900=CARTESIAN_POINT ( 'NONE',  ( 752.4576283171824116, -285.0783235625958127, 317.7880784355627952 ) ) ;
#21902=CARTESIAN_POINT ( 'NONE',  ( 813.9316612368132837, -55.44195992623293989, 348.6739635108323228 ) ) ;
#21907=ORIENTED_EDGE ( 'NONE', *, *, #2430, .F. ) ;
#21908=CARTESIAN_POINT ( 'NONE',  ( 787.4397851343537695, -381.7255117493284615, 374.2001403089903988 ) ) ;
#21914=CARTESIAN_POINT ( 'NONE',  ( 759.0159684113467620, -256.9181544815163534, 325.8855110935213020 ) ) ;
#21915=CARTESIAN_POINT ( 'NONE',  ( 791.9812246680005501, -164.6346026584200217, 361.9419747391813189 ) ) ;
#21918=CARTESIAN_POINT ( 'NONE',  ( 786.6156483768007774, -313.4419599262320730, 315.5913626894246136 ) ) ;
#21921=CARTESIAN_POINT ( 'NONE',  ( 745.5313806188320314, -39.28179084515331709, 333.7943932421247268 ) ) ;
#21925=CARTESIAN_POINT ( 'NONE',  ( 810.7187646348534145, -210.4527844766016926, 356.7737145352016341 ) ) ;
#21926=CARTESIAN_POINT ( 'NONE',  ( 754.8072714833581358, -124.8164208402383508, 338.1981804954720587 ) ) ;
#21930=CARTESIAN_POINT ( 'NONE',  ( 760.0363995740630116, -442.9181544815157849, 368.7758568127991907 ) ) ;
#21933=CARTESIAN_POINT ( 'NONE',  ( 769.1273215169530886, -406.7146871989590409, 317.4527132478988847 ) ) ;
#21938=CARTESIAN_POINT ( 'NONE',  ( 799.4546378042377910, -57.07832356259658013, 356.1575198192848006 ) ) ;
#21940=CARTESIAN_POINT ( 'NONE',  ( 815.1787889125755555, -198.8965053807779384, 343.7953271457877804 ) ) ;
#21941=CARTESIAN_POINT ( 'NONE',  ( 803.4237431249931660, -39.18005720387496638, 331.2633955100225194 ) ) ;
#21945=CARTESIAN_POINT ( 'NONE',  ( 755.3201227861273992, -243.7255117493287742, 345.3687786644892981 ) ) ;
#21948=CARTESIAN_POINT ( 'NONE',  ( 804.6798772138710092, -351.7255117493284615, 334.6312213355106451 ) ) ;
#21951=CARTESIAN_POINT ( 'NONE',  ( 787.6308680596127942, -35.26014174441480264, 364.1105419155492768 ) ) ;
#21953=CARTESIAN_POINT ( 'NONE',  ( 800.9747183278959710, -276.9982390220559978, 311.9810565676471583 ) ) ;
#21954=CARTESIAN_POINT ( 'NONE',  ( 756.1443688327750579, 2.376221891948710585, 314.3581564841659315 ) ) ;
#21962=CARTESIAN_POINT ( 'NONE',  ( 811.0346526505616112, -278.6346026584196807, 323.0537975583477532 ) ) ;
#21965=CARTESIAN_POINT ( 'NONE',  ( 790.9844846989617508, -142.3726999360620766, 317.2208543904092721 ) ) ;
#21966=CARTESIAN_POINT ( 'NONE',  ( 788.8264449731200330, -45.18005720387493085, 363.6646147819171233 ) ) ;
#21970=CARTESIAN_POINT ( 'NONE',  ( 815.3608509340175488, -266.7363362996981095, 341.2497674668889545 ) ) ;
#21971=CARTESIAN_POINT ( 'NONE',  ( 756.7813123517142913, -235.9874144716868898, 329.9779781133712504 ) ) ;
#21974=CARTESIAN_POINT ( 'NONE',  ( 756.5762568750052424, -3.180057203875080063, 348.7366044899774238 ) ) ;
#21976=CARTESIAN_POINT ( 'NONE',  ( 754.9967657858570647, -49.54369356751129061, 365.0032342141425374 ) ) ;
#21977=CARTESIAN_POINT ( 'NONE',  ( 811.0346526505616112, -110.6346026584201638, 323.0537975583477532 ) ) ;
#21979=CARTESIAN_POINT ( 'NONE',  ( 745.1792804349281596, -398.1908817542431507, 343.7566961878542884 ) ) ;
#21981=CARTESIAN_POINT ( 'NONE',  ( 777.4774526936600978, -322.2709662947830225, 304.7301800767027657 ) ) ;
#21984=CARTESIAN_POINT ( 'NONE',  ( 804.9363028652555840, -424.2709662947829088, 338.2165204200192079 ) ) ;
#21985=CARTESIAN_POINT ( 'NONE',  ( 790.0220218866281812, -199.0999726633346825, 363.2186876482849129 ) ) ;
#21988=CARTESIAN_POINT ( 'NONE',  ( 751.2241431872005251, -112.1692326535054889, 359.9636004259367610 ) ) ;
#21989=CARTESIAN_POINT ( 'NONE',  ( 804.9363028652555840, -448.2709662947827951, 338.2165204200192079 ) ) ;
#21991=CARTESIAN_POINT ( 'NONE',  ( 797.6776695296629214, -451.5436935675099903, 357.6776695296636603 ) ) ;
#21996=CARTESIAN_POINT ( 'NONE',  ( 804.9363028652555840, -280.2709662947833067, 338.2165204200192079 ) ) ;
#21997=CARTESIAN_POINT ( 'NONE',  ( 805.1927285166399315, -232.8164208402379529, 341.8018195045277707 ) ) ;
#21999=ORIENTED_EDGE ( 'NONE', *, *, #18455, .T. ) ;
#22000=CARTESIAN_POINT ( 'NONE',  ( 792.1044303154645831, -420.4527844766009252, 317.8323909638837677 ) ) ;
#22002=CARTESIAN_POINT ( 'NONE',  ( 748.9653473494365699, -194.6346026584199080, 356.9462024416520762 ) ) ;
#22003=CARTESIAN_POINT ( 'NONE',  ( 786.5483106153019435, -271.6454272087889876, 364.1601925771022366 ) ) ;
#22006=CARTESIAN_POINT ( 'NONE',  ( 764.3348316497523456, -214.7146871989597230, 308.6759233522265617 ) ) ;
#22011=CARTESIAN_POINT ( 'NONE',  ( 756.1348686366196716, -257.2601417444141134, 347.5531968255698416 ) ) ;
#22018=CARTESIAN_POINT ( 'NONE',  ( 797.8822607201568644, -174.5545181178801784, 370.1134526219340160 ) ) ;
#22024=CARTESIAN_POINT ( 'NONE',  ( 772.4837098697144029, -23.36187538569318889, 374.5518280994205611 ) ) ;
#22029=CARTESIAN_POINT ( 'NONE',  ( 762.3223304703356007, -7.543693567511430942, 322.3223304703362828 ) ) ;
#22030=CARTESIAN_POINT ( 'NONE',  ( 810.4231160770870019, -288.5545181178798657, 321.9338519418446936 ) ) ;
#22032=CARTESIAN_POINT ( 'NONE',  ( 763.0537975583475827, -216.4527844766016926, 371.0346526505627480 ) ) ;
#22036=CARTESIAN_POINT ( 'NONE',  ( 781.8018195045266339, -334.2709662947829656, 365.1927285166406705 ) ) ;
#22037=CARTESIAN_POINT ( 'NONE',  ( 804.8461984189677878, -98.19088175424404596, 336.9566956441385628 ) ) ;
#22041=CARTESIAN_POINT ( 'NONE',  ( 793.2243759319678702, -146.5328690171417350, 318.4439275373583200 ) ) ;
#22042=CARTESIAN_POINT ( 'NONE',  ( 804.9363028652555840, -376.2709662947829656, 338.2165204200192079 ) ) ;
#22045=CARTESIAN_POINT ( 'NONE',  ( 756.3353852180819104, -173.9073299311472169, 331.1735550268788302 ) ) ;
#22049=CARTESIAN_POINT ( 'NONE',  ( 782.4968714119720516, 13.18357915976123174, 305.0891759886411023 ) ) ;
#22051=CARTESIAN_POINT ( 'NONE',  ( 755.5713283507202505, -317.3618753856922581, 334.6858677611754729 ) ) ;
#22054=CARTESIAN_POINT ( 'NONE',  ( 801.9419747391806368, -450.4527844766009821, 351.9812246680014027 ) ) ;
#22060=CARTESIAN_POINT ( 'NONE',  ( 803.6646147819161570, 6.092670068852159559, 348.8264449731210561 ) ) ;
#22061=CARTESIAN_POINT ( 'NONE',  ( 802.7791456095903868, -148.7146871989598935, 329.0155153010375102 ) ) ;
#22064=CARTESIAN_POINT ( 'NONE',  ( 751.2241431872005251, -400.1692326535045936, 359.9636004259367610 ) ) ;
#22065=ORIENTED_EDGE ( 'NONE', *, *, #14268, .T. ) ;
#22070=CARTESIAN_POINT ( 'NONE',  ( 749.5768839229115201, -84.55451811788046257, 358.0661480581553064 ) ) ;
#22078=CARTESIAN_POINT ( 'NONE',  ( 799.2566176426618085, -408.0090635724249069, 324.0069404352559559 ) ) ;
#22084=CARTESIAN_POINT ( 'NONE',  ( 760.0363995740630116, -178.9181544815165239, 368.7758568127991907 ) ) ;
#22086=CARTESIAN_POINT ( 'NONE',  ( 782.4968714119720516, -130.8164208402383224, 305.0891759886411023 ) ) ;
#22090=CARTESIAN_POINT ( 'NONE',  ( 781.8018195045266339, -214.2709662947834488, 365.1927285166406705 ) ) ;
#22091=CARTESIAN_POINT ( 'NONE',  ( 746.4236121716829757, -447.8272453906067199, 328.8385539511384650 ) ) ;
#22095=CARTESIAN_POINT ( 'NONE',  ( 800.1688906516307043, -34.16923265350572336, 369.0717654672308186 ) ) ;
#22098=CARTESIAN_POINT ( 'NONE',  ( 785.3141322388236176, -21.72551174932956641, 364.4286716492789537 ) ) ;
#22100=CARTESIAN_POINT ( 'NONE',  ( 793.4146539503750546, -337.9874144716865771, 307.6481478633938877 ) ) ;
#22101=CARTESIAN_POINT ( 'NONE',  ( 802.1676090361155502, -158.6346026584200217, 327.8955696845344505 ) ) ;
#22103=CARTESIAN_POINT ( 'NONE',  ( 754.0944755984390895, -423.6237781080499190, 364.1009440267246760 ) ) ;
#22105=CARTESIAN_POINT ( 'NONE',  ( 785.3687786644884454, -347.3618753856922012, 315.3201227861279676 ) ) ;
#22109=VERTEX_POINT ( 'NONE', #6362 ) ;
#22111=CARTESIAN_POINT ( 'NONE',  ( 803.4237431249931660, -63.18005720387488822, 331.2633955100225194 ) ) ;
#22112=CARTESIAN_POINT ( 'NONE',  ( 772.4468031744293057, -369.8272453906068904, 363.8651313633793620 ) ) ;
#22114=CARTESIAN_POINT ( 'NONE',  ( 767.7687537140311633, -407.9073299311465348, 372.7932403749916830 ) ) ;
#22115=CARTESIAN_POINT ( 'NONE',  ( 746.7653713866222915, -281.2601417444139997, 351.0478386215610271 ) ) ;
#22116=CARTESIAN_POINT ( 'NONE',  ( 811.6461892240364477, -100.7146871989600356, 324.1737431748509835 ) ) ;
#22123=CARTESIAN_POINT ( 'NONE',  ( 814.5518280994195948, -423.7255117493281205, 332.4837098697145734 ) ) ;
#22127=CARTESIAN_POINT ( 'NONE',  ( 779.9999999999990905, 18.49609980828599376, 309.9999999999999432 ) ) ;
#22129=CARTESIAN_POINT ( 'NONE',  ( 804.1105419155481968, -291.8272453906071746, 347.6308680596136469 ) ) ;
#22130=CARTESIAN_POINT ( 'NONE',  ( 804.6798772138708955, -159.7255117493291436, 334.6312213355107019 ) ) ;
#22133=CARTESIAN_POINT ( 'NONE',  ( 783.0433043558608688, -312.8965053807775689, 315.1538015810313027 ) ) ;
#22136=CARTESIAN_POINT ( 'NONE',  ( 804.1009440267234822, -23.46360902697155026, 314.0944755984392600 ) ) ;
#22139=CARTESIAN_POINT ( 'NONE',  ( 774.6858677611749044, -129.7255117493292289, 315.5713283507209894 ) ) ;
#22140=CARTESIAN_POINT ( 'NONE',  ( 759.9999999999992042, 205.0000000000000568, 360.0000000000000000 ) ) ;
#22142=CARTESIAN_POINT ( 'NONE',  ( 793.0897708529556667, -30.55451811788062244, 361.3366627262616362 ) ) ;
#22145=CARTESIAN_POINT ( 'NONE',  ( 805.0264073115434940, -414.3510508353227237, 339.4763451958999099 ) ) ;
#22152=CARTESIAN_POINT ( 'NONE',  ( 754.0944755984390895, -231.6237781080504874, 364.1009440267246760 ) ) ;
#22153=CARTESIAN_POINT ( 'NONE',  ( 797.8594530101009923, -61.54369356751124798, 322.1405469898982119 ) ) ;
#22156=CARTESIAN_POINT ( 'NONE',  ( 781.7834795799800531, -226.8164208402380098, 315.0636971347436202 ) ) ;
#22163=CARTESIAN_POINT ( 'NONE',  ( 751.6929314249750860, -294.9982390220559978, 318.8095938919659034 ) ) ;
#22164=CARTESIAN_POINT ( 'NONE',  ( 810.1134526219336749, -8.532869017142163059, 357.8822607201570349 ) ) ;
#22170=CARTESIAN_POINT ( 'NONE',  ( 777.5031285880264704, -310.8164208402377540, 374.9108240113588408 ) ) ;
#22172=CARTESIAN_POINT ( 'NONE',  ( 800.7704444035546203, -364.1692326535046504, 326.0291762391768771 ) ) ;
#22174=CARTESIAN_POINT ( 'NONE',  ( 796.9571628226829034, -191.4636090269709996, 321.2382568024804641 ) ) ;
#22175=CARTESIAN_POINT ( 'NONE',  ( 792.1044303154645831, -60.45278447660215448, 317.8323909638837677 ) ) ;
#22180=CARTESIAN_POINT ( 'NONE',  ( 807.2620300519052989, -264.0090635724253616, 318.0141637701419768 ) ) ;
#22181=CARTESIAN_POINT ( 'NONE',  ( 763.2154366446407039, -237.6237781080505442, 321.4292242960311228 ) ) ;
#22185=CARTESIAN_POINT ( 'NONE',  ( 801.5560724626406000, -456.5545181178792404, 326.7756240680316182 ) ) ;
#22189=CARTESIAN_POINT ( 'NONE',  ( 787.4397851343537695, -45.72551174932949181, 374.2001403089903988 ) ) ;
#22190=CARTESIAN_POINT ( 'NONE',  ( 796.7737145352015204, -116.6346026584201780, 370.7187646348536987 ) ) ;
#22193=CARTESIAN_POINT ( 'NONE',  ( 745.7194118038753459, -373.6454272087887034, 348.7631598425976449 ) ) ;
#22195=CARTESIAN_POINT ( 'NONE',  ( 749.2812353651451076, -366.4527844766012095, 323.2262854647983090 ) ) ;
#22199=CARTESIAN_POINT ( 'NONE',  ( 774.6858677611749044, -417.7255117493283478, 315.5713283507209894 ) ) ;
#22200=CARTESIAN_POINT ( 'NONE',  ( 766.9102291470427417, -186.5545181178801215, 318.6633372737382501 ) ) ;
#22203=CARTESIAN_POINT ( 'NONE',  ( 778.7502325331095108, -120.3510508353236048, 304.6391490659818828 ) ) ;
#22204=CARTESIAN_POINT ( 'NONE',  ( 757.8323909638828582, -434.6346026584190554, 352.1044303154654358 ) ) ;
#22209=CARTESIAN_POINT ( 'NONE',  ( 804.6798772138708955, -255.7255117493287742, 334.6312213355107019 ) ) ;
#22210=CARTESIAN_POINT ( 'NONE',  ( 754.8072714833583632, -244.8164208402379245, 338.1981804954721156 ) ) ;
#22213=CARTESIAN_POINT ( 'NONE',  ( 787.6308680596127942, 12.73985825558503926, 364.1105419155492768 ) ) ;
#22215=CARTESIAN_POINT ( 'NONE',  ( 758.8095938919644823, -200.0891481129653471, 311.6929314249762797 ) ) ;
#22216=CARTESIAN_POINT ( 'NONE',  ( 766.0291762391763086, -274.9181544815161828, 360.7704444035551319 ) ) ;
#22219=CARTESIAN_POINT ( 'NONE',  ( 744.8212110874229666, -210.8965053807778816, 336.2046728542121627 ) ) ;
#22221=ORIENTED_EDGE ( 'NONE', *, *, #1890, .T. ) ;
#22224=CARTESIAN_POINT ( 'NONE',  ( 764.0069404352550464, -255.0783235625958980, 359.2566176426627180 ) ) ;
#22228=DIRECTION ( 'NONE',  ( -1.000000000000000000, 0.000000000000000000, 0.000000000000000000 ) ) ;
#22231=CARTESIAN_POINT ( 'NONE',  ( 766.4474001241216001, -163.0999726633347677, 307.3154664389482491 ) ) ;
#22241=CARTESIAN_POINT ( 'NONE',  ( 762.1405469898971887, -1.543693567511449150, 357.8594530101015607 ) ) ;
#22242=CARTESIAN_POINT ( 'NONE',  ( 776.2046728542105711, -284.1908817542434917, 304.8212110874238761 ) ) ;
#22244=CARTESIAN_POINT ( 'NONE',  ( 772.5602148656447525, -273.7255117493288026, 305.7998596910095443 ) ) ;
#22248=CARTESIAN_POINT ( 'NONE',  ( 755.3201227861273992, -339.7255117493285184, 345.3687786644892981 ) ) ;
#22249=CARTESIAN_POINT ( 'NONE',  ( 786.5483106153019435, -79.64542720878957027, 364.1601925771022366 ) ) ;
#22253=CARTESIAN_POINT ( 'NONE',  ( 815.1787889125755555, -126.8965053807781516, 343.7953271457877804 ) ) ;
#22254=CARTESIAN_POINT ( 'NONE',  ( 772.3691319403857278, -143.2601417444144829, 315.8894580844506663 ) ) ;
#22255=CARTESIAN_POINT ( 'NONE',  ( 785.3687786644884454, -395.3618753856918602, 315.3201227861279676 ) ) ;
#22259=CARTESIAN_POINT ( 'NONE',  ( 757.8323909638827445, -146.6346026584200217, 352.1044303154654358 ) ) ;
#22262=CARTESIAN_POINT ( 'NONE',  ( 814.5518280994195948, 8.274488250670337663, 332.4837098697145734 ) ) ;
#22264=CARTESIAN_POINT ( 'NONE',  ( 802.1676090361156639, -374.6346026584192828, 327.8955696845344505 ) ) ;
#22266=ORIENTED_EDGE ( 'NONE', *, *, #24740, .F. ) ;
#22267=CARTESIAN_POINT ( 'NONE',  ( 800.2193346964447755, -450.9982390220554294, 355.1360043628815788 ) ) ;
#22272=ORIENTED_EDGE ( 'NONE', *, *, #10052, .F. ) ;
#22274=CARTESIAN_POINT ( 'NONE',  ( 756.3353852180819104, -5.907329931147798696, 331.1735550268788302 ) ) ;
#22275=CARTESIAN_POINT ( 'NONE',  ( 792.3570229623688874, -237.1800572038742985, 373.1304606946836202 ) ) ;
#22276=CARTESIAN_POINT ( 'NONE',  ( 786.6156483768007774, -169.4419599262325562, 315.5913626894246136 ) ) ;
#22277=DIRECTION ( 'NONE',  ( 0.3826814224632300032, 0.000000000000000000, 0.9238803650373347276 ) ) ;
#22279=CARTESIAN_POINT ( 'NONE',  ( 813.9316612368132837, -415.4419599262318457, 348.6739635108323228 ) ) ;
#22284=CARTESIAN_POINT ( 'NONE',  ( 754.3581564841646241, -65.46360902697142592, 316.1443688327762516 ) ) ;
#22288=DIRECTION ( 'NONE',  ( 0.000000000000000000, 0.000000000000000000, 1.000000000000000000 ) ) ;
#22292=CARTESIAN_POINT ( 'NONE',  ( 776.9254006560222479, -404.1908817542431507, 314.8983024940802125 ) ) ;
#22294=CARTESIAN_POINT ( 'NONE',  ( 755.3028492785439312, -231.2817908451527558, 335.9200461376539693 ) ) ;
#22297=CARTESIAN_POINT ( 'NONE',  ( 764.1737431748507561, -178.3726999360619629, 371.6461892240376415 ) ) ;
#22299=CARTESIAN_POINT ( 'NONE',  ( 808.0189434323515343, -110.0891481129656597, 319.0252816721025511 ) ) ;
#22303=CARTESIAN_POINT ( 'NONE',  ( 762.3223304703356007, -223.5436935675107577, 322.3223304703362828 ) ) ;
#22304=CARTESIAN_POINT ( 'NONE',  ( 783.0745993439762742, -32.19088175424425913, 365.1016975059196739 ) ) ;
#22308=CARTESIAN_POINT ( 'NONE',  ( 754.0944755984390895, -15.62377810805123524, 364.1009440267246760 ) ) ;
#22311=CARTESIAN_POINT ( 'NONE',  ( 788.7366044899766848, -35.90732993114770011, 316.5762568750059813 ) ) ;
#22313=CARTESIAN_POINT ( 'NONE',  ( 744.8212110874229666, -354.8965053807774552, 336.2046728542121627 ) ) ;
#22316=CARTESIAN_POINT ( 'NONE',  ( 804.9363028652555840, -352.2709662947830225, 338.2165204200192079 ) ) ;
#22323=CARTESIAN_POINT ( 'NONE',  ( 757.8323909638827445, -74.63460265842032015, 352.1044303154654358 ) ) ;
#22324=CARTESIAN_POINT ( 'NONE',  ( 784.1219089521767955, -381.2817908451523294, 315.0488828828318333 ) ) ;
#22326=CARTESIAN_POINT ( 'NONE',  ( 763.2262854647970016, -392.6346026584193396, 309.2812353651462445 ) ) ;
#22327=CARTESIAN_POINT ( 'NONE',  ( 783.7566961878529810, -312.8965053807775689, 305.1792804349288417 ) ) ;
#22333=CARTESIAN_POINT ( 'NONE',  ( 755.2512626584698410, -415.5436935675102177, 315.2512626584710915 ) ) ;
#22340=CARTESIAN_POINT ( 'NONE',  ( 759.0159684113467620, -280.9181544815162965, 325.8855110935213020 ) ) ;
#22341=CARTESIAN_POINT ( 'NONE',  ( 771.2633955100217236, -143.9073299311473590, 363.4237431249939618 ) ) ;
#22344=CARTESIAN_POINT ( 'NONE',  ( 789.9200121543843807, -337.9874144716865771, 317.0176451133914384 ) ) ;
#22347=CARTESIAN_POINT ( 'NONE',  ( 745.7194118038753459, -61.64542720878961291, 348.7631598425976449 ) ) ;
#22349=CARTESIAN_POINT ( 'NONE',  ( 745.4481719005789273, -195.7255117493289731, 347.5162901302853129 ) ) ;
#22350=CARTESIAN_POINT ( 'NONE',  ( 781.7834795799800531, -130.8164208402383224, 315.0636971347436202 ) ) ;
#22354=CARTESIAN_POINT ( 'NONE',  ( 790.0220218866281812, -7.099972663335241130, 363.2186876482849129 ) ) ;
#22357=CARTESIAN_POINT ( 'NONE',  ( 799.4546378042377910, -393.0783235625954717, 356.1575198192848006 ) ) ;
#22363=CARTESIAN_POINT ( 'NONE',  ( 813.9316612368132837, -223.4419599262323857, 348.6739635108323228 ) ) ;
#22364=CARTESIAN_POINT ( 'NONE',  ( 804.4286716492782716, -65.36187538569306810, 345.3141322388244703 ) ) ;
#22367=CARTESIAN_POINT ( 'NONE',  ( 755.0636971347428243, -244.2709662947834204, 341.7834795799807353 ) ) ;
#22373=CARTESIAN_POINT ( 'NONE',  ( 811.0346526505617248, -302.6346026584195670, 323.0537975583478101 ) ) ;
#22375=CARTESIAN_POINT ( 'NONE',  ( 815.0009284576459549, -30.35105083532391390, 338.7629533639073429 ) ) ;
#22381=AXIS2_PLACEMENT_3D ( 'NONE', #38098, #9459, #41551 ) ;
#22383=CARTESIAN_POINT ( 'NONE',  ( 745.0891759886404770, -316.2709662947832499, 342.4968714119734159 ) ) ;
#22385=CARTESIAN_POINT ( 'NONE',  ( 763.8424801807145741, -210.0090635724255321, 320.5453621957614700 ) ) ;
#22388=CARTESIAN_POINT ( 'NONE',  ( 773.4516893846965786, -187.6454272087892434, 315.8398074228977066 ) ) ;
#22389=CARTESIAN_POINT ( 'NONE',  ( 804.4286716492782716, -41.36187538569314626, 345.3141322388244703 ) ) ;
#22390=EDGE_LOOP ( 'NONE', ( #40021, #9608, #24146, #20828 ) ) ;
#22393=CARTESIAN_POINT ( 'NONE',  ( 783.0433043558608688, -216.8965053807778816, 315.1538015810313027 ) ) ;
#22397=CARTESIAN_POINT ( 'NONE',  ( 796.9462024416508257, -420.4527844766009252, 308.9653473494370246 ) ) ;
#22401=CARTESIAN_POINT ( 'NONE',  ( 814.2001403089898304, -65.36187538569306810, 347.4397851343538264 ) ) ;
#22402=CARTESIAN_POINT ( 'NONE',  ( 782.4968714119720516, -106.8164208402383935, 305.0891759886411023 ) ) ;
#22403=LINE ( 'NONE', #5097, #37260 ) ;
#22406=CARTESIAN_POINT ( 'NONE',  ( 766.4474001241216001, -379.0999726633341993, 307.3154664389482491 ) ) ;
#22407=CARTESIAN_POINT ( 'NONE',  ( 745.5313806188320314, -399.2817908451522726, 333.7943932421247268 ) ) ;
#22410=CARTESIAN_POINT ( 'NONE',  ( 782.4968714119720516, -346.8164208402376971, 305.0891759886411023 ) ) ;
#22412=CARTESIAN_POINT ( 'NONE',  ( 801.9419747391806368, -450.4527844766009821, 351.9812246680014027 ) ) ;
#22417=CARTESIAN_POINT ( 'NONE',  ( 746.0683387631852383, -139.4419599262326699, 331.3260364891676204 ) ) ;
#22418=CARTESIAN_POINT ( 'NONE',  ( 801.9419747391806368, -426.4527844766010389, 351.9812246680014027 ) ) ;
#22423=CARTESIAN_POINT ( 'NONE',  ( 764.8639956371174549, -272.0891481129651197, 319.7806653035542013 ) ) ;
#22424=CARTESIAN_POINT ( 'NONE',  ( 771.1735550268780344, -249.1800572038742700, 316.3353852180828198 ) ) ;
#22427=CARTESIAN_POINT ( 'NONE',  ( 802.7791456095903868, 19.28531280103956647, 329.0155153010375102 ) ) ;
#22431=SHAPE_REPRESENTATION_RELATIONSHIP ( 'NONE' , 'NONE' ,  #2289, #44192 ) ;
#22433=CARTESIAN_POINT ( 'NONE',  ( 746.8695393053151292, -197.9073299311472169, 327.6429770376306578 ) ) ;
#22435=CARTESIAN_POINT ( 'NONE',  ( 763.0428371773158460, -299.4636090269707438, 358.7617431975195359 ) ) ;
#22436=CARTESIAN_POINT ( 'NONE',  ( 803.2186876482843445, -391.9874144716864066, 350.0220218866286928 ) ) ;
#22439=CARTESIAN_POINT ( 'NONE',  ( 803.8556311672234642, -225.6237781080506011, 365.6418435158340117 ) ) ;
#22444=CARTESIAN_POINT ( 'NONE',  ( 772.3691319403857278, -263.2601417444141134, 315.8894580844506663 ) ) ;
#22455=CARTESIAN_POINT ( 'NONE',  ( 757.7880784355613741, -162.0090635724256742, 312.4576283171834916 ) ) ;
#22460=CARTESIAN_POINT ( 'NONE',  ( 758.8095938919642549, -8.089148112965974136, 311.6929314249763365 ) ) ;
#22464=CARTESIAN_POINT ( 'NONE',  ( 801.9419747391806368, -42.45278447660223264, 351.9812246680014027 ) ) ;
#22465=CARTESIAN_POINT ( 'NONE',  ( 788.6739635108323228, -295.6454272087888739, 373.9316612368139090 ) ) ;
#22467=CARTESIAN_POINT ( 'NONE',  ( 813.1304606946830518, -257.9073299311469896, 352.3570229623690580 ) ) ;
#22472=CARTESIAN_POINT ( 'NONE',  ( 771.1735550268778070, -345.1800572038739006, 316.3353852180827630 ) ) ;
#22473=CARTESIAN_POINT ( 'NONE',  ( 790.0220218866281812, -79.09997266333503774, 363.2186876482849129 ) ) ;
#22477=CARTESIAN_POINT ( 'NONE',  ( 766.5853460496234675, -133.9874144716872024, 372.3518521366060554 ) ) ;
#22478=CARTESIAN_POINT ( 'NONE',  ( 757.8323909638827445, -386.6346026584191691, 352.1044303154654358 ) ) ;
#22481=CARTESIAN_POINT ( 'NONE',  ( 781.8018195045266339, -142.2709662947837330, 365.1927285166406705 ) ) ;
#22482=VECTOR ( 'NONE', #9249, 1000.000000000000000 ) ;
#22485=CARTESIAN_POINT ( 'NONE',  ( 814.9108240113580450, 7.729033705215793582, 337.5031285880265273 ) ) ;
#22487=CARTESIAN_POINT ( 'NONE',  ( 757.8323909638827445, -362.6346026584194533, 352.1044303154654358 ) ) ;
#22494=ORIENTED_EDGE ( 'NONE', *, *, #14195, .T. ) ;
#22499=CARTESIAN_POINT ( 'NONE',  ( 771.1735550268778070, 14.81994279612486309, 316.3353852180827630 ) ) ;
#22500=CARTESIAN_POINT ( 'NONE',  ( 756.7813123517142913, -163.9874144716871456, 329.9779781133712504 ) ) ;
#22509=CARTESIAN_POINT ( 'NONE',  ( 778.7629533639073998, -80.73633629969864955, 375.0009284576466371 ) ) ;
#22518=CARTESIAN_POINT ( 'NONE',  ( 802.9823548866075953, -409.0999726633340288, 330.0799878456151077 ) ) ;
#22524=CARTESIAN_POINT ( 'NONE',  ( 814.2805881961230625, -193.6454272087891582, 331.2368401574024119 ) ) ;
#22526=CARTESIAN_POINT ( 'NONE',  ( 796.9462024416508257, -156.4527844766018916, 308.9653473494370246 ) ) ;
#22531=CARTESIAN_POINT ( 'NONE',  ( 800.2193346964447755, -234.9982390220561683, 355.1360043628815788 ) ) ;
#22532=CARTESIAN_POINT ( 'NONE',  ( 763.8424801807145741, -18.00906357242611477, 320.5453621957614700 ) ) ;
#22537=CARTESIAN_POINT ( 'NONE',  ( 808.7758568127978833, -28.16923265350574468, 320.0363995740631822 ) ) ;
#22541=CARTESIAN_POINT ( 'NONE',  ( 757.8323909638827445, -26.63460265842045871, 352.1044303154654358 ) ) ;
#22545=CARTESIAN_POINT ( 'NONE',  ( 764.3348316497523456, -334.7146871989593251, 308.6759233522265617 ) ) ;
#22548=CARTESIAN_POINT ( 'NONE',  ( 751.2241431872005251, -424.1692326535044799, 359.9636004259367610 ) ) ;
#22550=CARTESIAN_POINT ( 'NONE',  ( 801.9419747391806368, -330.4527844766013231, 351.9812246680014027 ) ) ;
#22558=CARTESIAN_POINT ( 'NONE',  ( 804.9363028652555840, -64.27096629478397460, 338.2165204200192079 ) ) ;
#22559=CARTESIAN_POINT ( 'NONE',  ( 796.9571628226829034, -383.4636090269704596, 321.2382568024804641 ) ) ;
#22561=CARTESIAN_POINT ( 'NONE',  ( 814.5518280994195948, -447.7255117493281205, 332.4837098697145166 ) ) ;
#22563=CARTESIAN_POINT ( 'NONE',  ( 747.3154664389472828, -307.9874144716866340, 326.4474001241230781 ) ) ;
#22564=CARTESIAN_POINT ( 'NONE',  ( 813.2346286133761168, -101.2601417444146250, 328.9521613784389160 ) ) ;
#22568=CARTESIAN_POINT ( 'NONE',  ( 747.2067596250078623, -435.1800572038737869, 352.2312462859687230 ) ) ;
#22570=CARTESIAN_POINT ( 'NONE',  ( 759.2380499001254748, 21.41625977839825978, 318.3449445151863415 ) ) ;
#22576=CARTESIAN_POINT ( 'NONE',  ( 779.4763451958990572, -296.7363362996979390, 365.0264073115438919 ) ) ;
#22577=CARTESIAN_POINT ( 'NONE',  ( 774.6858677611749044, -177.7255117493290868, 315.5713283507209894 ) ) ;
#22578=VERTEX_POINT ( 'NONE', #32669 ) ;
#22580=CARTESIAN_POINT ( 'NONE',  ( 763.2154366446407039, -333.6237781080502600, 321.4292242960311228 ) ) ;
#22581=CARTESIAN_POINT ( 'NONE',  ( 745.7194118038753459, -85.64542720878952764, 348.7631598425976449 ) ) ;
#22584=CARTESIAN_POINT ( 'NONE',  ( 781.7834795799800531, -106.8164208402383935, 315.0636971347436202 ) ) ;
#22587=CARTESIAN_POINT ( 'NONE',  ( 801.5560724626406000, -24.55451811788064020, 326.7756240680316182 ) ) ;
#22590=CARTESIAN_POINT ( 'NONE',  ( 775.9200461376533440, -407.8055962898681628, 315.3028492785443291 ) ) ;
#22596=CARTESIAN_POINT ( 'NONE',  ( 759.8311093483677041, -238.1692326535050768, 310.9282345327691814 ) ) ;
#22597=CARTESIAN_POINT ( 'NONE',  ( 803.6646147819162707, -41.90732993114767879, 348.8264449731211130 ) ) ;
#22600=CARTESIAN_POINT ( 'NONE',  ( 803.6646147819161570, -233.9073299311470180, 348.8264449731210561 ) ) ;
#22610=CARTESIAN_POINT ( 'NONE',  ( 748.9653473494365699, -314.6346026584195101, 356.9462024416520762 ) ) ;
#22611=CARTESIAN_POINT ( 'NONE',  ( 773.7943932421234194, -23.80559628986938847, 305.5313806188329409 ) ) ;
#22618=CARTESIAN_POINT ( 'NONE',  ( 787.4397851343537695, -333.7255117493286320, 374.2001403089903988 ) ) ;
#22620=CARTESIAN_POINT ( 'NONE',  ( 760.5453621957607311, -357.0783235625956422, 323.8424801807151425 ) ) ;
#22622=AXIS2_PLACEMENT_3D ( 'NONE', #26542, #8993, #5519 ) ;
#22624=CARTESIAN_POINT ( 'NONE',  ( 757.0176451133909268, -205.0999726633346256, 349.9200121543848354 ) ) ;
#22625=CARTESIAN_POINT ( 'NONE',  ( 805.1927285166397041, -40.81642084023859951, 341.8018195045277707 ) ) ;
#22631=CARTESIAN_POINT ( 'NONE',  ( 804.1601925771018387, -223.4419599262323857, 346.5483106153029098 ) ) ;
#22635=CARTESIAN_POINT ( 'NONE',  ( 787.4397851343537695, -429.7255117493282910, 374.2001403089903988 ) ) ;
#22640=CARTESIAN_POINT ( 'NONE',  ( 772.5602148656447525, -33.72551174932952733, 305.7998596910095443 ) ) ;
#22641=CARTESIAN_POINT ( 'NONE',  ( 792.3570229623688874, -93.18005720387481006, 373.1304606946836202 ) ) ;
#22645=CARTESIAN_POINT ( 'NONE',  ( 777.4774526936600978, -346.2709662947830793, 304.7301800767027657 ) ) ;
#22647=ADVANCED_FACE ( 'NONE', ( #16233 ), #33331, .F. ) ;
#22648=CARTESIAN_POINT ( 'NONE',  ( 804.9511171171677688, 18.19440371013048008, 335.8780910478229202 ) ) ;
#22651=CARTESIAN_POINT ( 'NONE',  ( 793.4146539503750546, -145.9874144716871740, 307.6481478633938877 ) ) ;
#22652=CARTESIAN_POINT ( 'NONE',  ( 778.2165204200184689, -430.8164208402374129, 364.9363028652563230 ) ) ;
#22654=CARTESIAN_POINT ( 'NONE',  ( 756.1443688327750579, -165.6237781080507716, 314.3581564841659315 ) ) ;
#22658=CARTESIAN_POINT ( 'NONE',  ( 755.5713283507202505, -125.3618753856928834, 334.6858677611754729 ) ) ;
#22661=CARTESIAN_POINT ( 'NONE',  ( 759.9864689768902508, -266.0891481129651197, 354.9819416627836404 ) ) ;
#22662=CARTESIAN_POINT ( 'NONE',  ( 794.9819416627830151, -252.9982390220560831, 319.9864689768909898 ) ) ;
#22665=CARTESIAN_POINT ( 'NONE',  ( 795.9930595647434757, 20.92167643740319605, 320.7433823573372820 ) ) ;
#22670=CARTESIAN_POINT ( 'NONE',  ( 787.5162901302840055, -203.3618753856926276, 305.4481719005793252 ) ) ;
#22671=CARTESIAN_POINT ( 'NONE',  ( 772.4468031744293057, -297.8272453906070041, 363.8651313633793620 ) ) ;
#22672=CARTESIAN_POINT ( 'NONE',  ( 805.1016975059191054, -414.8965053807771710, 343.0745993439771837 ) ) ;
#22680=CARTESIAN_POINT ( 'NONE',  ( 786.6156483768007774, -265.4419599262323004, 315.5913626894246136 ) ) ;
#22687=CARTESIAN_POINT ( 'NONE',  ( 749.5768839229115201, -180.5545181178801499, 358.0661480581553064 ) ) ;
#22695=CARTESIAN_POINT ( 'NONE',  ( 800.2193346964447755, -42.99823902205675807, 355.1360043628815788 ) ) ;
#22697=CARTESIAN_POINT ( 'NONE',  ( 814.8207195650702488, -290.1908817542434349, 336.2433038121456548 ) ) ;
#22698=CARTESIAN_POINT ( 'NONE',  ( 782.4968714119720516, -274.8164208402378108, 305.0891759886411023 ) ) ;
#22703=CARTESIAN_POINT ( 'NONE',  ( 802.1676090361156639, -350.6346026584192828, 327.8955696845344505 ) ) ;
#22704=CARTESIAN_POINT ( 'NONE',  ( 755.5913626894240451, -109.6454272087894566, 346.6156483768012890 ) ) ;
#22708=CARTESIAN_POINT ( 'NONE',  ( 811.6461892240364477, -124.7146871989599930, 324.1737431748509835 ) ) ;
#22709=CARTESIAN_POINT ( 'NONE',  ( 755.5713283507202505, -389.3618753856919739, 334.6858677611754729 ) ) ;
#22715=CARTESIAN_POINT ( 'NONE',  ( 802.1676090361156639, -158.6346026584199933, 327.8955696845344505 ) ) ;
#22720=CARTESIAN_POINT ( 'NONE',  ( 771.1735550268778070, -345.1800572038739006, 316.3353852180827630 ) ) ;
#22724=CARTESIAN_POINT ( 'NONE',  ( 804.7487373415286811, -67.54369356751125508, 364.7487373415288516 ) ) ;
#22732=CARTESIAN_POINT ( 'NONE',  ( 778.1981804954714335, 13.72903370521577138, 314.8072714833589885 ) ) ;
#22733=CARTESIAN_POINT ( 'NONE',  ( 792.3570229623688874, -261.1800572038741848, 373.1304606946836202 ) ) ;
#22734=CARTESIAN_POINT ( 'NONE',  ( 755.8398074228967971, -163.4419599262325846, 333.4516893846970333 ) ) ;
#22737=CARTESIAN_POINT ( 'NONE',  ( 808.7758568127978833, -412.1692326535045936, 320.0363995740631822 ) ) ;
#22742=CARTESIAN_POINT ( 'NONE',  ( 809.0717654672305343, -52.91815448151692891, 360.1688906516309885 ) ) ;
#22751=CARTESIAN_POINT ( 'NONE',  ( 783.0745993439762742, -416.1908817542430938, 365.1016975059196739 ) ) ;
#22753=CARTESIAN_POINT ( 'NONE',  ( 773.4516893846965786, -235.6454272087890729, 315.8398074228977066 ) ) ;
#22757=CARTESIAN_POINT ( 'NONE',  ( 768.9521613784389729, -177.8272453906074304, 373.2346286133773106 ) ) ;
#22759=CARTESIAN_POINT ( 'NONE',  ( 815.2698199232961542, -136.8164208402382371, 342.5225473063383106 ) ) ;
#22763=CARTESIAN_POINT ( 'NONE',  ( 762.3223304703356007, -271.5436935675106156, 322.3223304703362828 ) ) ;
#22764=CARTESIAN_POINT ( 'NONE',  ( 787.5531968255692163, -21.82724539060792424, 316.1348686366205811 ) ) ;
#22770=CARTESIAN_POINT ( 'NONE',  ( 805.0264073115434940, -102.3510508353236901, 339.4763451958999099 ) ) ;
#22774=CARTESIAN_POINT ( 'NONE',  ( 785.3141322388236176, -69.72551174932942786, 364.4286716492789537 ) ) ;
#22777=CARTESIAN_POINT ( 'NONE',  ( 768.8385539511368734, -335.2601417444137724, 306.4236121716840557 ) ) ;
#22779=CARTESIAN_POINT ( 'NONE',  ( 811.6461892240364477, -436.7146871989589272, 324.1737431748509835 ) ) ;
#22781=CARTESIAN_POINT ( 'NONE',  ( 804.4286716492782716, -329.3618753856922581, 345.3141322388244703 ) ) ;
#22788=CARTESIAN_POINT ( 'NONE',  ( 759.7806653035534055, -102.9982390220565520, 324.8639956371180801 ) ) ;
#22789=CARTESIAN_POINT ( 'NONE',  ( 799.2566176426618085, -360.0090635724250774, 324.0069404352559559 ) ) ;
#22790=CARTESIAN_POINT ( 'NONE',  ( 787.4397851343537695, -429.7255117493282910, 374.2001403089903988 ) ) ;
#22792=CARTESIAN_POINT ( 'NONE',  ( 795.6651683502461765, -322.7146871989593819, 371.3240766477733814 ) ) ;
#22793=CARTESIAN_POINT ( 'NONE',  ( 791.1614460488616487, -107.2601417444145824, 373.5763878283158874 ) ) ;
#22798=CARTESIAN_POINT ( 'NONE',  ( 754.9967657858570647, -433.5436935675099903, 365.0032342141425374 ) ) ;
#22799=CARTESIAN_POINT ( 'NONE',  ( 787.0645410984409409, 17.59807796021646098, 310.5263297651933954 ) ) ;
#22804=CARTESIAN_POINT ( 'NONE',  ( 801.5560724626406000, -288.5545181178798657, 326.7756240680316182 ) ) ;
#22805=CARTESIAN_POINT ( 'NONE',  ( 804.9363028652555840, -184.2709662947835909, 338.2165204200192079 ) ) ;
#22808=FACE_OUTER_BOUND ( 'NONE', #37555, .T. ) ;
#22810=CARTESIAN_POINT ( 'NONE',  ( 757.7880784355613741, -90.00906357242590161, 312.4576283171834916 ) ) ;
#22813=CARTESIAN_POINT ( 'NONE',  ( 797.6776695296629214, -139.5436935675110135, 357.6776695296636603 ) ) ;
#22816=CARTESIAN_POINT ( 'NONE',  ( 783.0745993439762742, -32.19088175424425913, 365.1016975059196739 ) ) ;
#22818=DIRECTION ( 'NONE',  ( 1.000000000000000000, 0.000000000000000000, -0.000000000000000000 ) ) ;
#22819=CARTESIAN_POINT ( 'NONE',  ( 770.0799878456142551, -397.9874144716864066, 362.9823548866085616 ) ) ;
#22820=ORIENTED_EDGE ( 'NONE', *, *, #2106, .T. ) ;
#22823=CARTESIAN_POINT ( 'NONE',  ( 807.5423716828161105, -225.0783235625959833, 362.2119215644372048 ) ) ;
#22824=CARTESIAN_POINT ( 'NONE',  ( 804.6798772138710092, -87.72551174932935680, 334.6312213355106451 ) ) ;
#22828=CARTESIAN_POINT ( 'NONE',  ( 771.1735550268778070, -225.1800572038743269, 316.3353852180827630 ) ) ;
#22836=CARTESIAN_POINT ( 'NONE',  ( 745.4481719005789273, -339.7255117493285184, 347.5162901302853697 ) ) ;
#22837=CARTESIAN_POINT ( 'NONE',  ( 745.1769319972822814, -17.80559628986940979, 346.2694204179732083 ) ) ;
#22842=VERTEX_POINT ( 'NONE', #4940 ) ;
#22843=CARTESIAN_POINT ( 'NONE',  ( 771.2633955100217236, -215.9073299311471317, 363.4237431249939618 ) ) ;
#22845=ORIENTED_EDGE ( 'NONE', *, *, #17041, .T. ) ;
#22846=CARTESIAN_POINT ( 'NONE',  ( 755.2512626584698410, -319.5436935675104451, 315.2512626584710915 ) ) ;
#22850=CARTESIAN_POINT ( 'NONE',  ( 755.8894580844503253, -183.8272453906074020, 332.3691319403863531 ) ) ;
#22851=CARTESIAN_POINT ( 'NONE',  ( 797.8594530101008786, -85.54369356751118403, 322.1405469898980982 ) ) ;
#22855=CARTESIAN_POINT ( 'NONE',  ( 754.9735926884551418, -258.3510508353231785, 340.5236548041000333 ) ) ;
#22858=CARTESIAN_POINT ( 'NONE',  ( 746.8695393053150156, -437.9073299311463074, 327.6429770376306010 ) ) ;
#22862=CARTESIAN_POINT ( 'NONE',  ( 767.6429770376289525, -57.18005720387489532, 306.8695393053162093 ) ) ;
#22863=CARTESIAN_POINT ( 'NONE',  ( 787.5162901302840055, -131.3618753856928834, 305.4481719005792684 ) ) ;
#22868=CARTESIAN_POINT ( 'NONE',  ( 748.9653473494363425, -362.6346026584194533, 356.9462024416521331 ) ) ;
#22870=CARTESIAN_POINT ( 'NONE',  ( 797.6776695296629214, -451.5436935675099903, 357.6776695296636603 ) ) ;
#22874=CARTESIAN_POINT ( 'NONE',  ( 764.3348316497523456, -142.7146871989599219, 308.6759233522265617 ) ) ;
#22879=CARTESIAN_POINT ( 'NONE',  ( 803.6646147819161570, -137.9073299311473875, 348.8264449731210561 ) ) ;
#22882=CARTESIAN_POINT ( 'NONE',  ( 754.8072714833581358, -268.8164208402378108, 338.1981804954720587 ) ) ;
#22883=CARTESIAN_POINT ( 'NONE',  ( 804.4286716492782716, -257.3618753856924286, 345.3141322388244703 ) ) ;
#22886=CARTESIAN_POINT ( 'NONE',  ( 804.4286716492782716, -449.3618753856918602, 345.3141322388244703 ) ) ;
#22889=CARTESIAN_POINT ( 'NONE',  ( 782.5225473063383106, -214.2709662947834772, 375.2698199232970637 ) ) ;
#22890=CARTESIAN_POINT ( 'NONE',  ( 775.8780910478218402, -297.2817908451526137, 364.9511171171680530 ) ) ;
#22891=CARTESIAN_POINT ( 'NONE',  ( 754.9735926884551418, -402.3510508353228374, 340.5236548041000333 ) ) ;
#22895=EDGE_LOOP ( 'NONE', ( #43498, #4672, #16029, #34018 ) ) ;
#22898=CARTESIAN_POINT ( 'NONE',  ( 757.2208543904082489, -280.7146871989594956, 350.9844846989624330 ) ) ;
#22902=CARTESIAN_POINT ( 'NONE',  ( 802.1676090361156639, 9.365397341579420498, 327.8955696845344505 ) ) ;
#22903=EDGE_LOOP ( 'NONE', ( #11668, #25637, #40066, #36053, #644, #29653, #14396, #41080 ) ) ;
#22905=CARTESIAN_POINT ( 'NONE',  ( 755.8990559732751535, -203.4636090269709996, 365.9055244015606831 ) ) ;
#22908=DIRECTION ( 'NONE',  ( -1.000000000000000000, -0.000000000000000000, 0.000000000000000000 ) ) ;
#22911=CARTESIAN_POINT ( 'NONE',  ( 758.8095938919642549, -56.08914811296580893, 311.6929314249763365 ) ) ;
#22915=CARTESIAN_POINT ( 'NONE',  ( 762.1405469898971887, -49.54369356751129061, 357.8594530101015607 ) ) ;
#22916=CARTESIAN_POINT ( 'NONE',  ( 778.7629533639073998, -272.7363362996981095, 375.0009284576466371 ) ) ;
#22917=CARTESIAN_POINT ( 'NONE',  ( 745.7998596910086917, -269.3618753856924286, 332.5602148656461168 ) ) ;
#22920=LINE ( 'NONE', #5603, #13629 ) ;
#22921=CARTESIAN_POINT ( 'NONE',  ( 756.5762568750052424, -363.1800572038739006, 348.7366044899774238 ) ) ;
#22922=CARTESIAN_POINT ( 'NONE',  ( 787.5531968255692163, -117.8272453906076151, 316.1348686366205811 ) ) ;
#22926=CARTESIAN_POINT ( 'NONE',  ( 788.8264449731200330, -405.1800572038737300, 363.6646147819171233 ) ) ;
#22929=CARTESIAN_POINT ( 'NONE',  ( 778.2165204200184689, -142.8164208402382656, 364.9363028652563230 ) ) ;
#22930=CARTESIAN_POINT ( 'NONE',  ( 759.7806653035535192, -150.9982390220564241, 324.8639956371181370 ) ) ;
#22934=CARTESIAN_POINT ( 'NONE',  ( 758.0580252608178853, -342.4527844766013231, 328.0187753319985404 ) ) ;
#22937=CARTESIAN_POINT ( 'NONE',  ( 815.2698199232962679, -112.8164208402383650, 342.5225473063383674 ) ) ;
#22942=CARTESIAN_POINT ( 'NONE',  ( 813.1304606946830518, -257.9073299311469896, 352.3570229623690580 ) ) ;
#22943=CARTESIAN_POINT ( 'NONE',  ( 787.6308680596127942, -155.2601417444144261, 364.1105419155492768 ) ) ;
#22952=CARTESIAN_POINT ( 'NONE',  ( 781.2370466360911223, -116.7363362996985217, 304.9990715423533629 ) ) ;
#22958=CARTESIAN_POINT ( 'NONE',  ( 787.4999999999992042, -462.9681489794447771, 310.9526249034443026 ) ) ;
#22963=CARTESIAN_POINT ( 'NONE',  ( 801.5560724626406000, -432.5545181178793541, 326.7756240680316182 ) ) ;
#22965=CARTESIAN_POINT ( 'NONE',  ( 804.1105419155481968, -243.8272453906072030, 347.6308680596136469 ) ) ;
#22969=CARTESIAN_POINT ( 'NONE',  ( 805.6418435158337843, -197.4636090269709996, 363.8556311672236916 ) ) ;
#22971=CARTESIAN_POINT ( 'NONE',  ( 745.4481719005789273, -147.7255117493291152, 347.5162901302853129 ) ) ;
#22974=CARTESIAN_POINT ( 'NONE',  ( 774.6312213355099630, -239.3618753856924570, 364.6798772138717482 ) ) ;
#22975=CARTESIAN_POINT ( 'NONE',  ( 769.0155153010367712, -34.37269993606243901, 362.7791456095907279 ) ) ;
#22982=CARTESIAN_POINT ( 'NONE',  ( 755.8398074228967971, -91.44195992623282621, 333.4516893846970333 ) ) ;
#22986=CARTESIAN_POINT ( 'NONE',  ( 757.8323909638827445, -50.63460265842036989, 352.1044303154654358 ) ) ;
#22989=CARTESIAN_POINT ( 'NONE',  ( 813.9316612368132837, -367.4419599262319025, 348.6739635108323228 ) ) ;
#22991=CARTESIAN_POINT ( 'NONE',  ( 815.1787889125755555, -438.8965053807771710, 343.7953271457877804 ) ) ;
#22993=CARTESIAN_POINT ( 'NONE',  ( 765.0180583372156207, -360.9982390220557704, 360.0135310231089534 ) ) ;
#23001=CARTESIAN_POINT ( 'NONE',  ( 804.6798772138708955, -87.72551174932937101, 334.6312213355107019 ) ) ;
#23002=CARTESIAN_POINT ( 'NONE',  ( 763.0428371773158460, -395.4636090269705164, 358.7617431975195359 ) ) ;
#23003=CARTESIAN_POINT ( 'NONE',  ( 777.4774526936600978, -442.2709662947827383, 304.7301800767028226 ) ) ;
#23005=CARTESIAN_POINT ( 'NONE',  ( 764.3348316497523456, -334.7146871989593251, 308.6759233522265617 ) ) ;
#23006=ADVANCED_FACE ( 'NONE', ( #13692 ), #27771, .T. ) ;
#23010=CARTESIAN_POINT ( 'NONE',  ( 788.6739635108323228, -7.645427208789786100, 373.9316612368139090 ) ) ;
#23018=CARTESIAN_POINT ( 'NONE',  ( 755.5913626894240451, -301.6454272087889308, 346.6156483768012890 ) ) ;
#23020=CARTESIAN_POINT ( 'NONE',  ( 768.9521613784389729, -273.8272453906071746, 373.2346286133773106 ) ) ;
#23024=CARTESIAN_POINT ( 'NONE',  ( 781.2370466360911223, -92.73633629969860692, 304.9990715423533629 ) ) ;
#23026=FACE_OUTER_BOUND ( 'NONE', #6311, .T. ) ;
#23027=CARTESIAN_POINT ( 'NONE',  ( 764.8639956371174549, -152.0891481129655460, 319.7806653035542013 ) ) ;
#23031=CARTESIAN_POINT ( 'NONE',  ( 779.4763451958990572, -32.73633629969879877, 365.0264073115438919 ) ) ;
#23034=CARTESIAN_POINT ( 'NONE',  ( 783.0433043558608688, -432.8965053807771142, 315.1538015810313027 ) ) ;
#23039=CARTESIAN_POINT ( 'NONE',  ( 745.1769319972822814, -233.8055962898687028, 346.2694204179732083 ) ) ;
#23042=CARTESIAN_POINT ( 'NONE',  ( 797.6776695296629214, -283.5436935675105019, 357.6776695296636603 ) ) ;
#23050=CARTESIAN_POINT ( 'NONE',  ( 796.7737145352015204, -332.6346026584195101, 370.7187646348536987 ) ) ;
#23051=CARTESIAN_POINT ( 'NONE',  ( 781.2497674668890113, -36.35105083532390324, 375.3608509340180603 ) ) ;
#23056=CARTESIAN_POINT ( 'NONE',  ( 800.0135310231082713, -206.0891481129653471, 325.0180583372163028 ) ) ;
#23059=CARTESIAN_POINT ( 'NONE',  ( 744.7301800767019131, -340.8164208402376971, 337.4774526936615757 ) ) ;
#23063=CARTESIAN_POINT ( 'NONE',  ( 761.4292242960306112, -209.4636090269709996, 323.2154366446414429 ) ) ;
#23064=CARTESIAN_POINT ( 'NONE',  ( 788.8264449731200330, -93.18005720387481006, 363.6646147819171233 ) ) ;
#23070=CARTESIAN_POINT ( 'NONE',  ( 803.8651313633788504, -269.2601417444139997, 332.4468031744301015 ) ) ;
#23073=CARTESIAN_POINT ( 'NONE',  ( 747.2067596250078623, -435.1800572038737869, 352.2312462859687230 ) ) ;
#23077=CARTESIAN_POINT ( 'NONE',  ( 813.1304606946830518, -89.90732993114750116, 352.3570229623690580 ) ) ;
#23078=CARTESIAN_POINT ( 'NONE',  ( 808.3070685750230950, -138.9982390220563957, 361.1904061080339261 ) ) ;
#23083=CARTESIAN_POINT ( 'NONE',  ( 804.7487373415286811, -355.5436935675103882, 364.7487373415288516 ) ) ;
#23085=CARTESIAN_POINT ( 'NONE',  ( 804.9363028652555840, -448.2709662947827951, 338.2165204200192079 ) ) ;
#23088=CARTESIAN_POINT ( 'NONE',  ( 815.0009284576459549, -150.3510508353235480, 338.7629533639073429 ) ) ;
#23089=CARTESIAN_POINT ( 'NONE',  ( 800.0135310231082713, 9.910851887033969021, 325.0180583372163028 ) ) ;
#23093=CARTESIAN_POINT ( 'NONE',  ( 805.1927285166397041, -112.8164208402383508, 341.8018195045277707 ) ) ;
#23095=CARTESIAN_POINT ( 'NONE',  ( 788.7366044899766848, -275.9073299311469896, 316.5762568750059813 ) ) ;
#23099=CARTESIAN_POINT ( 'NONE',  ( 803.4237431249931660, -447.1800572038736732, 331.2633955100225194 ) ) ;
#23100=AXIS2_PLACEMENT_3D ( 'NONE', #15929, #5295, #43863 ) ;
#23103=CARTESIAN_POINT ( 'NONE',  ( 801.1904061080338124, -212.0891481129653187, 368.3070685750236066 ) ) ;
#23104=CARTESIAN_POINT ( 'NONE',  ( 804.1105419155481968, -315.8272453906070609, 347.6308680596136469 ) ) ;
#23105=CARTESIAN_POINT ( 'NONE',  ( 769.1273215169530886, -382.7146871989591546, 317.4527132478988847 ) ) ;
#23113=CARTESIAN_POINT ( 'NONE',  ( 779.4709603349208464, -288.3510508353231216, 314.7162404726379918 ) ) ;
#23116=CARTESIAN_POINT ( 'NONE',  ( 797.8594530101008786, 10.45630643248850866, 322.1405469898980982 ) ) ;
#23123=CARTESIAN_POINT ( 'NONE',  ( 796.9462024416508257, -36.45278447660223975, 308.9653473494370246 ) ) ;
#23129=CARTESIAN_POINT ( 'NONE',  ( 785.3687786644884454, -59.36187538569306810, 315.3201227861279676 ) ) ;
#23130=CARTESIAN_POINT ( 'NONE',  ( 773.7305795820266212, -321.2817908451525000, 374.8230680027170365 ) ) ;
#23131=CARTESIAN_POINT ( 'NONE',  ( 787.4397851343537695, -261.7255117493288026, 374.2001403089903988 ) ) ;
#23135=CARTESIAN_POINT ( 'NONE',  ( 767.8955696845333705, -360.4527844766010958, 362.1676090361162323 ) ) ;
#23136=CARTESIAN_POINT ( 'NONE',  ( 755.3028492785439312, -135.2817908451530116, 335.9200461376539693 ) ) ;
#23138=CARTESIAN_POINT ( 'NONE',  ( 767.8955696845334842, -384.4527844766011526, 362.1676090361161755 ) ) ;
#23139=DIRECTION ( 'NONE',  ( 0.000000000000000000, 0.000000000000000000, 1.000000000000000000 ) ) ;
#23141=CARTESIAN_POINT ( 'NONE',  ( 799.9999999999993179, -512.9681489794448908, 309.9999999999998863 ) ) ;
#23142=CARTESIAN_POINT ( 'NONE',  ( 755.0636971347428243, -412.2709662947829088, 341.7834795799807353 ) ) ;
#23145=CARTESIAN_POINT ( 'NONE',  ( 764.8639956371174549, -200.0891481129653187, 319.7806653035542013 ) ) ;
#23146=CARTESIAN_POINT ( 'NONE',  ( 756.5762568750052424, -147.1800572038746395, 348.7366044899774238 ) ) ;
#23151=CARTESIAN_POINT ( 'NONE',  ( 755.5713283507202505, -365.3618753856920875, 334.6858677611754729 ) ) ;
#23153=CARTESIAN_POINT ( 'NONE',  ( 0.000000000000000000, 0.000000000000000000, 0.000000000000000000 ) ) ;
#23155=CARTESIAN_POINT ( 'NONE',  ( 814.5518280994195948, -111.7255117493292857, 332.4837098697145166 ) ) ;
#23163=CARTESIAN_POINT ( 'NONE',  ( 767.6429770376289525, -249.1800572038742416, 306.8695393053162093 ) ) ;
#23164=CARTESIAN_POINT ( 'NONE',  ( 786.6156483768007774, -193.4419599262325278, 315.5913626894246136 ) ) ;
#23174=CARTESIAN_POINT ( 'NONE',  ( 807.2620300519052989, -120.0090635724258021, 318.0141637701419768 ) ) ;
#23175=VECTOR ( 'NONE', #23505, 1000.000000000000000 ) ;
#23176=DIRECTION ( 'NONE',  ( 0.000000000000000000, 0.000000000000000000, -1.000000000000000000 ) ) ;
#23184=CARTESIAN_POINT ( 'NONE',  ( 766.9102291470427417, -426.5545181178794678, 318.6633372737382501 ) ) ;
#23188=DIRECTION ( 'NONE',  ( -1.000000000000000000, -0.000000000000000000, 0.000000000000000000 ) ) ;
#23191=CARTESIAN_POINT ( 'NONE',  ( 805.6418435158337843, -221.4636090269709428, 363.8556311672236916 ) ) ;
#23193=CARTESIAN_POINT ( 'NONE',  ( 751.9810565676468741, -146.0891481129655176, 360.9747183278973921 ) ) ;
#23196=CARTESIAN_POINT ( 'NONE',  ( 774.6312213355099630, -263.3618753856924855, 364.6798772138717482 ) ) ;
#23197=CARTESIAN_POINT ( 'NONE',  ( 804.8461984189677878, -26.19088175424427334, 336.9566956441385628 ) ) ;
#23202=CARTESIAN_POINT ( 'NONE',  ( 799.4546378042377910, -105.0783235625964096, 356.1575198192848006 ) ) ;
#23203=CARTESIAN_POINT ( 'NONE',  ( 805.1927285166397041, -304.8164208402376403, 341.8018195045277707 ) ) ;
#23205=EDGE_CURVE ( 'NONE', #3123, #30414, #45070, .T. ) ;
#23207=CARTESIAN_POINT ( 'NONE',  ( 795.1360043628807261, -44.08914811296584446, 360.2193346964456282 ) ) ;
#23211=CARTESIAN_POINT ( 'NONE',  ( 803.8556311672234642, -393.6237781080500326, 365.6418435158340117 ) ) ;
#23214=CARTESIAN_POINT ( 'NONE',  ( 749.2812353651451076, -6.452784476602343666, 323.2262854647983090 ) ) ;
#23217=CARTESIAN_POINT ( 'NONE',  ( 762.3223304703356007, -367.5436935675102745, 322.3223304703362828 ) ) ;
#23228=CARTESIAN_POINT ( 'NONE',  ( 781.8018195045266339, -94.27096629478386092, 365.1927285166406705 ) ) ;
#23229=CARTESIAN_POINT ( 'NONE',  ( 759.0159684113467620, -400.9181544815159555, 325.8855110935213020 ) ) ;
#23230=CARTESIAN_POINT ( 'NONE',  ( 784.0799538623451781, -107.8055962898691433, 364.6971507214555572 ) ) ;
#23231=CARTESIAN_POINT ( 'NONE',  ( 811.0346526505617248, -422.6346026584191691, 323.0537975583478101 ) ) ;
#23233=CARTESIAN_POINT ( 'NONE',  ( 764.3348316497523456, -310.7146871989593251, 308.6759233522265617 ) ) ;
#23239=EDGE_CURVE ( 'NONE', #13477, #25691, #24372, .T. ) ;
#23240=CARTESIAN_POINT ( 'NONE',  ( 810.7187646348534145, -450.4527844766009821, 356.7737145352016341 ) ) ;
#23248=CARTESIAN_POINT ( 'NONE',  ( 769.0155153010367712, -322.3726999360615082, 362.7791456095907279 ) ) ;
#23249=CARTESIAN_POINT ( 'NONE',  ( 801.9419747391806368, -186.4527844766017779, 351.9812246680014027 ) ) ;
#23250=EDGE_CURVE ( 'NONE', #8526, #27321, #34322, .T. ) ;
#23252=CARTESIAN_POINT ( 'NONE',  ( 793.5525998758768083, -319.0999726633342561, 372.6845335610516941 ) ) ;
#23256=CARTESIAN_POINT ( 'NONE',  ( 814.4686193811664907, -75.28179084515321051, 346.2056067578752732 ) ) ;
#23260=CARTESIAN_POINT ( 'NONE',  ( 788.7366044899766848, -155.9073299311473306, 316.5762568750059813 ) ) ;
#23262=CARTESIAN_POINT ( 'NONE',  ( 762.1177392798416577, -402.5545181178795247, 309.8865473780659272 ) ) ;
#23266=CARTESIAN_POINT ( 'NONE',  ( 776.9254006560222479, -68.19088175424413123, 314.8983024940802125 ) ) ;
#23269=CARTESIAN_POINT ( 'NONE',  ( 798.7617431975189675, -435.6237781080499190, 323.0428371773161871 ) ) ;
#23274=CARTESIAN_POINT ( 'NONE',  ( 778.7502325331095108, -264.3510508353232353, 304.6391490659818828 ) ) ;
#23275=CARTESIAN_POINT ( 'NONE',  ( 758.0580252608178853, -78.45278447660211896, 328.0187753319985404 ) ) ;
#23280=CARTESIAN_POINT ( 'NONE',  ( 781.8018195045266339, -286.2709662947833635, 365.1927285166406705 ) ) ;
#23283=LINE ( 'NONE', #12664, #14342 ) ;
#23287=AXIS2_PLACEMENT_3D ( 'NONE', #23141, #26619, #40717 ) ;
#23290=CARTESIAN_POINT ( 'NONE',  ( 751.6929314249750860, -342.9982390220557704, 318.8095938919659034 ) ) ;
#23291=CARTESIAN_POINT ( 'NONE',  ( 811.6461892240364477, -220.7146871989596661, 324.1737431748509835 ) ) ;
#23292=CARTESIAN_POINT ( 'NONE',  ( 759.8311093483677041, -22.16923265350575889, 310.9282345327691814 ) ) ;
#23298=CARTESIAN_POINT ( 'NONE',  ( 808.0189434323515343, -374.0891481129647786, 319.0252816721025511 ) ) ;
#23301=CARTESIAN_POINT ( 'NONE',  ( 793.3891180349545493, 16.45630643248849978, 314.6660875939051607 ) ) ;
#23303=CARTESIAN_POINT ( 'NONE',  ( 798.5707757039680246, -221.4636090269709428, 356.7845633553585003 ) ) ;
#23304=CARTESIAN_POINT ( 'NONE',  ( 781.7834795799800531, -82.81642084023846451, 315.0636971347436202 ) ) ;
#23308=CARTESIAN_POINT ( 'NONE',  ( 803.2186876482843445, -247.9874144716867761, 350.0220218866286928 ) ) ;
#23311=CARTESIAN_POINT ( 'NONE',  ( 759.0252816721024374, -432.9982390220555999, 368.0189434323527280 ) ) ;
#23315=CARTESIAN_POINT ( 'NONE',  ( 748.9653473494363425, -74.63460265842032015, 356.9462024416521331 ) ) ;
#23316=CARTESIAN_POINT ( 'NONE',  ( 758.8095938919642549, -152.0891481129655460, 311.6929314249763365 ) ) ;
#23322=CARTESIAN_POINT ( 'NONE',  ( 804.7487373415286811, -403.5436935675101608, 364.7487373415288516 ) ) ;
#23323=CARTESIAN_POINT ( 'NONE',  ( 747.2067596250078623, -3.180057203875080063, 352.2312462859687230 ) ) ;
#23327=CARTESIAN_POINT ( 'NONE',  ( 763.2154366446407039, 2.376221891948710585, 321.4292242960311228 ) ) ;
#23330=CARTESIAN_POINT ( 'NONE',  ( 815.1787889125755555, -174.8965053807779952, 343.7953271457877804 ) ) ;
#23333=CARTESIAN_POINT ( 'NONE',  ( 755.5713283507202505, -173.3618753856927128, 334.6858677611754729 ) ) ;
#23336=CARTESIAN_POINT ( 'NONE',  ( 781.8018195045266339, -286.2709662947833635, 365.1927285166406705 ) ) ;
#23337=CARTESIAN_POINT ( 'NONE',  ( 767.8955696845334842, -288.4527844766014937, 362.1676090361161755 ) ) ;
#23338=FACE_BOUND ( 'NONE', #26528, .T. ) ;
#23340=CARTESIAN_POINT ( 'NONE',  ( 800.7704444035546203, -4.169232653505813069, 326.0291762391768771 ) ) ;
#23345=CARTESIAN_POINT ( 'NONE',  ( 787.5162901302840055, -227.3618753856925423, 305.4481719005793252 ) ) ;
#23346=CARTESIAN_POINT ( 'NONE',  ( 805.2837595273609850, -314.7363362996979959, 340.5290396650784714 ) ) ;
#23347=CARTESIAN_POINT ( 'NONE',  ( 766.7756240680305382, -398.5328690171409107, 361.5560724626415663 ) ) ;
#23348=EDGE_LOOP ( 'NONE', ( #22266, #31924 ) ) ;
#23355=CARTESIAN_POINT ( 'NONE',  ( 773.3843516231979720, -301.4419599262320730, 364.4086373105754433 ) ) ;
#23362=CARTESIAN_POINT ( 'NONE',  ( 799.9636004259356241, -190.9181544815164955, 311.2241431872006956 ) ) ;
#23366=CARTESIAN_POINT ( 'NONE',  ( 751.6929314249748586, -54.99823902205672255, 318.8095938919659034 ) ) ;
#23369=CARTESIAN_POINT ( 'NONE',  ( 800.0135310231082713, -62.08914811296580183, 325.0180583372163028 ) ) ;
#23370=CARTESIAN_POINT ( 'NONE',  ( 795.8262568251477660, -334.3726999360615082, 308.3538107759623585 ) ) ;
#23371=CARTESIAN_POINT ( 'NONE',  ( 759.9999999999992042, -512.9681489794448908, 339.9999999999999432 ) ) ;
#23372=CARTESIAN_POINT ( 'NONE',  ( 796.7737145352015204, -284.6346026584196807, 370.7187646348536987 ) ) ;
#23374=CIRCLE ( 'NONE', #22622, 30.00000000000008171 ) ;
#23377=CARTESIAN_POINT ( 'NONE',  ( 803.4237431249931660, -375.1800572038739574, 331.2633955100225194 ) ) ;
#23378=CARTESIAN_POINT ( 'NONE',  ( 775.8780910478218402, -105.2817908451530968, 364.9511171171680530 ) ) ;
#23380=CARTESIAN_POINT ( 'NONE',  ( 814.8230680027162407, -29.80559628986937781, 333.7305795820267917 ) ) ;
#23381=CARTESIAN_POINT ( 'NONE',  ( 754.8072714833583632, -364.8164208402375266, 338.1981804954721156 ) ) ;
#23385=CARTESIAN_POINT ( 'NONE',  ( 771.1735550268778070, -441.1800572038735027, 316.3353852180827630 ) ) ;
#23389=CARTESIAN_POINT ( 'NONE',  ( 803.4237431249931660, -207.1800572038744406, 331.2633955100225194 ) ) ;
#23390=CARTESIAN_POINT ( 'NONE',  ( 802.1676090361155502, -206.6346026584198796, 327.8955696845344505 ) ) ;
#23394=CARTESIAN_POINT ( 'NONE',  ( 759.9864689768902508, -386.0891481129647786, 354.9819416627836404 ) ) ;
#23397=CARTESIAN_POINT ( 'NONE',  ( 796.9462024416508257, -132.4527844766019200, 308.9653473494370246 ) ) ;
#23398=ORIENTED_EDGE ( 'NONE', *, *, #18811, .T. ) ;
#23403=CARTESIAN_POINT ( 'NONE',  ( 814.5518280994195948, -255.7255117493287742, 332.4837098697145734 ) ) ;
#23404=CARTESIAN_POINT ( 'NONE',  ( 798.7617431975189675, -195.6237781080506863, 323.0428371773161871 ) ) ;
#23415=CARTESIAN_POINT ( 'NONE',  ( 814.8207195650702488, -98.19088175424404596, 336.2433038121456548 ) ) ;
#23424=CARTESIAN_POINT ( 'NONE',  ( 761.4292242960306112, -425.4636090269703459, 323.2154366446414429 ) ) ;
#23431=CARTESIAN_POINT ( 'NONE',  ( 760.0363995740630116, -202.9181544815164386, 368.7758568127991907 ) ) ;
#23433=CARTESIAN_POINT ( 'NONE',  ( 787.4397851343537695, -165.7255117493291152, 374.2001403089903988 ) ) ;
#23436=CARTESIAN_POINT ( 'NONE',  ( 757.8323909638827445, -242.6346026584197659, 352.1044303154654358 ) ) ;
#23437=CARTESIAN_POINT ( 'NONE',  ( 800.9840315886518738, -52.91815448151692891, 354.1144889064786412 ) ) ;
#23441=CARTESIAN_POINT ( 'NONE',  ( 804.1601925771018387, -103.4419599262327836, 346.5483106153029098 ) ) ;
#23445=CARTESIAN_POINT ( 'NONE',  ( 758.0580252608178853, -54.45278447660219001, 328.0187753319985404 ) ) ;
#23448=CARTESIAN_POINT ( 'NONE',  ( 747.3154664389472828, -379.9874144716865203, 326.4474001241230781 ) ) ;
#23450=CARTESIAN_POINT ( 'NONE',  ( 810.7187646348534145, 5.547215523397618142, 356.7737145352016341 ) ) ;
#23452=CARTESIAN_POINT ( 'NONE',  ( 791.9812246680005501, -380.6346026584192828, 361.9419747391813189 ) ) ;
#23460=CARTESIAN_POINT ( 'NONE',  ( 788.7366044899766848, -83.90732993114754379, 316.5762568750059813 ) ) ;
#23461=CARTESIAN_POINT ( 'NONE',  ( 783.0745993439762742, -416.1908817542430938, 365.1016975059196739 ) ) ;
#23462=CARTESIAN_POINT ( 'NONE',  ( 786.6156483768007774, -97.44195992623281199, 315.5913626894246136 ) ) ;
#23463=CARTESIAN_POINT ( 'NONE',  ( 800.9747183278959710, -444.9982390220554862, 311.9810565676471583 ) ) ;
#23465=CARTESIAN_POINT ( 'NONE',  ( 800.1688906516307043, -370.1692326535045936, 369.0717654672308186 ) ) ;
#23469=CARTESIAN_POINT ( 'NONE',  ( 814.8207195650702488, -2.190881754244347945, 336.2433038121456548 ) ) ;
#23476=CARTESIAN_POINT ( 'NONE',  ( 766.9102291470427417, -330.5545181178796952, 318.6633372737382501 ) ) ;
#23478=CARTESIAN_POINT ( 'NONE',  ( 807.2620300519052989, -312.0090635724251911, 318.0141637701419768 ) ) ;
#23482=CARTESIAN_POINT ( 'NONE',  ( 805.6418435158337843, -101.4636090269713264, 363.8556311672236916 ) ) ;
#23485=LINE ( 'NONE', #38285, #35532 ) ;
#23486=CARTESIAN_POINT ( 'NONE',  ( 792.1044303154645831, -156.4527844766018916, 317.8323909638837677 ) ) ;
#23488=CARTESIAN_POINT ( 'NONE',  ( 748.6759233522253680, -424.3726999360612808, 324.3348316497537098 ) ) ;
#23491=CARTESIAN_POINT ( 'NONE',  ( 779.4763451958990572, -56.73633629969872771, 365.0264073115438919 ) ) ;
#23494=CARTESIAN_POINT ( 'NONE',  ( 759.8311093483677041, 25.83076734649409545, 310.9282345327691814 ) ) ;
#23496=CARTESIAN_POINT ( 'NONE',  ( 799.4546378042377910, -81.07832356259649487, 356.1575198192848006 ) ) ;
#23499=CARTESIAN_POINT ( 'NONE',  ( 805.9055244015594326, -267.6237781080504305, 315.8990559732753240 ) ) ;
#23500=CARTESIAN_POINT ( 'NONE',  ( 802.1676090361155502, -86.63460265842024910, 327.8955696845344505 ) ) ;
#23502=CARTESIAN_POINT ( 'NONE',  ( 802.1676090361156639, -254.6346026584196238, 327.8955696845344505 ) ) ;
#23505=DIRECTION ( 'NONE',  ( 0.000000000000000000, 1.000000000000000000, 0.000000000000000000 ) ) ;
#23510=CARTESIAN_POINT ( 'NONE',  ( 772.4837098697145166, -335.3618753856921444, 374.5518280994205611 ) ) ;
#23511=CARTESIAN_POINT ( 'NONE',  ( 788.7631598425961101, -265.4419599262323004, 305.7194118038759143 ) ) ;
#23515=CARTESIAN_POINT ( 'NONE',  ( 758.0580252608178853, -198.4527844766017495, 328.0187753319985404 ) ) ;
#23518=CARTESIAN_POINT ( 'NONE',  ( 777.4774526936600978, -346.2709662947830793, 304.7301800767027657 ) ) ;
#23520=CARTESIAN_POINT ( 'NONE',  ( 762.3223304703356007, 16.45630643248849267, 322.3223304703362828 ) ) ;
#23522=ADVANCED_FACE ( 'NONE', ( #31991 ), #14224, .F. ) ;
#23523=CARTESIAN_POINT ( 'NONE',  ( 755.8894580844503253, -231.8272453906072315, 332.3691319403863531 ) ) ;
#23524=CARTESIAN_POINT ( 'NONE',  ( 774.6858677611749044, -81.72551174932937101, 315.5713283507209894 ) ) ;
#23525=ORIENTED_EDGE ( 'NONE', *, *, #12291, .T. ) ;
#23528=CARTESIAN_POINT ( 'NONE',  ( 798.7617431975189675, -267.6237781080504305, 323.0428371773161871 ) ) ;
#23531=CARTESIAN_POINT ( 'NONE',  ( 745.1792804349281596, -14.19088175424431242, 343.7566961878542884 ) ) ;
#23536=CARTESIAN_POINT ( 'NONE',  ( 763.0537975583475827, -96.45278447660203369, 371.0346526505627480 ) ) ;
#23537=CARTESIAN_POINT ( 'NONE',  ( 796.7737145352015204, -140.6346026584201070, 370.7187646348536987 ) ) ;
#23541=CARTESIAN_POINT ( 'NONE',  ( 766.4474001241216001, -403.0999726633339719, 307.3154664389482491 ) ) ;
#23544=CARTESIAN_POINT ( 'NONE',  ( 801.1904061080336987, -380.0891481129646650, 368.3070685750235498 ) ) ;
#23545=CARTESIAN_POINT ( 'NONE',  ( 782.5225473063383106, 1.729033705215812233, 375.2698199232970637 ) ) ;
#23547=CARTESIAN_POINT ( 'NONE',  ( 759.2295555964440155, -16.16923265350578021, 353.9708237608231229 ) ) ;
#23551=CARTESIAN_POINT ( 'NONE',  ( 766.5853460496234675, -157.9874144716871456, 372.3518521366060554 ) ) ;
#23554=EDGE_LOOP ( 'NONE', ( #8928, #21651 ) ) ;
#23557=CARTESIAN_POINT ( 'NONE',  ( 756.5762568750052424, -147.1800572038746395, 348.7366044899774238 ) ) ;
#23559=CARTESIAN_POINT ( 'NONE',  ( 755.5713283507202505, -293.3618753856923718, 334.6858677611754729 ) ) ;
#23563=CARTESIAN_POINT ( 'NONE',  ( 793.2243759319678702, -2.532869017142183932, 318.4439275373583200 ) ) ;
#23565=VERTEX_POINT ( 'NONE', #17704 ) ;
#23567=CARTESIAN_POINT ( 'NONE',  ( 805.0032342141413437, -205.5436935675108145, 314.9967657858572352 ) ) ;
#23568=CARTESIAN_POINT ( 'NONE',  ( 805.2837595273609850, -338.7363362996978822, 340.5290396650784714 ) ) ;
#23569=CARTESIAN_POINT ( 'NONE',  ( 780.5290396650775619, -420.3510508353225532, 365.2837595273619513 ) ) ;
#23576=ADVANCED_FACE ( 'NONE', ( #817 ), #39868, .T. ) ;
#23577=CARTESIAN_POINT ( 'NONE',  ( 798.7617431975189675, -315.6237781080503169, 323.0428371773161871 ) ) ;
#23578=CARTESIAN_POINT ( 'NONE',  ( 793.4459926374332781, -455.5444164708248422, 371.6295267004306879 ) ) ;
#23581=CARTESIAN_POINT ( 'NONE',  ( 798.5707757039680246, -125.4636090269712412, 356.7845633553585003 ) ) ;
#23582=CARTESIAN_POINT ( 'NONE',  ( 800.0135310231082713, 9.910851887033969021, 325.0180583372163028 ) ) ;
#23585=CARTESIAN_POINT ( 'NONE',  ( 762.1177392798416577, -210.5545181178800647, 309.8865473780659272 ) ) ;
#23589=CARTESIAN_POINT ( 'NONE',  ( 808.0189434323515343, -62.08914811296580183, 319.0252816721025511 ) ) ;
#23590=CARTESIAN_POINT ( 'NONE',  ( 809.0082352070306797, -452.9681489794448908, 335.5949598064873385 ) ) ;
#23592=CARTESIAN_POINT ( 'NONE',  ( 779.9999999999992042, -462.9681489794448339, 339.9999999999999432 ) ) ;
#23593=CARTESIAN_POINT ( 'NONE',  ( 746.4236121716829757, -303.8272453906071178, 328.8385539511384650 ) ) ;
#23595=CARTESIAN_POINT ( 'NONE',  ( 814.5518280994195948, -303.7255117493287457, 332.4837098697145734 ) ) ;
#23599=CARTESIAN_POINT ( 'NONE',  ( 778.1981804954714335, -394.2709662947827951, 314.8072714833589885 ) ) ;
#23600=CARTESIAN_POINT ( 'NONE',  ( 758.4439275373578084, -132.5545181178802920, 353.2243759319684386 ) ) ;
#23602=CARTESIAN_POINT ( 'NONE',  ( 745.1769319972822814, -65.80559628986925702, 346.2694204179732083 ) ) ;
#23603=CARTESIAN_POINT ( 'NONE',  ( 785.3687786644885591, -371.3618753856920307, 315.3201227861280813 ) ) ;
#23605=CARTESIAN_POINT ( 'NONE',  ( 779.9999999999992042, -462.9681489794448339, 339.9999999999999432 ) ) ;
#23606=CARTESIAN_POINT ( 'NONE',  ( 803.4237431249931660, -423.1800572038737300, 331.2633955100225194 ) ) ;
#23610=CARTESIAN_POINT ( 'NONE',  ( 754.8072714833581358, -196.8164208402380950, 338.1981804954720587 ) ) ;
#23611=CARTESIAN_POINT ( 'NONE',  ( 803.4237431249931660, -207.1800572038744406, 331.2633955100225194 ) ) ;
#23615=CARTESIAN_POINT ( 'NONE',  ( 765.0180583372156207, -384.9982390220556567, 360.0135310231089534 ) ) ;
#23618=CARTESIAN_POINT ( 'NONE',  ( 782.4968714119720516, -106.8164208402383935, 305.0891759886411023 ) ) ;
#23624=CARTESIAN_POINT ( 'NONE',  ( 751.6929314249748586, -270.9982390220561115, 318.8095938919659034 ) ) ;
#23625=CARTESIAN_POINT ( 'NONE',  ( 780.5290396650775619, -204.3510508353233774, 365.2837595273619513 ) ) ;
#23626=CARTESIAN_POINT ( 'NONE',  ( 809.4421496042219815, -454.3218287316016699, 345.7584569706272077 ) ) ;
#23629=ORIENTED_EDGE ( 'NONE', *, *, #15427, .F. ) ;
#23631=DIRECTION ( 'NONE',  ( 0.000000000000000000, 0.000000000000000000, 1.000000000000000000 ) ) ;
#23635=CARTESIAN_POINT ( 'NONE',  ( 799.9636004259356241, -94.91815448151677970, 311.2241431872006956 ) ) ;
#23643=CARTESIAN_POINT ( 'NONE',  ( 757.0176451133909268, -445.0999726633338582, 349.9200121543848354 ) ) ;
#23644=CARTESIAN_POINT ( 'NONE',  ( 815.3608509340175488, -362.7363362996977116, 341.2497674668889545 ) ) ;
#23651=CARTESIAN_POINT ( 'NONE',  ( 797.8822607201568644, -222.5545181178800362, 370.1134526219340160 ) ) ;
#23653=CARTESIAN_POINT ( 'NONE',  ( 782.5225473063381969, -190.2709662947835909, 375.2698199232970637 ) ) ;
#23656=CARTESIAN_POINT ( 'NONE',  ( 755.5713283507202505, -269.3618753856924286, 334.6858677611754729 ) ) ;
#23657=CARTESIAN_POINT ( 'NONE',  ( 780.5236548040995785, -68.73633629969867798, 314.9735926884559944 ) ) ;
#23660=DIRECTION ( 'NONE',  ( -0.000000000000000000, 1.000000000000000000, -0.000000000000000000 ) ) ;
#23661=CARTESIAN_POINT ( 'NONE',  ( 775.9200461376533440, -95.80559628986917176, 315.3028492785443291 ) ) ;
#23662=CARTESIAN_POINT ( 'NONE',  ( 755.5713283507202505, -341.3618753856922012, 334.6858677611754729 ) ) ;
#23665=CARTESIAN_POINT ( 'NONE',  ( 755.3201227861273992, -75.72551174932937101, 345.3687786644892981 ) ) ;
#23668=CARTESIAN_POINT ( 'NONE',  ( 788.7631598425961101, -385.4419599262319593, 305.7194118038759143 ) ) ;
#23670=CARTESIAN_POINT ( 'NONE',  ( 797.8594530101008786, -301.5436935675105588, 322.1405469898980982 ) ) ;
#23671=CARTESIAN_POINT ( 'NONE',  ( 812.7932403749906598, 8.819942796124882634, 327.7687537140311633 ) ) ;
#23674=CARTESIAN_POINT ( 'NONE',  ( 801.9419747391806368, -378.4527844766011526, 351.9812246680014027 ) ) ;
#23676=CIRCLE ( 'NONE', #14110, 30.00000000000008171 ) ;
#23678=EDGE_LOOP ( 'NONE', ( #37906, #26507, #19424, #40923 ) ) ;
#23681=CARTESIAN_POINT ( 'NONE',  ( 755.3201227861273992, -99.72551174932928575, 345.3687786644892981 ) ) ;
#23682=CARTESIAN_POINT ( 'NONE',  ( 776.9254006560222479, -404.1908817542431507, 314.8983024940802125 ) ) ;
#23683=CARTESIAN_POINT ( 'NONE',  ( 775.9200461376533440, -95.80559628986917176, 315.3028492785443291 ) ) ;
#23684=CARTESIAN_POINT ( 'NONE',  ( 813.1304606946831655, -449.9073299311464211, 352.3570229623691716 ) ) ;
#23686=CARTESIAN_POINT ( 'NONE',  ( 751.2241431872005251, -352.1692326535046504, 359.9636004259367610 ) ) ;
#23687=CARTESIAN_POINT ( 'NONE',  ( 744.8212110874229666, -114.8965053807782226, 336.2046728542121627 ) ) ;
#23691=CARTESIAN_POINT ( 'NONE',  ( 796.9462024416508257, -444.4527844766009821, 308.9653473494370246 ) ) ;
#23693=CARTESIAN_POINT ( 'NONE',  ( 767.9999999999992042, 240.0000000000000853, 320.0000000000000000 ) ) ;
#23698=CARTESIAN_POINT ( 'NONE',  ( 784.1219089521767955, -333.2817908451523863, 315.0488828828318333 ) ) ;
#23700=CARTESIAN_POINT ( 'NONE',  ( 771.3260364891663130, -307.6454272087888171, 306.0683387631859773 ) ) ;
#23703=CARTESIAN_POINT ( 'NONE',  ( 813.5763878283155464, -99.82724539060768620, 351.1614460488615350 ) ) ;
#23708=CARTESIAN_POINT ( 'NONE',  ( 755.5713283507202505, -149.3618753856928265, 334.6858677611754729 ) ) ;
#23710=CARTESIAN_POINT ( 'NONE',  ( 804.1009440267234822, -431.4636090269702322, 314.0944755984392600 ) ) ;
#23713=CARTESIAN_POINT ( 'NONE',  ( 793.9708237608222134, -46.91815448151694312, 319.2295555964448681 ) ) ;
#23716=CARTESIAN_POINT ( 'NONE',  ( 788.7631598425961101, 22.55804007376682918, 305.7194118038759143 ) ) ;
#23720=CARTESIAN_POINT ( 'NONE',  ( 815.1787889125755555, -270.8965053807777394, 343.7953271457877804 ) ) ;
#23721=CARTESIAN_POINT ( 'NONE',  ( 754.8072714833583632, -100.8164208402383935, 338.1981804954721156 ) ) ;
#23724=CARTESIAN_POINT ( 'NONE',  ( 800.0135310231082713, -278.0891481129651197, 325.0180583372163028 ) ) ;
#23733=CARTESIAN_POINT ( 'NONE',  ( 814.2001403089898304, -353.3618753856922012, 347.4397851343538264 ) ) ;
#23734=CARTESIAN_POINT ( 'NONE',  ( 756.1443688327750579, -261.6237781080504305, 314.3581564841659315 ) ) ;
#23739=CARTESIAN_POINT ( 'NONE',  ( 758.0580252608178853, -246.4527844766016074, 328.0187753319985404 ) ) ;
#23744=CARTESIAN_POINT ( 'NONE',  ( 766.0291762391763086, -226.9181544815163534, 360.7704444035551319 ) ) ;
#23745=CARTESIAN_POINT ( 'NONE',  ( 755.0636971347428243, -76.27096629478394618, 341.7834795799807353 ) ) ;
#23749=CARTESIAN_POINT ( 'NONE',  ( 775.9200461376533440, -263.8055962898686175, 315.3028492785443291 ) ) ;
#23752=CARTESIAN_POINT ( 'NONE',  ( 811.3240766477731540, -4.372699936062523385, 355.6651683502462902 ) ) ;
#23756=CARTESIAN_POINT ( 'NONE',  ( 751.9810565676468741, -74.08914811296577341, 360.9747183278973921 ) ) ;
#23758=CARTESIAN_POINT ( 'NONE',  ( 810.7187646348534145, -138.4527844766019200, 356.7737145352016341 ) ) ;
#23760=CARTESIAN_POINT ( 'NONE',  ( 779.9911637788978851, -452.9681489794448339, 340.0036600600989232 ) ) ;
#23762=CARTESIAN_POINT ( 'NONE',  ( 814.4686193811664907, -411.2817908451521589, 346.2056067578752732 ) ) ;
#23765=CARTESIAN_POINT ( 'NONE',  ( 787.5162901302840055, -395.3618753856918602, 305.4481719005792684 ) ) ;
#23766=CARTESIAN_POINT ( 'NONE',  ( 767.7687537140311633, 0.09267006885218045942, 372.7932403749916830 ) ) ;
#23768=CARTESIAN_POINT ( 'NONE',  ( 776.9566956441375396, -12.89650538077851216, 364.8461984189686405 ) ) ;
#23771=CARTESIAN_POINT ( 'NONE',  ( 771.2368401574024119, -181.4419599262325278, 374.2805881961240857 ) ) ;
#23772=CARTESIAN_POINT ( 'NONE',  ( 785.3141322388236176, 2.274488250670355871, 364.4286716492789537 ) ) ;
#23777=CARTESIAN_POINT ( 'NONE',  ( 795.1360043628807261, -164.0891481129655176, 360.2193346964456282 ) ) ;
#23780=CARTESIAN_POINT ( 'NONE',  ( 801.9419747391806368, -282.4527844766014937, 351.9812246680014027 ) ) ;
#23781=CARTESIAN_POINT ( 'NONE',  ( 781.8018195045267476, -310.2709662947832499, 365.1927285166407273 ) ) ;
#23783=VERTEX_POINT ( 'NONE', #28544 ) ;
#23784=CARTESIAN_POINT ( 'NONE',  ( 758.6633372737375112, -20.53286901714212931, 326.9102291470432533 ) ) ;
#23788=CARTESIAN_POINT ( 'NONE',  ( 787.4397851343537695, -213.7255117493289731, 374.2001403089903988 ) ) ;
#23789=CARTESIAN_POINT ( 'NONE',  ( 763.8424801807145741, -330.0090635724251342, 320.5453621957614700 ) ) ;
#23790=CARTESIAN_POINT ( 'NONE',  ( 755.0488828828309806, -425.8055962898680491, 344.1219089521771934 ) ) ;
#23797=CARTESIAN_POINT ( 'NONE',  ( 754.9735926884551418, -306.3510508353230648, 340.5236548041000333 ) ) ;
#23800=CARTESIAN_POINT ( 'NONE',  ( 773.4516893846965786, -115.6454272087894424, 315.8398074228977066 ) ) ;
#23805=CARTESIAN_POINT ( 'NONE',  ( 776.2046728542105711, -236.1908817542436338, 304.8212110874238761 ) ) ;
#23810=CARTESIAN_POINT ( 'NONE',  ( 811.0346526505616112, -62.63460265842031305, 323.0537975583477532 ) ) ;
#23814=CARTESIAN_POINT ( 'NONE',  ( 749.5768839229115201, -324.5545181178796952, 358.0661480581553064 ) ) ;
#23816=CARTESIAN_POINT ( 'NONE',  ( 808.3070685750230950, -306.9982390220558273, 361.1904061080339261 ) ) ;
#23820=CARTESIAN_POINT ( 'NONE',  ( 804.4286716492782716, -401.3618753856920307, 345.3141322388244703 ) ) ;
#23822=CARTESIAN_POINT ( 'NONE',  ( 793.9708237608222134, -142.9181544815166376, 319.2295555964448681 ) ) ;
#23824=CARTESIAN_POINT ( 'NONE',  ( 759.8311093483677041, -70.16923265350563099, 310.9282345327691814 ) ) ;
#23825=CARTESIAN_POINT ( 'NONE',  ( 795.1360043628808398, -356.0891481129648355, 360.2193346964456282 ) ) ;
#23829=CARTESIAN_POINT ( 'NONE',  ( 758.0580252608178853, -414.4527844766010389, 328.0187753319985404 ) ) ;
#23833=CARTESIAN_POINT ( 'NONE',  ( 800.0135310231082713, -206.0891481129653471, 325.0180583372163028 ) ) ;
#23834=CARTESIAN_POINT ( 'NONE',  ( 759.9864689768902508, -194.0891481129654039, 354.9819416627836404 ) ) ;
#23838=CARTESIAN_POINT ( 'NONE',  ( 804.9363028652555840, -376.2709662947829656, 338.2165204200192079 ) ) ;
#23844=CARTESIAN_POINT ( 'NONE',  ( 751.6929314249750860, -126.9982390220565094, 318.8095938919659034 ) ) ;
#23850=CARTESIAN_POINT ( 'NONE',  ( 756.1348686366196716, -185.2601417444143692, 347.5531968255698416 ) ) ;
#23851=CARTESIAN_POINT ( 'NONE',  ( 808.6142084849417415, -454.8672832770561740, 349.9915990122670451 ) ) ;
#23861=CARTESIAN_POINT ( 'NONE',  ( 781.2370466360911223, -92.73633629969860692, 304.9990715423533629 ) ) ;
#23869=CARTESIAN_POINT ( 'NONE',  ( 755.1538015810308480, -422.1908817542430370, 343.0433043558613804 ) ) ;
#23870=CARTESIAN_POINT ( 'NONE',  ( 811.3240766477731540, -364.3726999360614514, 355.6651683502462902 ) ) ;
#23874=CARTESIAN_POINT ( 'NONE',  ( 768.0187753319979720, 15.36539734157940629, 318.0580252608186242 ) ) ;
#23877=CARTESIAN_POINT ( 'NONE',  ( 812.3518521366052028, -217.0999726633345972, 326.5853460496235243 ) ) ;
#23879=CARTESIAN_POINT ( 'NONE',  ( 763.2262854647970016, -200.6346026584199365, 309.2812353651462445 ) ) ;
#23882=CARTESIAN_POINT ( 'NONE',  ( 762.3223304703356007, -295.5436935675105588, 322.3223304703362828 ) ) ;
#23883=CARTESIAN_POINT ( 'NONE',  ( 805.2837595273609850, -74.73633629969866377, 340.5290396650784714 ) ) ;
#23888=CARTESIAN_POINT ( 'NONE',  ( 756.7813123517142913, -115.9874144716872877, 329.9779781133712504 ) ) ;
#23889=CARTESIAN_POINT ( 'NONE',  ( 757.8323909638827445, -338.6346026584195101, 352.1044303154654358 ) ) ;
#23894=CARTESIAN_POINT ( 'NONE',  ( 762.1405469898971887, -97.54369356751112718, 357.8594530101015607 ) ) ;
#23898=CARTESIAN_POINT ( 'NONE',  ( 786.2056067578752163, -395.8055962898682765, 374.4686193811670023 ) ) ;
#23899=VERTEX_POINT ( 'NONE', #43978 ) ;
#23900=CARTESIAN_POINT ( 'NONE',  ( 756.3353852180819104, -293.9073299311468759, 331.1735550268788302 ) ) ;
#23903=CARTESIAN_POINT ( 'NONE',  ( 797.8594530101008786, -373.5436935675101040, 322.1405469898980982 ) ) ;
#23907=VERTEX_POINT ( 'NONE', #33148 ) ;
#23911=CARTESIAN_POINT ( 'NONE',  ( 754.7162404726377645, -422.7363362996975980, 339.4709603349214717 ) ) ;
#23914=CARTESIAN_POINT ( 'NONE',  ( 814.8230680027162407, -341.8055962898683333, 333.7305795820267917 ) ) ;
#23919=CARTESIAN_POINT ( 'NONE',  ( 749.5768839229115201, -12.55451811788067751, 358.0661480581553064 ) ) ;
#23926=CARTESIAN_POINT ( 'NONE',  ( 783.0745993439762742, -320.1908817542434349, 365.1016975059196739 ) ) ;
#23928=CARTESIAN_POINT ( 'NONE',  ( 813.5763878283155464, -291.8272453906071746, 351.1614460488615350 ) ) ;
#23933=CARTESIAN_POINT ( 'NONE',  ( 755.8990559732751535, -107.4636090269713122, 365.9055244015606831 ) ) ;
#23937=CARTESIAN_POINT ( 'NONE',  ( 803.4237431249931660, -183.1800572038744974, 331.2633955100225194 ) ) ;
#23939=CARTESIAN_POINT ( 'NONE',  ( 797.8822607201568644, -438.5545181178793541, 370.1134526219340160 ) ) ;
#23942=AXIS2_PLACEMENT_3D ( 'NONE', #1072, #11030, #15181 ) ;
#23943=CARTESIAN_POINT ( 'NONE',  ( 758.4439275373578084, -60.55451811788051941, 353.2243759319684386 ) ) ;
#23946=CARTESIAN_POINT ( 'NONE',  ( 772.3691319403857278, -431.2601417444136018, 315.8894580844506663 ) ) ;
#23951=CARTESIAN_POINT ( 'NONE',  ( 803.8556311672234642, -273.6237781080504305, 365.6418435158340117 ) ) ;
#23952=CARTESIAN_POINT ( 'NONE',  ( 774.6312213355098493, -119.3618753856928834, 364.6798772138717482 ) ) ;
#23954=CARTESIAN_POINT ( 'NONE',  ( 781.7834795799800531, -274.8164208402378108, 315.0636971347436202 ) ) ;
#23957=FACE_OUTER_BOUND ( 'NONE', #33858, .T. ) ;
#23964=CARTESIAN_POINT ( 'NONE',  ( 808.3070685750232087, -354.9982390220557136, 361.1904061080339829 ) ) ;
#23965=CARTESIAN_POINT ( 'NONE',  ( 801.9858362298568863, -267.0783235625958696, 312.7379699480935642 ) ) ;
#23970=CARTESIAN_POINT ( 'NONE',  ( 764.8639956371174549, -248.0891481129651481, 319.7806653035542013 ) ) ;
#23971=CARTESIAN_POINT ( 'NONE',  ( 814.5518280994195948, -351.7255117493284047, 332.4837098697145734 ) ) ;
#23975=CARTESIAN_POINT ( 'NONE',  ( 794.6702036691820012, 16.45630643248850689, 314.5864782580647443 ) ) ;
#23978=CARTESIAN_POINT ( 'NONE',  ( 804.4086373105744769, -241.6454272087890729, 333.3843516231986541 ) ) ;
#23979=CARTESIAN_POINT ( 'NONE',  ( 792.1044303154645831, -132.4527844766018916, 317.8323909638837677 ) ) ;
#23983=CARTESIAN_POINT ( 'NONE',  ( 758.6633372737375112, -284.5328690171412518, 326.9102291470432533 ) ) ;
#23986=CARTESIAN_POINT ( 'NONE',  ( 795.8262568251477660, 1.627300063937458408, 308.3538107759623585 ) ) ;
#23988=CARTESIAN_POINT ( 'NONE',  ( 796.7737145352015204, -92.63460265842026331, 370.7187646348536987 ) ) ;
#23989=CARTESIAN_POINT ( 'NONE',  ( 813.1304606946830518, -161.9073299311472454, 352.3570229623690580 ) ) ;
#23992=CARTESIAN_POINT ( 'NONE',  ( 759.9999999999992042, 205.0000000000000568, 360.0000000000000000 ) ) ;
#23994=AXIS2_PLACEMENT_3D ( 'NONE', #35239, #27179, #20909 ) ;
#23995=CARTESIAN_POINT ( 'NONE',  ( 781.2370466360911223, -428.7363362996975980, 304.9990715423533629 ) ) ;
#23998=CARTESIAN_POINT ( 'NONE',  ( 796.9462024416508257, -396.4527844766010389, 308.9653473494370246 ) ) ;
#23999=CARTESIAN_POINT ( 'NONE',  ( 811.0346526505617248, -14.63460265842049779, 323.0537975583478101 ) ) ;
#24002=CARTESIAN_POINT ( 'NONE',  ( 794.1144889064781864, -34.16923265350572336, 360.9840315886528401 ) ) ;
#24006=CARTESIAN_POINT ( 'NONE',  ( 756.1443688327750579, -165.6237781080507716, 314.3581564841659315 ) ) ;
#24007=CARTESIAN_POINT ( 'NONE',  ( 774.6312213355098493, 0.6381246143067237364, 364.6798772138717482 ) ) ;
#24011=CARTESIAN_POINT ( 'NONE',  ( 764.8639956371174549, -176.0891481129653755, 319.7806653035542013 ) ) ;
#24015=CARTESIAN_POINT ( 'NONE',  ( 768.0187753319979720, -296.6346026584195670, 318.0580252608186242 ) ) ;
#24016=CARTESIAN_POINT ( 'NONE',  ( 797.6776695296629214, -283.5436935675105019, 357.6776695296636603 ) ) ;
#24019=ORIENTED_EDGE ( 'NONE', *, *, #14281, .F. ) ;
#24020=CARTESIAN_POINT ( 'NONE',  ( 773.3843516231979720, -13.44195992623305713, 364.4086373105754433 ) ) ;
#24022=CARTESIAN_POINT ( 'NONE',  ( 748.9653473494365699, -266.6346026584197375, 356.9462024416520762 ) ) ;
#24023=CARTESIAN_POINT ( 'NONE',  ( 761.4292242960306112, -329.4636090269706870, 323.2154366446414429 ) ) ;
#24024=CARTESIAN_POINT ( 'NONE',  ( 773.7943932421234194, 24.19440371013046231, 305.5313806188329409 ) ) ;
#24029=CARTESIAN_POINT ( 'NONE',  ( 764.0069404352550464, -351.0783235625955854, 359.2566176426627180 ) ) ;
#24032=CARTESIAN_POINT ( 'NONE',  ( 759.0159684113467620, -136.9181544815166376, 325.8855110935213020 ) ) ;
#24033=CARTESIAN_POINT ( 'NONE',  ( 759.7806653035534055, -30.99823902205680071, 324.8639956371180801 ) ) ;
#24037=CARTESIAN_POINT ( 'NONE',  ( 757.7880784355613741, -234.0090635724255037, 312.4576283171834916 ) ) ;
#24038=CARTESIAN_POINT ( 'NONE',  ( 789.9200121543843807, -193.9874144716870319, 317.0176451133914384 ) ) ;
#24045=CARTESIAN_POINT ( 'NONE',  ( 794.5458710602071051, -452.9681489794447771, 360.4198067286714604 ) ) ;
#24048=CARTESIAN_POINT ( 'NONE',  ( 745.7194118038753459, -325.6454272087888739, 348.7631598425976449 ) ) ;
#24049=CARTESIAN_POINT ( 'NONE',  ( 779.9999999999992042, -462.9681489794448339, 339.9999999999999432 ) ) ;
#24050=CARTESIAN_POINT ( 'NONE',  ( 796.7737145352015204, -308.6346026584195670, 370.7187646348536987 ) ) ;
#24055=CARTESIAN_POINT ( 'NONE',  ( 767.8955696845333705, -408.4527844766009252, 362.1676090361162323 ) ) ;
#24056=CARTESIAN_POINT ( 'NONE',  ( 780.5236548040995785, -140.7363362996984506, 314.9735926884559944 ) ) ;
#24059=CARTESIAN_POINT ( 'NONE',  ( 813.9316612368132837, -55.44195992623293989, 348.6739635108323228 ) ) ;
#24060=CARTESIAN_POINT ( 'NONE',  ( 795.1360043628808398, -380.0891481129647218, 360.2193346964456282 ) ) ;
#24063=( LENGTH_UNIT ( ) NAMED_UNIT ( * ) SI_UNIT ( .MILLI., .METRE. ) );
#24064=CARTESIAN_POINT ( 'NONE',  ( 792.1044303154645831, -420.4527844766009252, 317.8323909638837677 ) ) ;
#24067=VECTOR ( 'NONE', #35408, 1000.000000000000000 ) ;
#24069=CARTESIAN_POINT ( 'NONE',  ( 781.8018195045266339, -190.2709662947835909, 365.1927285166406705 ) ) ;
#24070=CARTESIAN_POINT ( 'NONE',  ( 795.1360043628808398, -188.0891481129653755, 360.2193346964456282 ) ) ;
#24075=CARTESIAN_POINT ( 'NONE',  ( 792.1044303154645831, -396.4527844766010389, 317.8323909638837677 ) ) ;
#24078=VERTEX_POINT ( 'NONE', #5393 ) ;
#24081=CARTESIAN_POINT ( 'NONE',  ( 814.5518280994195948, -135.7255117493291721, 332.4837098697145166 ) ) ;
#24087=CARTESIAN_POINT ( 'NONE',  ( 757.2208543904082489, -208.7146871989596946, 350.9844846989624330 ) ) ;
#24096=CARTESIAN_POINT ( 'NONE',  ( 797.8822607201568644, -126.5545181178803205, 370.1134526219340160 ) ) ;
#24107=CARTESIAN_POINT ( 'NONE',  ( 773.7305795820266212, -369.2817908451523294, 374.8230680027170365 ) ) ;
#24115=CARTESIAN_POINT ( 'NONE',  ( 745.1792804349281596, -206.1908817542437191, 343.7566961878542884 ) ) ;
#24117=CARTESIAN_POINT ( 'NONE',  ( 805.0032342141412300, -205.5436935675108430, 314.9967657858571783 ) ) ;
#24123=CARTESIAN_POINT ( 'NONE',  ( 792.1044303154645831, -276.4527844766013800, 317.8323909638837677 ) ) ;
#24124=CARTESIAN_POINT ( 'NONE',  ( 804.4086373105744769, -49.64542720878965554, 333.3843516231986541 ) ) ;
#24128=CARTESIAN_POINT ( 'NONE',  ( 773.3843516231979720, -133.4419599262326699, 364.4086373105754433 ) ) ;
#24129=CARTESIAN_POINT ( 'NONE',  ( 803.4237431249931660, -327.1800572038741279, 331.2633955100225194 ) ) ;
#24132=CARTESIAN_POINT ( 'NONE',  ( 756.3353852180819104, -77.90732993114757221, 331.1735550268788302 ) ) ;
#24135=CARTESIAN_POINT ( 'NONE',  ( 778.7502325331095108, -432.3510508353226669, 304.6391490659818828 ) ) ;
#24138=CARTESIAN_POINT ( 'NONE',  ( 765.0180583372156207, -288.9982390220559978, 360.0135310231089534 ) ) ;
#24139=( BOUNDED_CURVE ( )  B_SPLINE_CURVE ( 2, ( #22570, #429, #43152, #14533, #11747, #14979, #4137 ),
 .UNSPECIFIED., .F., .T. ) 
 B_SPLINE_CURVE_WITH_KNOTS ( ( 3, 2, 2, 3 ),
 ( 0.000000000000000000, 0.002272727272727272617, 0.004545454545454545234, 0.006081874955971018626 ),
 .UNSPECIFIED. ) 
 CURVE ( )  GEOMETRIC_REPRESENTATION_ITEM ( )  RATIONAL_B_SPLINE_CURVE ( ( 0.5000002209606653203, 0.4949109396520706694, 0.5000002209606653203, 0.4949109396520706694, 0.5000002209606653203, 0.4965597396626160176, 0.4977709609702910543 ) ) 
 REPRESENTATION_ITEM ( '' )  );
#24140=ADVANCED_FACE ( 'NONE', ( #16259 ), #12784, .F. ) ;
#24143=CARTESIAN_POINT ( 'NONE',  ( 771.1735550268778070, -417.1800572038736163, 316.3353852180827630 ) ) ;
#24146=ORIENTED_EDGE ( 'NONE', *, *, #10015, .T. ) ;
#24150=CARTESIAN_POINT ( 'NONE',  ( 755.3201227861273992, -123.7255117493292147, 345.3687786644892981 ) ) ;
#24151=CARTESIAN_POINT ( 'NONE',  ( 755.8894580844503253, -447.8272453906067199, 332.3691319403863531 ) ) ;
#24152=CARTESIAN_POINT ( 'NONE',  ( 805.0264073115434940, -102.3510508353236901, 339.4763451958999099 ) ) ;
#24154=CARTESIAN_POINT ( 'NONE',  ( 799.9999999999993179, 205.0000000000000568, 360.0000000000000000 ) ) ;
#24155=CARTESIAN_POINT ( 'NONE',  ( 776.2433038121456548, -372.8965053807773415, 374.8207195650711014 ) ) ;
#24161=CARTESIAN_POINT ( 'NONE',  ( 776.2046728542105711, -44.19088175424421649, 304.8212110874238761 ) ) ;
#24162=EDGE_CURVE ( 'NONE', #34493, #38419, #3786, .T. ) ;
#24170=CARTESIAN_POINT ( 'NONE',  ( 772.4468031744293057, -321.8272453906070609, 363.8651313633793620 ) ) ;
#24172=CARTESIAN_POINT ( 'NONE',  ( 810.4231160770870019, -288.5545181178798657, 321.9338519418446936 ) ) ;
#24175=CARTESIAN_POINT ( 'NONE',  ( 793.5525998758768083, -103.0999726633349525, 372.6845335610516941 ) ) ;
#24180=CARTESIAN_POINT ( 'NONE',  ( 774.6858677611749044, -201.7255117493290015, 315.5713283507209894 ) ) ;
#24182=CARTESIAN_POINT ( 'NONE',  ( 799.9636004259356241, -430.9181544815157849, 311.2241431872006956 ) ) ;
#24186=CARTESIAN_POINT ( 'NONE',  ( 757.4527132478984868, -64.37269993606231822, 329.1273215169538844 ) ) ;
#24189=CARTESIAN_POINT ( 'NONE',  ( 813.2346286133761168, 18.73985825558501972, 328.9521613784389160 ) ) ;
#24193=CARTESIAN_POINT ( 'NONE',  ( 744.8212110874229666, -282.8965053807776258, 336.2046728542121627 ) ) ;
#24194=CARTESIAN_POINT ( 'NONE',  ( 771.1735550268780344, -105.1800572038747390, 316.3353852180828198 ) ) ;
#24196=CARTESIAN_POINT ( 'NONE',  ( 771.2633955100217236, -311.9073299311468759, 363.4237431249939618 ) ) ;
#24198=CARTESIAN_POINT ( 'NONE',  ( 791.9445882927475395, -448.7226863535211123, 370.2744874727277420 ) ) ;
#24201=CARTESIAN_POINT ( 'NONE',  ( 804.4286716492782716, -41.36187538569314626, 345.3141322388244703 ) ) ;
#24203=CARTESIAN_POINT ( 'NONE',  ( 812.7932403749906598, -375.1800572038739574, 327.7687537140311633 ) ) ;
#24204=CARTESIAN_POINT ( 'NONE',  ( 754.0944755984390895, -255.6237781080504874, 364.1009440267246760 ) ) ;
#24209=CARTESIAN_POINT ( 'NONE',  ( 797.8594530101008786, -253.5436935675104735, 322.1405469898980982 ) ) ;
#24212=CARTESIAN_POINT ( 'NONE',  ( 800.9747183278959710, -348.9982390220558273, 311.9810565676471583 ) ) ;
#24214=PRODUCT_DEFINITION ( 'UNKNOWN', '', #1676, #8864 ) ;
#24218=CARTESIAN_POINT ( 'NONE',  ( 761.4292242960306112, -233.4636090269708575, 323.2154366446414429 ) ) ;
#24219=CARTESIAN_POINT ( 'NONE',  ( 765.0180583372156207, -120.9982390220565378, 360.0135310231089534 ) ) ;
#24223=CARTESIAN_POINT ( 'NONE',  ( 795.9930595647434757, -291.0783235625957559, 320.7433823573372820 ) ) ;
#24226=CARTESIAN_POINT ( 'NONE',  ( 812.3518521366052028, -1.099972663335260226, 326.5853460496235243 ) ) ;
#24228=CARTESIAN_POINT ( 'NONE',  ( 751.6929314249748586, -174.9982390220563673, 318.8095938919659034 ) ) ;
#24229=CARTESIAN_POINT ( 'NONE',  ( 797.6776695296629214, -91.54369356751116982, 357.6776695296636603 ) ) ;
#24233=CARTESIAN_POINT ( 'NONE',  ( 746.4236121716829757, -423.8272453906067199, 328.8385539511384650 ) ) ;
#24236=CARTESIAN_POINT ( 'NONE',  ( 745.0891759886404770, -388.2709662947829656, 342.4968714119734159 ) ) ;
#24237=CARTESIAN_POINT ( 'NONE',  ( 772.5602148656447525, -9.725511749329603717, 305.7998596910095443 ) ) ;
#24239=CARTESIAN_POINT ( 'NONE',  ( 803.2186876482843445, -7.987414471687621642, 350.0220218866286928 ) ) ;
#24242=CARTESIAN_POINT ( 'NONE',  ( 759.8311093483677041, -166.1692326535053041, 310.9282345327691814 ) ) ;
#24243=CARTESIAN_POINT ( 'NONE',  ( 800.2193346964446619, -18.99823902205684689, 355.1360043628816925 ) ) ;
#24249=CARTESIAN_POINT ( 'NONE',  ( 797.6776695296629214, -163.5436935675109567, 357.6776695296636603 ) ) ;
#24251=CARTESIAN_POINT ( 'NONE',  ( 759.7806653035535192, -318.9982390220558841, 324.8639956371181370 ) ) ;
#24253=ORIENTED_EDGE ( 'NONE', *, *, #5775, .T. ) ;
#24254=CARTESIAN_POINT ( 'NONE',  ( 804.1601925771018387, -31.44195992623299674, 346.5483106153029098 ) ) ;
#24256=CARTESIAN_POINT ( 'NONE',  ( 796.7737145352015204, -260.6346026584197375, 370.7187646348536987 ) ) ;
#24257=CARTESIAN_POINT ( 'NONE',  ( 793.0897708529556667, -318.5545181178796952, 361.3366627262616362 ) ) ;
#24258=CARTESIAN_POINT ( 'NONE',  ( 760.5453621957607311, -429.0783235625953580, 323.8424801807151425 ) ) ;
#24263=CARTESIAN_POINT ( 'NONE',  ( 798.7617431975189675, -339.6237781080502600, 323.0428371773161871 ) ) ;
#24265=CARTESIAN_POINT ( 'NONE',  ( 766.9102291470427417, -138.5545181178802636, 318.6633372737382501 ) ) ;
#24266=CARTESIAN_POINT ( 'NONE',  ( 785.3687786644884454, -11.36187538569323863, 315.3201227861279676 ) ) ;
#24271=CARTESIAN_POINT ( 'NONE',  ( 796.1575198192839480, -222.0090635724254184, 359.4546378042384163 ) ) ;
#24272=CARTESIAN_POINT ( 'NONE',  ( 746.4236121716829757, -231.8272453906072315, 328.8385539511384650 ) ) ;
#24274=CARTESIAN_POINT ( 'NONE',  ( 787.6308680596127942, -203.2601417444143124, 364.1105419155492768 ) ) ;
#24278=CARTESIAN_POINT ( 'NONE',  ( 772.5602148656447525, -81.72551174932937101, 305.7998596910095443 ) ) ;
#24279=CARTESIAN_POINT ( 'NONE',  ( 799.5976253717891495, -452.9681489794447771, 356.1016198435977458 ) ) ;
#24282=CARTESIAN_POINT ( 'NONE',  ( 802.2119215644370342, -366.0090635724250774, 367.5423716828165084 ) ) ;
#24288=CARTESIAN_POINT ( 'NONE',  ( 805.1927285166397041, -400.8164208402373561, 341.8018195045277707 ) ) ;
#24289=CARTESIAN_POINT ( 'NONE',  ( 800.9840315886518738, -148.9181544815166092, 354.1144889064786412 ) ) ;
#24292=CARTESIAN_POINT ( 'NONE',  ( 803.8556311672234642, -81.62377810805104161, 365.6418435158340117 ) ) ;
#24293=CARTESIAN_POINT ( 'NONE',  ( 802.1676090361155502, -422.6346026584191691, 327.8955696845344505 ) ) ;
#24294=CARTESIAN_POINT ( 'NONE',  ( 787.5162901302840055, 12.63812461430668677, 305.4481719005793252 ) ) ;
#24296=CARTESIAN_POINT ( 'NONE',  ( 754.0944755984390895, -135.6237781080508853, 364.1009440267246760 ) ) ;
#24297=CARTESIAN_POINT ( 'NONE',  ( 797.8594530101008786, -421.5436935675101040, 322.1405469898980982 ) ) ;
#24298=ORIENTED_EDGE ( 'NONE', *, *, #42804, .F. ) ;
#24301=CARTESIAN_POINT ( 'NONE',  ( 795.1360043628807261, -212.0891481129652902, 360.2193346964456282 ) ) ;
#24302=CARTESIAN_POINT ( 'NONE',  ( 800.0135310231082713, -182.0891481129654323, 325.0180583372163028 ) ) ;
#24305=EDGE_LOOP ( 'NONE', ( #11205, #9275, #42207, #34889 ) ) ;
#24306=CARTESIAN_POINT ( 'NONE',  ( 781.8018195045266339, -382.2709662947828519, 365.1927285166406705 ) ) ;
#24307=VECTOR ( 'NONE', #43145, 1000.000000000000000 ) ;
#24311=CARTESIAN_POINT ( 'NONE',  ( 787.5162901302840055, -155.3618753856927697, 305.4481719005793252 ) ) ;
#24318=CARTESIAN_POINT ( 'NONE',  ( 804.1601925771018387, -247.4419599262323004, 346.5483106153029098 ) ) ;
#24327=CARTESIAN_POINT ( 'NONE',  ( 748.6759233522253680, -136.3726999360621051, 324.3348316497537098 ) ) ;
#24334=CARTESIAN_POINT ( 'NONE',  ( 788.6739635108323228, -391.6454272087885897, 373.9316612368139090 ) ) ;
#24341=CARTESIAN_POINT ( 'NONE',  ( 812.3518521366052028, -241.0999726633345119, 326.5853460496235243 ) ) ;
#24343=CARTESIAN_POINT ( 'NONE',  ( 782.4968714119720516, -178.8164208402381519, 305.0891759886411023 ) ) ;
#24345=CARTESIAN_POINT ( 'NONE',  ( 779.9999999999992042, -452.9681489794448339, 339.9999999999999432 ) ) ;
#24346=CARTESIAN_POINT ( 'NONE',  ( 785.3141322388236176, -285.7255117493286889, 364.4286716492789537 ) ) ;
#24347=CARTESIAN_POINT ( 'NONE',  ( 757.0176451133909268, -61.09997266333506616, 349.9200121543848354 ) ) ;
#24351=CARTESIAN_POINT ( 'NONE',  ( 757.2208543904082489, -136.7146871989600072, 350.9844846989624330 ) ) ;
#24352=CARTESIAN_POINT ( 'NONE',  ( 771.1735550268778070, -321.1800572038740142, 316.3353852180827630 ) ) ;
#24355=CARTESIAN_POINT ( 'NONE',  ( 788.7366044899766848, -83.90732993114754379, 316.5762568750059813 ) ) ;
#24358=CARTESIAN_POINT ( 'NONE',  ( 803.8556311672234642, -417.6237781080499190, 365.6418435158340117 ) ) ;
#24360=CARTESIAN_POINT ( 'NONE',  ( 797.8594530101008786, -277.5436935675105019, 322.1405469898980982 ) ) ;
#24364=CARTESIAN_POINT ( 'NONE',  ( 797.8594530101008786, -397.5436935675100472, 322.1405469898980982 ) ) ;
#24370=CARTESIAN_POINT ( 'NONE',  ( 788.7366044899766848, -131.9073299311473875, 316.5762568750059813 ) ) ;
#24371=CARTESIAN_POINT ( 'NONE',  ( 760.5453621957607311, -117.0783235625963528, 323.8424801807151425 ) ) ;
#24372=LINE ( 'NONE', #14005, #11523 ) ;
#24374=CARTESIAN_POINT ( 'NONE',  ( 813.2346286133761168, -365.2601417444137155, 328.9521613784389160 ) ) ;
#24380=CARTESIAN_POINT ( 'NONE',  ( 791.0478386215596629, -21.82724539060792424, 306.7653713866226326 ) ) ;
#24388=CARTESIAN_POINT ( 'NONE',  ( 755.8894580844503253, -375.8272453906069472, 332.3691319403863531 ) ) ;
#24389=CARTESIAN_POINT ( 'NONE',  ( 812.3518521366052028, -337.0999726633342561, 326.5853460496235243 ) ) ;
#24393=CARTESIAN_POINT ( 'NONE',  ( 745.7194118038753459, -157.6454272087893287, 348.7631598425976449 ) ) ;
#24399=CARTESIAN_POINT ( 'NONE',  ( 795.1360043628807261, -188.0891481129653187, 360.2193346964456282 ) ) ;
#24401=CARTESIAN_POINT ( 'NONE',  ( 810.4231160770870019, -432.5545181178793541, 321.9338519418446936 ) ) ;
#24406=CARTESIAN_POINT ( 'NONE',  ( 815.1787889125755555, -6.896505380778533478, 343.7953271457877804 ) ) ;
#24410=CARTESIAN_POINT ( 'NONE',  ( 815.0009284576459549, -318.3510508353230080, 338.7629533639073429 ) ) ;
#24411=CARTESIAN_POINT ( 'NONE',  ( 794.9819416627830151, -132.9982390220564810, 319.9864689768909898 ) ) ;
#24414=CARTESIAN_POINT ( 'NONE',  ( 755.3201227861273992, -315.7255117493286320, 345.3687786644892981 ) ) ;
#24415=ADVANCED_FACE ( 'NONE', ( #11793 ), #29568, .F. ) ;
#24417=CARTESIAN_POINT ( 'NONE',  ( 789.4860707548003802, -452.3212000445050762, 363.1417840971553233 ) ) ;
#24420=VERTEX_POINT ( 'NONE', #39530 ) ;
#24421=CARTESIAN_POINT ( 'NONE',  ( 803.4237431249931660, -39.18005720387496638, 331.2633955100225194 ) ) ;
#24424=CARTESIAN_POINT ( 'NONE',  ( 787.5162901302840055, -347.3618753856922012, 305.4481719005793252 ) ) ;
#24425=CARTESIAN_POINT ( 'NONE',  ( 759.8311093483677041, -238.1692326535050768, 310.9282345327691814 ) ) ;
#24427=CARTESIAN_POINT ( 'NONE',  ( 805.9055244015594326, -75.62377810805104161, 315.8990559732753240 ) ) ;
#24432=CARTESIAN_POINT ( 'NONE',  ( 792.1044303154645831, -228.4527844766015789, 317.8323909638837677 ) ) ;
#24434=CARTESIAN_POINT ( 'NONE',  ( 767.7687537140311633, -407.9073299311465348, 372.7932403749916830 ) ) ;
#24437=DIRECTION ( 'NONE',  ( 0.000000000000000000, 0.000000000000000000, -1.000000000000000000 ) ) ;
#24439=CARTESIAN_POINT ( 'NONE',  ( 761.4292242960306112, -257.4636090269708575, 323.2154366446414429 ) ) ;
#24440=CARTESIAN_POINT ( 'NONE',  ( 768.0187753319979720, -104.6346026584202207, 318.0580252608186242 ) ) ;
#24445=CARTESIAN_POINT ( 'NONE',  ( 757.2208543904082489, -304.7146871989594388, 350.9844846989624330 ) ) ;
#24446=CARTESIAN_POINT ( 'NONE',  ( 799.9999999999993179, 205.0000000000000568, 319.9999999999999432 ) ) ;
#24447=CARTESIAN_POINT ( 'NONE',  ( 776.2046728542105711, 3.809118245755632959, 304.8212110874238761 ) ) ;
#24449=CARTESIAN_POINT ( 'NONE',  ( 782.5225473063381969, -190.2709662947835909, 375.2698199232970637 ) ) ;
#24450=CARTESIAN_POINT ( 'NONE',  ( 795.1360043628807261, -68.08914811296575920, 360.2193346964456282 ) ) ;
#24453=CARTESIAN_POINT ( 'NONE',  ( 748.6759233522253680, -448.3726999360611103, 324.3348316497537098 ) ) ;
#24456=CARTESIAN_POINT ( 'NONE',  ( 804.1601925771018387, -367.4419599262319025, 346.5483106153029098 ) ) ;
#24457=CARTESIAN_POINT ( 'NONE',  ( 763.0537975583476964, -48.45278447660221133, 371.0346526505628617 ) ) ;
#24460=CARTESIAN_POINT ( 'NONE',  ( 798.7617431975189675, -3.623778108051270319, 323.0428371773161871 ) ) ;
#24463=CARTESIAN_POINT ( 'NONE',  ( 807.5423716828161105, -201.0783235625961254, 362.2119215644372048 ) ) ;
#24464=CARTESIAN_POINT ( 'NONE',  ( 785.3687786644885591, -11.36187538569323863, 315.3201227861280813 ) ) ;
#24465=EDGE_CURVE ( 'NONE', #13889, #32644, #15489, .T. ) ;
#24466=CARTESIAN_POINT ( 'NONE',  ( 784.0799538623451781, -371.8055962898682765, 364.6971507214555572 ) ) ;
#24469=CARTESIAN_POINT ( 'NONE',  ( 804.4286716492782716, -185.3618753856926844, 345.3141322388244703 ) ) ;
#24471=CARTESIAN_POINT ( 'NONE',  ( 765.0180583372156207, -336.9982390220558273, 360.0135310231089534 ) ) ;
#24474=VERTEX_POINT ( 'NONE', #12014 ) ;
#24475=CARTESIAN_POINT ( 'NONE',  ( 756.7813123517142913, -67.98741447168742980, 329.9779781133712504 ) ) ;
#24478=CARTESIAN_POINT ( 'NONE',  ( 763.0537975583476964, -240.4527844766015789, 371.0346526505628617 ) ) ;
#24479=CARTESIAN_POINT ( 'NONE',  ( 759.0159684113467620, -352.9181544815159555, 325.8855110935213020 ) ) ;
#24480=CARTESIAN_POINT ( 'NONE',  ( 808.7758568127978833, 19.83076734649410966, 320.0363995740631822 ) ) ;
#24485=CARTESIAN_POINT ( 'NONE',  ( 767.6429770376289525, -297.1800572038740711, 306.8695393053162093 ) ) ;
#24486=CARTESIAN_POINT ( 'NONE',  ( 804.1601925771018387, -319.4419599262320730, 346.5483106153029098 ) ) ;
#24488=CARTESIAN_POINT ( 'NONE',  ( 804.1105419155481968, -123.8272453906076009, 347.6308680596136469 ) ) ;
#24489=CARTESIAN_POINT ( 'NONE',  ( 788.8264449731200330, -21.18005720387502677, 363.6646147819171233 ) ) ;
#24494=CARTESIAN_POINT ( 'NONE',  ( 778.7629533639073998, -248.7363362996981380, 375.0009284576466371 ) ) ;
#24495=CARTESIAN_POINT ( 'NONE',  ( 794.1144889064781864, -178.1692326535052473, 360.9840315886528401 ) ) ;
#24499=CARTESIAN_POINT ( 'NONE',  ( 747.2067596250078623, -27.18005720387500901, 352.2312462859687230 ) ) ;
#24500=CARTESIAN_POINT ( 'NONE',  ( 755.2512626584698410, -79.54369356751119824, 315.2512626584710915 ) ) ;
#24504=CARTESIAN_POINT ( 'NONE',  ( 755.8990559732751535, -347.4636090269705733, 365.9055244015606831 ) ) ;
#24506=CARTESIAN_POINT ( 'NONE',  ( 759.0252816721024374, -312.9982390220559409, 368.0189434323527280 ) ) ;
#24510=CARTESIAN_POINT ( 'NONE',  ( 801.9419747391806368, -402.4527844766010389, 351.9812246680014027 ) ) ;
#24511=CARTESIAN_POINT ( 'NONE',  ( 790.0220218866281812, -151.0999726633347677, 363.2186876482849129 ) ) ;
#24514=CARTESIAN_POINT ( 'NONE',  ( 814.8230680027162407, -53.80559628986930676, 333.7305795820267917 ) ) ;
#24515=CARTESIAN_POINT ( 'NONE',  ( 759.9864689768902508, -410.0891481129647218, 354.9819416627836404 ) ) ;
#24518=CARTESIAN_POINT ( 'NONE',  ( 807.5423716828161105, -153.0783235625962675, 362.2119215644372048 ) ) ;
#24524=CARTESIAN_POINT ( 'NONE',  ( 803.4237431249931660, -231.1800572038743553, 331.2633955100225194 ) ) ;
#24525=CARTESIAN_POINT ( 'NONE',  ( 756.5762568750052424, -243.1800572038743269, 348.7366044899774238 ) ) ;
#24530=CARTESIAN_POINT ( 'NONE',  ( 774.6858677611749044, -441.7255117493282910, 315.5713283507209894 ) ) ;
#24533=CARTESIAN_POINT ( 'NONE',  ( 758.8095938919644823, -152.0891481129655460, 311.6929314249762797 ) ) ;
#24534=ORIENTED_EDGE ( 'NONE', *, *, #23250, .T. ) ;
#24539=CARTESIAN_POINT ( 'NONE',  ( 786.6156483768007774, -217.4419599262324141, 315.5913626894246136 ) ) ;
#24548=CARTESIAN_POINT ( 'NONE',  ( 814.4686193811664907, -147.2817908451529547, 346.2056067578752732 ) ) ;
#24562=CARTESIAN_POINT ( 'NONE',  ( 814.2805881961230625, -241.6454272087890729, 331.2368401574024119 ) ) ;
#24564=CARTESIAN_POINT ( 'NONE',  ( 796.9462024416508257, -180.4527844766017211, 308.9653473494370246 ) ) ;
#24567=CARTESIAN_POINT ( 'NONE',  ( 791.9812246680005501, -284.6346026584196807, 361.9419747391813189 ) ) ;
#24568=CARTESIAN_POINT ( 'NONE',  ( 793.9708237608222134, -94.91815448151677970, 319.2295555964448681 ) ) ;
#24573=CARTESIAN_POINT ( 'NONE',  ( 756.7813123517142913, -139.9874144716872024, 329.9779781133712504 ) ) ;
#24574=CARTESIAN_POINT ( 'NONE',  ( 754.8072714833581358, -316.8164208402377540, 338.1981804954720587 ) ) ;
#24577=CARTESIAN_POINT ( 'NONE',  ( 804.4286716492782716, -89.36187538569299704, 345.3141322388244703 ) ) ;
#24581=CARTESIAN_POINT ( 'NONE',  ( 758.0141637701419768, -423.0783235625953580, 367.2620300519063790 ) ) ;
#24583=CARTESIAN_POINT ( 'NONE',  ( 803.4237431249931660, -303.1800572038740711, 331.2633955100225194 ) ) ;
#24587=CARTESIAN_POINT ( 'NONE',  ( 794.9819416627830151, -396.9982390220556567, 319.9864689768909898 ) ) ;
#24592=CARTESIAN_POINT ( 'NONE',  ( 804.6798772138708955, -135.7255117493291152, 334.6312213355107019 ) ) ;
#24593=CARTESIAN_POINT ( 'NONE',  ( 766.0291762391763086, -442.9181544815157849, 360.7704444035551319 ) ) ;
#24594=CARTESIAN_POINT ( 'NONE',  ( 756.7813123517142913, -115.9874144716872877, 329.9779781133712504 ) ) ;
#24597=CARTESIAN_POINT ( 'NONE',  ( 764.3348316497523456, -406.7146871989590409, 308.6759233522265617 ) ) ;
#24603=CARTESIAN_POINT ( 'NONE',  ( 783.7953271457878373, -32.19088175424425913, 375.1787889125761239 ) ) ;
#24612=CARTESIAN_POINT ( 'NONE',  ( 776.9254006560222479, -356.1908817542432075, 314.8983024940802125 ) ) ;
#24613=CARTESIAN_POINT ( 'NONE',  ( 814.4686193811664907, -339.2817908451524431, 346.2056067578752732 ) ) ;
#24617=CARTESIAN_POINT ( 'NONE',  ( 812.3518521366052028, -145.0999726633347677, 326.5853460496235243 ) ) ;
#24623=CARTESIAN_POINT ( 'NONE',  ( 781.7834795799800531, -178.8164208402381519, 315.0636971347436202 ) ) ;
#24627=CARTESIAN_POINT ( 'NONE',  ( 745.1792804349281596, -446.1908817542429802, 343.7566961878542884 ) ) ;
#24632=CARTESIAN_POINT ( 'NONE',  ( 795.6651683502461765, -10.71468719896033761, 371.3240766477733814 ) ) ;
#24637=CARTESIAN_POINT ( 'NONE',  ( 815.1787889125755555, -294.8965053807775689, 343.7953271457877804 ) ) ;
#24638=CARTESIAN_POINT ( 'NONE',  ( 785.3687786644885591, -107.3618753856928976, 315.3201227861280813 ) ) ;
#24642=CARTESIAN_POINT ( 'NONE',  ( 803.4237431249931660, -303.1800572038740711, 331.2633955100225194 ) ) ;
#24649=ORIENTED_EDGE ( 'NONE', *, *, #39488, .T. ) ;
#24652=CARTESIAN_POINT ( 'NONE',  ( 756.5762568750052424, -27.18005720387500901, 348.7366044899774238 ) ) ;
#24654=CARTESIAN_POINT ( 'NONE',  ( 787.4397851343537695, -357.7255117493285184, 374.2001403089903988 ) ) ;
#24655=CARTESIAN_POINT ( 'NONE',  ( 805.9055244015594326, -291.6237781080503169, 315.8990559732753240 ) ) ;
#24656=CARTESIAN_POINT ( 'NONE',  ( 795.6651683502461765, -82.71468719896012090, 371.3240766477733814 ) ) ;
#24663=CARTESIAN_POINT ( 'NONE',  ( 801.9419747391806368, -258.4527844766016074, 351.9812246680014027 ) ) ;
#24664=CARTESIAN_POINT ( 'NONE',  ( 767.6429770376289525, -393.1800572038737300, 306.8695393053162093 ) ) ;
#24670=CARTESIAN_POINT ( 'NONE',  ( 793.0897708529556667, -246.5545181178799510, 361.3366627262616362 ) ) ;
#24671=CARTESIAN_POINT ( 'NONE',  ( 788.7366044899766848, -107.9073299311474727, 316.5762568750059813 ) ) ;
#24675=CARTESIAN_POINT ( 'NONE',  ( 756.7813123517142913, -283.9874144716867477, 329.9779781133712504 ) ) ;
#24679=CARTESIAN_POINT ( 'NONE',  ( 755.8990559732751535, -35.46360902697151829, 365.9055244015606831 ) ) ;
#24683=CARTESIAN_POINT ( 'NONE',  ( 804.9363028652555840, -88.27096629478390355, 338.2165204200192079 ) ) ;
#24686=CARTESIAN_POINT ( 'NONE',  ( 797.8822607201568644, -462.5545181178792973, 370.1134526219340160 ) ) ;
#24689=CARTESIAN_POINT ( 'NONE',  ( 796.7845633553578182, -345.6237781080501463, 358.5707757039688204 ) ) ;
#24690=CARTESIAN_POINT ( 'NONE',  ( 804.7487373415286811, -43.54369356751131903, 364.7487373415288516 ) ) ;
#24694=CARTESIAN_POINT ( 'NONE',  ( 755.0488828828309806, -41.80559628986934229, 344.1219089521771934 ) ) ;
#24697=CARTESIAN_POINT ( 'NONE',  ( 768.8385539511368734, -215.2601417444141987, 306.4236121716840557 ) ) ;
#24698=CARTESIAN_POINT ( 'NONE',  ( 802.1676090361155502, -14.63460265842049779, 327.8955696845344505 ) ) ;
#24702=CARTESIAN_POINT ( 'NONE',  ( 788.8264449731200330, -189.1800572038744122, 363.6646147819171233 ) ) ;
#24704=CARTESIAN_POINT ( 'NONE',  ( 762.1405469898973024, -313.5436935675103882, 357.8594530101016176 ) ) ;
#24708=CARTESIAN_POINT ( 'NONE',  ( 760.5453621957607311, -45.07832356259660145, 323.8424801807151425 ) ) ;
#24713=CARTESIAN_POINT ( 'NONE',  ( 782.5225473063383106, -262.2709662947832499, 375.2698199232970637 ) ) ;
#24715=CARTESIAN_POINT ( 'NONE',  ( 776.2433038121456548, 11.10349461922141145, 374.8207195650711014 ) ) ;
#24720=CARTESIAN_POINT ( 'NONE',  ( 745.4481719005789273, -291.7255117493285752, 347.5162901302853129 ) ) ;
#24722=CARTESIAN_POINT ( 'NONE',  ( 760.5453621957607311, -333.0783235625956991, 323.8424801807151425 ) ) ;
#24724=CARTESIAN_POINT ( 'NONE',  ( 776.9254006560222479, -140.1908817542438896, 314.8983024940802125 ) ) ;
#24725=CARTESIAN_POINT ( 'NONE',  ( 781.8018195045266339, -22.27096629478410250, 365.1927285166406705 ) ) ;
#24730=CARTESIAN_POINT ( 'NONE',  ( 793.0897708529556667, -222.5545181178800362, 361.3366627262616362 ) ) ;
#24731=CARTESIAN_POINT ( 'NONE',  ( 760.0363995740630116, -250.9181544815163534, 368.7758568127991907 ) ) ;
#24732=CARTESIAN_POINT ( 'NONE',  ( 765.8855110935204493, -190.1692326535052189, 319.0159684113471599 ) ) ;
#24733=AXIS2_PLACEMENT_3D ( 'NONE', #1541, #26486, #33411 ) ;
#24736=CARTESIAN_POINT ( 'NONE',  ( 796.1575198192839480, -462.0090635724247932, 359.4546378042384163 ) ) ;
#24740=EDGE_CURVE ( 'NONE', #8326, #755, #7128, .T. ) ;
#24741=CARTESIAN_POINT ( 'NONE',  ( 748.9653473494363425, -2.634602658420536869, 356.9462024416521331 ) ) ;
#24746=CARTESIAN_POINT ( 'NONE',  ( 811.3240766477731540, -364.3726999360614514, 355.6651683502462902 ) ) ;
#24748=CARTESIAN_POINT ( 'NONE',  ( 808.0189434323515343, -326.0891481129649492, 319.0252816721025511 ) ) ;
#24753=CARTESIAN_POINT ( 'NONE',  ( 764.8639956371174549, -416.0891481129645513, 319.7806653035542013 ) ) ;
#24754=CARTESIAN_POINT ( 'NONE',  ( 802.9823548866075953, -169.0999726633347393, 330.0799878456151077 ) ) ;
#24757=CARTESIAN_POINT ( 'NONE',  ( 745.1769319972822814, -113.8055962898691149, 346.2694204179732083 ) ) ;
#24758=CARTESIAN_POINT ( 'NONE',  ( 765.0180583372156207, -408.9982390220556567, 360.0135310231089534 ) ) ;
#24764=CARTESIAN_POINT ( 'NONE',  ( 754.8072714833581358, -244.8164208402378961, 338.1981804954720587 ) ) ;
#24765=CARTESIAN_POINT ( 'NONE',  ( 795.1360043628808398, -212.0891481129653187, 360.2193346964456282 ) ) ;
#24768=CARTESIAN_POINT ( 'NONE',  ( 759.0252816721024374, -0.9982390220569063999, 368.0189434323527280 ) ) ;
#24771=CARTESIAN_POINT ( 'NONE',  ( 788.8264449731200330, -429.1800572038737869, 363.6646147819171233 ) ) ;
#24776=CARTESIAN_POINT ( 'NONE',  ( 814.2001403089898304, -137.3618753856928265, 347.4397851343538264 ) ) ;
#24783=CARTESIAN_POINT ( 'NONE',  ( 787.6308680596127942, -227.2601417444141987, 364.1105419155492768 ) ) ;
#24793=CARTESIAN_POINT ( 'NONE',  ( 788.6739635108323228, -151.6454272087892718, 373.9316612368139090 ) ) ;
#24799=CARTESIAN_POINT ( 'NONE',  ( 813.5763878283155464, -387.8272453906067767, 351.1614460488615350 ) ) ;
#24803=CARTESIAN_POINT ( 'NONE',  ( 755.5713283507202505, -5.361875385693257279, 334.6858677611754729 ) ) ;
#24805=CARTESIAN_POINT ( 'NONE',  ( 802.2119215644370342, -246.0090635724253900, 367.5423716828165084 ) ) ;
#24807=CARTESIAN_POINT ( 'NONE',  ( 745.0891759886404770, -220.2709662947834772, 342.4968714119734159 ) ) ;
#24811=CARTESIAN_POINT ( 'NONE',  ( 771.2633955100217236, -287.9073299311468759, 363.4237431249939618 ) ) ;
#24812=CARTESIAN_POINT ( 'NONE',  ( 787.5531968255692163, -93.82724539060770041, 316.1348686366205811 ) ) ;
#24816=CARTESIAN_POINT ( 'NONE',  ( 770.0799878456142551, -133.9874144716872024, 362.9823548866085616 ) ) ;
#24817=CARTESIAN_POINT ( 'NONE',  ( 803.6646147819161570, -377.9073299311466485, 348.8264449731210561 ) ) ;
#24821=CARTESIAN_POINT ( 'NONE',  ( 794.9819416627830151, -108.9982390220565804, 319.9864689768909898 ) ) ;
#24824=CARTESIAN_POINT ( 'NONE',  ( 764.3348316497523456, -406.7146871989590409, 308.6759233522265617 ) ) ;
#24826=CARTESIAN_POINT ( 'NONE',  ( 804.6798772138708955, -327.7255117493285184, 334.6312213355107019 ) ) ;
#24830=CARTESIAN_POINT ( 'NONE',  ( 755.5713283507202505, -413.3618753856920307, 334.6858677611754729 ) ) ;
#24837=CARTESIAN_POINT ( 'NONE',  ( 802.5472867521000353, -436.3726999360612240, 350.8726784830461156 ) ) ;
#24838=CARTESIAN_POINT ( 'NONE',  ( 765.8855110935204493, -118.1692326535054463, 319.0159684113471599 ) ) ;
#24840=DIRECTION ( 'NONE',  ( 0.000000000000000000, -1.000000000000000000, -1.110223024625155554E-15 ) ) ;
#24842=CARTESIAN_POINT ( 'NONE',  ( 768.8385539511368734, -383.2601417444137155, 306.4236121716840557 ) ) ;
#24847=CARTESIAN_POINT ( 'NONE',  ( 766.4474001241216001, -19.09997266333520116, 307.3154664389482491 ) ) ;
#24852=DIRECTION ( 'NONE',  ( -1.000000000000000000, -0.000000000000000000, 0.000000000000000000 ) ) ;
#24857=CARTESIAN_POINT ( 'NONE',  ( 773.4516893846965786, -355.6454272087887603, 315.8398074228977066 ) ) ;
#24858=CARTESIAN_POINT ( 'NONE',  ( 752.7379699480933368, -348.0090635724251342, 361.9858362298580232 ) ) ;
#24862=CARTESIAN_POINT ( 'NONE',  ( 750.9282345327678740, -160.9181544815165807, 319.8311093483690115 ) ) ;
#24864=CARTESIAN_POINT ( 'NONE',  ( 777.4774526936600978, -106.2709662947838467, 304.7301800767027657 ) ) ;
#24868=CARTESIAN_POINT ( 'NONE',  ( 771.2633955100217236, -167.9073299311473022, 363.4237431249939618 ) ) ;
#24869=CARTESIAN_POINT ( 'NONE',  ( 787.5531968255692163, 2.172754609392001601, 316.1348686366205811 ) ) ;
#24874=CARTESIAN_POINT ( 'NONE',  ( 800.1688906516307043, -10.16923265350579442, 369.0717654672308186 ) ) ;
#24879=CARTESIAN_POINT ( 'NONE',  ( 771.2368401574024119, -325.4419599262320162, 374.2805881961240857 ) ) ;
#24880=CARTESIAN_POINT ( 'NONE',  ( 804.9363028652555840, -136.2709662947837330, 338.2165204200192079 ) ) ;
#24883=CARTESIAN_POINT ( 'NONE',  ( 795.1360043628807261, -308.0891481129650629, 360.2193346964456282 ) ) ;
#24885=CARTESIAN_POINT ( 'NONE',  ( 796.7737145352015204, -92.63460265842026331, 370.7187646348536987 ) ) ;
#24889=PRODUCT_CONTEXT ( 'NONE', #34917, 'mechanical' ) ;
#24890=CARTESIAN_POINT ( 'NONE',  ( 754.8072714833581358, -28.81642084023863148, 338.1981804954720587 ) ) ;
#24892=CARTESIAN_POINT ( 'NONE',  ( 814.2001403089898304, -401.3618753856920307, 347.4397851343538264 ) ) ;
#24893=CARTESIAN_POINT ( 'NONE',  ( 795.6651683502461765, -298.7146871989593251, 371.3240766477733814 ) ) ;
#24894=CARTESIAN_POINT ( 'NONE',  ( 771.2368401574024119, -85.44195992623282621, 374.2805881961240857 ) ) ;
#24900=CARTESIAN_POINT ( 'NONE',  ( 814.5518280994195948, -375.7255117493283478, 332.4837098697145734 ) ) ;
#24906=EDGE_CURVE ( 'NONE', #23907, #56, #2509, .T. ) ;
#24907=CARTESIAN_POINT ( 'NONE',  ( 802.9823548866075953, -265.0999726633344267, 330.0799878456151077 ) ) ;
#24908=CARTESIAN_POINT ( 'NONE',  ( 759.7806653035534055, -126.9982390220565094, 324.8639956371180801 ) ) ;
#24912=CARTESIAN_POINT ( 'NONE',  ( 800.7704444035546203, -292.1692326535048210, 326.0291762391768771 ) ) ;
#24915=CARTESIAN_POINT ( 'NONE',  ( 744.6391490659812007, -38.73633629969877035, 338.7502325331110455 ) ) ;
#24917=CARTESIAN_POINT ( 'NONE',  ( 796.9462024416508257, -180.4527844766017211, 308.9653473494370246 ) ) ;
#24918=CARTESIAN_POINT ( 'NONE',  ( 804.6798772138708955, -87.72551174932937101, 334.6312213355107019 ) ) ;
#24921=CARTESIAN_POINT ( 'NONE',  ( 797.8822607201568644, -438.5545181178793541, 370.1134526219340160 ) ) ;
#24924=CARTESIAN_POINT ( 'NONE',  ( 795.9930595647434757, -363.0783235625955854, 320.7433823573372820 ) ) ;
#24925=CARTESIAN_POINT ( 'NONE',  ( 767.6429770376291799, -57.18005720387490243, 306.8695393053162093 ) ) ;
#24927=CARTESIAN_POINT ( 'NONE',  ( 773.3843516231979720, -61.44195992623291147, 364.4086373105754433 ) ) ;
#24930=CARTESIAN_POINT ( 'NONE',  ( 808.7758568127978833, -220.1692326535051052, 320.0363995740631822 ) ) ;
#24931=CARTESIAN_POINT ( 'NONE',  ( 764.8639956371174549, -32.08914811296589420, 319.7806653035542581 ) ) ;
#24934=CARTESIAN_POINT ( 'NONE',  ( 756.3353852180819104, -197.9073299311472169, 331.1735550268788302 ) ) ;
#24936=CARTESIAN_POINT ( 'NONE',  ( 768.0187753319979720, -344.6346026584195101, 318.0580252608186242 ) ) ;
#24940=CARTESIAN_POINT ( 'NONE',  ( 770.0799878456142551, -61.98741447168745822, 362.9823548866085616 ) ) ;
#24943=CARTESIAN_POINT ( 'NONE',  ( 749.2812353651451076, -246.4527844766016074, 323.2262854647983090 ) ) ;
#24945=CARTESIAN_POINT ( 'NONE',  ( 791.1614460488616487, 12.73985825558503926, 373.5763878283158874 ) ) ;
#24951=CARTESIAN_POINT ( 'NONE',  ( 763.2262854647970016, -272.6346026584196807, 309.2812353651462445 ) ) ;
#24953=CARTESIAN_POINT ( 'NONE',  ( 787.6308680596127942, -347.2601417444138860, 364.1105419155492768 ) ) ;
#24956=CARTESIAN_POINT ( 'NONE',  ( 784.1219089521767955, -165.2817908451529547, 315.0488828828318333 ) ) ;
#24957=CARTESIAN_POINT ( 'NONE',  ( 756.5762568750052424, -27.18005720387500901, 348.7366044899774238 ) ) ;
#24958=ORIENTED_EDGE ( 'NONE', *, *, #8906, .T. ) ;
#24961=CARTESIAN_POINT ( 'NONE',  ( 755.5913626894240451, -229.6454272087890729, 346.6156483768012890 ) ) ;
#24962=CARTESIAN_POINT ( 'NONE',  ( 783.7953271457878373, -272.1908817542434917, 375.1787889125761239 ) ) ;
#24963=CARTESIAN_POINT ( 'NONE',  ( 793.2243759319678702, -170.5328690171416781, 318.4439275373583200 ) ) ;
#24965=CARTESIAN_POINT ( 'NONE',  ( 785.3141322388236176, 2.274488250670355871, 364.4286716492789537 ) ) ;
#24968=CARTESIAN_POINT ( 'NONE',  ( 796.7737145352015204, -20.63460265842048003, 370.7187646348536987 ) ) ;
#24969=CARTESIAN_POINT ( 'NONE',  ( 804.7487373415286811, -67.54369356751125508, 364.7487373415288516 ) ) ;
#24970=DIRECTION ( 'NONE',  ( 0.000000000000000000, 0.000000000000000000, -1.000000000000000000 ) ) ;
#24974=CARTESIAN_POINT ( 'NONE',  ( 768.9521613784389729, -369.8272453906068904, 373.2346286133773106 ) ) ;
#24977=CARTESIAN_POINT ( 'NONE',  ( 745.4481719005789273, -339.7255117493285184, 347.5162901302853129 ) ) ;
#24981=CARTESIAN_POINT ( 'NONE',  ( 755.5713283507202505, -437.3618753856919170, 334.6858677611754729 ) ) ;
#24983=CARTESIAN_POINT ( 'NONE',  ( 763.0428371773158460, -179.4636090269710849, 358.7617431975195359 ) ) ;
#24986=CARTESIAN_POINT ( 'NONE',  ( 805.9055244015594326, -99.62377810805098477, 315.8990559732753240 ) ) ;
#24987=CARTESIAN_POINT ( 'NONE',  ( 762.3223304703356007, -391.5436935675101608, 322.3223304703362828 ) ) ;
#24988=CARTESIAN_POINT ( 'NONE',  ( 814.8230680027162407, -149.8055962898689870, 333.7305795820267917 ) ) ;
#24990=VERTEX_POINT ( 'NONE', #9676 ) ;
#24993=CARTESIAN_POINT ( 'NONE',  ( 797.8594530101008786, -229.5436935675106440, 322.1405469898980982 ) ) ;
#24994=CARTESIAN_POINT ( 'NONE',  ( 778.2165204200184689, -238.8164208402379813, 364.9363028652563230 ) ) ;
#24999=CARTESIAN_POINT ( 'NONE',  ( 785.3687786644884454, -419.3618753856918033, 315.3201227861279676 ) ) ;
#25003=CARTESIAN_POINT ( 'NONE',  ( 777.4774526936600978, -154.2709662947836762, 304.7301800767028226 ) ) ;
#25005=CARTESIAN_POINT ( 'NONE',  ( 763.8424801807145741, -282.0090635724253048, 320.5453621957614700 ) ) ;
#25008=CARTESIAN_POINT ( 'NONE',  ( 808.7758568127978833, -196.1692326535052473, 320.0363995740631822 ) ) ;
#25014=CARTESIAN_POINT ( 'NONE',  ( 760.5453621957607311, -237.0783235625960117, 323.8424801807151425 ) ) ;
#25024=CARTESIAN_POINT ( 'NONE',  ( 814.2805881961230625, -145.6454272087893287, 331.2368401574024119 ) ) ;
#25028=CARTESIAN_POINT ( 'NONE',  ( 754.3581564841646241, -377.4636090269704596, 316.1443688327762516 ) ) ;
#25033=CARTESIAN_POINT ( 'NONE',  ( 778.1981804954714335, -10.27096629478414691, 314.8072714833589885 ) ) ;
#25034=CARTESIAN_POINT ( 'NONE',  ( 791.0478386215596629, -237.8272453906072599, 306.7653713866226326 ) ) ;
#25036=CARTESIAN_POINT ( 'NONE',  ( 812.7932403749906598, -231.1800572038743553, 327.7687537140311633 ) ) ;
#25039=CARTESIAN_POINT ( 'NONE',  ( 778.2165204200184689, -310.8164208402377540, 364.9363028652563230 ) ) ;
#25040=CARTESIAN_POINT ( 'NONE',  ( 755.1538015810308480, -86.19088175424408860, 343.0433043558613804 ) ) ;
#25041=CARTESIAN_POINT ( 'NONE',  ( 772.4468031744293057, -81.82724539060772884, 363.8651313633793620 ) ) ;
#25046=CARTESIAN_POINT ( 'NONE',  ( 798.7617431975189675, -147.6237781080508285, 323.0428371773161871 ) ) ;
#25047=CARTESIAN_POINT ( 'NONE',  ( 774.6312213355099630, -359.3618753856920875, 364.6798772138717482 ) ) ;
#25050=CARTESIAN_POINT ( 'NONE',  ( 804.9363028652555840, -136.2709662947837330, 338.2165204200192079 ) ) ;
#25053=CARTESIAN_POINT ( 'NONE',  ( 756.1443688327750579, -405.6237781080500326, 314.3581564841659315 ) ) ;
#25055=CARTESIAN_POINT ( 'NONE',  ( 800.0135310231082713, -326.0891481129649492, 325.0180583372163028 ) ) ;
#25059=CARTESIAN_POINT ( 'NONE',  ( 781.8018195045266339, -406.2709662947829088, 365.1927285166406705 ) ) ;
#25061=ORIENTED_EDGE ( 'NONE', *, *, #16217, .T. ) ;
#25065=CARTESIAN_POINT ( 'NONE',  ( 804.1601925771018387, -127.4419599262326983, 346.5483106153029098 ) ) ;
#25068=CARTESIAN_POINT ( 'NONE',  ( 788.7631598425961101, -385.4419599262319593, 305.7194118038759143 ) ) ;
#25073=CARTESIAN_POINT ( 'NONE',  ( 776.2046728542105711, -20.19088175424429110, 304.8212110874238761 ) ) ;
#25075=DIRECTION ( 'NONE',  ( 0.000000000000000000, 0.000000000000000000, 1.000000000000000000 ) ) ;
#25081=CARTESIAN_POINT ( 'NONE',  ( 760.7433823573367135, -372.0090635724250205, 355.9930595647440441 ) ) ;
#25082=CARTESIAN_POINT ( 'NONE',  ( 750.9282345327678740, -328.9181544815160692, 319.8311093483690115 ) ) ;
#25086=CARTESIAN_POINT ( 'NONE',  ( 783.7953271457878373, -152.1908817542438612, 375.1787889125761239 ) ) ;
#25088=CARTESIAN_POINT ( 'NONE',  ( 800.9747183278959710, -132.9982390220564810, 311.9810565676471583 ) ) ;
#25092=CARTESIAN_POINT ( 'NONE',  ( 800.2193346964447755, -210.9982390220561967, 355.1360043628815788 ) ) ;
#25093=CARTESIAN_POINT ( 'NONE',  ( 814.2805881961230625, -457.6454272087884760, 331.2368401574024119 ) ) ;
#25097=CARTESIAN_POINT ( 'NONE',  ( 776.2433038121456548, 11.10349461922141145, 374.8207195650711014 ) ) ;
#25101=CARTESIAN_POINT ( 'NONE',  ( 786.2056067578752163, -323.8055962898684470, 374.4686193811670023 ) ) ;
#25102=CARTESIAN_POINT ( 'NONE',  ( 804.6798772138710092, -159.7255117493291436, 334.6312213355106451 ) ) ;
#25104=CARTESIAN_POINT ( 'NONE',  ( 774.6312213355099630, -311.3618753856922581, 364.6798772138717482 ) ) ;
#25107=CARTESIAN_POINT ( 'NONE',  ( 772.5602148656447525, -81.72551174932937101, 305.7998596910095443 ) ) ;
#25112=CARTESIAN_POINT ( 'NONE',  ( 781.8018195045266339, -22.27096629478410250, 365.1927285166406705 ) ) ;
#25114=CARTESIAN_POINT ( 'NONE',  ( 801.1904061080338124, -380.0891481129647218, 368.3070685750236066 ) ) ;
#25115=CARTESIAN_POINT ( 'NONE',  ( 793.4146539503750546, -289.9874144716866908, 307.6481478633938877 ) ) ;
#25116=CARTESIAN_POINT ( 'NONE',  ( 810.1134526219336749, -80.53286901714194812, 357.8822607201570349 ) ) ;
#25122=EDGE_LOOP ( 'NONE', ( #8469, #39272, #42586, #16156 ) ) ;
#25123=CARTESIAN_POINT ( 'NONE',  ( 812.7932403749906598, -375.1800572038739574, 327.7687537140311633 ) ) ;
#25127=DIRECTION ( 'NONE',  ( -1.000000000000000000, -0.000000000000000000, -0.000000000000000000 ) ) ;
#25128=DIRECTION ( 'NONE',  ( 0.000000000000000000, 0.000000000000000000, -1.000000000000000000 ) ) ;
#25129=CARTESIAN_POINT ( 'NONE',  ( 763.0428371773158460, -275.4636090269708575, 358.7617431975195359 ) ) ;
#25130=CARTESIAN_POINT ( 'NONE',  ( 767.8955696845333705, -168.4527844766018347, 362.1676090361162323 ) ) ;
#25134=CARTESIAN_POINT ( 'NONE',  ( 779.4709603349208464, -336.3510508353228943, 314.7162404726379918 ) ) ;
#25136=CARTESIAN_POINT ( 'NONE',  ( 745.7194118038753459, -37.64542720878968396, 348.7631598425976449 ) ) ;
#25138=CARTESIAN_POINT ( 'NONE',  ( 751.9810565676468741, -194.0891481129654039, 360.9747183278973921 ) ) ;
#25139=CARTESIAN_POINT ( 'NONE',  ( 802.1676090361156639, -110.6346026584201638, 327.8955696845344505 ) ) ;
#25142=CARTESIAN_POINT ( 'NONE',  ( 804.1009440267234822, -455.4636090269701754, 314.0944755984392600 ) ) ;
#25145=CARTESIAN_POINT ( 'NONE',  ( 794.1144889064781864, -370.1692326535045936, 360.9840315886528401 ) ) ;
#25146=CARTESIAN_POINT ( 'NONE',  ( 808.0189434323515343, -62.08914811296580183, 319.0252816721025511 ) ) ;
#25148=CARTESIAN_POINT ( 'NONE',  ( 758.6633372737375112, -68.53286901714197654, 326.9102291470432533 ) ) ;
#25152=CARTESIAN_POINT ( 'NONE',  ( 815.1787889125755555, -222.8965053807778531, 343.7953271457877804 ) ) ;
#25153=CARTESIAN_POINT ( 'NONE',  ( 759.9864689768902508, -2.089148112965993231, 354.9819416627836404 ) ) ;
#25156=CARTESIAN_POINT ( 'NONE',  ( 757.8323909638827445, -194.6346026584198796, 352.1044303154654358 ) ) ;
#25159=CARTESIAN_POINT ( 'NONE',  ( 781.7834795799800531, -322.8164208402377540, 315.0636971347436202 ) ) ;
#25164=CARTESIAN_POINT ( 'NONE',  ( 802.7791456095903868, -52.71468719896020616, 329.0155153010375102 ) ) ;
#25166=CARTESIAN_POINT ( 'NONE',  ( 758.8095938919644823, -296.0891481129650629, 311.6929314249762797 ) ) ;
#25167=CARTESIAN_POINT ( 'NONE',  ( 807.5423716828161105, -9.078323562596708030, 362.2119215644372048 ) ) ;
#25172=CARTESIAN_POINT ( 'NONE',  ( 755.2512626584698410, -295.5436935675105588, 315.2512626584710915 ) ) ;
#25174=CARTESIAN_POINT ( 'NONE',  ( 755.8398074228967971, -355.4419599262319593, 333.4516893846970333 ) ) ;
#25176=CARTESIAN_POINT ( 'NONE',  ( 784.1219089521767955, -141.2817908451530400, 315.0488828828318333 ) ) ;
#25177=CARTESIAN_POINT ( 'NONE',  ( 797.6776695296629214, -43.54369356751131903, 357.6776695296636603 ) ) ;
#25181=CARTESIAN_POINT ( 'NONE',  ( 771.3260364891663130, -259.6454272087890445, 306.0683387631859773 ) ) ;
#25182=CARTESIAN_POINT ( 'NONE',  ( 766.7756240680305382, -230.5328690171415076, 361.5560724626415663 ) ) ;
#25184=CARTESIAN_POINT ( 'NONE',  ( 755.3201227861273992, -3.725511749329622813, 345.3687786644892981 ) ) ;
#25187=CARTESIAN_POINT ( 'NONE',  ( 745.0891759886404770, -28.27096629478409540, 342.4968714119734159 ) ) ;
#25188=CARTESIAN_POINT ( 'NONE',  ( 814.2001403089898304, -113.3618753856929260, 347.4397851343538264 ) ) ;
#25189=DIRECTION ( 'NONE',  ( 0.000000000000000000, 0.000000000000000000, 1.000000000000000000 ) ) ;
#25191=DIRECTION ( 'NONE',  ( 0.000000000000000000, 1.000000000000000000, 0.000000000000000000 ) ) ;
#25192=CARTESIAN_POINT ( 'NONE',  ( 747.6481478633932056, -373.0999726633340856, 353.4146539503763620 ) ) ;
#25194=CARTESIAN_POINT ( 'NONE',  ( 746.8695393053150156, -341.9073299311465917, 327.6429770376306010 ) ) ;
#25200=CARTESIAN_POINT ( 'NONE',  ( 797.6776695296629214, -427.5436935675101040, 357.6776695296636603 ) ) ;
#25202=CARTESIAN_POINT ( 'NONE',  ( 786.5483106153019435, -175.6454272087892718, 364.1601925771022366 ) ) ;
#25205=CARTESIAN_POINT ( 'NONE',  ( 795.6651683502461765, -106.7146871989600498, 371.3240766477733814 ) ) ;
#25206=CARTESIAN_POINT ( 'NONE',  ( 781.7834795799800531, -418.8164208402374129, 315.0636971347436202 ) ) ;
#25212=CARTESIAN_POINT ( 'NONE',  ( 755.5713283507202505, -221.3618753856925707, 334.6858677611754729 ) ) ;
#25213=CARTESIAN_POINT ( 'NONE',  ( 781.8018195045267476, -238.2709662947833920, 365.1927285166407273 ) ) ;
#25217=CARTESIAN_POINT ( 'NONE',  ( 757.8323909638827445, -434.6346026584190554, 352.1044303154654358 ) ) ;
#25221=CARTESIAN_POINT ( 'NONE',  ( 782.4968714119720516, -178.8164208402381519, 305.0891759886411023 ) ) ;
#25222=CARTESIAN_POINT ( 'NONE',  ( 758.4439275373578084, -252.5545181178799226, 353.2243759319684386 ) ) ;
#25223=CARTESIAN_POINT ( 'NONE',  ( 754.9735926884551418, -378.3510508353227806, 340.5236548041000333 ) ) ;
#25226=CARTESIAN_POINT ( 'NONE',  ( 749.8865473780648472, -188.5328690171416497, 322.1177392798429082 ) ) ;
#25233=CARTESIAN_POINT ( 'NONE',  ( 802.7791456095903868, -244.7146871989596093, 329.0155153010375102 ) ) ;
#25243=CARTESIAN_POINT ( 'NONE',  ( 762.1177392798416577, -186.5545181178801215, 309.8865473780659272 ) ) ;
#25247=CARTESIAN_POINT ( 'NONE',  ( 814.5518280994195948, -15.72551174932958951, 332.4837098697145734 ) ) ;
#25248=DIRECTION ( 'NONE',  ( 0.000000000000000000, 0.000000000000000000, -1.000000000000000000 ) ) ;
#25252=CARTESIAN_POINT ( 'NONE',  ( 801.9419747391806368, 5.547215523397618142, 351.9812246680014027 ) ) ;
#25254=CARTESIAN_POINT ( 'NONE',  ( 810.4231160770870019, -264.5545181178798657, 321.9338519418446936 ) ) ;
#25256=CARTESIAN_POINT ( 'NONE',  ( 787.4397851343537695, -237.7255117493289163, 374.2001403089903988 ) ) ;
#25260=CARTESIAN_POINT ( 'NONE',  ( 768.0187753319979720, -320.6346026584195670, 318.0580252608186242 ) ) ;
#25262=CARTESIAN_POINT ( 'NONE',  ( 804.6971507214547046, -99.28179084515313946, 344.0799538623459739 ) ) ;
#25263=CARTESIAN_POINT ( 'NONE',  ( 775.8780910478218402, -81.28179084515319630, 364.9511171171680530 ) ) ;
#25267=CARTESIAN_POINT ( 'NONE',  ( 799.4546378042377910, -153.0783235625962675, 356.1575198192848006 ) ) ;
#25268=CARTESIAN_POINT ( 'NONE',  ( 800.2193346964447755, -354.9982390220557704, 355.1360043628815788 ) ) ;
#25273=CARTESIAN_POINT ( 'NONE',  ( 768.0187753319979720, -128.6346026584201354, 318.0580252608186242 ) ) ;
#25276=CARTESIAN_POINT ( 'NONE',  ( 792.2312462859673587, 12.09267006885214180, 307.2067596250082602 ) ) ;
#25278=CARTESIAN_POINT ( 'NONE',  ( 781.8018195045266339, -334.2709662947829656, 365.1927285166406705 ) ) ;
#25281=CARTESIAN_POINT ( 'NONE',  ( 794.9819416627830151, -444.9982390220554862, 319.9864689768909898 ) ) ;
#25288=CARTESIAN_POINT ( 'NONE',  ( 791.9460785601769430, -462.7578698805381237, 362.0383033825738721 ) ) ;
#25289=CARTESIAN_POINT ( 'NONE',  ( 749.2812353651451076, -222.4527844766016642, 323.2262854647983090 ) ) ;
#25290=CARTESIAN_POINT ( 'NONE',  ( 756.1348686366196716, -113.2601417444145682, 347.5531968255698416 ) ) ;
#25293=CARTESIAN_POINT ( 'NONE',  ( 768.8385539511368734, -407.2601417444137155, 306.4236121716840557 ) ) ;
#25300=CARTESIAN_POINT ( 'NONE',  ( 791.0478386215596629, -69.82724539060775726, 306.7653713866226326 ) ) ;
#25308=CARTESIAN_POINT ( 'NONE',  ( 800.9840315886518738, -364.9181544815158986, 354.1144889064786412 ) ) ;
#25309=CARTESIAN_POINT ( 'NONE',  ( 748.6759233522253680, -352.3726999360614514, 324.3348316497537098 ) ) ;
#25314=CARTESIAN_POINT ( 'NONE',  ( 804.1009440267234822, -143.4636090269711701, 314.0944755984392600 ) ) ;
#25316=CARTESIAN_POINT ( 'NONE',  ( 810.7187646348534145, -114.4527844766020053, 356.7737145352016341 ) ) ;
#25321=CARTESIAN_POINT ( 'NONE',  ( 785.3687786644884454, -203.3618753856925991, 315.3201227861279676 ) ) ;
#25322=CARTESIAN_POINT ( 'NONE',  ( 798.5707757039680246, -5.463609026971610660, 356.7845633553585003 ) ) ;
#25326=CARTESIAN_POINT ( 'NONE',  ( 791.1614460488616487, -35.26014174441480264, 373.5763878283158874 ) ) ;
#25330=CARTESIAN_POINT ( 'NONE',  ( 805.1927285166397041, -40.81642084023859951, 341.8018195045277707 ) ) ;
#25333=CARTESIAN_POINT ( 'NONE',  ( 814.8230680027162407, -293.8055962898685607, 333.7305795820267917 ) ) ;
#25334=CARTESIAN_POINT ( 'NONE',  ( 781.8018195045267476, -166.2709662947836478, 365.1927285166407273 ) ) ;
#25336=CARTESIAN_POINT ( 'NONE',  ( 797.8594530101008786, -325.5436935675105019, 322.1405469898980982 ) ) ;
#25338=CARTESIAN_POINT ( 'NONE',  ( 804.7487373415286811, -91.54369356751116982, 364.7487373415288516 ) ) ;
#25344=CARTESIAN_POINT ( 'NONE',  ( 774.6312213355099630, -47.36187538569312494, 364.6798772138717482 ) ) ;
#25345=CARTESIAN_POINT ( 'NONE',  ( 779.4763451958990572, -368.7363362996977685, 365.0264073115438919 ) ) ;
#25347=CARTESIAN_POINT ( 'NONE',  ( 805.0032342141413437, -397.5436935675101040, 314.9967657858572352 ) ) ;
#25348=CARTESIAN_POINT ( 'NONE',  ( 810.1134526219336749, -296.5328690171411949, 357.8822607201570349 ) ) ;
#25349=CARTESIAN_POINT ( 'NONE',  ( 748.3538107759620743, -64.71468719896019195, 355.8262568251490165 ) ) ;
#25356=CARTESIAN_POINT ( 'NONE',  ( 777.4774526936600978, -394.2709662947827951, 304.7301800767027657 ) ) ;
#25362=CARTESIAN_POINT ( 'NONE',  ( 754.7162404726377645, -278.7363362996980527, 339.4709603349214717 ) ) ;
#25363=CARTESIAN_POINT ( 'NONE',  ( 774.6312213355099630, -167.3618753856927412, 364.6798772138717482 ) ) ;
#25369=CARTESIAN_POINT ( 'NONE',  ( 802.7791456095903868, -316.7146871989593819, 329.0155153010375102 ) ) ;
#25371=CARTESIAN_POINT ( 'NONE',  ( 768.9521613784389729, -57.82724539060780700, 373.2346286133773106 ) ) ;
#25373=CARTESIAN_POINT ( 'NONE',  ( 792.2312462859673587, -203.9073299311471885, 307.2067596250082602 ) ) ;
#25374=CARTESIAN_POINT ( 'NONE',  ( 765.0180583372156207, -120.9982390220565378, 360.0135310231089534 ) ) ;
#25378=CARTESIAN_POINT ( 'NONE',  ( 814.2805881961230625, -457.6454272087884760, 331.2368401574024119 ) ) ;
#25381=CARTESIAN_POINT ( 'NONE',  ( 766.7756240680305382, -350.5328690171411381, 361.5560724626415663 ) ) ;
#25384=CARTESIAN_POINT ( 'NONE',  ( 759.2295555964440155, -64.16923265350563099, 353.9708237608231229 ) ) ;
#25387=CARTESIAN_POINT ( 'NONE',  ( 813.9316612368132837, -199.4419599262324709, 348.6739635108323228 ) ) ;
#25388=CARTESIAN_POINT ( 'NONE',  ( 788.8264449731201466, -69.18005720387488111, 363.6646147819170665 ) ) ;
#25391=CARTESIAN_POINT ( 'NONE',  ( 778.2165204200184689, -190.8164208402381234, 364.9363028652563230 ) ) ;
#25393=CARTESIAN_POINT ( 'NONE',  ( 797.8594530101009923, -349.5436935675103314, 322.1405469898982119 ) ) ;
#25398=CARTESIAN_POINT ( 'NONE',  ( 755.8398074228967971, -43.44195992623296831, 333.4516893846970333 ) ) ;
#25400=CARTESIAN_POINT ( 'NONE',  ( 763.0537975583476964, -288.4527844766014937, 371.0346526505628617 ) ) ;
#25401=CARTESIAN_POINT ( 'NONE',  ( 759.8311093483677041, 1.830767346494167391, 310.9282345327691814 ) ) ;
#25407=CARTESIAN_POINT ( 'NONE',  ( 782.5225473063381969, -286.2709662947833635, 375.2698199232970637 ) ) ;
#25408=AXIS2_PLACEMENT_3D ( 'NONE', #29555, #8976, #8764 ) ;
#25410=CARTESIAN_POINT ( 'NONE',  ( 802.9823548866075953, -217.0999726633345972, 330.0799878456151077 ) ) ;
#25413=CARTESIAN_POINT ( 'NONE',  ( 798.5707757039680246, -149.4636090269711417, 356.7845633553585003 ) ) ;
#25414=CARTESIAN_POINT ( 'NONE',  ( 800.2193346964447755, -42.99823902205675807, 355.1360043628815788 ) ) ;
#25418=CARTESIAN_POINT ( 'NONE',  ( 757.7880784355613741, -258.0090635724253616, 312.4576283171834916 ) ) ;
#25419=CARTESIAN_POINT ( 'NONE',  ( 770.0799878456142551, -229.9874144716869466, 362.9823548866085616 ) ) ;
#25421=CARTESIAN_POINT ( 'NONE',  ( 779.9999999999992042, -462.9681489794448339, 339.9999999999999432 ) ) ;
#25422=CARTESIAN_POINT ( 'NONE',  ( 800.0135310231082713, 9.910851887033969021, 325.0180583372163028 ) ) ;
#25425=CARTESIAN_POINT ( 'NONE',  ( 777.4774526936600978, -58.27096629478398171, 304.7301800767027657 ) ) ;
#25426=CARTESIAN_POINT ( 'NONE',  ( 808.3070685750230950, -114.9982390220565236, 361.1904061080339261 ) ) ;
#25428=DIRECTION ( 'NONE',  ( 0.000000000000000000, 0.000000000000000000, 1.000000000000000000 ) ) ;
#25430=LINE ( 'NONE', #4641, #26152 ) ;
#25432=CARTESIAN_POINT ( 'NONE',  ( 762.1177392798416577, -378.5545181178795247, 309.8865473780659272 ) ) ;
#25434=CARTESIAN_POINT ( 'NONE',  ( 763.0537975583475827, -312.4527844766012663, 371.0346526505627480 ) ) ;
#25437=CARTESIAN_POINT ( 'NONE',  ( 800.0135310231082713, -446.0891481129646081, 325.0180583372163028 ) ) ;
#25439=CARTESIAN_POINT ( 'NONE',  ( 802.9823548866075953, -193.0999726633346256, 330.0799878456151077 ) ) ;
#25442=CARTESIAN_POINT ( 'NONE',  ( 761.9338519418445230, -110.5328690171418629, 370.4231160770881957 ) ) ;
#25443=CARTESIAN_POINT ( 'NONE',  ( 797.6776695296629214, -427.5436935675101040, 357.6776695296636603 ) ) ;
#25450=CIRCLE ( 'NONE', #30629, 10.00000000000000888 ) ;
#25452=CARTESIAN_POINT ( 'NONE',  ( 803.4237431249931660, -279.1800572038741848, 331.2633955100225194 ) ) ;
#25453=CARTESIAN_POINT ( 'NONE',  ( 774.6312213355098493, -215.3618753856925707, 364.6798772138717482 ) ) ;
#25456=CARTESIAN_POINT ( 'NONE',  ( 804.6798772138708955, -423.7255117493281205, 334.6312213355107019 ) ) ;
#25458=CARTESIAN_POINT ( 'NONE',  ( 745.4481719005789273, -171.7255117493290868, 347.5162901302853697 ) ) ;
#25460=CARTESIAN_POINT ( 'NONE',  ( 790.0220218866281812, -271.0999726633344267, 363.2186876482849129 ) ) ;
#25463=CARTESIAN_POINT ( 'NONE',  ( 746.0683387631852383, -235.4419599262323857, 331.3260364891676204 ) ) ;
#25469=AXIS2_PLACEMENT_3D ( 'NONE', #31893, #10904, #24970 ) ;
#25470=CARTESIAN_POINT ( 'NONE',  ( 754.9735926884551418, -282.3510508353230080, 340.5236548041000333 ) ) ;
#25479=CARTESIAN_POINT ( 'NONE',  ( 754.3581564841646241, -161.4636090269711133, 316.1443688327762516 ) ) ;
#25488=CARTESIAN_POINT ( 'NONE',  ( 748.9653473494363425, -26.63460265842045871, 356.9462024416521331 ) ) ;
#25493=CARTESIAN_POINT ( 'NONE',  ( 801.9419747391806368, -18.45278447660230725, 351.9812246680014027 ) ) ;
#25494=CARTESIAN_POINT ( 'NONE',  ( 752.7379699480933368, -276.0090635724253048, 361.9858362298580232 ) ) ;
#25496=CARTESIAN_POINT ( 'NONE',  ( 767.7687537140311633, -239.9073299311470748, 372.7932403749916830 ) ) ;
#25500=CARTESIAN_POINT ( 'NONE',  ( 803.4237431249931660, -327.1800572038741279, 331.2633955100225194 ) ) ;
#25502=CARTESIAN_POINT ( 'NONE',  ( 796.9571628226829034, -95.46360902697132644, 321.2382568024804641 ) ) ;
#25507=CARTESIAN_POINT ( 'NONE',  ( 755.8398074228967971, -163.4419599262325846, 333.4516893846970333 ) ) ;
#25508=CARTESIAN_POINT ( 'NONE',  ( 804.6798772138708955, -375.7255117493283478, 334.6312213355107019 ) ) ;
#25511=CARTESIAN_POINT ( 'NONE',  ( 758.0580252608178853, -174.4527844766018063, 328.0187753319985404 ) ) ;
#25514=CARTESIAN_POINT ( 'NONE',  ( 811.6461892240364477, -436.7146871989589272, 324.1737431748509835 ) ) ;
#25515=VERTEX_POINT ( 'NONE', #17762 ) ;
#25516=CARTESIAN_POINT ( 'NONE',  ( 767.8955696845333705, -312.4527844766012663, 362.1676090361162323 ) ) ;
#25519=CARTESIAN_POINT ( 'NONE',  ( 797.6776695296629214, -427.5436935675101040, 357.6776695296636603 ) ) ;
#25527=CARTESIAN_POINT ( 'NONE',  ( 790.7339360641449275, -462.9631818684622999, 362.6136660859752965 ) ) ;
#25528=CARTESIAN_POINT ( 'NONE',  ( 814.2001403089898304, -233.3618753856925423, 347.4397851343538264 ) ) ;
#25529=CARTESIAN_POINT ( 'NONE',  ( 804.1601925771018387, -151.4419599262326415, 346.5483106153029098 ) ) ;
#25532=CARTESIAN_POINT ( 'NONE',  ( 764.3348316497523456, -382.7146871989591546, 308.6759233522265617 ) ) ;
#25538=CARTESIAN_POINT ( 'NONE',  ( 810.4231160770870019, -72.55451811788049099, 321.9338519418446936 ) ) ;
#25548=CARTESIAN_POINT ( 'NONE',  ( 754.7162404726377645, -398.7363362996976548, 339.4709603349214717 ) ) ;
#25553=CARTESIAN_POINT ( 'NONE',  ( 795.8262568251477660, -166.3726999360620198, 308.3538107759623585 ) ) ;
#25555=CARTESIAN_POINT ( 'NONE',  ( 767.6429770376289525, -105.1800572038747248, 306.8695393053162093 ) ) ;
#25560=CARTESIAN_POINT ( 'NONE',  ( 804.6798772138708955, -207.7255117493289447, 334.6312213355107019 ) ) ;
#25561=CARTESIAN_POINT ( 'NONE',  ( 766.4474001241216001, -451.0999726633339151, 307.3154664389482491 ) ) ;
#25567=CARTESIAN_POINT ( 'NONE',  ( 744.8212110874229666, -18.89650538077849617, 336.2046728542121627 ) ) ;
#25570=CARTESIAN_POINT ( 'NONE',  ( 762.3223304703356007, -7.543693567511430942, 322.3223304703362828 ) ) ;
#25573=CARTESIAN_POINT ( 'NONE',  ( 798.0661480581538854, -338.5328690171411381, 309.5768839229118043 ) ) ;
#25574=CARTESIAN_POINT ( 'NONE',  ( 795.1360043628808398, -140.0891481129655176, 360.2193346964456282 ) ) ;
#25577=CARTESIAN_POINT ( 'NONE',  ( 771.1735550268778070, -345.1800572038739006, 316.3353852180827630 ) ) ;
#25588=CARTESIAN_POINT ( 'NONE',  ( 762.3223304703356007, -55.54369356751127640, 322.3223304703362828 ) ) ;
#25589=CARTESIAN_POINT ( 'NONE',  ( 787.5531968255692163, -381.8272453906068336, 316.1348686366205811 ) ) ;
#25592=CARTESIAN_POINT ( 'NONE',  ( 801.1904061080338124, -404.0891481129646650, 368.3070685750236066 ) ) ;
#25593=CARTESIAN_POINT ( 'NONE',  ( 751.2241431872005251, -304.1692326535048210, 359.9636004259367610 ) ) ;
#25601=CARTESIAN_POINT ( 'NONE',  ( 745.7998596910086917, -437.3618753856919170, 332.5602148656461168 ) ) ;
#25607=CARTESIAN_POINT ( 'NONE',  ( 799.2566176426618085, -288.0090635724252479, 324.0069404352559559 ) ) ;
#25608=CARTESIAN_POINT ( 'NONE',  ( 774.6858677611749044, -153.7255117493291721, 315.5713283507209894 ) ) ;
#25611=CARTESIAN_POINT ( 'NONE',  ( 800.7704444035546203, -316.1692326535048210, 326.0291762391768771 ) ) ;
#25613=CARTESIAN_POINT ( 'NONE',  ( 812.3518521366052028, -25.09997266333519050, 326.5853460496235243 ) ) ;
#25616=CARTESIAN_POINT ( 'NONE',  ( 756.5762568750052424, -123.1800572038747106, 348.7366044899774238 ) ) ;
#25620=CARTESIAN_POINT ( 'NONE',  ( 780.5236548040995785, -20.73633629969883430, 314.9735926884559944 ) ) ;
#25623=CARTESIAN_POINT ( 'NONE',  ( 803.8651313633788504, -413.2601417444136018, 332.4468031744301015 ) ) ;
#25624=VERTEX_POINT ( 'NONE', #39473 ) ;
#25626=AXIS2_PLACEMENT_3D ( 'NONE', #36161, #32702, #11690 ) ;
#25630=CARTESIAN_POINT ( 'NONE',  ( 746.7653713866222915, -233.2601417444141987, 351.0478386215610271 ) ) ;
#25631=CARTESIAN_POINT ( 'NONE',  ( 774.6858677611749044, -57.72551174932945628, 315.5713283507209894 ) ) ;
#25634=CARTESIAN_POINT ( 'NONE',  ( 774.6858677611749044, -225.7255117493289163, 315.5713283507209894 ) ) ;
#25637=ORIENTED_EDGE ( 'NONE', *, *, #39667, .F. ) ;
#25640=CARTESIAN_POINT ( 'NONE',  ( 792.3570229623691148, -285.1800572038741279, 373.1304606946836770 ) ) ;
#25641=CARTESIAN_POINT ( 'NONE',  ( 798.0661480581538854, -2.532869017142183932, 309.5768839229118043 ) ) ;
#25649=CARTESIAN_POINT ( 'NONE',  ( 805.0032342141412300, -325.5436935675105019, 314.9967657858571783 ) ) ;
#25650=DIRECTION ( 'NONE',  ( 0.000000000000000000, -1.000000000000000000, 0.000000000000000000 ) ) ;
#25651=CARTESIAN_POINT ( 'NONE',  ( 756.7813123517142913, -355.9874144716865203, 329.9779781133712504 ) ) ;
#25653=CARTESIAN_POINT ( 'NONE',  ( 763.0428371773158460, -155.4636090269711417, 358.7617431975195359 ) ) ;
#25654=CARTESIAN_POINT ( 'NONE',  ( 768.0187753319979720, -56.63460265842036279, 318.0580252608186242 ) ) ;
#25658=CARTESIAN_POINT ( 'NONE',  ( 791.0478386215596629, -261.8272453906071746, 306.7653713866226326 ) ) ;
#25659=CARTESIAN_POINT ( 'NONE',  ( 758.6633372737375112, -236.5328690171414792, 326.9102291470432533 ) ) ;
#25662=CARTESIAN_POINT ( 'NONE',  ( 794.9819416627830151, 11.00176097794305541, 319.9864689768909898 ) ) ;
#25665=CARTESIAN_POINT ( 'NONE',  ( 814.2001403089898304, -41.36187538569314626, 347.4397851343538264 ) ) ;
#25666=CARTESIAN_POINT ( 'NONE',  ( 767.7687537140311633, -119.9073299311474443, 372.7932403749916830 ) ) ;
#25669=CARTESIAN_POINT ( 'NONE',  ( 773.7305795820266212, -393.2817908451522726, 374.8230680027170365 ) ) ;
#25670=LINE ( 'NONE', #39994, #27223 ) ;
#25671=CARTESIAN_POINT ( 'NONE',  ( 767.6429770376289525, -369.1800572038739574, 306.8695393053162093 ) ) ;
#25674=CARTESIAN_POINT ( 'NONE',  ( 794.9819416627830151, -420.9982390220555999, 319.9864689768909898 ) ) ;
#25675=CARTESIAN_POINT ( 'NONE',  ( 804.6971507214547046, -195.2817908451528410, 344.0799538623459739 ) ) ;
#25678=CARTESIAN_POINT ( 'NONE',  ( 773.7943932421234194, -95.80559628986917176, 305.5313806188329409 ) ) ;
#25679=CARTESIAN_POINT ( 'NONE',  ( 804.6798772138710092, -423.7255117493282341, 334.6312213355106451 ) ) ;
#25681=CARTESIAN_POINT ( 'NONE',  ( 805.9055244015594326, -171.6237781080507432, 315.8990559732753240 ) ) ;
#25686=CARTESIAN_POINT ( 'NONE',  ( 791.9812246680005501, -260.6346026584197375, 361.9419747391813189 ) ) ;
#25687=CARTESIAN_POINT ( 'NONE',  ( 800.0135310231082713, -278.0891481129651197, 325.0180583372163028 ) ) ;
#25690=CARTESIAN_POINT ( 'NONE',  ( 775.9200461376533440, 24.19440371013046231, 315.3028492785443291 ) ) ;
#25691=VERTEX_POINT ( 'NONE', #4800 ) ;
#25693=CARTESIAN_POINT ( 'NONE',  ( 772.4837098697145166, -191.3618753856926276, 374.5518280994205611 ) ) ;
#25694=CARTESIAN_POINT ( 'NONE',  ( 804.1105419155481968, -267.8272453906071746, 347.6308680596136469 ) ) ;
#25695=CARTESIAN_POINT ( 'NONE',  ( 756.1348686366196716, -377.2601417444137724, 347.5531968255698416 ) ) ;
#25698=CARTESIAN_POINT ( 'NONE',  ( 791.1614460488616487, -203.2601417444143124, 373.5763878283158874 ) ) ;
#25703=CARTESIAN_POINT ( 'NONE',  ( 784.0799538623451781, -251.8055962898686744, 364.6971507214555572 ) ) ;
#25707=DIRECTION ( 'NONE',  ( 0.000000000000000000, 0.000000000000000000, -1.000000000000000000 ) ) ;
#25710=CARTESIAN_POINT ( 'NONE',  ( 745.1792804349281596, -158.1908817542438612, 343.7566961878542884 ) ) ;
#25716=CARTESIAN_POINT ( 'NONE',  ( 759.0252816721024374, -24.99823902205683268, 368.0189434323527280 ) ) ;
#25721=CARTESIAN_POINT ( 'NONE',  ( 755.3201227861273992, -27.72551174932954510, 345.3687786644892981 ) ) ;
#25722=CARTESIAN_POINT ( 'NONE',  ( 762.1177392798416577, -282.5545181178798657, 309.8865473780659272 ) ) ;
#25724=CARTESIAN_POINT ( 'NONE',  ( 745.4481719005789273, -219.7255117493289447, 347.5162901302853129 ) ) ;
#25728=CARTESIAN_POINT ( 'NONE',  ( 762.1405469898971887, -337.5436935675102177, 357.8594530101015607 ) ) ;
#25729=CARTESIAN_POINT ( 'NONE',  ( 793.9708237608222134, -70.91815448151683654, 319.2295555964448681 ) ) ;
#25733=CARTESIAN_POINT ( 'NONE',  ( 775.9200461376533440, -167.8055962898689586, 315.3028492785443291 ) ) ;
#25734=CARTESIAN_POINT ( 'NONE',  ( 804.9363028652555840, -352.2709662947830225, 338.2165204200192079 ) ) ;
#25737=CARTESIAN_POINT ( 'NONE',  ( 774.6858677611749044, -153.7255117493291721, 315.5713283507209894 ) ) ;
#25740=CARTESIAN_POINT ( 'NONE',  ( 777.4774526936600978, 13.72903370521577138, 304.7301800767027657 ) ) ;
#25742=CARTESIAN_POINT ( 'NONE',  ( 774.6858677611749044, -321.7255117493286320, 315.5713283507209894 ) ) ;
#25746=CARTESIAN_POINT ( 'NONE',  ( 754.8072714833581358, -436.8164208402372992, 338.1981804954720587 ) ) ;
#25753=CARTESIAN_POINT ( 'NONE',  ( 759.9864689768902508, -2.089148112965993231, 354.9819416627836404 ) ) ;
#25754=CARTESIAN_POINT ( 'NONE',  ( 796.7737145352015204, -236.6346026584198228, 370.7187646348536987 ) ) ;
#25755=CARTESIAN_POINT ( 'NONE',  ( 770.0799878456142551, -157.9874144716871456, 362.9823548866085616 ) ) ;
#25762=CARTESIAN_POINT ( 'NONE',  ( 788.6739635108323228, -55.64542720878963422, 373.9316612368139090 ) ) ;
#25770=CARTESIAN_POINT ( 'NONE',  ( 804.8461984189677878, -386.1908817542432075, 336.9566956441385628 ) ) ;
#25775=CARTESIAN_POINT ( 'NONE',  ( 776.2046728542105711, -164.1908817542438612, 304.8212110874238761 ) ) ;
#25777=CARTESIAN_POINT ( 'NONE',  ( 777.4774526936600978, -130.2709662947837899, 304.7301800767027657 ) ) ;
#25781=CARTESIAN_POINT ( 'NONE',  ( 756.3353852180819104, -221.9073299311470464, 331.1735550268788302 ) ) ;
#25782=CARTESIAN_POINT ( 'NONE',  ( 802.5472867521000353, -28.37269993606244967, 350.8726784830461156 ) ) ;
#25785=CARTESIAN_POINT ( 'NONE',  ( 771.2368401574024119, -37.44195992623299674, 374.2805881961240857 ) ) ;
#25789=CARTESIAN_POINT ( 'NONE',  ( 800.0135310231082713, -14.08914811296595460, 325.0180583372163028 ) ) ;
#25791=CARTESIAN_POINT ( 'NONE',  ( 749.8865473780648472, -332.5328690171411381, 322.1177392798429082 ) ) ;
#25794=CARTESIAN_POINT ( 'NONE',  ( 797.6776695296629214, -331.5436935675104451, 357.6776695296636603 ) ) ;
#25797=CARTESIAN_POINT ( 'NONE',  ( 764.0069404352550464, -87.07832356259646645, 359.2566176426627180 ) ) ;
#25800=ORIENTED_EDGE ( 'NONE', *, *, #11114, .T. ) ;
#25802=CARTESIAN_POINT ( 'NONE',  ( 765.0180583372156207, -72.99823902205667991, 360.0135310231089534 ) ) ;
#25803=CARTESIAN_POINT ( 'NONE',  ( 793.9708237608222134, -382.9181544815159555, 319.2295555964448681 ) ) ;
#25805=CARTESIAN_POINT ( 'NONE',  ( 751.9810565676468741, -410.0891481129647218, 360.9747183278973921 ) ) ;
#25806=CARTESIAN_POINT ( 'NONE',  ( 758.0141637701419768, -327.0783235625956991, 367.2620300519063790 ) ) ;
#25812=CARTESIAN_POINT ( 'NONE',  ( 759.0252816721024374, -408.9982390220556567, 368.0189434323527280 ) ) ;
#25819=CARTESIAN_POINT ( 'NONE',  ( 790.9844846989617508, -286.3726999360617356, 317.2208543904092721 ) ) ;
#25820=CARTESIAN_POINT ( 'NONE',  ( 754.8072714833581358, -148.8164208402382656, 338.1981804954720587 ) ) ;
#25823=CARTESIAN_POINT ( 'NONE',  ( 758.6633372737375112, -332.5328690171411381, 326.9102291470432533 ) ) ;
#25826=CARTESIAN_POINT ( 'NONE',  ( 744.6391490659812007, -62.73633629969871350, 338.7502325331110455 ) ) ;
#25828=CARTESIAN_POINT ( 'NONE',  ( 814.9108240113580450, -208.2709662947835341, 337.5031285880265273 ) ) ;
#25829=CARTESIAN_POINT ( 'NONE',  ( 768.0187753319979720, -104.6346026584202207, 318.0580252608186242 ) ) ;
#25832=EDGE_CURVE ( 'NONE', #36800, #14626, #24139, .T. ) ;
#25833=CARTESIAN_POINT ( 'NONE',  ( 804.4086373105744769, -1.645427208789804308, 333.3843516231986541 ) ) ;
#25836=CARTESIAN_POINT ( 'NONE',  ( 756.1348686366196716, -401.2601417444137155, 347.5531968255698416 ) ) ;
#25843=CARTESIAN_POINT ( 'NONE',  ( 795.6651683502461765, -250.7146871989595809, 371.3240766477733814 ) ) ;
#25844=CARTESIAN_POINT ( 'NONE',  ( 800.0135310231082713, -62.08914811296580183, 325.0180583372163028 ) ) ;
#25848=CARTESIAN_POINT ( 'NONE',  ( 795.1360043628807261, -236.0891481129651766, 360.2193346964456282 ) ) ;
#25855=CARTESIAN_POINT ( 'NONE',  ( 772.5602148656447525, -273.7255117493288026, 305.7998596910095443 ) ) ;
#25856=CARTESIAN_POINT ( 'NONE',  ( 808.7758568127978833, -28.16923265350574468, 320.0363995740631822 ) ) ;
#25865=CARTESIAN_POINT ( 'NONE',  ( 779.4763451958990572, -200.7363362996982801, 365.0264073115438919 ) ) ;
#25866=CARTESIAN_POINT ( 'NONE',  ( 768.0187753319979720, -32.63460265842044095, 318.0580252608186242 ) ) ;
#25870=CARTESIAN_POINT ( 'NONE',  ( 801.3366627262608972, -224.5328690171415076, 353.0897708529566899 ) ) ;
#25873=CARTESIAN_POINT ( 'NONE',  ( 814.5518280994195948, -423.7255117493281205, 332.4837098697145734 ) ) ;
#25877=CARTESIAN_POINT ( 'NONE',  ( 796.9462024416508257, -60.45278447660215448, 308.9653473494370246 ) ) ;
#25878=CARTESIAN_POINT ( 'NONE',  ( 772.4837098697144029, -95.36187538569294020, 374.5518280994205611 ) ) ;
#25880=CARTESIAN_POINT ( 'NONE',  ( 791.0478386215596629, -381.8272453906068336, 306.7653713866226326 ) ) ;
#25883=CARTESIAN_POINT ( 'NONE',  ( 811.0346526505616112, -350.6346026584192828, 323.0537975583477532 ) ) ;
#25885=CARTESIAN_POINT ( 'NONE',  ( 783.0433043558608688, 23.10349461922137237, 315.1538015810313027 ) ) ;
#25888=CARTESIAN_POINT ( 'NONE',  ( 795.6651683502461765, -130.7146871989599504, 371.3240766477733814 ) ) ;
#25889=CARTESIAN_POINT ( 'NONE',  ( 803.6646147819162707, -449.9073299311464211, 348.8264449731211130 ) ) ;
#25890=( BOUNDED_SURFACE ( )  B_SPLINE_SURFACE ( 3, 2, ( 
 ( #26594, #6034, #19441, #19908, #20354, #33984, #2336, #16436, #9516, #8834, #9047, #23116, #23582, #22902, #37687, #2572, #34450, #13217, #27294, #2813, #16904, #30985, #12308, #36993, #33535, #13661, #3034, #34677, #41846, #42284, #27743, #17122, #21270, #38596, #14118, #41606, #28425, #35570, #10646, #6722, #31207, #38846, #6502, #42064, #42524, #21037, #10413, #27968, #31437, #27508, #10190, #24266, #26, #13438, #20797, #35349, #10890, #38374, #3725, #7199, #31659, #45543, #17813, #28191, #34894, #3260, #17352, #13894, #20581, #24489, #6953, #24725, #35124, #31879, #38153, #3502, #21493, #17588, #251, #14348, #24957, #39071, #7419, #3947, #18042, #45082, #9963, #24033, #8325, #11797, #25866, #5084, #4194, #1389, #36052, #32585, #32361, #4856, #18287, #32122, #487, #28667, #927, #39976, #40200, #22625, #22389, #35815, #15493, #25414, #25177, #14594, #39534, #21966, #8561, #15031, #21722, #7891, #42745, #1163, #11107, #4414, #18506, #29119, #36493, #39288, #43202, #717, #11573, #14815, #43429, #18956, #12018, #15271, #25654, #39767, #29357, #28888, #4626, #8115, #42968, #22175, #33052, #32810, #36726, #36270, #11335, #29573, #18723, #43649, #26086, #7643, #37164, #5523, #16155, #19618, #33260, #33714, #1606, #40869, #40643, #15703, #33931, #19391, #12684, #26326, #2063, #44102, #30237, #36944, #23745, #12466, #44803, #9681, #44329, #2514, #43868, #26763, #9233, #37857, #23524, #30707, #23304, #33478, #16620, #26545, #8996, #22851, #13160, #5297, #41108, #37406, #27239, #5763, #19851, #2282, #41332, #16381, #1824, #29788, #37626, #23064, #19175, #12247, #40431, #30458, #44562, #12924, #15932, #27009, #9461, #5977, #30016, #20068, #34143, #8783, #3446, #17768, #31150, #45247, #27456, #30935, #24440, #17543, #35304, #20977, #17072, #21223, #24671, #45489, #20534, #42239, #7145, #38790, #2985, #17295, #28368, #9906, #31833, #10144, #2761, #3681, #38545, #31616, #28145, #204, #14296, #6897, #13383, #45719, #41794, #41553, #24219, #35074, #34390, #27924, #13607, #42470, #13846, #42019, #10836, #27690, #20749, #24908, #14072, #6206, #10365, #38327, #10595, #20299, #38100, #16855, #6673, #23979, #45029, #6455, #34840, #31385, #34628, #3204, #4366, #437, #11964, #43386, #7840, #36442, #36219, #4806, #18236, #32311, #14539, #17993, #11525, #4583, #22341, #8068, #4143, #8276, #11753, #32536, #7596, #29312, #39932, #25820, #35764, #18457, #15448, #42699, #18911, #42920, #35524, #33004, #25608, #18674, #15225, #1344, #29524, #39718, #28617, #32763, #28840, #11063, #11286, #22130, #21448, #14985, #667, #43598, #882, #29070, #39022, #14768, #21915, #7372, #1110, #3900, #43158, #25363, #32065, #25130, #39243, #21672, #39480, #36002, #44282, #12196, #33426, #5470, #40388, #8508, #33662, #1555, #26033, #44510, #40144, #44051, #22577, #2011, #1768, #36679, #40819, #26276, #16108, #15653, #8950, #15879, #30192, #8739, #22805, #9173, #5932, #36898, #23249, #9409, #37352, #5713, #19800, #33884, #12870, #37577, #2237, #16332, #34099, #26952, #41052, #43393, #28625, #8283, #19841, #37156, #9452, #40635, #44093, #26537, #23515, #12458, #43855, #12010, #2274, #36936, #27001, #20059, #5969, #5290, #19383, #8988, #15695, #5514, #23056, #19610, #26317, #33703, #37616, #12676, #30006, #2053, #40861, #8775, #16147, #33469, #12238, #1814, #16373, #44321, #34136, #30230, #22843, #37398, #26756, #5752, #15922, #1597, #9222, #33923, #30450, #44554, #41097, #2506, #16611, #29780, #43641, #26074, #40188, #8553, #36716, #5076, #19167, #33251, #34382, #24432, #37849, #27681, #28136, #6666, #41786, #13599, #17064, #13150, #13374, #27447, #31375, #44795, #38092, #6889, #42231, #2751, #35065, #38537, #17286, #31141, #20968, #45482, #30926, #45021, #16846, #20289, #6198, #6447, #41545, #13838, #38319, #27915, #23739, #9898, #7136, #23970, #20526, #3438, #20740, #34620, #45238, #10585, #2976, #17535, #10136, #24209, #31608, #10356, #45712, #3673, #34833, #14063, #3196, #42012, #24663, #38778, #21214, #30699, #27231, #41323, #35295, #9673, #28112, #41303, #45690, #20269, #14043, #6425, #9653, #34360, #31119, #2729, #39899, #36866, #37314, #30164, #19103, #16304, #30387, #6376, #41478, #20458, #6816, #2437, #45172, #20222, #13532, #6131, #27847, #24360, #34545, #27606, #2905, #44950, #45406, #16774, #34306, #38464, #41713, #17213, #44719, #31542, #38700, #41942, #9830, #2678, #10286, #9609, #10069, #45643, #24138, #38248, #31072, #16996, #30622, #30854, #13306, #3124, #16539, #23900, #20894, #13992, #27382, #34992, #3367, #34762, #6593, #17459, #31300, #38020, #20671, #28063, #37783, #23670, #42156, #10507, #24583, #7059, #21143, #41253, #13081, #27165, #38946, #31976, #11431, #11206, #39167, #4046, #15130, #28530, #7985, #347, #7296, #25516, #14905, #28987, #8197, #21371, #4504, #7517, #35671, #35447, #22051, #3817, #35226, #3604, #31751, #18145, #43068, #43299, #25742, #39630, #17908, #18596, #42625, #28280, #17691, #10986, #25055, #11666, #32224, #24826, #21590, #121, #4286, #14211, #584, #14685, #28762, #36142, #42380, #42842, #14450, #25278, #39389, #805, #32680, #29220, #18377, #7742, #21820, #32457, #35914, #1028, #39856, #10748, #12109, #26630, #22934, #30325, #26416, #33135, #1922, #22720, #30108, #15572, #25952, #40302, #36597, #40059, #44194, #15791, #37028, #18824, #5620, #12771, #19476, #29654, #8419, #16028, #29440, #19254, #19716, #43965, #33342, #5170, #8656, #4720, #4953, #19045, #5382, #36361, #43731, #12555, #33802, #22487, #40727, #9084, #8869, #36815, #23151, #33571, #1472, #26188, #1686, #11881, #43515, #29880, #12342, #37259, #40517, #2154, #15362, #16246, #44418, #26852, #40961, #22264, #32916, #1260, #23838, #34937, #2613, #27785, #20162, #27107, #31247, #34712, #3070, #28008, #41198, #24306, #13251, #37953, #9553, #41884, #23615, #9324, #23394, #5855, #6308, #17161, #17398, #45585, #45344, #13017, #38413, #16713, #2375, #37495, #30798, #44891, #31481, #20392, #44656, #27329, #19943, #24075, #34019, #41422, #34489, #2848, #13706, #16473, #16941, #37722, #31021, #6073, #20617, #10228, #3303, #38192, #45119, #13476, #6537, #34238, #27546, #41650, #10006, #6764, #20838, #13933, #30555, #528, #7242, #21764, #42570, #4235, #35389, #14158, #14390, #28469, #39110, #10931, #38887, #39329, #35613, #7930, #7460, #24999, #21533, #22000, #3986, #42323, #10453, #756, #3762, #25456, #18544, #4455, #17852, #31919, #18083, #28229, #32163, #14634, #28706, #24771, #42785, #11147, #39575, #7684, #36089, #21313, #290, #17633, #21085, #25217, #35858, #32623, #18327, #32407, #11373, #14854, #28931, #10688, #43010, #967, #15071, #42103, #24530, #38641, #7000, #35169, #3547, #31698, #12501, #1638, #26361, #5330, #23099, #26577, #15738, #36306, #22886, #18994, #18762, #1424, #12285, #11612, #5118, #8362, #19657 ),
 ( #2100, #33516, #43241, #15526, #25690, #19206, #4894, #39802, #43908, #29391, #22665, #4664, #29606, #22427, #43684, #1200, #33750, #36536, #9029, #29158, #26127, #40675, #8150, #12055, #33293, #22213, #1865, #37199, #40242, #43463, #5565, #33087, #8599, #32852, #15308, #11830, #19425, #25901, #36762, #29826, #40465, #8817, #40011, #36977, #15971, #30053, #44136, #9719, #30971, #12719, #45287, #6708, #13423, #23563, #19889, #9947, #23340, #13201, #13645, #37898, #27279, #44838, #2553, #44364, #44601, #12963, #16890, #30271, #37666, #38138, #27729, #33967, #20568, #24020, #2798, #16660, #6489, #45068, #16417, #30498, #2319, #5803, #37443, #6016, #27049, #27492, #23784, #41592, #9273, #41147, #38362, #9499, #20107, #34663, #6248, #34182, #30744, #41831, #41372, #3023, #20338, #34431, #17109, #31191, #10177, #34879, #24254, #20785, #16190, #26799, #40903, #21706, #21018, #21951, #17332, #45527, #17799, #28651, #11320, #39518, #42729, #6937, #18274, #42270, #42051, #3244, #10631, #38830, #25398, #3712, #38582, #24708, #31421, #18027, #27955, #7180, #21255, #35335, #7628, #13879, #236, #35108, #14332, #3484, #14576, #25164, #28872, #32105, #31865, #42508, #473, #31645, #21479, #28410, #17574, #10874, #35801, #3932, #7874, #7405, #14104, #11093, #24940, #39273, #39056, #4179, #32347, #42953, #702, #35557, #14798, #10399, #13, #24475, #28178, #18703, #4839, #1146, #16124, #9429, #5488, #40405, #12655, #40616, #37371, #36913, #19146, #5267, #19359, #44300, #19819, #33902, #16351, #1573, #30431, #44531, #12889, #23496, #29542, #37596, #5950, #33023, #1361, #15464, #43617, #40162, #11983, #26051, #25797, #34321, #44961, #9621, #5698, #2450, #16552, #20471, #19785, #30637, #45181, #17227, #41034, #27617, #31084, #34558, #23683, #13544, #2917, #23462, #37561, #26931, #12850, #44492, #44732, #9393, #41726, #13318, #24152, #27177, #41265, #45420, #37794, #38261, #6606, #31313, #27861, #41956, #23230, #3615, #28774, #21153, #28073, #32236, #35685, #4060, #28997, #42168, #25290, #14223, #10762, #10519, #42852, #24594, #10298, #24371, #6827, #24838, #18161, #18387, #816, #597, #14004, #39402, #17703, #3380, #38476, #31764, #134, #32467, #38958, #45654, #28292, #20907, #25065, #35003, #42392, #7308, #21385, #14698, #17472, #35458, #38712, #3831, #7073, #35237, #7753, #17920, #31990, #362, #11219, #14464, #31554, #28542, #42637, #10998, #21832, #14916, #39179, #35925, #7529, #4296, #21603, #36152, #43081, #4734, #32929, #19487, #43526, #32692, #18836, #11445, #12120, #22061, #1273, #36372, #15373, #1696, #25529, #40070, #15144, #8432, #1039, #8670, #19265, #22943, #26202, #29452, #36611, #40316, #25755, #15583, #11891, #11679, #25964, #15801, #43741, #5392, #1484, #8208, #22734, #22500, #5179, #4967, #29234, #19058, #33147, #29665, #36828, #39867, #33354, #22276, #43310, #29891, #43977, #12352, #39642, #26429, #33584, #40530, #8879, #37040, #1934, #4514, #16037, #7996, #18607, #41209, #13028, #16486, #12567, #12783, #26865, #30808, #44207, #37507, #6321, #27558, #2167, #34499, #23850, #16724, #30567, #20403, #44902, #30337, #44429, #33814, #19726, #5632, #5866, #16258, #13261, #37734, #27339, #23164, #40974, #6549, #9335, #23404, #2859, #6086, #34030, #44668, #10020, #19955, #16951, #2387, #27118, #31029, #9783, #37966, #3080, #9565, #41432, #23625, #20174, #45128, #34253, #13486, #26642, #41664, #20628, #24087, #2625, #38201, #34721, #37272, #30120, #40738, #9094, #28238, #75, #3559, #45359, #45597, #13944, #17863, #31258, #24539, #39123, #14646, #34947, #21544, #10943, #3773, #17647, #7474, #31931, #17413, #31493, #20849, #6773, #38422, #38652, #3317, #302, #24783, #14404, #10239, #28018, #39343, #42112, #10463, #35626, #38901, #21099, #31708, #42801, #7010, #3998, #35183, #14167, #18099, #42583, #25014, #35872, #42333, #32180, #10701, #7254, #21325, #542, #35402, #17171, #13720, #27799, #28483, #28722, #25233, #7696, #11161, #21778, #41894, #24318, #43024, #4248, #11625, #39815, #26376, #4680, #39588, #25703, #18338, #19006, #28944, #8161, #43254, #22224, #8614, #32419, #1213, #22011, #15321, #7944, #15537, #26144, #29840, #33098, #36319, #43475, #1436, #32637, #22444, #18777, #18556, #32867, #22680, #4908, #12301, #8377, #15085, #29618, #29403, #12069, #11843, #36102, #25914, #40024, #36551, #43696, #4466, #40259, #36776, #5132, #11386, #29172, #40479, #981, #19219, #33306, #1651, #15753, #43924, #8831, #22898, #768, #14868, #25470, #13213, #16673, #30759, #9959, #9044, #6262, #40919, #37457, #37215, #9731, #23113, #36990, #5344, #33531, #5818, #44851, #45078, #27504, #27290, #40689, #20349, #30285, #30070, #19438, #44378, #26814, #13434, #19904, #26591, #12734, #1879, #6030, #15990, #9286, #23355, #33981, #41384, #44151, #2332, #5581, #16432, #19672, #2567, #23797, #16900, #20122, #30513, #44615, #34198, #33766, #9512, #12979, #2116, #27067, #37909, #37681, #41603, #41161, #16205, #34445, #23577, #2809, #30981, #12517, #42061, #10410, #21032, #24486, #20794, #21267, #38371, #41842, #248, #17585, #38842, #20578, #7416, #14591, #35346, #31433, #27739, #17810, #31203, #35120, #21490, #23, #3498, #6949, #38593, #6499, #6719, #34891, #24722, #38149, #45540, #14344, #35567, #10187, #28422, #31876, #10642, #31656, #42520, #7194, #24263, #3256, #17346, #13657, #45299, #13891, #27965, #14115, #10886, #28188, #3722, #34674, #3944, #28663, #24953, #42281, #39068, #18038, #32119, #483, #42740, #24029, #3031, #17119, #43199, #39285, #39531, #32581, #11794, #25174, #25651, #29569, #22620, #28885, #26081, #40194, #8321, #39764, #36722, #5080, #11332, #8112, #14810, #713, #32358, #22172, #42965, #33256, #18720, #1602, #36266, #4621, #1160, #15267, #29354, #10651, #28431, #493, #3704, #24466, #10622, #6927, #7172, #21246, #28398, #32095, #32629, #10693, #28476, #25695, #14639, #25223, #39116, #39806, #7465, #38893, #28712, #42793, #12293, #23105, #5809, #33974, #37207, #1428, #12725, #36768, #36541, #43467, #5124, #33299, #19897, #43914, #33091, #19212, #11835, #12507, #22436, #1644, #15745, #29833, #2108, #25906, #40471, #15530, #8823, #29611, #9035, #19663, #23347, #26583, #26369, #36983, #40681, #26135, #15978, #22891, #12061, #5336, #16197, #44143, #2325, #1871, #8607, #5571, #19431, #33756, #33523, #43688, #30062, #30277, #44370, #26805, #40250, #40911, #9278, #37450, #16423, #40015, #22672, #8367, #4900, #18999, #6023, #37902, #20114, #45293, #38143, #13652, #23569, #41377, #6942, #34189, #27284, #6712, #6494, #34437, #45073, #10403, #23790, #3248, #9726, #2560, #20789, #10182, #24258, #3490, #16665, #45532, #2803, #30975, #30750, #17340, #44844, #30505, #44608, #27058, #13428, #38366, #38586, #21025, #34884, #13206, #13884, #6256, #37674, #12969, #20343, #16894, #35113, #27498, #41597, #9954 ),
 ( #31426, #31195, #41154, #34668, #24024, #27959, #20572, #42055, #3027, #17114, #27733, #41836, #24480, #9505, #14336, #14802, #31869, #35339, #39523, #11097, #32351, #14107, #915, #8102, #28876, #24945, #21260, #11323, #24715, #14581, #15017, #39276, #28655, #476, #3935, #16, #239, #28414, #18277, #31648, #39060, #7878, #29106, #3715, #21954, #25401, #21482, #28181, #43190, #35806, #42956, #36040, #11559, #25641, #4182, #38833, #4403, #7408, #7186, #35560, #705, #42273, #7631, #42512, #22164, #25167, #21709, #36253, #18030, #32111, #39754, #18493, #17578, #32570, #42733, #10634, #17802, #10877, #1810, #15481, #39966, #22837, #36480, #43635, #29772, #18944, #32797, #15690, #11785, #23292, #8982, #18707, #22611, #1151, #26312, #26068, #15256, #19378, #4844, #43850, #25856, #36711, #29561, #5071, #22375, #9217, #12004, #30225, #40854, #1591, #33698, #29345, #33246, #40418, #4611, #23051, #16142, #19162, #33040, #2048, #40182, #8547, #8311, #44316, #1378, #26532, #12233, #12671, #8770, #36931, #5285, #26751, #33462, #15917, #43418, #37149, #30001, #44087, #12453, #40630, #5509, #19605, #30921, #30695, #45017, #13370, #27676, #10131, #20734, #26996, #21902, #21660, #35986, #3668, #17755, #45708, #3433, #42684, #35750, #7823, #39230, #35290, #39463, #42906, #17980, #38773, #28826, #25349, #11273, #21209, #35511, #868, #28131, #4351, #14059, #17530, #11051, #4129, #18442, #7583, #31819, #32520, #14971, #32050, #7131, #29056, #43142, #24427, #190, #3886, #38530, #10579, #6884, #28351, #20961, #35059, #25116, #18221, #651, #31603, #24656, #32296, #14282, #42454, #10822, #24894, #39008, #7359, #21435, #421, #14526, #28602, #19118, #33207, #16095, #32991, #26019, #5456, #12182, #30179, #1544, #29511, #1757, #15865, #43373, #8728, #4792, #1096, #29722, #11739, #1329, #36668, #8262, #22116, #22564, #32749, #15210, #44038, #29298, #43583, #11951, #15639, #5028, #43800, #40377, #22793, #36888, #5240, #19330, #33413, #12408, #26488, #40589, #8935, #19551, #33647, #44739, #38036, #37340, #23687, #37798, #45185, #27397, #20476, #6147, #12856, #34563, #9398, #16792, #19789, #2921, #16320, #41492, #44270, #5702, #19246, #40291, #22708, #19705, #33333, #8409, #22253, #44182, #29644, #16236, #36351, #32903, #12100, #37018, #5373, #11871, #1910, #16018, #26620, #22477, #15351, #43504, #24296, #17150, #38402, #44880, #41412, #37940, #30546, #6297, #16931, #27535, #41637, #37712, #6752, #41188, #27097, #3291, #17386, #26842, #19934, #40951, #2363, #16463, #9542, #17618, #21752, #21072, #24988, #39565, #32153, #7448, #21523, #14378, #24518, #42312, #38875, #39317, #38628, #17841, #32396, #18533, #53, #14845, #28920, #3534, #7231, #31908, #29816, #1191, #25891, #8352, #36523, #33076, #26117, #40231, #12275, #22654, #36967, #39793, #36752, #5555, #5321, #33506, #15962, #30044, #19648, #43231, #25681, #8141, #20559, #27039, #5794, #3013, #13413, #45276, #2091, #16408, #13635, #6004, #34172, #20097, #27718, #13189, #41361, #37886, #6237, #34420, #38353, #2788, #16880, #30560, #3309, #32174, #3554, #10233, #3075, #17639, #31703, #25226, #70, #17405, #38895, #17167, #31925, #27792, #7249, #297, #14397, #537, #31252, #42578, #45590, #25008, #13938, #28715, #42796, #11156, #39338, #45353, #13714, #28013, #18550, #8370, #43249, #4461, #25698, #40853, #36544, #44547, #40019, #975, #16141, #36313, #44315, #18772, #25909, #26995, #9216, #2269, #22219, #32632, #33918, #29165, #11620, #39582, #16366, #22006, #12670, #29398, #30445, #32858, #4674, #1208, #12908, #15316, #36096, #4243, #23291, #39809, #19835, #41092, #9447, #8156, #43470, #11838, #7939, #22439, #5508, #19604, #15078, #33697, #2046, #35866, #30224, #18333, #26750, #37392, #11381, #14863, #5747, #32413, #762, #28939, #43016, #25463, #42007, #17058, #37845, #13833, #24425, #10350, #20285, #34614, #45707, #27227, #3432, #27441, #20054, #6883, #41781, #20733, #45477, #17529, #20959, #10130, #30694, #17278, #13369, #13146, #41540, #6660, #5965, #45232, #2747, #14058, #31135, #13593, #28129, #30920, #38087, #31602, #24204, #42225, #27675, #9891, #27910, #38529, #9668, #34827, #34378, #41319, #38313, #23734, #16842, #2970, #6193, #34132, #3191, #44791, #23511, #35058, #37611, #23965, #2500, #31369, #45016, #16607, #6442, #20521, #4127, #17754, #42683, #35510, #11050, #28350, #15209, #3885, #36204, #1095, #7582, #39703, #35289, #7130, #8051, #28825, #7821, #32519, #4568, #22115, #42905, #31818, #4350, #420, #188, #28601, #21900, #38772, #32295, #17978, #29297, #18220, #650, #10578, #32048, #25115, #18659, #11272, #24655, #14752, #39229, #867, #14970, #42453, #35985, #21434, #14280, #25348, #10821, #14525, #35747, #24893, #21208, #21659, #39007, #3667, #29055, #7358, #18441, #43141, #11508, #25593, #32748, #12407, #43582, #36887, #4791, #29721, #22563, #43799, #15432, #2225, #36667, #23233, #33872, #40376, #26705, #22327, #26263, #33412, #16319, #1999, #9160, #12180, #11950, #40803, #5027, #19117, #1328, #37339, #29509, #19549, #5238, #5701, #8727, #22792, #19328, #19788, #1756, #26018, #11737, #16094, #33205, #25806, #39919, #8261, #1542, #15638, #15863, #40129, #29954, #44037, #26487, #8492, #40588, #8934, #36428, #23005, #18895, #37099, #5455, #32990, #33646, #30178, #44269, #12627, #45184, #41268, #45423, #3139, #23914, #44737, #20686, #31316, #17230, #27180, #41491, #6830, #34087, #10301, #34324, #34776, #13785, #16555, #27620, #9624, #20011, #2920, #30640, #23686, #9845, #13097, #12853, #38035, #37564, #3383, #27864, #44495, #2694, #26935, #6392, #6146, #41037, #13547, #37797, #20474, #5921, #16790, #20236, #30869, #2453, #35006, #44964, #24374, #20910, #27396, #41959, #9397, #13321, #34561, #30401, #38479, #23465, #17009, #31087, #41729, #10083, #24155, #38264, #6610, #3618, #39405, #11001, #29000, #14467, #17923, #365, #43084, #31993, #17706, #31557, #21835, #10765, #819, #39645, #25532, #24842, #38961, #28546, #35240, #25068, #42640, #39182, #137, #7532, #21606, #14919, #14701, #11448, #42395, #7311, #38715, #42172, #35688, #28777, #7999, #32240, #28296, #32470, #35929, #4063, #31767, #7756, #18390, #4299, #14226, #18164, #22064, #21157, #36155, #21388, #14007, #17476, #600, #42855, #45657, #28076, #10522, #11222, #24597, #25293, #35461, #7076, #3834, #1699, #29237, #40319, #19061, #4517, #22737, #15804, #43314, #26432, #44210, #11682, #22279, #18839, #5013, #18881, #32736, #8248, #26003, #15195, #29042, #11936, #8037, #19534, #5224, #43127, #32973, #22103, #22548, #36416, #4556, #8713, #1081, #40114, #18646, #1316, #4778, #15418, #29279, #5440, #29495, #26474, #857, #43567, #12395, #43358, #8478, #19104, #11723, #19313, #40575, #22779, #36873, #8921, #15848, #22991, #37324, #63, #19774, #38638, #27166, #14155, #30624, #2438, #16540 ),
 ( #19998, #26917, #44720, #6997, #1983, #13082, #5683, #41254, #33859, #44951, #21082, #28226, #2679, #9610, #23671, #27383, #16305, #6132, #9383, #30388, #23450, #3544, #34308, #42320, #37784, #44479, #17630, #20223, #31695, #16775, #12836, #10685, #24768, #38884, #7239, #16081, #30165, #44255, #12614, #26691, #40788, #9145, #23214, #8629, #15765, #22460, #32653, #28959, #1447, #32432, #18792, #5146, #1227, #32882, #43488, #11855, #40035, #35886, #19231, #25247, #36567, #29188, #43037, #29628, #781, #25926, #33317, #8390, #4921, #12082, #11639, #18352, #7956, #22024, #40274, #39357, #25716, #1663, #14881, #25488, #36113, #4478, #18569, #39828, #2583, #27078, #12529, #26603, #16001, #1894, #33544, #19685, #30083, #41171, #19915, #9525, #5356, #23123, #34459, #44166, #9057, #34209, #33992, #16218, #26824, #37920, #5594, #30771, #37228, #40702, #16686, #37694, #6044, #30992, #33778, #27302, #30295, #12745, #2129, #44862, #44389, #26390, #40491, #8843, #40931, #20133, #20365, #2821, #13225, #9297, #41396, #23366, #19449, #22911, #37468, #5830, #16913, #2343, #16444, #30526, #37002, #9743, #44626, #12991, #23589, #23810, #6277, #45090, #42074, #17133, #10423, #3043, #38859, #21283, #24969, #14129, #31451, #38608, #42295, #27754, #17598, #6733, #13673, #34907, #3736, #28201, #7431, #7210, #10200, #35361, #13905, #17824, #20807, #31217, #17364, #27979, #24500, #6967, #41856, #31891, #24278, #45311, #263, #28440, #21052, #42539, #3272, #35135, #10903, #21504, #35582, #3960, #18053, #13447, #27515, #41616, #20590, #34685, #1176, #28679, #15505, #22641, #29370, #39549, #35830, #25878, #39300, #29130, #29585, #8127, #43214, #15044, #18518, #14607, #14827, #28902, #32824, #500, #7906, #8339, #43661, #4207, #36507, #39991, #18737, #32597, #22402, #15285, #32377, #730, #18299, #21733, #7655, #21977, #42982, #43441, #39779, #11809, #25188, #11348, #8576, #25426, #36063, #4869, #22190, #4430, #940, #12033, #11588, #18971, #25666, #36283, #33064, #1401, #26101, #5096, #4639, #40213, #36738, #32135, #42756, #11119, #36956, #37871, #33272, #15717, #33728, #44576, #27253, #9693, #12935, #22863, #34156, #12478, #12259, #19186, #26557, #9008, #41344, #19633, #8795, #5309, #1618, #2528, #23758, #23078, #40655, #37177, #23537, #29803, #16167, #19405, #30249, #33491, #30472, #41122, #44815, #33944, #5536, #12696, #16393, #1839, #37420, #2075, #15948, #44341, #37638, #19863, #43882, #23316, #30030, #27023, #26340, #26776, #16632, #40882, #9246, #5777, #2295, #40443, #44114, #9475, #5990, #20081, #30720, #13172, #3689, #23989, #38799, #32700, #38553, #38336, #42247, #20990, #6466, #34637, #9918, #41565, #27466, #13618, #38111, #35082, #13855, #3456, #45041, #17083, #28378, #2994, #31161, #28155, #42027, #24228, #20758, #31842, #45257, #7156, #27700, #41804, #21232, #14080, #35312, #24917, #6682, #17776, #34850, #3214, #17305, #212, #31394, #6219, #34403, #2773, #45499, #14306, #42480, #10846, #16865, #10373, #30946, #24449, #13396, #6909, #17551, #28848, #29532, #39491, #25138, #7604, #21456, #22349, #43606, #42929, #32322, #11294, #43395, #39031, #18464, #21682, #32543, #35775, #29321, #11762, #18918, #8075, #25373, #11533, #36227, #4152, #39727, #676, #14777, #7847, #25828, #39942, #11973, #8286, #21925, #36453, #4817, #33013, #7380, #35534, #3908, #18003, #32076, #444, #44290, #32928, #18386, #39401, #43525, #15143, #36371, #18160, #4966, #26201, #15372, #43080, #25289, #36151, #19057, #25963, #11444, #40069, #40315, #39866, #596, #8207, #8431, #1483, #36610, #32466, #32235, #14697, #11678, #815, #28773, #21831, #25528, #39641, #32691, #7995, #4513, #18606, #25754, #22275, #37733, #26864, #5865, #30566, #3253, #6085, #40973, #15800, #2386, #44206, #43976, #26641, #37506, #36827, #30336, #33583, #45539, #16257, #44428, #13890, #16036, #23163, #17345, #9334, #27964, #12782, #40737, #44667, #13027, #40529, #19954, #19486, #12351, #23403, #8878, #1933, #33813, #22942, #5178, #19725, #29890, #8669, #27117, #22733, #9093, #19264, #34029, #30119, #33353, #16485, #37039, #2166, #26428, #37271, #12566, #5631, #5391, #1695, #41208, #34890, #9564, #23624, #20173, #31432, #24951, #32117, #32579, #710, #7885, #28419, #10639, #39529, #35344, #3720, #21, #21962, #28186, #18283, #35565, #36047, #39066, #42518, #7413, #4409, #10883, #42279, #10409, #14808, #17807, #25407, #18499, #922, #31874, #246, #21488, #14113, #3942, #18035, #14588, #24720, #28660, #35811, #3496, #42738, #15026, #11103, #25172, #39283, #7639, #24485, #38839, #7192, #21715, #38592, #14341, #32356, #42060, #21265, #28882, #4188, #42962, #11330, #6947, #21030, #35119, #17583, #31654, #18717, #4618, #36486, #32803, #43858, #36720, #12241, #22170, #39972, #5517, #1158, #8318, #5292, #5078, #33048, #43644, #8991, #22383, #1817, #4852, #15263, #19386, #8778, #22846, #2057, #29352, #44097, #1384, #29567, #43425, #15925, #11792, #29112, #43197, #25649, #12013, #36939, #37159, #19613, #33472, #18951, #12461, #15488, #36261, #11567, #26078, #40191, #33707, #8556, #22618, #19170, #39762, #26540, #8109, #33254, #1600, #15698, #30009, #29783, #26321, #40426, #40638, #23059, #27449, #38094, #41788, #30928, #2508, #9675, #13376, #44557, #34384, #23518, #30453, #5972, #20528, #16849, #24212, #20291, #27004, #41547, #16613, #23971, #9456, #19844, #34138, #30701, #13153, #44797, #12916, #9900, #41101, #33926, #6449, #37851, #45023, #12679, #45240, #6667, #34622, #37619, #2277, #13601, #16376, #2978, #17066, #2754, #27233, #31143, #27683, #20062, #41325, #6200, #5756, #37401, #10138, #38321, #20741, #34834, #16150, #9225, #44324, #40864, #23298, #45713, #25123, #24900, #7137, #17761, #28834, #42232, #21665, #14065, #20970, #39236, #28609, #42691, #21908, #3440, #18228, #21216, #3674, #17536, #35757, #31610, #3197, #17288, #45483, #31825, #11056, #11279, #39471, #7589, #6891, #32304, #10587, #42013, #31377, #24664, #38779, #25356, #196, #38538, #28137, #13839, #659, #7830, #35297, #14288, #28359, #4135, #27918, #10828, #39015, #7365, #21441, #14532, #14760, #42913, #17985, #35517, #3893, #428, #32057, #10358, #24434, #4575, #25812, #40381, #36672, #44043, #40136, #15216, #15644, #36435, #43804, #29304, #39711, #8268, #22333, #32997, #4799, #32756, #33211, #18667, #8060, #12187, #29517, #5032, #32528, #19334, #26492, #1548, #43378, #22123, #29726, #43150, #1335, #33418, #11957, #15440, #18901, #43590, #18449, #11746, #39925, #19123, #4360, #26025, #26267, #8500, #8732, #22798, #29958, #1761, #22568, #11515, #36891, #5244, #25601, #15870, #12412, #875, #40593, #8940, #35994, #14978, #29063, #36211, #30406, #37569, #17014, #23691, #13552, #13101, #41042, #13325, #27401, #9165, #20241, #33877, #12631, #41274, #23240, #16324, #2457, #37344, #5461, #34092, #30184 ),
 ( #27185, #27625, #41498, #34567, #9402, #5706, #20480, #44498, #12860, #26709, #2926, #19793, #44970, #16561, #31091, #20015, #23469, #5925, #45190, #44743, #2229, #37104, #9848, #26942, #6397, #41733, #23010, #9628, #37803, #6151, #40808, #34329, #2699, #16796, #30873, #23919, #38041, #19556, #33651, #2003, #16100, #44274, #28301, #34782, #42401, #21393, #39187, #24847, #20915, #25073, #28552, #3623, #24380, #371, #11006, #42645, #6836, #21163, #32245, #13791, #35694, #14013, #6617, #7537, #31772, #35012, #605, #17711, #143, #14706, #17482, #24603, #4071, #10770, #28782, #14233, #28082, #14472, #21612, #41965, #7316, #3390, #45428, #38966, #10308, #31562, #35245, #38484, #38270, #35466, #17235, #10087, #18169, #24161, #42178, #20691, #3839, #45662, #3145, #17931, #10528, #31999, #31322, #38721, #7082, #27869, #14924, #1706, #36160, #22742, #33361, #39874, #26210, #21841, #25762, #32936, #15809, #1492, #8677, #29242, #11455, #40324, #4522, #18614, #825, #36835, #29007, #19066, #36380, #5187, #8215, #43320, #22284, #19274, #11689, #43089, #11227, #15590, #32701, #42860, #25300, #39410, #1046, #15153, #4742, #25538, #18846, #1281, #15381, #39651, #29460, #43533, #7764, #40079, #11900, #29672, #35934, #25971, #4304, #8439, #22509, #18395, #36618, #8004, #12127, #43750, #4973, #22070, #33155, #32475, #16735, #26650, #40986, #6332, #33593, #9793, #33824, #26438, #13270, #2398, #27128, #6095, #23861, #27348, #16498, #37048, #23635, #19736, #19495, #2177, #13038, #12361, #23415, #44216, #20185, #30817, #44912, #40747, #9345, #20414, #1943, #37977, #16269, #40537, #41442, #30578, #41218, #34263, #34510, #2869, #44681, #5400, #37745, #30348, #16045, #44439, #9575, #8886, #5876, #9106, #29900, #37517, #19966, #43984, #37283, #12796, #22952, #2638, #30128, #34041, #26877, #12574, #23174, #5642, #14177, #27808, #6559, #35192, #3090, #10249, #42122, #31267, #45136, #28028, #24096, #35636, #21334, #31037, #34957, #27570, #38663, #38431, #41673, #31717, #17179, #10473, #38210, #3328, #41903, #17424, #34730, #21554, #24327, #10952, #7484, #13953, #311, #10031, #45606, #7019, #16960, #35412, #28494, #31502, #45368, #14414, #6782, #20858, #20636, #25024, #13731, #38910, #24548, #39133, #21109, #3568, #17656, #84, #42344, #10710, #24793, #3782, #7263, #17874, #31940, #12076, #43031, #11395, #4473, #21786, #11633, #32647, #25710, #32427, #39822, #18564, #1443, #1221, #25479, #22455, #26153, #22231, #28731, #36328, #15328, #33105, #18786, #14876, #19013, #36559, #39596, #7951, #989, #35881, #8168, #15094, #4688, #776, #32875, #29180, #15544, #29411, #22018, #4916, #40268, #43482, #42811, #11850, #25921, #43703, #40031, #28952, #8623, #22687, #8385, #18346, #4010, #18109, #32190, #36109, #551, #14654, #7707, #11171, #25243, #39352, #4256, #9292, #2339, #12987, #30767, #20129, #23362, #43932, #44622, #26597, #26384, #9052, #19911, #19226, #12740, #15997, #27297, #44384, #26820, #41391, #44158, #5587, #44858, #37463, #9739, #40926, #37223, #41168, #9519, #22905, #16439, #1886, #40485, #5825, #36996, #30078, #16212, #5351, #15760, #2124, #12311, #36783, #23585, #5140, #19679, #29848, #37690, #12523, #8837, #6038, #19444, #34205, #33539, #33773, #40696, #2577, #13220, #28430, #17126, #3729, #14352, #20801, #7203, #2817, #6727, #13899, #42529, #28195, #35354, #10195, #38158, #21275, #31211, #45306, #27511, #17817, #9968, #30, #17358, #31885, #34898, #24272, #3264, #255, #38379, #24037, #37916, #42288, #13667, #23805, #6271, #20357, #34455, #16908, #30988, #27748, #41850, #31442, #10650, #45085, #45548, #41611, #27972, #6508, #35128, #14123, #13441, #38601, #42068, #10418, #21042, #20585, #24494, #6958, #3038, #3507, #24731, #17592, #31663, #38851, #21726, #36274, #11339, #18727, #4199, #14598, #28892, #42974, #7896, #25418, #7647, #8119, #25181, #28671, #32815, #4419, #25658, #7424, #40601, #2013, #22180, #18291, #42749, #4631, #18046, #21970, #8952, #32589, #36056, #39539, #18509, #39075, #39293, #35820, #11578, #24962, #32366, #1770, #23020, #11111, #15881, #29969, #43207, #932, #44053, #39771, #721, #14819, #15035, #492, #32127, #29123, #12420, #5472, #19566, #33664, #3953, #30194, #10894, #21497, #35575, #20489, #20249, #2467, #13112, #24172, #37579, #17022, #9411, #16334, #34575, #23928, #38049, #17245, #30415, #13560, #16573, #44753, #44512, #31099, #12872, #44284, #12640, #40821, #41283, #6407, #6625, #34791, #2935, #2239, #27634, #5934, #37354, #26720, #20024, #34101, #20700, #9636, #33886, #26954, #23700, #45198, #30656, #41054, #37812, #6161, #34341, #2711, #23478, #41507, #16804, #30884, #41743, #44979, #13333, #9176, #10096, #3154, #9858, #27410, #38280, #23252, #5715, #19802, #28791, #7325, #42410, #14242, #17719, #13801, #14024, #28093, #32009, #45439, #38731, #7546, #42869, #3399, #35706, #25082, #17941, #31783, #21623, #381, #31571, #45671, #35021, #20925, #6845, #7093, #17493, #14484, #38975, #28563, #24389, #42187, #7776, #10537, #24613, #4081, #21401, #35254, #153, #11236, #21174, #18180, #3632, #28311, #32256, #11015, #39196, #4312, #10781, #614, #24858, #35475, #3850, #14715, #42653, #31331, #27878, #41976, #25309, #39422, #21853, #35946, #10318, #38493, #11467, #19284, #36170, #5411, #12807, #30590, #27578, #27138, #9116, #9584, #30138, #34519, #13504, #23644, #37755, #6104, #23870, #19506, #20194, #41451, #37989, #20426, #16969, #41684, #10038, #24107, #44226, #31724, #3790, #20865, #10719, #45614, #6789, #28036, #10959, #38918, #557, #42350, #3338, #28500, #25028, #21560, #7270, #17431, #35642, #4015, #91, #34964, #14659, #28736, #42816, #31511, #14183, #11178, #41913, #38219, #42129, #17186, #6566, #24799, #20644, #31274, #13739, #27816, #21341, #10257, #24334, #10480, #38438, #38670, #13962, #7029, #35199, #42374, #10743, #31971, #9252, #4644, #36741, #8342, #22407, #38117, #27935, #27471, #9697, #27707, #41811, #23541, #34643, #2532, #27027, #9922, #37643, #30725, #16869, #5993, #19869, #2777, #44580, #10377, #10157, #5781, #23762, #33948, #13400, #13177, #2299, #6470, #20086, #30951, #12941, #37875, #16637, #6223, #9478, #42031, #44819, #17310, #37424, #34408, #20765, #16397, #20315, #41570, #30477, #24233, #3220, #45045, #34161, #34856, #27258, #41348, #41126, #31401, #23995, #13623, #20546, #45506, #3000, #17088, #31167, #13859, #45263, #38342, #6687, #28852, #17780, #7852, #893, #32547, #31845, #217, #24921, #42252, #32080, #7384, #450, #7161, #14554, #39035, #21930, #21686, #14311, #42933, #14996, #42710, #3462, #11074, #28383, #11300, #24453, #21460, #10610, #35538, #28159, #35779, #680, #4378, #39255, #10852, #18008, #4157, #21235, #25142, #42485, #38805, #3914, #25378, #7609, #29083, #28632, #35315, #18252, #32326, #14780, #39495, #24686, #36015, #18468 ),
 ( #3693, #43170, #38560, #6914, #20994, #35087, #17555, #31627, #13512, #14084, #43824, #43612, #1783, #26287, #11765, #25833, #15236, #1123, #32776, #18923, #29325, #40400, #19141, #8750, #4592, #22354, #33675, #43399, #8290, #33440, #33228, #15459, #26046, #37126, #4821, #29979, #36459, #39945, #15893, #36908, #5262, #30205, #33018, #26510, #29537, #11978, #1356, #44066, #40157, #11538, #25620, #8080, #8522, #19354, #19580, #2025, #12431, #22587, #40611, #36691, #18687, #39731, #5050, #1568, #16119, #15666, #29746, #12208, #22142, #8962, #36231, #22816, #23031, #5483, #37591, #2251, #16588, #30670, #41298, #44767, #41066, #41520, #12884, #16346, #20502, #37824, #13348, #40833, #27650, #35432, #9872, #5945, #30426, #38063, #5728, #9648, #41759, #20264, #23713, #27204, #13126, #26730, #26969, #9424, #44992, #12650, #20036, #34591, #10109, #44526, #2948, #6420, #30898, #6175, #17036, #27423, #23491, #34113, #2480, #33897, #19814, #34355, #2724, #23943, #16820, #31114, #37366, #45210, #21354, #13573, #24186, #38292, #6639, #3803, #17894, #44295, #9191, #23266, #42829, #4031, #8184, #11653, #25729, #4937, #18130, #1244, #35900, #32445, #32209, #4705, #571, #31961, #332, #28516, #793, #39842, #40047, #22473, #22249, #35657, #15347, #25263, #25041, #14435, #39372, #21804, #8404, #14893, #21575, #14672, #42612, #29427, #36580, #4273, #7726, #18365, #36347, #10972, #28973, #28748, #43054, #11190, #43283, #18808, #11867, #1010, #11416, #25502, #29204, #39615, #4491, #7970, #22037, #36128, #32898, #32667, #39151, #18583, #15115, #43500, #25940, #7503, #40945, #16456, #36802, #23378, #12757, #5605, #5368, #9308, #33789, #19242, #33329, #22704, #8642, #40286, #26402, #5158, #2140, #26616, #16229, #12095, #29867, #41182, #1674, #15778, #37481, #40714, #22922, #33557, #44641, #12329, #5842, #43950, #40504, #19928, #44402, #26836, #37706, #8855, #34003, #37014, #19462, #1905, #2357, #16014, #19033, #33124, #15560, #30095, #30539, #27090, #9536, #13002, #44177, #23600, #12541, #26174, #1460, #9070, #23136, #29640, #37242, #19699, #30308, #43720, #35148, #14141, #9987, #45102, #24056, #10436, #6055, #3055, #23822, #17144, #9757, #17379, #27990, #31680, #20819, #38174, #45325, #3284, #34472, #24289, #13459, #20376, #41628, #24511, #6745, #28212, #10212, #16924, #31462, #6523, #13918, #27528, #37933, #20601, #34696, #31229, #13687, #2832, #45566, #31004, #6291, #42085, #27766, #34920, #2597, #3525, #42306, #38620, #41868, #38395, #6980, #13236, #21065, #17611, #47, #10670, #24754, #20146, #34222, #16698, #30783, #44874, #27314, #41407, #28913, #29378, #43226, #4650, #25202, #7443, #36292, #32148, #511, #42552, #18747, #24983, #15056, #32390, #32835, #35843, #7668, #21746, #1186, #4218, #39093, #7224, #11597, #14619, #22200, #15294, #43450, #28691, #42770, #18311, #10914, #741, #14840, #42994, #21518, #11360, #25439, #11817, #36074, #11130, #25675, #38869, #39560, #17836, #7915, #4441, #21295, #21985, #3972, #8136, #39788, #18527, #35595, #29142, #35373, #3748, #18066, #32609, #31903, #950, #275, #14372, #28453, #33279, #36049, #15028, #8111, #22385, #15265, #4411, #7415, #11569, #21718, #14590, #4190, #924, #28421, #7887, #42964, #36489, #25410, #18502, #17809, #29115, #36264, #4620, #18719, #32806, #10417, #24271, #24730, #38850, #6507, #42528, #10194, #38378, #38600, #6726, #17357, #45547, #13898, #34454, #6957, #24961, #2816, #16907, #22294, #29684, #36390, #19286, #33167, #4753, #29913, #36631, #22753, #1293, #12140, #4985, #26222, #43544, #8225, #8689, #11910, #1503, #26665, #40337, #26449, #1717, #43998, #22965, #37060, #40762, #5413, #33605, #1957, #16057, #44229, #12586, #21769, #28936, #32628, #18089, #7936, #42792, #3991, #25222, #39805, #36093, #43466, #39579, #534, #15075, #35863, #43246, #28711, #39115, #7689, #4240, #32410, #18330, #32171, #972, #14638, #7464, #11617, #43013, #4458, #31923, #18769, #25905, #29162, #11153, #21537, #25694, #42576, #759, #32855, #11377, #14860, #25460, #22003, #17857, #39334, #18547, #8153, #3767, #22216, #36309, #1205, #35619, #4671, #15313, #29395, #11834, #40014, #8366, #35394, #295, #14395, #25005, #10935, #28475, #12060, #37206, #30061, #5570, #15529, #33298, #44607, #26134, #19211, #44369, #44142, #26368, #36982, #2324, #15744, #40910, #1643, #40249, #12724, #2107, #16196, #41153, #8606, #37449, #40470, #22890, #22671, #9277, #36767, #22435, #36540, #18998, #5335, #30276, #30504, #12968, #26804, #5123, #5808, #29832, #29610, #4899, #43913, #12292, #27057, #19430, #8822, #33522, #33090, #19896, #1427, #1870, #15977, #43687, #12506, #26582, #40680, #23346, #9034, #23104, #19662, #33755, #33973, #16422, #24257, #9725, #3026, #16664, #41596, #34436, #9952, #27283, #14749, #2802, #35744, #647, #6493, #38585, #34188, #38142, #45292, #28822, #13883, #21023, #24023, #23789, #6941, #16893, #30974, #13205, #4123, #41376, #31425, #17113, #18217, #20571, #34667, #31194, #32292, #13651, #37901, #23568, #27958, #45072, #9504, #37673, #6022, #13427, #27497, #27732, #6254, #41835, #10181, #38365, #20342, #6711, #20788, #20113, #34883, #3247, #42054, #2559, #17338, #30749, #45531, #10402, #44843, #24479, #8048, #12177, #15635, #36425, #11504, #33202, #43796, #29718, #39700, #8258, #19324, #865, #22789, #1092, #39460, #26259, #15429, #40125, #19114, #36884, #40372, #29506, #4347, #36663, #32746, #32516, #15205, #26014, #25345, #18891, #22112, #33409, #4788, #32986, #1753, #4565, #11733, #5235, #43579, #15860, #1325, #29293, #1538, #8724, #29052, #8488, #36202, #14967, #11947, #43138, #18656, #22324, #25589, #43369, #25803, #22559, #11269, #39916, #42902, #7818, #5024, #21896, #35982, #18438, #16316, #20233, #44731, #30175, #44266, #33642, #19546, #5452, #37335, #1995, #13094, #37560, #27176, #23002, #40800, #6388, #16091, #26702, #6143, #5918, #33869, #44491, #9842, #23229, #2690, #9157, #12624, #34320, #9620, #23682, #2916, #5697, #44960, #2222, #30398, #19784, #16787, #12849, #29949, #44033, #26484, #26930, #37793, #38032, #20470, #30866, #41033, #13317, #9392, #37096, #12404, #23461, #20008, #34557, #34084, #2449, #16551, #40585, #27393, #8931, #30636, #41264, #41488, #23911, #17006, #14003, #34773, #28072, #20683, #28291, #38957, #42636, #31763, #3379, #10518, #14222, #45419, #35236, #38475, #31312, #6826, #21384, #17702, #39178, #21152, #27860, #42391, #17471, #24837, #10297, #3136, #35002, #31553, #42167, #45653, #13781, #10761, #41955, #17226, #7307, #24593, #133, #13543, #361, #7528, #3830, #20906, #38711, #17919, #24151, #7072, #14463, #3614, #31989, #28541, #10997, #41725, #21602, #10079, #35684, #31083, #38260, #6605, #11443, #25962, #1482, #21830, #8430, #43524, #36370, #36150, #40068, #18835, #4295, #18385, #7752, #39400, #25288, #25527 ),
 ( #7994, #4512, #32465, #22499, #35924, #22732, #18159, #595, #18605, #29451, #12119, #40314, #11890, #814, #19056, #43079, #42851, #4059, #39640, #22060, #26200, #32690, #14915, #28996, #32234, #33146, #8668, #1038, #15142, #29233, #36609, #14696, #43309, #11677, #25753, #39865, #15371, #4965, #29664, #32927, #8206, #22274, #1272, #4733, #15582, #43740, #28772, #11218, #39004, #35286, #42681, #38769, #45473, #14276, #3428, #42449, #27907, #38310, #6880, #17526, #31599, #45704, #31366, #31815, #3188, #6656, #10817, #28126, #3664, #31132, #32045, #25112, #185, #42004, #20730, #28347, #41777, #14055, #417, #10575, #24652, #7126, #34824, #24890, #21205, #17751, #45229, #14521, #39226, #7355, #10347, #17275, #21431, #10127, #35507, #28598, #3882, #11047, #7579, #34610, #17055, #13830, #24421, #2967, #13590, #38526, #24201, #19113, #39459, #26013, #15428, #8257, #8047, #11946, #36424, #21895, #35981, #25344, #11268, #42901, #29051, #7817, #4787, #29292, #18890, #14748, #32515, #43795, #4346, #18437, #43578, #43368, #25588, #36201, #1537, #14966, #40124, #864, #43137, #8487, #1324, #29505, #40371, #11503, #36662, #39699, #22111, #4564, #22558, #18655, #21656, #35743, #18216, #32745, #5023, #29717, #12176, #33201, #1091, #15634, #15204, #28821, #4122, #11732, #25802, #26258, #39915, #22323, #32985, #32291, #646, #16786, #12623, #1994, #26701, #13093, #8723, #5696, #26483, #19783, #12403, #20007, #30635, #34319, #23460, #40799, #2221, #5917, #37095, #26929, #16090, #23001, #44265, #27175, #9391, #30865, #12848, #19545, #34083, #9156, #16550, #30174, #40584, #23228, #37334, #33868, #16315, #5451, #2448, #33641, #44730, #27392, #8930, #23681, #30397, #44490, #41032, #41263, #37559, #22788, #36883, #5234, #9619, #37792, #44959, #13316, #6142, #20232, #2689, #19323, #1752, #33408, #15859, #29948, #44032, #41954, #31082, #45180, #38031, #38956, #3829, #45418, #34772, #13780, #14221, #41487, #38474, #13542, #6825, #27616, #7071, #17701, #21383, #10517, #27859, #3378, #38710, #24150, #14002, #3135, #10078, #31311, #42390, #42166, #360, #28071, #6604, #35235, #10296, #31762, #17225, #41724, #24370, #20905, #17470, #31552, #38259, #10760, #20682, #24592, #7306, #35457, #6387, #20469, #34556, #2915, #17005, #115, #38940, #19250, #32675, #22481, #22929, #1467, #36591, #8414, #11875, #7978, #8192, #22259, #26183, #39625, #32910, #1682, #37022, #43294, #29875, #33337, #12104, #25947, #15786, #40297, #25737, #39850, #29213, #15124, #1021, #1254, #11661, #8652, #33131, #22715, #18591, #36356, #1916, #4715, #18818, #43960, #15567, #29435, #40054, #5377, #15356, #12338, #43508, #4949, #26411, #5165, #40512, #8862, #19040, #36810, #29648, #43727, #19470, #33566, #16023, #30102, #44188, #22045, #25511, #36137, #4499, #16936, #26624, #30550, #40722, #34233, #34014, #9079, #27324, #12766, #6067, #19711, #44650, #37490, #13012, #30320, #17155, #5850, #38187, #3065, #9547, #41644, #37252, #41193, #2607, #31241, #31015, #24069, #27102, #26847, #9999, #19938, #2369, #16241, #6532, #44411, #34484, #20157, #20612, #23610, #37717, #16708, #34707, #30793, #40956, #23145, #45113, #16467, #12549, #5615, #33797, #44885, #13246, #41417, #9318, #9766, #23833, #37948, #23389, #6302, #20386, #2149, #2843, #13470, #27540, #21759, #17847, #24301, #31913, #10925, #28701, #14385, #10448, #14629, #18078, #38881, #13928, #35607, #523, #32158, #42097, #10682, #35853, #3297, #25212, #3540, #41879, #42780, #285, #42563, #21528, #39323, #11142, #28463, #6758, #39104, #35161, #34931, #17626, #24993, #27779, #21307, #24524, #4230, #7236, #35384, #18322, #6994, #14152, #7679, #7454, #45337, #3757, #31692, #13699, #38634, #38407, #10223, #21077, #60, #20831, #28222, #17391, #31476, #45580, #28003, #42317, #24764, #3981, #36302, #36758, #32402, #29387, #4451, #43459, #36085, #43680, #8595, #12281, #1420, #18758, #25896, #29602, #15067, #4889, #39798, #962, #22209, #5114, #33083, #40461, #36532, #43237, #12051, #32848, #40238, #25686, #18539, #4659, #1196, #11826, #15304, #29154, #26123, #11608, #32619, #22661, #40007, #15522, #28927, #15733, #22882, #19202, #8146, #8357, #33289, #39571, #22423, #29822, #18990, #1634, #43904, #26357, #14850, #8813, #36973, #5326, #752, #43005, #11369, #25452, #7926, #21996, #13197, #6011, #5799, #23780, #16656, #19653, #44359, #37195, #9025, #40671, #23336, #12715, #27276, #27045, #41368, #12497, #37439, #9943, #16413, #30493, #37893, #41143, #37662, #6244, #45064, #20334, #34427, #2794, #16886, #24015, #1861, #30049, #44132, #26573, #45013, #5745, #13366, #40851, #9212, #1026, #40104, #8468, #5003, #26466, #23203, #15616, #19304, #37312, #15839, #12605, #33851, #27156, #20662, #13760, #31533, #17205, #13297, #17450, #20886, #41705, #16764, #38456, #3359, #34981, #44940, #13524, #24574, #6123, #28055, #6365, #44710, #45634, #34754, #45397, #24352, #42148, #13983, #3115, #9602, #41933, #38011, #37774, #20448, #31292, #30613, #24129, #27373, #38691, #10059, #38239, #7050, #9821, #16987, #10499, #27838, #21134, #6585, #34537, #6807, #2428, #34297, #10278, #41468, #20213, #16529, #2668, #23889, #27597, #30844, #13070, #41245, #23662, #2896, #31064, #45162, #7508, #17682, #11196, #10977, #31742, #4278, #35437, #28754, #42370, #21580, #14442, #35663, #7288, #39847, #28521, #15120, #25734, #32214, #18588, #14203, #18136, #25268, #8189, #39621, #1017, #4036, #3808, #32672, #42617, #25047, #38937, #29210, #21361, #11421, #42834, #43289, #576, #14677, #39378, #11658, #7732, #17900, #3594, #7975, #39157, #35218, #111, #28271, #21810, #35905, #18370, #31967, #32450, #798, #14898, #337, #28979, #43059, #10739, #25508, #22042, #36134, #4496, #24817, #15564, #1679, #36586, #4711, #33334, #29432, #40952, #26621, #36353, #40292, #18814, #43955, #43724, #32905, #37019, #22478, #15783, #43505, #8648, #1464, #22709, #40051, #26843, #29645, #2146, #12763, #19247, #5611, #1250, #5162, #12334, #22255, #40718, #33794, #36806, #4942, #19706, #12101, #26178, #25944, #16237, #8410, #44183, #29871, #30314, #26407, #40508, #8859, #44408, #22926, #19037, #15353, #9076, #5374, #11872, #33128, #19467, #33561, #1911, #16019, #30099, #12545, #23142, #37247, #37713, #16932, #23829, #6753, #6528, #2603, #27772, #31470, #27536, #34010, #41638, #20608, #38403, #24064, #20151, #24297, #41875, #2839, #23606, #45332, #10219, #20826, #6062, #20381, #45573, #13008, #34927, #13242, #5847, #3292, #9994, #34703, #31237, #17387, #13924, #38182, #16464, #3062, #44881, #44646, #27320, #17151, #37487, #31011, #34228, #27997, #45109, #13466, #9314, #16703, #37941, #23385, #13694, #19935, #2364, #41413, #30547, #27098, #41189, #9543, #30789, #9762, #6298, #34480, #54, #38876, #18317, #18072, #281, #10920, #21991, #35378, #14846, #7232, #14147 ) ),
 .UNSPECIFIED., .T., .F., .T. ) 
 B_SPLINE_SURFACE_WITH_KNOTS ( ( 4, 3, 4 ),
 ( 3, 2, 2, 2, 2, 2, 2, 2, 2, 2, 2, 2, 2, 2, 2, 2, 2, 2, 2, 2, 2, 2, 2, 2, 2, 2, 2, 2, 2, 2, 2, 2, 2, 2, 2, 2, 2, 2, 2, 2, 2, 2, 2, 2, 2, 2, 2, 2, 2, 2, 2, 2, 2, 2, 2, 2, 2, 2, 2, 2, 2, 2, 2, 2, 2, 2, 2, 2, 2, 2, 2, 2, 2, 2, 2, 2, 2, 2, 2, 2, 2, 2, 2, 2, 2, 2, 2, 2, 2, 2, 2, 2, 2, 2, 2, 2, 2, 2, 2, 2, 2, 2, 2, 2, 2, 2, 2, 2, 2, 2, 2, 2, 2, 2, 2, 2, 2, 2, 2, 2, 2, 2, 2, 2, 2, 2, 2, 2, 2, 2, 2, 2, 2, 2, 2, 2, 2, 2, 2, 2, 2, 2, 2, 2, 2, 2, 2, 2, 2, 2, 2, 2, 2, 2, 2, 2, 2, 2, 2, 2, 2, 2, 2, 2, 2, 2, 2, 2, 2, 2, 2, 2, 2, 2, 2, 2, 2, 2, 2, 2, 2, 2, 2, 2, 2, 2, 2, 2, 2, 2, 2, 2, 2, 2, 2, 2, 2, 2, 2, 2, 2, 2, 2, 2, 2, 2, 2, 2, 2, 2, 2, 2, 2, 2, 2, 2, 2, 2, 2, 2, 2, 2, 2, 2, 2, 2, 2, 2, 2, 2, 2, 2, 2, 2, 2, 2, 2, 2, 2, 2, 2, 2, 2, 2, 2, 2, 2, 2, 2, 2, 2, 2, 2, 2, 2, 2, 2, 2, 2, 2, 2, 2, 2, 2, 2, 2, 2, 2, 2, 2, 2, 2, 2, 2, 2, 2, 2, 2, 2, 2, 2, 2, 2, 2, 2, 2, 2, 2, 2, 2, 2, 2, 2, 2, 2, 2, 2, 2, 2, 2, 2, 2, 2, 2, 2, 2, 2, 2, 2, 2, 2, 2, 2, 2, 2, 2, 2, 2, 2, 2, 2, 2, 2, 2, 2, 2, 2, 2, 2, 2, 2, 2, 2, 2, 2, 2, 2, 2, 2, 2, 2, 2, 2, 2, 2, 2, 2, 2, 2, 2, 2, 2, 2, 2, 2, 2, 2, 2, 2, 2, 2, 2, 2, 2, 2, 2, 2, 2, 2, 2, 2, 2, 2, 2, 2, 2, 2, 2, 2, 2, 2, 2, 2, 2, 2, 2, 2, 2, 2, 2, 2, 2, 2, 2, 2, 2, 2, 2, 2, 2, 2, 2, 2, 2, 2, 2, 2, 2, 2, 2, 2, 2, 2, 2, 2, 2, 2, 2, 2, 2, 2, 2, 2, 2, 2, 2, 2, 2, 2, 2, 2, 3 ),
 ( 0.000000000000000000, 0.5000000000000000000, 1.000000000000000000 ),
 ( 0.000000000000000000, 0.002272727272727272617, 0.004545454545454545234, 0.006818181818181817851, 0.009090909090909090468, 0.01136363636363636395, 0.01363636363636363570, 0.01590909090909090745, 0.01818181818181818094, 0.02045454545454545442, 0.02272727272727272790, 0.02500000000000000139, 0.02727272727272727140, 0.02954545454545454489, 0.03181818181818181490, 0.03409090909090908839, 0.03636363636363636187, 0.03863636363636363535, 0.04090909090909090884, 0.04318181818181818232, 0.04545454545454545581, 0.04772727272727272929, 0.05000000000000000278, 0.05227272727272726932, 0.05454545454545454281, 0.05681818181818181629, 0.05909090909090908977, 0.06136363636363636326, 0.06363636363636362980, 0.06590909090909090329, 0.06818181818181817677, 0.07045454545454545026, 0.07272727272727272374, 0.07499999999999999722, 0.07727272727272727071, 0.07954545454545454419, 0.08181818181818181768, 0.08409090909090909116, 0.08636363636363636465, 0.08863636363636363813, 0.09090909090909091161, 0.09318181818181818510, 0.09545454545454545858, 0.09772727272727273207, 0.1000000000000000056, 0.1022727272727272790, 0.1045454545454545386, 0.1068181818181818121, 0.1090909090909090856, 0.1113636363636363591, 0.1136363636363636326, 0.1159090909090909061, 0.1181818181818181795, 0.1204545454545454530, 0.1227272727272727265, 0.1250000000000000000, 0.1272727272727272596, 0.1295454545454545470, 0.1318181818181818066, 0.1340909090909090939, 0.1363636363636363535, 0.1386363636363636409, 0.1409090909090909005, 0.1431818181818181879, 0.1454545454545454475, 0.1477272727272727348, 0.1499999999999999944, 0.1522727272727272818, 0.1545454545454545414, 0.1568181818181818288, 0.1590909090909090884, 0.1613636363636363757, 0.1636363636363636354, 0.1659090909090909227, 0.1681818181818181823, 0.1704545454545454419, 0.1727272727272727293, 0.1749999999999999889, 0.1772727272727272763, 0.1795454545454545359, 0.1818181818181818232, 0.1840909090909090828, 0.1863636363636363702, 0.1886363636363636298, 0.1909090909090909172, 0.1931818181818181768, 0.1954545454545454641, 0.1977272727272727237, 0.2000000000000000111, 0.2022727272727272707, 0.2045454545454545581, 0.2068181818181818177, 0.2090909090909090773, 0.2113636363636363646, 0.2136363636363636243, 0.2159090909090909116, 0.2181818181818181712, 0.2204545454545454586, 0.2227272727272727182, 0.2250000000000000056, 0.2272727272727272652, 0.2295454545454545525, 0.2318181818181818121, 0.2340909090909090995, 0.2363636363636363591, 0.2386363636363636465, 0.2409090909090909061, 0.2431818181818181934, 0.2454545454545454530, 0.2477272727272727404, 0.2500000000000000000, 0.2522727272727272596, 0.2545454545454545192, 0.2568181818181818343, 0.2590909090909090939, 0.2613636363636363535, 0.2636363636363636131, 0.2659090909090909283, 0.2681818181818181879, 0.2704545454545454475, 0.2727272727272727071, 0.2750000000000000222, 0.2772727272727272818, 0.2795454545454545414, 0.2818181818181818010, 0.2840909090909091161, 0.2863636363636363757, 0.2886363636363636354, 0.2909090909090908950, 0.2931818181818181546, 0.2954545454545454697, 0.2977272727272727293, 0.2999999999999999889, 0.3022727272727272485, 0.3045454545454545636, 0.3068181818181818232, 0.3090909090909090828, 0.3113636363636363424, 0.3136363636363636576, 0.3159090909090909172, 0.3181818181818181768, 0.3204545454545454364, 0.3227272727272727515, 0.3250000000000000111, 0.3272727272727272707, 0.3295454545454545303, 0.3318181818181818454, 0.3340909090909091050, 0.3363636363636363646, 0.3386363636363636243, 0.3409090909090908839, 0.3431818181818181990, 0.3454545454545454586, 0.3477272727272727182, 0.3499999999999999778, 0.3522727272727272929, 0.3545454545454545525, 0.3568181818181818121, 0.3590909090909090717, 0.3613636363636363869, 0.3636363636363636465, 0.3659090909090909061, 0.3681818181818181657, 0.3704545454545454808, 0.3727272727272727404, 0.3750000000000000000, 0.3772727272727272596, 0.3795454545454545192, 0.3818181818181818343, 0.3840909090909090939, 0.3863636363636363535, 0.3886363636363636131, 0.3909090909090909283, 0.3931818181818181879, 0.3954545454545454475, 0.3977272727272727071, 0.4000000000000000222, 0.4022727272727272818, 0.4045454545454545414, 0.4068181818181818010, 0.4090909090909091161, 0.4113636363636363757, 0.4136363636363636354, 0.4159090909090908950, 0.4181818181818181546, 0.4204545454545454697, 0.4227272727272727293, 0.4249999999999999889, 0.4272727272727272485, 0.4295454545454545636, 0.4318181818181818232, 0.4340909090909090828, 0.4363636363636363424, 0.4386363636363636576, 0.4409090909090909172, 0.4431818181818181768, 0.4454545454545454364, 0.4477272727272727515, 0.4500000000000000111, 0.4522727272727272707, 0.4545454545454545303, 0.4568181818181818454, 0.4590909090909091050, 0.4613636363636363646, 0.4636363636363636243, 0.4659090909090908839, 0.4681818181818181990, 0.4704545454545454586, 0.4727272727272727182, 0.4749999999999999778, 0.4772727272727272929, 0.4795454545454545525, 0.4818181818181818121, 0.4840909090909090717, 0.4863636363636363869, 0.4886363636363636465, 0.4909090909090909061, 0.4931818181818181657, 0.4954545454545454808, 0.4977272727272727404, 0.5000000000000000000, 0.5022727272727273151, 0.5045454545454545192, 0.5068181818181818343, 0.5090909090909090384, 0.5113636363636363535, 0.5136363636363636687, 0.5159090909090908728, 0.5181818181818181879, 0.5204545454545455030, 0.5227272727272727071, 0.5250000000000000222, 0.5272727272727272263, 0.5295454545454545414, 0.5318181818181818565, 0.5340909090909090606, 0.5363636363636363757, 0.5386363636363636909, 0.5409090909090908950, 0.5431818181818182101, 0.5454545454545454142, 0.5477272727272727293, 0.5500000000000000444, 0.5522727272727272485, 0.5545454545454545636, 0.5568181818181817677, 0.5590909090909090828, 0.5613636363636363980, 0.5636363636363636020, 0.5659090909090909172, 0.5681818181818182323, 0.5704545454545454364, 0.5727272727272727515, 0.5749999999999999556, 0.5772727272727272707, 0.5795454545454545858, 0.5818181818181817899, 0.5840909090909091050, 0.5863636363636363091, 0.5886363636363636243, 0.5909090909090909394, 0.5931818181818181435, 0.5954545454545454586, 0.5977272727272727737, 0.5999999999999999778, 0.6022727272727272929, 0.6045454545454544970, 0.6068181818181818121, 0.6090909090909091272, 0.6113636363636363313, 0.6136363636363636465, 0.6159090909090909616, 0.6181818181818181657, 0.6204545454545454808, 0.6227272727272726849, 0.6250000000000000000, 0.6272727272727273151, 0.6295454545454545192, 0.6318181818181818343, 0.6340909090909090384, 0.6363636363636363535, 0.6386363636363636687, 0.6409090909090908728, 0.6431818181818181879, 0.6454545454545455030, 0.6477272727272727071, 0.6500000000000000222, 0.6522727272727272263, 0.6545454545454545414, 0.6568181818181818565, 0.6590909090909090606, 0.6613636363636363757, 0.6636363636363636909, 0.6659090909090908950, 0.6681818181818182101, 0.6704545454545454142, 0.6727272727272727293, 0.6750000000000000444, 0.6772727272727272485, 0.6795454545454545636, 0.6818181818181817677, 0.6840909090909090828, 0.6863636363636363980, 0.6886363636363636020, 0.6909090909090909172, 0.6931818181818182323, 0.6954545454545454364, 0.6977272727272727515, 0.6999999999999999556, 0.7022727272727272707, 0.7045454545454545858, 0.7068181818181817899, 0.7090909090909091050, 0.7113636363636363091, 0.7136363636363636243, 0.7159090909090909394, 0.7181818181818181435, 0.7204545454545454586, 0.7227272727272727737, 0.7249999999999999778, 0.7272727272727272929, 0.7295454545454544970, 0.7318181818181818121, 0.7340909090909091272, 0.7363636363636363313, 0.7386363636363636465, 0.7409090909090909616, 0.7431818181818181657, 0.7454545454545454808, 0.7477272727272726849, 0.7500000000000000000, 0.7522727272727273151, 0.7545454545454545192, 0.7568181818181818343, 0.7590909090909090384, 0.7613636363636363535, 0.7636363636363636687, 0.7659090909090908728, 0.7681818181818181879, 0.7704545454545455030, 0.7727272727272727071, 0.7750000000000000222, 0.7772727272727272263, 0.7795454545454545414, 0.7818181818181818565, 0.7840909090909090606, 0.7863636363636363757, 0.7886363636363636909, 0.7909090909090908950, 0.7931818181818182101, 0.7954545454545454142, 0.7977272727272727293, 0.8000000000000000444, 0.8022727272727272485, 0.8045454545454545636, 0.8068181818181817677, 0.8090909090909090828, 0.8113636363636363980, 0.8136363636363636020, 0.8159090909090909172, 0.8181818181818182323, 0.8204545454545454364, 0.8227272727272727515, 0.8249999999999999556, 0.8272727272727272707, 0.8295454545454545858, 0.8318181818181817899, 0.8340909090909091050, 0.8363636363636363091, 0.8386363636363636243, 0.8409090909090909394, 0.8431818181818181435, 0.8454545454545454586, 0.8477272727272727737, 0.8499999999999999778, 0.8522727272727272929, 0.8545454545454544970, 0.8568181818181818121, 0.8590909090909091272, 0.8613636363636363313, 0.8636363636363636465, 0.8659090909090909616, 0.8681818181818181657, 0.8704545454545454808, 0.8727272727272726849, 0.8750000000000000000, 0.8772727272727273151, 0.8795454545454545192, 0.8818181818181818343, 0.8840909090909090384, 0.8863636363636363535, 0.8886363636363636687, 0.8909090909090908728, 0.8931818181818181879, 0.8954545454545455030, 0.8977272727272727071, 0.9000000000000000222, 0.9022727272727272263, 0.9045454545454545414, 0.9068181818181818565, 0.9090909090909090606, 0.9113636363636363757, 0.9136363636363636909, 0.9159090909090908950, 0.9181818181818182101, 0.9204545454545454142, 0.9227272727272727293, 0.9250000000000000444, 0.9272727272727272485, 0.9295454545454545636, 0.9318181818181817677, 0.9340909090909090828, 0.9363636363636363980, 0.9386363636363636020, 0.9409090909090909172, 0.9431818181818182323, 0.9454545454545454364, 0.9477272727272727515, 0.9499999999999999556, 0.9522727272727272707, 0.9545454545454545858, 0.9568181818181817899, 0.9590909090909091050, 0.9613636363636363091, 0.9636363636363636243, 0.9659090909090909394, 0.9681818181818181435, 0.9704545454545454586, 0.9727272727272727737, 0.9749999999999999778, 0.9772727272727272929, 0.9781254700864303597 ),
 .UNSPECIFIED. ) 
 GEOMETRIC_REPRESENTATION_ITEM ( )  RATIONAL_B_SPLINE_SURFACE ( (
 ( 1.000000000000000000, 0.9898214418809326842, 1.000000000000000000, 0.9898214418809326842, 1.000000000000000000, 0.9898214418809326842, 1.000000000000000000, 0.9898214418809326842, 1.000000000000000000, 0.9898214418809326842, 1.000000000000000000, 0.9898214418809326842, 1.000000000000000000, 0.9898214418809326842, 1.000000000000000000, 0.9898214418809326842, 1.000000000000000000, 0.9898214418809326842, 1.000000000000000000, 0.9898214418809326842, 1.000000000000000000, 0.9898214418809326842, 1.000000000000000000, 0.9898214418809326842, 1.000000000000000000, 0.9898214418809326842, 1.000000000000000000, 0.9898214418809326842, 1.000000000000000000, 0.9898214418809326842, 1.000000000000000000, 0.9898214418809326842, 1.000000000000000000, 0.9898214418809326842, 1.000000000000000000, 0.9898214418809326842, 1.000000000000000000, 0.9898214418809326842, 1.000000000000000000, 0.9898214418809326842, 1.000000000000000000, 0.9898214418809326842, 1.000000000000000000, 0.9898214418809326842, 1.000000000000000000, 0.9898214418809326842, 1.000000000000000000, 0.9898214418809326842, 1.000000000000000000, 0.9898214418809326842, 1.000000000000000000, 0.9898214418809326842, 1.000000000000000000, 0.9898214418809326842, 1.000000000000000000, 0.9898214418809326842, 1.000000000000000000, 0.9898214418809326842, 1.000000000000000000, 0.9898214418809326842, 1.000000000000000000, 0.9898214418809326842, 1.000000000000000000, 0.9898214418809326842, 1.000000000000000000, 0.9898214418809326842, 1.000000000000000000, 0.9898214418809326842, 1.000000000000000000, 0.9898214418809326842, 1.000000000000000000, 0.9898214418809326842, 1.000000000000000000, 0.9898214418809326842, 1.000000000000000000, 0.9898214418809326842, 1.000000000000000000, 0.9898214418809326842, 1.000000000000000000, 0.9898214418809326842, 1.000000000000000000, 0.9898214418809326842, 1.000000000000000000, 0.9898214418809326842, 1.000000000000000000, 0.9898214418809326842, 1.000000000000000000, 0.9898214418809326842, 1.000000000000000000, 0.9898214418809326842, 1.000000000000000000, 0.9898214418809326842, 1.000000000000000000, 0.9898214418809326842, 1.000000000000000000, 0.9898214418809326842, 1.000000000000000000, 0.9898214418809326842, 1.000000000000000000, 0.9898214418809326842, 1.000000000000000000, 0.9898214418809326842, 1.000000000000000000, 0.9898214418809326842, 1.000000000000000000, 0.9898214418809326842, 1.000000000000000000, 0.9898214418809326842, 1.000000000000000000, 0.9898214418809326842, 1.000000000000000000, 0.9898214418809326842, 1.000000000000000000, 0.9898214418809326842, 1.000000000000000000, 0.9898214418809326842, 1.000000000000000000, 0.9898214418809326842, 1.000000000000000000, 0.9898214418809326842, 1.000000000000000000, 0.9898214418809326842, 1.000000000000000000, 0.9898214418809326842, 1.000000000000000000, 0.9898214418809326842, 1.000000000000000000, 0.9898214418809326842, 1.000000000000000000, 0.9898214418809326842, 1.000000000000000000, 0.9898214418809326842, 1.000000000000000000, 0.9898214418809326842, 1.000000000000000000, 0.9898214418809326842, 1.000000000000000000, 0.9898214418809326842, 1.000000000000000000, 0.9898214418809326842, 1.000000000000000000, 0.9898214418809326842, 1.000000000000000000, 0.9898214418809326842, 1.000000000000000000, 0.9898214418809326842, 1.000000000000000000, 0.9898214418809326842, 1.000000000000000000, 0.9898214418809326842, 1.000000000000000000, 0.9898214418809326842, 1.000000000000000000, 0.9898214418809326842, 1.000000000000000000, 0.9898214418809326842, 1.000000000000000000, 0.9898214418809326842, 1.000000000000000000, 0.9898214418809326842, 1.000000000000000000, 0.9898214418809326842, 1.000000000000000000, 0.9898214418809326842, 1.000000000000000000, 0.9898214418809326842, 1.000000000000000000, 0.9898214418809326842, 1.000000000000000000, 0.9898214418809326842, 1.000000000000000000, 0.9898214418809326842, 1.000000000000000000, 0.9898214418809326842, 1.000000000000000000, 0.9898214418809326842, 1.000000000000000000, 0.9898214418809326842, 1.000000000000000000, 0.9898214418809326842, 1.000000000000000000, 0.9898214418809326842, 1.000000000000000000, 0.9898214418809326842, 1.000000000000000000, 0.9898214418809326842, 1.000000000000000000, 0.9898214418809326842, 1.000000000000000000, 0.9898214418809326842, 1.000000000000000000, 0.9898214418809326842, 1.000000000000000000, 0.9898214418809326842, 1.000000000000000000, 0.9898214418809326842, 1.000000000000000000, 0.9898214418809326842, 1.000000000000000000, 0.9898214418809326842, 1.000000000000000000, 0.9898214418809326842, 1.000000000000000000, 0.9898214418809326842, 1.000000000000000000, 0.9898214418809326842, 1.000000000000000000, 0.9898214418809326842, 1.000000000000000000, 0.9898214418809326842, 1.000000000000000000, 0.9898214418809326842, 1.000000000000000000, 0.9898214418809326842, 1.000000000000000000, 0.9898214418809326842, 1.000000000000000000, 0.9898214418809326842, 1.000000000000000000, 0.9898214418809326842, 1.000000000000000000, 0.9898214418809326842, 1.000000000000000000, 0.9898214418809326842, 1.000000000000000000, 0.9898214418809326842, 1.000000000000000000, 0.9898214418809326842, 1.000000000000000000, 0.9898214418809326842, 1.000000000000000000, 0.9898214418809326842, 1.000000000000000000, 0.9898214418809326842, 1.000000000000000000, 0.9898214418809326842, 1.000000000000000000, 0.9898214418809326842, 1.000000000000000000, 0.9898214418809326842, 1.000000000000000000, 0.9898214418809326842, 1.000000000000000000, 0.9898214418809326842, 1.000000000000000000, 0.9898214418809326842, 1.000000000000000000, 0.9898214418809326842, 1.000000000000000000, 0.9898214418809326842, 1.000000000000000000, 0.9898214418809326842, 1.000000000000000000, 0.9898214418809326842, 1.000000000000000000, 0.9898214418809326842, 1.000000000000000000, 0.9898214418809326842, 1.000000000000000000, 0.9898214418809326842, 1.000000000000000000, 0.9898214418809326842, 1.000000000000000000, 0.9898214418809326842, 1.000000000000000000, 0.9898214418809326842, 1.000000000000000000, 0.9898214418809326842, 1.000000000000000000, 0.9898214418809326842, 1.000000000000000000, 0.9898214418809326842, 1.000000000000000000, 0.9898214418809326842, 1.000000000000000000, 0.9898214418809326842, 1.000000000000000000, 0.9898214418809326842, 1.000000000000000000, 0.9898214418809326842, 1.000000000000000000, 0.9898214418809326842, 1.000000000000000000, 0.9898214418809326842, 1.000000000000000000, 0.9898214418809326842, 1.000000000000000000, 0.9898214418809326842, 1.000000000000000000, 0.9898214418809326842, 1.000000000000000000, 0.9898214418809326842, 1.000000000000000000, 0.9898214418809326842, 1.000000000000000000, 0.9898214418809326842, 1.000000000000000000, 0.9898214418809326842, 1.000000000000000000, 0.9898214418809326842, 1.000000000000000000, 0.9898214418809326842, 1.000000000000000000, 0.9898214418809326842, 1.000000000000000000, 0.9898214418809326842, 1.000000000000000000, 0.9898214418809326842, 1.000000000000000000, 0.9898214418809326842, 1.000000000000000000, 0.9898214418809326842, 1.000000000000000000, 0.9898214418809326842, 1.000000000000000000, 0.9898214418809326842, 1.000000000000000000, 0.9898214418809326842, 1.000000000000000000, 0.9898214418809326842, 1.000000000000000000, 0.9898214418809326842, 1.000000000000000000, 0.9898214418809326842, 1.000000000000000000, 0.9898214418809326842, 1.000000000000000000, 0.9898214418809326842, 1.000000000000000000, 0.9898214418809326842, 1.000000000000000000, 0.9898214418809326842, 1.000000000000000000, 0.9898214418809326842, 1.000000000000000000, 0.9898214418809326842, 1.000000000000000000, 0.9898214418809326842, 1.000000000000000000, 0.9898214418809326842, 1.000000000000000000, 0.9898214418809326842, 1.000000000000000000, 0.9898214418809326842, 1.000000000000000000, 0.9898214418809326842, 1.000000000000000000, 0.9898214418809326842, 1.000000000000000000, 0.9898214418809326842, 1.000000000000000000, 0.9898214418809326842, 1.000000000000000000, 0.9898214418809326842, 1.000000000000000000, 0.9898214418809326842, 1.000000000000000000, 0.9898214418809326842, 1.000000000000000000, 0.9898214418809326842, 1.000000000000000000, 0.9898214418809326842, 1.000000000000000000, 0.9898214418809326842, 1.000000000000000000, 0.9898214418809326842, 1.000000000000000000, 0.9898214418809326842, 1.000000000000000000, 0.9898214418809326842, 1.000000000000000000, 0.9898214418809326842, 1.000000000000000000, 0.9898214418809326842, 1.000000000000000000, 0.9898214418809326842, 1.000000000000000000, 0.9898214418809326842, 1.000000000000000000, 0.9898214418809326842, 1.000000000000000000, 0.9898214418809326842, 1.000000000000000000, 0.9898214418809326842, 1.000000000000000000, 0.9898214418809326842, 1.000000000000000000, 0.9898214418809326842, 1.000000000000000000, 0.9898214418809326842, 1.000000000000000000, 0.9898214418809326842, 1.000000000000000000, 0.9898214418809326842, 1.000000000000000000, 0.9898214418809326842, 1.000000000000000000, 0.9898214418809326842, 1.000000000000000000, 0.9898214418809326842, 1.000000000000000000, 0.9898214418809326842, 1.000000000000000000, 0.9898214418809326842, 1.000000000000000000, 0.9898214418809326842, 1.000000000000000000, 0.9898214418809326842, 1.000000000000000000, 0.9898214418809326842, 1.000000000000000000, 0.9898214418809326842, 1.000000000000000000, 0.9898214418809326842, 1.000000000000000000, 0.9898214418809326842, 1.000000000000000000, 0.9898214418809326842, 1.000000000000000000, 0.9898214418809326842, 1.000000000000000000, 0.9898214418809326842, 1.000000000000000000, 0.9898214418809326842, 1.000000000000000000, 0.9898214418809326842, 1.000000000000000000, 0.9898214418809326842, 1.000000000000000000, 0.9898214418809326842, 1.000000000000000000, 0.9898214418809326842, 1.000000000000000000, 0.9898214418809326842, 1.000000000000000000, 0.9898214418809326842, 1.000000000000000000, 0.9898214418809326842, 1.000000000000000000, 0.9898214418809326842, 1.000000000000000000, 0.9898214418809326842, 1.000000000000000000, 0.9898214418809326842, 1.000000000000000000, 0.9898214418809326842, 1.000000000000000000, 0.9898214418809326842, 1.000000000000000000, 0.9898214418809326842, 1.000000000000000000, 0.9898214418809326842, 1.000000000000000000, 0.9898214418809326842, 1.000000000000000000, 0.9898214418809326842, 1.000000000000000000, 0.9898214418809326842, 1.000000000000000000, 0.9898214418809326842, 1.000000000000000000, 0.9898214418809326842, 1.000000000000000000, 0.9898214418809326842, 1.000000000000000000, 0.9898214418809326842, 1.000000000000000000, 0.9898214418809326842, 1.000000000000000000, 0.9898214418809326842, 1.000000000000000000, 0.9898214418809326842, 1.000000000000000000, 0.9898214418809326842, 1.000000000000000000, 0.9898214418809326842, 1.000000000000000000, 0.9898214418809326842, 1.000000000000000000, 0.9898214418809326842, 1.000000000000000000, 0.9898214418809326842, 1.000000000000000000, 0.9898214418809326842, 1.000000000000000000, 0.9898214418809326842, 1.000000000000000000, 0.9898214418809326842, 1.000000000000000000, 0.9898214418809326842, 1.000000000000000000, 0.9898214418809326842, 1.000000000000000000, 0.9898214418809326842, 1.000000000000000000, 0.9898214418809326842, 1.000000000000000000, 0.9898214418809326842, 1.000000000000000000, 0.9898214418809326842, 1.000000000000000000, 0.9898214418809326842, 1.000000000000000000, 0.9898214418809326842, 1.000000000000000000, 0.9898214418809326842, 1.000000000000000000, 0.9898214418809326842, 1.000000000000000000, 0.9898214418809326842, 1.000000000000000000, 0.9898214418809326842, 1.000000000000000000, 0.9898214418809326842, 1.000000000000000000, 0.9898214418809326842, 1.000000000000000000, 0.9898214418809326842, 1.000000000000000000, 0.9898214418809326842, 1.000000000000000000, 0.9898214418809326842, 1.000000000000000000, 0.9898214418809326842, 1.000000000000000000, 0.9898214418809326842, 1.000000000000000000, 0.9898214418809326842, 1.000000000000000000, 0.9898214418809326842, 1.000000000000000000, 0.9898214418809326842, 1.000000000000000000, 0.9898214418809326842, 1.000000000000000000, 0.9898214418809326842, 1.000000000000000000, 0.9898214418809326842, 1.000000000000000000, 0.9898214418809326842, 1.000000000000000000, 0.9898214418809326842, 1.000000000000000000, 0.9898214418809326842, 1.000000000000000000, 0.9898214418809326842, 1.000000000000000000, 0.9898214418809326842, 1.000000000000000000, 0.9898214418809326842, 1.000000000000000000, 0.9898214418809326842, 1.000000000000000000, 0.9898214418809326842, 1.000000000000000000, 0.9898214418809326842, 1.000000000000000000, 0.9898214418809326842, 1.000000000000000000, 0.9898214418809326842, 1.000000000000000000, 0.9898214418809326842, 1.000000000000000000, 0.9898214418809326842, 1.000000000000000000, 0.9898214418809326842, 1.000000000000000000, 0.9898214418809326842, 1.000000000000000000, 0.9898214418809326842, 1.000000000000000000, 0.9898214418809326842, 1.000000000000000000, 0.9898214418809326842, 1.000000000000000000, 0.9898214418809326842, 1.000000000000000000, 0.9898214418809326842, 1.000000000000000000, 0.9898214418809326842, 1.000000000000000000, 0.9898214418809326842, 1.000000000000000000, 0.9898214418809326842, 1.000000000000000000, 0.9898214418809326842, 1.000000000000000000, 0.9898214418809326842, 1.000000000000000000, 0.9898214418809326842, 1.000000000000000000, 0.9898214418809326842, 1.000000000000000000, 0.9898214418809326842, 1.000000000000000000, 0.9898214418809326842, 1.000000000000000000, 0.9898214418809326842, 1.000000000000000000, 0.9898214418809326842, 1.000000000000000000, 0.9898214418809326842, 1.000000000000000000, 0.9898214418809326842, 1.000000000000000000, 0.9898214418809326842, 1.000000000000000000, 0.9898214418809326842, 1.000000000000000000, 0.9898214418809326842, 1.000000000000000000, 0.9898214418809326842, 1.000000000000000000, 0.9898214418809326842, 1.000000000000000000, 0.9898214418809326842, 1.000000000000000000, 0.9898214418809326842, 1.000000000000000000, 0.9898214418809326842, 1.000000000000000000, 0.9898214418809326842, 1.000000000000000000, 0.9898214418809326842, 1.000000000000000000, 0.9898214418809326842, 1.000000000000000000, 0.9898214418809326842, 1.000000000000000000, 0.9898214418809326842, 1.000000000000000000, 0.9898214418809326842, 1.000000000000000000, 0.9898214418809326842, 1.000000000000000000, 0.9898214418809326842, 1.000000000000000000, 0.9898214418809326842, 1.000000000000000000, 0.9898214418809326842, 1.000000000000000000, 0.9898214418809326842, 1.000000000000000000, 0.9898214418809326842, 1.000000000000000000, 0.9898214418809326842, 1.000000000000000000, 0.9898214418809326842, 1.000000000000000000, 0.9898214418809326842, 1.000000000000000000, 0.9898214418809326842, 1.000000000000000000, 0.9898214418809326842, 1.000000000000000000, 0.9898214418809326842, 1.000000000000000000, 0.9898214418809326842, 1.000000000000000000, 0.9898214418809326842, 1.000000000000000000, 0.9898214418809326842, 1.000000000000000000, 0.9898214418809326842, 1.000000000000000000, 0.9898214418809326842, 1.000000000000000000, 0.9898214418809326842, 1.000000000000000000, 0.9898214418809326842, 1.000000000000000000, 0.9898214418809326842, 1.000000000000000000, 0.9898214418809326842, 1.000000000000000000, 0.9898214418809326842, 1.000000000000000000, 0.9898214418809326842, 1.000000000000000000, 0.9898214418809326842, 1.000000000000000000, 0.9898214418809326842, 1.000000000000000000, 0.9898214418809326842, 1.000000000000000000, 0.9898214418809326842, 1.000000000000000000, 0.9898214418809326842, 1.000000000000000000, 0.9898214418809326842, 1.000000000000000000, 0.9898214418809326842, 1.000000000000000000, 0.9898214418809326842, 1.000000000000000000, 0.9898214418809326842, 1.000000000000000000, 0.9898214418809326842, 1.000000000000000000, 0.9898214418809326842, 1.000000000000000000, 0.9898214418809326842, 1.000000000000000000, 0.9898214418809326842, 1.000000000000000000, 0.9898214418809326842, 1.000000000000000000, 0.9898214418809326842, 1.000000000000000000, 0.9898214418809326842, 1.000000000000000000, 0.9898214418809326842, 1.000000000000000000, 0.9898214418809326842, 1.000000000000000000, 0.9898214418809326842, 1.000000000000000000, 0.9898214418809326842, 1.000000000000000000, 0.9898214418809326842, 1.000000000000000000, 0.9898214418809326842, 1.000000000000000000, 0.9898214418809326842, 1.000000000000000000, 0.9898214418809326842, 1.000000000000000000, 0.9898214418809326842, 1.000000000000000000, 0.9898214418809326842, 1.000000000000000000, 0.9898214418809326842, 1.000000000000000000, 0.9898214418809326842, 1.000000000000000000, 0.9898214418809326842, 1.000000000000000000, 0.9898214418809326842, 1.000000000000000000, 0.9898214418809326842, 1.000000000000000000, 0.9898214418809326842, 1.000000000000000000, 0.9898214418809326842, 1.000000000000000000, 0.9898214418809326842, 1.000000000000000000, 0.9898214418809326842, 1.000000000000000000, 0.9898214418809326842, 1.000000000000000000, 0.9898214418809326842, 1.000000000000000000, 0.9898214418809326842, 1.000000000000000000, 0.9898214418809326842, 1.000000000000000000, 0.9898214418809326842, 1.000000000000000000, 0.9898214418809326842, 1.000000000000000000, 0.9898214418809326842, 1.000000000000000000, 0.9898214418809326842, 1.000000000000000000, 0.9898214418809326842, 1.000000000000000000, 0.9898214418809326842, 1.000000000000000000, 0.9898214418809326842, 1.000000000000000000, 0.9898214418809326842, 1.000000000000000000, 0.9898214418809326842, 1.000000000000000000, 0.9898214418809326842, 1.000000000000000000, 0.9898214418809326842, 1.000000000000000000, 0.9898214418809326842, 1.000000000000000000, 0.9898214418809326842, 1.000000000000000000, 0.9898214418809326842, 1.000000000000000000, 0.9898214418809326842, 1.000000000000000000, 0.9898214418809326842, 1.000000000000000000, 0.9898214418809326842, 1.000000000000000000, 0.9898214418809326842, 1.000000000000000000, 0.9898214418809326842, 1.000000000000000000, 0.9898214418809326842, 1.000000000000000000, 0.9898214418809326842, 1.000000000000000000, 0.9898214418809326842, 1.000000000000000000, 0.9898214418809326842, 1.000000000000000000, 0.9898214418809326842, 1.000000000000000000, 0.9898214418809326842, 1.000000000000000000, 0.9898214418809326842, 1.000000000000000000, 0.9898214418809326842, 1.000000000000000000, 0.9898214418809326842, 1.000000000000000000, 0.9898214418809326842, 1.000000000000000000, 0.9898214418809326842, 1.000000000000000000, 0.9898214418809326842, 1.000000000000000000, 0.9898214418809326842, 1.000000000000000000, 0.9898214418809326842, 1.000000000000000000, 0.9898214418809326842, 1.000000000000000000, 0.9898214418809326842, 1.000000000000000000, 0.9898214418809326842, 1.000000000000000000, 0.9898214418809326842, 1.000000000000000000, 0.9898214418809326842, 1.000000000000000000, 0.9898214418809326842, 1.000000000000000000, 0.9898214418809326842, 1.000000000000000000, 0.9898214418809326842, 1.000000000000000000, 0.9898214418809326842, 1.000000000000000000, 0.9898214418809326842, 1.000000000000000000, 0.9898214418809326842, 1.000000000000000000, 0.9898214418809326842, 1.000000000000000000, 0.9898214418809326842, 1.000000000000000000, 0.9898214418809326842, 1.000000000000000000, 0.9898214418809326842, 1.000000000000000000, 0.9898214418809326842, 1.000000000000000000, 0.9898214418809326842, 1.000000000000000000, 0.9898214418809326842, 1.000000000000000000, 0.9898214418809326842, 1.000000000000000000, 0.9961809353924466759, 0.9952277490961531914),
 ( 0.3333333333333333703, 0.3299404806269776169, 0.3333333333333333703, 0.3299404806269776169, 0.3333333333333333703, 0.3299404806269776169, 0.3333333333333333703, 0.3299404806269776169, 0.3333333333333333703, 0.3299404806269776169, 0.3333333333333333703, 0.3299404806269776169, 0.3333333333333333703, 0.3299404806269776169, 0.3333333333333333703, 0.3299404806269776169, 0.3333333333333333703, 0.3299404806269776169, 0.3333333333333333703, 0.3299404806269776169, 0.3333333333333333703, 0.3299404806269776169, 0.3333333333333333703, 0.3299404806269776169, 0.3333333333333333703, 0.3299404806269776169, 0.3333333333333333703, 0.3299404806269776169, 0.3333333333333333703, 0.3299404806269776169, 0.3333333333333333703, 0.3299404806269776169, 0.3333333333333333703, 0.3299404806269776169, 0.3333333333333333703, 0.3299404806269776169, 0.3333333333333333703, 0.3299404806269776169, 0.3333333333333333703, 0.3299404806269776169, 0.3333333333333333703, 0.3299404806269776169, 0.3333333333333333703, 0.3299404806269776169, 0.3333333333333333703, 0.3299404806269776169, 0.3333333333333333703, 0.3299404806269776169, 0.3333333333333333703, 0.3299404806269776169, 0.3333333333333333703, 0.3299404806269776169, 0.3333333333333333703, 0.3299404806269776169, 0.3333333333333333703, 0.3299404806269776169, 0.3333333333333333703, 0.3299404806269776169, 0.3333333333333333703, 0.3299404806269776169, 0.3333333333333333703, 0.3299404806269776169, 0.3333333333333333703, 0.3299404806269776169, 0.3333333333333333703, 0.3299404806269776169, 0.3333333333333333703, 0.3299404806269776169, 0.3333333333333333703, 0.3299404806269776169, 0.3333333333333333703, 0.3299404806269776169, 0.3333333333333333703, 0.3299404806269776169, 0.3333333333333333703, 0.3299404806269776169, 0.3333333333333333703, 0.3299404806269776169, 0.3333333333333333703, 0.3299404806269776169, 0.3333333333333333703, 0.3299404806269776169, 0.3333333333333333703, 0.3299404806269776169, 0.3333333333333333703, 0.3299404806269776169, 0.3333333333333333703, 0.3299404806269776169, 0.3333333333333333703, 0.3299404806269776169, 0.3333333333333333703, 0.3299404806269776169, 0.3333333333333333703, 0.3299404806269776169, 0.3333333333333333703, 0.3299404806269776169, 0.3333333333333333703, 0.3299404806269776169, 0.3333333333333333703, 0.3299404806269776169, 0.3333333333333333703, 0.3299404806269776169, 0.3333333333333333703, 0.3299404806269776169, 0.3333333333333333703, 0.3299404806269776169, 0.3333333333333333703, 0.3299404806269776169, 0.3333333333333333703, 0.3299404806269776169, 0.3333333333333333703, 0.3299404806269776169, 0.3333333333333333703, 0.3299404806269776169, 0.3333333333333333703, 0.3299404806269776169, 0.3333333333333333703, 0.3299404806269776169, 0.3333333333333333703, 0.3299404806269776169, 0.3333333333333333703, 0.3299404806269776169, 0.3333333333333333703, 0.3299404806269776169, 0.3333333333333333703, 0.3299404806269776169, 0.3333333333333333703, 0.3299404806269776169, 0.3333333333333333703, 0.3299404806269776169, 0.3333333333333333703, 0.3299404806269776169, 0.3333333333333333703, 0.3299404806269776169, 0.3333333333333333703, 0.3299404806269776169, 0.3333333333333333703, 0.3299404806269776169, 0.3333333333333333703, 0.3299404806269776169, 0.3333333333333333703, 0.3299404806269776169, 0.3333333333333333703, 0.3299404806269776169, 0.3333333333333333703, 0.3299404806269776169, 0.3333333333333333703, 0.3299404806269776169, 0.3333333333333333703, 0.3299404806269776169, 0.3333333333333333703, 0.3299404806269776169, 0.3333333333333333703, 0.3299404806269776169, 0.3333333333333333703, 0.3299404806269776169, 0.3333333333333333703, 0.3299404806269776169, 0.3333333333333333703, 0.3299404806269776169, 0.3333333333333333703, 0.3299404806269776169, 0.3333333333333333703, 0.3299404806269776169, 0.3333333333333333703, 0.3299404806269776169, 0.3333333333333333703, 0.3299404806269776169, 0.3333333333333333703, 0.3299404806269776169, 0.3333333333333333703, 0.3299404806269776169, 0.3333333333333333703, 0.3299404806269776169, 0.3333333333333333703, 0.3299404806269776169, 0.3333333333333333703, 0.3299404806269776169, 0.3333333333333333703, 0.3299404806269776169, 0.3333333333333333703, 0.3299404806269776169, 0.3333333333333333703, 0.3299404806269776169, 0.3333333333333333703, 0.3299404806269776169, 0.3333333333333333703, 0.3299404806269776169, 0.3333333333333333703, 0.3299404806269776169, 0.3333333333333333703, 0.3299404806269776169, 0.3333333333333333703, 0.3299404806269776169, 0.3333333333333333703, 0.3299404806269776169, 0.3333333333333333703, 0.3299404806269776169, 0.3333333333333333703, 0.3299404806269776169, 0.3333333333333333703, 0.3299404806269776169, 0.3333333333333333703, 0.3299404806269776169, 0.3333333333333333703, 0.3299404806269776169, 0.3333333333333333703, 0.3299404806269776169, 0.3333333333333333703, 0.3299404806269776169, 0.3333333333333333703, 0.3299404806269776169, 0.3333333333333333703, 0.3299404806269776169, 0.3333333333333333703, 0.3299404806269776169, 0.3333333333333333703, 0.3299404806269776169, 0.3333333333333333703, 0.3299404806269776169, 0.3333333333333333703, 0.3299404806269776169, 0.3333333333333333703, 0.3299404806269776169, 0.3333333333333333703, 0.3299404806269776169, 0.3333333333333333703, 0.3299404806269776169, 0.3333333333333333703, 0.3299404806269776169, 0.3333333333333333703, 0.3299404806269776169, 0.3333333333333333703, 0.3299404806269776169, 0.3333333333333333703, 0.3299404806269776169, 0.3333333333333333703, 0.3299404806269776169, 0.3333333333333333703, 0.3299404806269776169, 0.3333333333333333703, 0.3299404806269776169, 0.3333333333333333703, 0.3299404806269776169, 0.3333333333333333703, 0.3299404806269776169, 0.3333333333333333703, 0.3299404806269776169, 0.3333333333333333703, 0.3299404806269776169, 0.3333333333333333703, 0.3299404806269776169, 0.3333333333333333703, 0.3299404806269776169, 0.3333333333333333703, 0.3299404806269776169, 0.3333333333333333703, 0.3299404806269776169, 0.3333333333333333703, 0.3299404806269776169, 0.3333333333333333703, 0.3299404806269776169, 0.3333333333333333703, 0.3299404806269776169, 0.3333333333333333703, 0.3299404806269776169, 0.3333333333333333703, 0.3299404806269776169, 0.3333333333333333703, 0.3299404806269776169, 0.3333333333333333703, 0.3299404806269776169, 0.3333333333333333703, 0.3299404806269776169, 0.3333333333333333703, 0.3299404806269776169, 0.3333333333333333703, 0.3299404806269776169, 0.3333333333333333703, 0.3299404806269776169, 0.3333333333333333703, 0.3299404806269776169, 0.3333333333333333703, 0.3299404806269776169, 0.3333333333333333703, 0.3299404806269776169, 0.3333333333333333703, 0.3299404806269776169, 0.3333333333333333703, 0.3299404806269776169, 0.3333333333333333703, 0.3299404806269776169, 0.3333333333333333703, 0.3299404806269776169, 0.3333333333333333703, 0.3299404806269776169, 0.3333333333333333703, 0.3299404806269776169, 0.3333333333333333703, 0.3299404806269776169, 0.3333333333333333703, 0.3299404806269776169, 0.3333333333333333703, 0.3299404806269776169, 0.3333333333333333703, 0.3299404806269776169, 0.3333333333333333703, 0.3299404806269776169, 0.3333333333333333703, 0.3299404806269776169, 0.3333333333333333703, 0.3299404806269776169, 0.3333333333333333703, 0.3299404806269776169, 0.3333333333333333703, 0.3299404806269776169, 0.3333333333333333703, 0.3299404806269776169, 0.3333333333333333703, 0.3299404806269776169, 0.3333333333333333703, 0.3299404806269776169, 0.3333333333333333703, 0.3299404806269776169, 0.3333333333333333703, 0.3299404806269776169, 0.3333333333333333703, 0.3299404806269776169, 0.3333333333333333703, 0.3299404806269776169, 0.3333333333333333703, 0.3299404806269776169, 0.3333333333333333703, 0.3299404806269776169, 0.3333333333333333703, 0.3299404806269776169, 0.3333333333333333703, 0.3299404806269776169, 0.3333333333333333703, 0.3299404806269776169, 0.3333333333333333703, 0.3299404806269776169, 0.3333333333333333703, 0.3299404806269776169, 0.3333333333333333703, 0.3299404806269776169, 0.3333333333333333703, 0.3299404806269776169, 0.3333333333333333703, 0.3299404806269776169, 0.3333333333333333703, 0.3299404806269776169, 0.3333333333333333703, 0.3299404806269776169, 0.3333333333333333703, 0.3299404806269776169, 0.3333333333333333703, 0.3299404806269776169, 0.3333333333333333703, 0.3299404806269776169, 0.3333333333333333703, 0.3299404806269776169, 0.3333333333333333703, 0.3299404806269776169, 0.3333333333333333703, 0.3299404806269776169, 0.3333333333333333703, 0.3299404806269776169, 0.3333333333333333703, 0.3299404806269776169, 0.3333333333333333703, 0.3299404806269776169, 0.3333333333333333703, 0.3299404806269776169, 0.3333333333333333703, 0.3299404806269776169, 0.3333333333333333703, 0.3299404806269776169, 0.3333333333333333703, 0.3299404806269776169, 0.3333333333333333703, 0.3299404806269776169, 0.3333333333333333703, 0.3299404806269776169, 0.3333333333333333703, 0.3299404806269776169, 0.3333333333333333703, 0.3299404806269776169, 0.3333333333333333703, 0.3299404806269776169, 0.3333333333333333703, 0.3299404806269776169, 0.3333333333333333703, 0.3299404806269776169, 0.3333333333333333703, 0.3299404806269776169, 0.3333333333333333703, 0.3299404806269776169, 0.3333333333333333703, 0.3299404806269776169, 0.3333333333333333703, 0.3299404806269776169, 0.3333333333333333703, 0.3299404806269776169, 0.3333333333333333703, 0.3299404806269776169, 0.3333333333333333703, 0.3299404806269776169, 0.3333333333333333703, 0.3299404806269776169, 0.3333333333333333703, 0.3299404806269776169, 0.3333333333333333703, 0.3299404806269776169, 0.3333333333333333703, 0.3299404806269776169, 0.3333333333333333703, 0.3299404806269776169, 0.3333333333333333703, 0.3299404806269776169, 0.3333333333333333703, 0.3299404806269776169, 0.3333333333333333703, 0.3299404806269776169, 0.3333333333333333703, 0.3299404806269776169, 0.3333333333333333703, 0.3299404806269776169, 0.3333333333333333703, 0.3299404806269776169, 0.3333333333333333703, 0.3299404806269776169, 0.3333333333333333703, 0.3299404806269776169, 0.3333333333333333703, 0.3299404806269776169, 0.3333333333333333703, 0.3299404806269776169, 0.3333333333333333703, 0.3299404806269776169, 0.3333333333333333703, 0.3299404806269776169, 0.3333333333333333703, 0.3299404806269776169, 0.3333333333333333703, 0.3299404806269776169, 0.3333333333333333703, 0.3299404806269776169, 0.3333333333333333703, 0.3299404806269776169, 0.3333333333333333703, 0.3299404806269776169, 0.3333333333333333703, 0.3299404806269776169, 0.3333333333333333703, 0.3299404806269776169, 0.3333333333333333703, 0.3299404806269776169, 0.3333333333333333703, 0.3299404806269776169, 0.3333333333333333703, 0.3299404806269776169, 0.3333333333333333703, 0.3299404806269776169, 0.3333333333333333703, 0.3299404806269776169, 0.3333333333333333703, 0.3299404806269776169, 0.3333333333333333703, 0.3299404806269776169, 0.3333333333333333703, 0.3299404806269776169, 0.3333333333333333703, 0.3299404806269776169, 0.3333333333333333703, 0.3299404806269776169, 0.3333333333333333703, 0.3299404806269776169, 0.3333333333333333703, 0.3299404806269776169, 0.3333333333333333703, 0.3299404806269776169, 0.3333333333333333703, 0.3299404806269776169, 0.3333333333333333703, 0.3299404806269776169, 0.3333333333333333703, 0.3299404806269776169, 0.3333333333333333703, 0.3299404806269776169, 0.3333333333333333703, 0.3299404806269776169, 0.3333333333333333703, 0.3299404806269776169, 0.3333333333333333703, 0.3299404806269776169, 0.3333333333333333703, 0.3299404806269776169, 0.3333333333333333703, 0.3299404806269776169, 0.3333333333333333703, 0.3299404806269776169, 0.3333333333333333703, 0.3299404806269776169, 0.3333333333333333703, 0.3299404806269776169, 0.3333333333333333703, 0.3299404806269776169, 0.3333333333333333703, 0.3299404806269776169, 0.3333333333333333703, 0.3299404806269776169, 0.3333333333333333703, 0.3299404806269776169, 0.3333333333333333703, 0.3299404806269776169, 0.3333333333333333703, 0.3299404806269776169, 0.3333333333333333703, 0.3299404806269776169, 0.3333333333333333703, 0.3299404806269776169, 0.3333333333333333703, 0.3299404806269776169, 0.3333333333333333703, 0.3299404806269776169, 0.3333333333333333703, 0.3299404806269776169, 0.3333333333333333703, 0.3299404806269776169, 0.3333333333333333703, 0.3299404806269776169, 0.3333333333333333703, 0.3299404806269776169, 0.3333333333333333703, 0.3299404806269776169, 0.3333333333333333703, 0.3299404806269776169, 0.3333333333333333703, 0.3299404806269776169, 0.3333333333333333703, 0.3299404806269776169, 0.3333333333333333703, 0.3299404806269776169, 0.3333333333333333703, 0.3299404806269776169, 0.3333333333333333703, 0.3299404806269776169, 0.3333333333333333703, 0.3299404806269776169, 0.3333333333333333703, 0.3299404806269776169, 0.3333333333333333703, 0.3299404806269776169, 0.3333333333333333703, 0.3299404806269776169, 0.3333333333333333703, 0.3299404806269776169, 0.3333333333333333703, 0.3299404806269776169, 0.3333333333333333703, 0.3299404806269776169, 0.3333333333333333703, 0.3299404806269776169, 0.3333333333333333703, 0.3299404806269776169, 0.3333333333333333703, 0.3299404806269776169, 0.3333333333333333703, 0.3299404806269776169, 0.3333333333333333703, 0.3299404806269776169, 0.3333333333333333703, 0.3299404806269776169, 0.3333333333333333703, 0.3299404806269776169, 0.3333333333333333703, 0.3299404806269776169, 0.3333333333333333703, 0.3299404806269776169, 0.3333333333333333703, 0.3299404806269776169, 0.3333333333333333703, 0.3299404806269776169, 0.3333333333333333703, 0.3299404806269776169, 0.3333333333333333703, 0.3299404806269776169, 0.3333333333333333703, 0.3299404806269776169, 0.3333333333333333703, 0.3299404806269776169, 0.3333333333333333703, 0.3299404806269776169, 0.3333333333333333703, 0.3299404806269776169, 0.3333333333333333703, 0.3299404806269776169, 0.3333333333333333703, 0.3299404806269776169, 0.3333333333333333703, 0.3299404806269776169, 0.3333333333333333703, 0.3299404806269776169, 0.3333333333333333703, 0.3299404806269776169, 0.3333333333333333703, 0.3299404806269776169, 0.3333333333333333703, 0.3299404806269776169, 0.3333333333333333703, 0.3299404806269776169, 0.3333333333333333703, 0.3299404806269776169, 0.3333333333333333703, 0.3299404806269776169, 0.3333333333333333703, 0.3299404806269776169, 0.3333333333333333703, 0.3299404806269776169, 0.3333333333333333703, 0.3299404806269776169, 0.3333333333333333703, 0.3299404806269776169, 0.3333333333333333703, 0.3299404806269776169, 0.3333333333333333703, 0.3299404806269776169, 0.3333333333333333703, 0.3299404806269776169, 0.3333333333333333703, 0.3299404806269776169, 0.3333333333333333703, 0.3299404806269776169, 0.3333333333333333703, 0.3299404806269776169, 0.3333333333333333703, 0.3299404806269776169, 0.3333333333333333703, 0.3299404806269776169, 0.3333333333333333703, 0.3299404806269776169, 0.3333333333333333703, 0.3299404806269776169, 0.3333333333333333703, 0.3299404806269776169, 0.3333333333333333703, 0.3299404806269776169, 0.3333333333333333703, 0.3299404806269776169, 0.3333333333333333703, 0.3299404806269776169, 0.3333333333333333703, 0.3299404806269776169, 0.3333333333333333703, 0.3299404806269776169, 0.3333333333333333703, 0.3299404806269776169, 0.3333333333333333703, 0.3299404806269776169, 0.3333333333333333703, 0.3299404806269776169, 0.3333333333333333703, 0.3299404806269776169, 0.3333333333333333703, 0.3299404806269776169, 0.3333333333333333703, 0.3299404806269776169, 0.3333333333333333703, 0.3299404806269776169, 0.3333333333333333703, 0.3299404806269776169, 0.3333333333333333703, 0.3299404806269776169, 0.3333333333333333703, 0.3299404806269776169, 0.3333333333333333703, 0.3299404806269776169, 0.3333333333333333703, 0.3299404806269776169, 0.3333333333333333703, 0.3299404806269776169, 0.3333333333333333703, 0.3299404806269776169, 0.3333333333333333703, 0.3299404806269776169, 0.3333333333333333703, 0.3299404806269776169, 0.3333333333333333703, 0.3299404806269776169, 0.3333333333333333703, 0.3299404806269776169, 0.3333333333333333703, 0.3299404806269776169, 0.3333333333333333703, 0.3299404806269776169, 0.3333333333333333703, 0.3299404806269776169, 0.3333333333333333703, 0.3299404806269776169, 0.3333333333333333703, 0.3299404806269776169, 0.3333333333333333703, 0.3299404806269776169, 0.3333333333333333703, 0.3299404806269776169, 0.3333333333333333703, 0.3299404806269776169, 0.3333333333333333703, 0.3299404806269776169, 0.3333333333333333703, 0.3299404806269776169, 0.3333333333333333703, 0.3299404806269776169, 0.3333333333333333703, 0.3299404806269776169, 0.3333333333333333703, 0.3299404806269776169, 0.3333333333333333703, 0.3299404806269776169, 0.3333333333333333703, 0.3299404806269776169, 0.3333333333333333703, 0.3299404806269776169, 0.3333333333333333703, 0.3299404806269776169, 0.3333333333333333703, 0.3299404806269776169, 0.3333333333333333703, 0.3299404806269776169, 0.3333333333333333703, 0.3299404806269776169, 0.3333333333333333703, 0.3299404806269776169, 0.3333333333333333703, 0.3299404806269776169, 0.3333333333333333703, 0.3299404806269776169, 0.3333333333333333703, 0.3299404806269776169, 0.3333333333333333703, 0.3299404806269776169, 0.3333333333333333703, 0.3299404806269776169, 0.3333333333333333703, 0.3299404806269776169, 0.3333333333333333703, 0.3299404806269776169, 0.3333333333333333703, 0.3299404806269776169, 0.3333333333333333703, 0.3299404806269776169, 0.3333333333333333703, 0.3299404806269776169, 0.3333333333333333703, 0.3299404806269776169, 0.3333333333333333703, 0.3299404806269776169, 0.3333333333333333703, 0.3299404806269776169, 0.3333333333333333703, 0.3299404806269776169, 0.3333333333333333703, 0.3299404806269776169, 0.3333333333333333703, 0.3299404806269776169, 0.3333333333333333703, 0.3299404806269776169, 0.3333333333333333703, 0.3299404806269776169, 0.3333333333333333703, 0.3299404806269776169, 0.3333333333333333703, 0.3299404806269776169, 0.3333333333333333703, 0.3299404806269776169, 0.3333333333333333703, 0.3299404806269776169, 0.3333333333333333703, 0.3299404806269776169, 0.3333333333333333703, 0.3299404806269776169, 0.3333333333333333703, 0.3299404806269776169, 0.3333333333333333703, 0.3299404806269776169, 0.3333333333333333703, 0.3299404806269776169, 0.3333333333333333703, 0.3299404806269776169, 0.3333333333333333703, 0.3299404806269776169, 0.3333333333333333703, 0.3299404806269776169, 0.3333333333333333703, 0.3299404806269776169, 0.3333333333333333703, 0.3299404806269776169, 0.3333333333333333703, 0.3299404806269776169, 0.3333333333333333703, 0.3299404806269776169, 0.3333333333333333703, 0.3299404806269776169, 0.3333333333333333703, 0.3299404806269776169, 0.3333333333333333703, 0.3299404806269776169, 0.3333333333333333703, 0.3299404806269776169, 0.3333333333333333703, 0.3299404806269776169, 0.3333333333333333703, 0.3299404806269776169, 0.3333333333333333703, 0.3299404806269776169, 0.3333333333333333703, 0.3299404806269776169, 0.3333333333333333703, 0.3299404806269776169, 0.3333333333333333703, 0.3299404806269776169, 0.3333333333333333703, 0.3299404806269776169, 0.3333333333333333703, 0.3299404806269776169, 0.3333333333333333703, 0.3299404806269776169, 0.3333333333333333703, 0.3299404806269776169, 0.3333333333333333703, 0.3299404806269776169, 0.3333333333333333703, 0.3299404806269776169, 0.3333333333333333703, 0.3299404806269776169, 0.3333333333333333703, 0.3299404806269776169, 0.3333333333333333703, 0.3299404806269776169, 0.3333333333333333703, 0.3299404806269776169, 0.3333333333333333703, 0.3299404806269776169, 0.3333333333333333703, 0.3299404806269776169, 0.3333333333333333703, 0.3299404806269776169, 0.3333333333333333703, 0.3299404806269776169, 0.3333333333333333703, 0.3299404806269776169, 0.3333333333333333703, 0.3299404806269776169, 0.3333333333333333703, 0.3299404806269776169, 0.3333333333333333703, 0.3299404806269776169, 0.3333333333333333703, 0.3299404806269776169, 0.3333333333333333703, 0.3320603117974822438, 0.3317425830320511193),
 ( 0.3333333333333333703, 0.3299404806269776169, 0.3333333333333333703, 0.3299404806269776169, 0.3333333333333333703, 0.3299404806269776169, 0.3333333333333333703, 0.3299404806269776169, 0.3333333333333333703, 0.3299404806269776169, 0.3333333333333333703, 0.3299404806269776169, 0.3333333333333333703, 0.3299404806269776169, 0.3333333333333333703, 0.3299404806269776169, 0.3333333333333333703, 0.3299404806269776169, 0.3333333333333333703, 0.3299404806269776169, 0.3333333333333333703, 0.3299404806269776169, 0.3333333333333333703, 0.3299404806269776169, 0.3333333333333333703, 0.3299404806269776169, 0.3333333333333333703, 0.3299404806269776169, 0.3333333333333333703, 0.3299404806269776169, 0.3333333333333333703, 0.3299404806269776169, 0.3333333333333333703, 0.3299404806269776169, 0.3333333333333333703, 0.3299404806269776169, 0.3333333333333333703, 0.3299404806269776169, 0.3333333333333333703, 0.3299404806269776169, 0.3333333333333333703, 0.3299404806269776169, 0.3333333333333333703, 0.3299404806269776169, 0.3333333333333333703, 0.3299404806269776169, 0.3333333333333333703, 0.3299404806269776169, 0.3333333333333333703, 0.3299404806269776169, 0.3333333333333333703, 0.3299404806269776169, 0.3333333333333333703, 0.3299404806269776169, 0.3333333333333333703, 0.3299404806269776169, 0.3333333333333333703, 0.3299404806269776169, 0.3333333333333333703, 0.3299404806269776169, 0.3333333333333333703, 0.3299404806269776169, 0.3333333333333333703, 0.3299404806269776169, 0.3333333333333333703, 0.3299404806269776169, 0.3333333333333333703, 0.3299404806269776169, 0.3333333333333333703, 0.3299404806269776169, 0.3333333333333333703, 0.3299404806269776169, 0.3333333333333333703, 0.3299404806269776169, 0.3333333333333333703, 0.3299404806269776169, 0.3333333333333333703, 0.3299404806269776169, 0.3333333333333333703, 0.3299404806269776169, 0.3333333333333333703, 0.3299404806269776169, 0.3333333333333333703, 0.3299404806269776169, 0.3333333333333333703, 0.3299404806269776169, 0.3333333333333333703, 0.3299404806269776169, 0.3333333333333333703, 0.3299404806269776169, 0.3333333333333333703, 0.3299404806269776169, 0.3333333333333333703, 0.3299404806269776169, 0.3333333333333333703, 0.3299404806269776169, 0.3333333333333333703, 0.3299404806269776169, 0.3333333333333333703, 0.3299404806269776169, 0.3333333333333333703, 0.3299404806269776169, 0.3333333333333333703, 0.3299404806269776169, 0.3333333333333333703, 0.3299404806269776169, 0.3333333333333333703, 0.3299404806269776169, 0.3333333333333333703, 0.3299404806269776169, 0.3333333333333333703, 0.3299404806269776169, 0.3333333333333333703, 0.3299404806269776169, 0.3333333333333333703, 0.3299404806269776169, 0.3333333333333333703, 0.3299404806269776169, 0.3333333333333333703, 0.3299404806269776169, 0.3333333333333333703, 0.3299404806269776169, 0.3333333333333333703, 0.3299404806269776169, 0.3333333333333333703, 0.3299404806269776169, 0.3333333333333333703, 0.3299404806269776169, 0.3333333333333333703, 0.3299404806269776169, 0.3333333333333333703, 0.3299404806269776169, 0.3333333333333333703, 0.3299404806269776169, 0.3333333333333333703, 0.3299404806269776169, 0.3333333333333333703, 0.3299404806269776169, 0.3333333333333333703, 0.3299404806269776169, 0.3333333333333333703, 0.3299404806269776169, 0.3333333333333333703, 0.3299404806269776169, 0.3333333333333333703, 0.3299404806269776169, 0.3333333333333333703, 0.3299404806269776169, 0.3333333333333333703, 0.3299404806269776169, 0.3333333333333333703, 0.3299404806269776169, 0.3333333333333333703, 0.3299404806269776169, 0.3333333333333333703, 0.3299404806269776169, 0.3333333333333333703, 0.3299404806269776169, 0.3333333333333333703, 0.3299404806269776169, 0.3333333333333333703, 0.3299404806269776169, 0.3333333333333333703, 0.3299404806269776169, 0.3333333333333333703, 0.3299404806269776169, 0.3333333333333333703, 0.3299404806269776169, 0.3333333333333333703, 0.3299404806269776169, 0.3333333333333333703, 0.3299404806269776169, 0.3333333333333333703, 0.3299404806269776169, 0.3333333333333333703, 0.3299404806269776169, 0.3333333333333333703, 0.3299404806269776169, 0.3333333333333333703, 0.3299404806269776169, 0.3333333333333333703, 0.3299404806269776169, 0.3333333333333333703, 0.3299404806269776169, 0.3333333333333333703, 0.3299404806269776169, 0.3333333333333333703, 0.3299404806269776169, 0.3333333333333333703, 0.3299404806269776169, 0.3333333333333333703, 0.3299404806269776169, 0.3333333333333333703, 0.3299404806269776169, 0.3333333333333333703, 0.3299404806269776169, 0.3333333333333333703, 0.3299404806269776169, 0.3333333333333333703, 0.3299404806269776169, 0.3333333333333333703, 0.3299404806269776169, 0.3333333333333333703, 0.3299404806269776169, 0.3333333333333333703, 0.3299404806269776169, 0.3333333333333333703, 0.3299404806269776169, 0.3333333333333333703, 0.3299404806269776169, 0.3333333333333333703, 0.3299404806269776169, 0.3333333333333333703, 0.3299404806269776169, 0.3333333333333333703, 0.3299404806269776169, 0.3333333333333333703, 0.3299404806269776169, 0.3333333333333333703, 0.3299404806269776169, 0.3333333333333333703, 0.3299404806269776169, 0.3333333333333333703, 0.3299404806269776169, 0.3333333333333333703, 0.3299404806269776169, 0.3333333333333333703, 0.3299404806269776169, 0.3333333333333333703, 0.3299404806269776169, 0.3333333333333333703, 0.3299404806269776169, 0.3333333333333333703, 0.3299404806269776169, 0.3333333333333333703, 0.3299404806269776169, 0.3333333333333333703, 0.3299404806269776169, 0.3333333333333333703, 0.3299404806269776169, 0.3333333333333333703, 0.3299404806269776169, 0.3333333333333333703, 0.3299404806269776169, 0.3333333333333333703, 0.3299404806269776169, 0.3333333333333333703, 0.3299404806269776169, 0.3333333333333333703, 0.3299404806269776169, 0.3333333333333333703, 0.3299404806269776169, 0.3333333333333333703, 0.3299404806269776169, 0.3333333333333333703, 0.3299404806269776169, 0.3333333333333333703, 0.3299404806269776169, 0.3333333333333333703, 0.3299404806269776169, 0.3333333333333333703, 0.3299404806269776169, 0.3333333333333333703, 0.3299404806269776169, 0.3333333333333333703, 0.3299404806269776169, 0.3333333333333333703, 0.3299404806269776169, 0.3333333333333333703, 0.3299404806269776169, 0.3333333333333333703, 0.3299404806269776169, 0.3333333333333333703, 0.3299404806269776169, 0.3333333333333333703, 0.3299404806269776169, 0.3333333333333333703, 0.3299404806269776169, 0.3333333333333333703, 0.3299404806269776169, 0.3333333333333333703, 0.3299404806269776169, 0.3333333333333333703, 0.3299404806269776169, 0.3333333333333333703, 0.3299404806269776169, 0.3333333333333333703, 0.3299404806269776169, 0.3333333333333333703, 0.3299404806269776169, 0.3333333333333333703, 0.3299404806269776169, 0.3333333333333333703, 0.3299404806269776169, 0.3333333333333333703, 0.3299404806269776169, 0.3333333333333333703, 0.3299404806269776169, 0.3333333333333333703, 0.3299404806269776169, 0.3333333333333333703, 0.3299404806269776169, 0.3333333333333333703, 0.3299404806269776169, 0.3333333333333333703, 0.3299404806269776169, 0.3333333333333333703, 0.3299404806269776169, 0.3333333333333333703, 0.3299404806269776169, 0.3333333333333333703, 0.3299404806269776169, 0.3333333333333333703, 0.3299404806269776169, 0.3333333333333333703, 0.3299404806269776169, 0.3333333333333333703, 0.3299404806269776169, 0.3333333333333333703, 0.3299404806269776169, 0.3333333333333333703, 0.3299404806269776169, 0.3333333333333333703, 0.3299404806269776169, 0.3333333333333333703, 0.3299404806269776169, 0.3333333333333333703, 0.3299404806269776169, 0.3333333333333333703, 0.3299404806269776169, 0.3333333333333333703, 0.3299404806269776169, 0.3333333333333333703, 0.3299404806269776169, 0.3333333333333333703, 0.3299404806269776169, 0.3333333333333333703, 0.3299404806269776169, 0.3333333333333333703, 0.3299404806269776169, 0.3333333333333333703, 0.3299404806269776169, 0.3333333333333333703, 0.3299404806269776169, 0.3333333333333333703, 0.3299404806269776169, 0.3333333333333333703, 0.3299404806269776169, 0.3333333333333333703, 0.3299404806269776169, 0.3333333333333333703, 0.3299404806269776169, 0.3333333333333333703, 0.3299404806269776169, 0.3333333333333333703, 0.3299404806269776169, 0.3333333333333333703, 0.3299404806269776169, 0.3333333333333333703, 0.3299404806269776169, 0.3333333333333333703, 0.3299404806269776169, 0.3333333333333333703, 0.3299404806269776169, 0.3333333333333333703, 0.3299404806269776169, 0.3333333333333333703, 0.3299404806269776169, 0.3333333333333333703, 0.3299404806269776169, 0.3333333333333333703, 0.3299404806269776169, 0.3333333333333333703, 0.3299404806269776169, 0.3333333333333333703, 0.3299404806269776169, 0.3333333333333333703, 0.3299404806269776169, 0.3333333333333333703, 0.3299404806269776169, 0.3333333333333333703, 0.3299404806269776169, 0.3333333333333333703, 0.3299404806269776169, 0.3333333333333333703, 0.3299404806269776169, 0.3333333333333333703, 0.3299404806269776169, 0.3333333333333333703, 0.3299404806269776169, 0.3333333333333333703, 0.3299404806269776169, 0.3333333333333333703, 0.3299404806269776169, 0.3333333333333333703, 0.3299404806269776169, 0.3333333333333333703, 0.3299404806269776169, 0.3333333333333333703, 0.3299404806269776169, 0.3333333333333333703, 0.3299404806269776169, 0.3333333333333333703, 0.3299404806269776169, 0.3333333333333333703, 0.3299404806269776169, 0.3333333333333333703, 0.3299404806269776169, 0.3333333333333333703, 0.3299404806269776169, 0.3333333333333333703, 0.3299404806269776169, 0.3333333333333333703, 0.3299404806269776169, 0.3333333333333333703, 0.3299404806269776169, 0.3333333333333333703, 0.3299404806269776169, 0.3333333333333333703, 0.3299404806269776169, 0.3333333333333333703, 0.3299404806269776169, 0.3333333333333333703, 0.3299404806269776169, 0.3333333333333333703, 0.3299404806269776169, 0.3333333333333333703, 0.3299404806269776169, 0.3333333333333333703, 0.3299404806269776169, 0.3333333333333333703, 0.3299404806269776169, 0.3333333333333333703, 0.3299404806269776169, 0.3333333333333333703, 0.3299404806269776169, 0.3333333333333333703, 0.3299404806269776169, 0.3333333333333333703, 0.3299404806269776169, 0.3333333333333333703, 0.3299404806269776169, 0.3333333333333333703, 0.3299404806269776169, 0.3333333333333333703, 0.3299404806269776169, 0.3333333333333333703, 0.3299404806269776169, 0.3333333333333333703, 0.3299404806269776169, 0.3333333333333333703, 0.3299404806269776169, 0.3333333333333333703, 0.3299404806269776169, 0.3333333333333333703, 0.3299404806269776169, 0.3333333333333333703, 0.3299404806269776169, 0.3333333333333333703, 0.3299404806269776169, 0.3333333333333333703, 0.3299404806269776169, 0.3333333333333333703, 0.3299404806269776169, 0.3333333333333333703, 0.3299404806269776169, 0.3333333333333333703, 0.3299404806269776169, 0.3333333333333333703, 0.3299404806269776169, 0.3333333333333333703, 0.3299404806269776169, 0.3333333333333333703, 0.3299404806269776169, 0.3333333333333333703, 0.3299404806269776169, 0.3333333333333333703, 0.3299404806269776169, 0.3333333333333333703, 0.3299404806269776169, 0.3333333333333333703, 0.3299404806269776169, 0.3333333333333333703, 0.3299404806269776169, 0.3333333333333333703, 0.3299404806269776169, 0.3333333333333333703, 0.3299404806269776169, 0.3333333333333333703, 0.3299404806269776169, 0.3333333333333333703, 0.3299404806269776169, 0.3333333333333333703, 0.3299404806269776169, 0.3333333333333333703, 0.3299404806269776169, 0.3333333333333333703, 0.3299404806269776169, 0.3333333333333333703, 0.3299404806269776169, 0.3333333333333333703, 0.3299404806269776169, 0.3333333333333333703, 0.3299404806269776169, 0.3333333333333333703, 0.3299404806269776169, 0.3333333333333333703, 0.3299404806269776169, 0.3333333333333333703, 0.3299404806269776169, 0.3333333333333333703, 0.3299404806269776169, 0.3333333333333333703, 0.3299404806269776169, 0.3333333333333333703, 0.3299404806269776169, 0.3333333333333333703, 0.3299404806269776169, 0.3333333333333333703, 0.3299404806269776169, 0.3333333333333333703, 0.3299404806269776169, 0.3333333333333333703, 0.3299404806269776169, 0.3333333333333333703, 0.3299404806269776169, 0.3333333333333333703, 0.3299404806269776169, 0.3333333333333333703, 0.3299404806269776169, 0.3333333333333333703, 0.3299404806269776169, 0.3333333333333333703, 0.3299404806269776169, 0.3333333333333333703, 0.3299404806269776169, 0.3333333333333333703, 0.3299404806269776169, 0.3333333333333333703, 0.3299404806269776169, 0.3333333333333333703, 0.3299404806269776169, 0.3333333333333333703, 0.3299404806269776169, 0.3333333333333333703, 0.3299404806269776169, 0.3333333333333333703, 0.3299404806269776169, 0.3333333333333333703, 0.3299404806269776169, 0.3333333333333333703, 0.3299404806269776169, 0.3333333333333333703, 0.3299404806269776169, 0.3333333333333333703, 0.3299404806269776169, 0.3333333333333333703, 0.3299404806269776169, 0.3333333333333333703, 0.3299404806269776169, 0.3333333333333333703, 0.3299404806269776169, 0.3333333333333333703, 0.3299404806269776169, 0.3333333333333333703, 0.3299404806269776169, 0.3333333333333333703, 0.3299404806269776169, 0.3333333333333333703, 0.3299404806269776169, 0.3333333333333333703, 0.3299404806269776169, 0.3333333333333333703, 0.3299404806269776169, 0.3333333333333333703, 0.3299404806269776169, 0.3333333333333333703, 0.3299404806269776169, 0.3333333333333333703, 0.3299404806269776169, 0.3333333333333333703, 0.3299404806269776169, 0.3333333333333333703, 0.3299404806269776169, 0.3333333333333333703, 0.3299404806269776169, 0.3333333333333333703, 0.3299404806269776169, 0.3333333333333333703, 0.3299404806269776169, 0.3333333333333333703, 0.3299404806269776169, 0.3333333333333333703, 0.3299404806269776169, 0.3333333333333333703, 0.3299404806269776169, 0.3333333333333333703, 0.3299404806269776169, 0.3333333333333333703, 0.3299404806269776169, 0.3333333333333333703, 0.3299404806269776169, 0.3333333333333333703, 0.3299404806269776169, 0.3333333333333333703, 0.3299404806269776169, 0.3333333333333333703, 0.3299404806269776169, 0.3333333333333333703, 0.3299404806269776169, 0.3333333333333333703, 0.3299404806269776169, 0.3333333333333333703, 0.3299404806269776169, 0.3333333333333333703, 0.3299404806269776169, 0.3333333333333333703, 0.3299404806269776169, 0.3333333333333333703, 0.3299404806269776169, 0.3333333333333333703, 0.3299404806269776169, 0.3333333333333333703, 0.3299404806269776169, 0.3333333333333333703, 0.3299404806269776169, 0.3333333333333333703, 0.3299404806269776169, 0.3333333333333333703, 0.3299404806269776169, 0.3333333333333333703, 0.3299404806269776169, 0.3333333333333333703, 0.3299404806269776169, 0.3333333333333333703, 0.3299404806269776169, 0.3333333333333333703, 0.3299404806269776169, 0.3333333333333333703, 0.3299404806269776169, 0.3333333333333333703, 0.3299404806269776169, 0.3333333333333333703, 0.3299404806269776169, 0.3333333333333333703, 0.3299404806269776169, 0.3333333333333333703, 0.3299404806269776169, 0.3333333333333333703, 0.3299404806269776169, 0.3333333333333333703, 0.3299404806269776169, 0.3333333333333333703, 0.3299404806269776169, 0.3333333333333333703, 0.3299404806269776169, 0.3333333333333333703, 0.3299404806269776169, 0.3333333333333333703, 0.3299404806269776169, 0.3333333333333333703, 0.3299404806269776169, 0.3333333333333333703, 0.3299404806269776169, 0.3333333333333333703, 0.3299404806269776169, 0.3333333333333333703, 0.3299404806269776169, 0.3333333333333333703, 0.3299404806269776169, 0.3333333333333333703, 0.3299404806269776169, 0.3333333333333333703, 0.3299404806269776169, 0.3333333333333333703, 0.3299404806269776169, 0.3333333333333333703, 0.3299404806269776169, 0.3333333333333333703, 0.3299404806269776169, 0.3333333333333333703, 0.3299404806269776169, 0.3333333333333333703, 0.3299404806269776169, 0.3333333333333333703, 0.3299404806269776169, 0.3333333333333333703, 0.3299404806269776169, 0.3333333333333333703, 0.3299404806269776169, 0.3333333333333333703, 0.3299404806269776169, 0.3333333333333333703, 0.3299404806269776169, 0.3333333333333333703, 0.3299404806269776169, 0.3333333333333333703, 0.3299404806269776169, 0.3333333333333333703, 0.3299404806269776169, 0.3333333333333333703, 0.3299404806269776169, 0.3333333333333333703, 0.3299404806269776169, 0.3333333333333333703, 0.3299404806269776169, 0.3333333333333333703, 0.3299404806269776169, 0.3333333333333333703, 0.3299404806269776169, 0.3333333333333333703, 0.3299404806269776169, 0.3333333333333333703, 0.3299404806269776169, 0.3333333333333333703, 0.3299404806269776169, 0.3333333333333333703, 0.3299404806269776169, 0.3333333333333333703, 0.3299404806269776169, 0.3333333333333333703, 0.3299404806269776169, 0.3333333333333333703, 0.3299404806269776169, 0.3333333333333333703, 0.3299404806269776169, 0.3333333333333333703, 0.3299404806269776169, 0.3333333333333333703, 0.3299404806269776169, 0.3333333333333333703, 0.3299404806269776169, 0.3333333333333333703, 0.3299404806269776169, 0.3333333333333333703, 0.3299404806269776169, 0.3333333333333333703, 0.3299404806269776169, 0.3333333333333333703, 0.3299404806269776169, 0.3333333333333333703, 0.3299404806269776169, 0.3333333333333333703, 0.3299404806269776169, 0.3333333333333333703, 0.3299404806269776169, 0.3333333333333333703, 0.3299404806269776169, 0.3333333333333333703, 0.3299404806269776169, 0.3333333333333333703, 0.3299404806269776169, 0.3333333333333333703, 0.3299404806269776169, 0.3333333333333333703, 0.3299404806269776169, 0.3333333333333333703, 0.3299404806269776169, 0.3333333333333333703, 0.3299404806269776169, 0.3333333333333333703, 0.3299404806269776169, 0.3333333333333333703, 0.3299404806269776169, 0.3333333333333333703, 0.3299404806269776169, 0.3333333333333333703, 0.3299404806269776169, 0.3333333333333333703, 0.3299404806269776169, 0.3333333333333333703, 0.3299404806269776169, 0.3333333333333333703, 0.3299404806269776169, 0.3333333333333333703, 0.3299404806269776169, 0.3333333333333333703, 0.3299404806269776169, 0.3333333333333333703, 0.3299404806269776169, 0.3333333333333333703, 0.3299404806269776169, 0.3333333333333333703, 0.3299404806269776169, 0.3333333333333333703, 0.3299404806269776169, 0.3333333333333333703, 0.3299404806269776169, 0.3333333333333333703, 0.3299404806269776169, 0.3333333333333333703, 0.3299404806269776169, 0.3333333333333333703, 0.3299404806269776169, 0.3333333333333333703, 0.3299404806269776169, 0.3333333333333333703, 0.3299404806269776169, 0.3333333333333333703, 0.3299404806269776169, 0.3333333333333333703, 0.3299404806269776169, 0.3333333333333333703, 0.3299404806269776169, 0.3333333333333333703, 0.3299404806269776169, 0.3333333333333333703, 0.3299404806269776169, 0.3333333333333333703, 0.3299404806269776169, 0.3333333333333333703, 0.3299404806269776169, 0.3333333333333333703, 0.3299404806269776169, 0.3333333333333333703, 0.3299404806269776169, 0.3333333333333333703, 0.3299404806269776169, 0.3333333333333333703, 0.3299404806269776169, 0.3333333333333333703, 0.3299404806269776169, 0.3333333333333333703, 0.3299404806269776169, 0.3333333333333333703, 0.3299404806269776169, 0.3333333333333333703, 0.3299404806269776169, 0.3333333333333333703, 0.3299404806269776169, 0.3333333333333333703, 0.3299404806269776169, 0.3333333333333333703, 0.3299404806269776169, 0.3333333333333333703, 0.3299404806269776169, 0.3333333333333333703, 0.3299404806269776169, 0.3333333333333333703, 0.3299404806269776169, 0.3333333333333333703, 0.3299404806269776169, 0.3333333333333333703, 0.3299404806269776169, 0.3333333333333333703, 0.3299404806269776169, 0.3333333333333333703, 0.3299404806269776169, 0.3333333333333333703, 0.3299404806269776169, 0.3333333333333333703, 0.3299404806269776169, 0.3333333333333333703, 0.3299404806269776169, 0.3333333333333333703, 0.3299404806269776169, 0.3333333333333333703, 0.3299404806269776169, 0.3333333333333333703, 0.3299404806269776169, 0.3333333333333333703, 0.3320603117974822438, 0.3317425830320511193),
 ( 1.000000000000000000, 0.9898214418809326842, 1.000000000000000000, 0.9898214418809326842, 1.000000000000000000, 0.9898214418809326842, 1.000000000000000000, 0.9898214418809326842, 1.000000000000000000, 0.9898214418809326842, 1.000000000000000000, 0.9898214418809326842, 1.000000000000000000, 0.9898214418809326842, 1.000000000000000000, 0.9898214418809326842, 1.000000000000000000, 0.9898214418809326842, 1.000000000000000000, 0.9898214418809326842, 1.000000000000000000, 0.9898214418809326842, 1.000000000000000000, 0.9898214418809326842, 1.000000000000000000, 0.9898214418809326842, 1.000000000000000000, 0.9898214418809326842, 1.000000000000000000, 0.9898214418809326842, 1.000000000000000000, 0.9898214418809326842, 1.000000000000000000, 0.9898214418809326842, 1.000000000000000000, 0.9898214418809326842, 1.000000000000000000, 0.9898214418809326842, 1.000000000000000000, 0.9898214418809326842, 1.000000000000000000, 0.9898214418809326842, 1.000000000000000000, 0.9898214418809326842, 1.000000000000000000, 0.9898214418809326842, 1.000000000000000000, 0.9898214418809326842, 1.000000000000000000, 0.9898214418809326842, 1.000000000000000000, 0.9898214418809326842, 1.000000000000000000, 0.9898214418809326842, 1.000000000000000000, 0.9898214418809326842, 1.000000000000000000, 0.9898214418809326842, 1.000000000000000000, 0.9898214418809326842, 1.000000000000000000, 0.9898214418809326842, 1.000000000000000000, 0.9898214418809326842, 1.000000000000000000, 0.9898214418809326842, 1.000000000000000000, 0.9898214418809326842, 1.000000000000000000, 0.9898214418809326842, 1.000000000000000000, 0.9898214418809326842, 1.000000000000000000, 0.9898214418809326842, 1.000000000000000000, 0.9898214418809326842, 1.000000000000000000, 0.9898214418809326842, 1.000000000000000000, 0.9898214418809326842, 1.000000000000000000, 0.9898214418809326842, 1.000000000000000000, 0.9898214418809326842, 1.000000000000000000, 0.9898214418809326842, 1.000000000000000000, 0.9898214418809326842, 1.000000000000000000, 0.9898214418809326842, 1.000000000000000000, 0.9898214418809326842, 1.000000000000000000, 0.9898214418809326842, 1.000000000000000000, 0.9898214418809326842, 1.000000000000000000, 0.9898214418809326842, 1.000000000000000000, 0.9898214418809326842, 1.000000000000000000, 0.9898214418809326842, 1.000000000000000000, 0.9898214418809326842, 1.000000000000000000, 0.9898214418809326842, 1.000000000000000000, 0.9898214418809326842, 1.000000000000000000, 0.9898214418809326842, 1.000000000000000000, 0.9898214418809326842, 1.000000000000000000, 0.9898214418809326842, 1.000000000000000000, 0.9898214418809326842, 1.000000000000000000, 0.9898214418809326842, 1.000000000000000000, 0.9898214418809326842, 1.000000000000000000, 0.9898214418809326842, 1.000000000000000000, 0.9898214418809326842, 1.000000000000000000, 0.9898214418809326842, 1.000000000000000000, 0.9898214418809326842, 1.000000000000000000, 0.9898214418809326842, 1.000000000000000000, 0.9898214418809326842, 1.000000000000000000, 0.9898214418809326842, 1.000000000000000000, 0.9898214418809326842, 1.000000000000000000, 0.9898214418809326842, 1.000000000000000000, 0.9898214418809326842, 1.000000000000000000, 0.9898214418809326842, 1.000000000000000000, 0.9898214418809326842, 1.000000000000000000, 0.9898214418809326842, 1.000000000000000000, 0.9898214418809326842, 1.000000000000000000, 0.9898214418809326842, 1.000000000000000000, 0.9898214418809326842, 1.000000000000000000, 0.9898214418809326842, 1.000000000000000000, 0.9898214418809326842, 1.000000000000000000, 0.9898214418809326842, 1.000000000000000000, 0.9898214418809326842, 1.000000000000000000, 0.9898214418809326842, 1.000000000000000000, 0.9898214418809326842, 1.000000000000000000, 0.9898214418809326842, 1.000000000000000000, 0.9898214418809326842, 1.000000000000000000, 0.9898214418809326842, 1.000000000000000000, 0.9898214418809326842, 1.000000000000000000, 0.9898214418809326842, 1.000000000000000000, 0.9898214418809326842, 1.000000000000000000, 0.9898214418809326842, 1.000000000000000000, 0.9898214418809326842, 1.000000000000000000, 0.9898214418809326842, 1.000000000000000000, 0.9898214418809326842, 1.000000000000000000, 0.9898214418809326842, 1.000000000000000000, 0.9898214418809326842, 1.000000000000000000, 0.9898214418809326842, 1.000000000000000000, 0.9898214418809326842, 1.000000000000000000, 0.9898214418809326842, 1.000000000000000000, 0.9898214418809326842, 1.000000000000000000, 0.9898214418809326842, 1.000000000000000000, 0.9898214418809326842, 1.000000000000000000, 0.9898214418809326842, 1.000000000000000000, 0.9898214418809326842, 1.000000000000000000, 0.9898214418809326842, 1.000000000000000000, 0.9898214418809326842, 1.000000000000000000, 0.9898214418809326842, 1.000000000000000000, 0.9898214418809326842, 1.000000000000000000, 0.9898214418809326842, 1.000000000000000000, 0.9898214418809326842, 1.000000000000000000, 0.9898214418809326842, 1.000000000000000000, 0.9898214418809326842, 1.000000000000000000, 0.9898214418809326842, 1.000000000000000000, 0.9898214418809326842, 1.000000000000000000, 0.9898214418809326842, 1.000000000000000000, 0.9898214418809326842, 1.000000000000000000, 0.9898214418809326842, 1.000000000000000000, 0.9898214418809326842, 1.000000000000000000, 0.9898214418809326842, 1.000000000000000000, 0.9898214418809326842, 1.000000000000000000, 0.9898214418809326842, 1.000000000000000000, 0.9898214418809326842, 1.000000000000000000, 0.9898214418809326842, 1.000000000000000000, 0.9898214418809326842, 1.000000000000000000, 0.9898214418809326842, 1.000000000000000000, 0.9898214418809326842, 1.000000000000000000, 0.9898214418809326842, 1.000000000000000000, 0.9898214418809326842, 1.000000000000000000, 0.9898214418809326842, 1.000000000000000000, 0.9898214418809326842, 1.000000000000000000, 0.9898214418809326842, 1.000000000000000000, 0.9898214418809326842, 1.000000000000000000, 0.9898214418809326842, 1.000000000000000000, 0.9898214418809326842, 1.000000000000000000, 0.9898214418809326842, 1.000000000000000000, 0.9898214418809326842, 1.000000000000000000, 0.9898214418809326842, 1.000000000000000000, 0.9898214418809326842, 1.000000000000000000, 0.9898214418809326842, 1.000000000000000000, 0.9898214418809326842, 1.000000000000000000, 0.9898214418809326842, 1.000000000000000000, 0.9898214418809326842, 1.000000000000000000, 0.9898214418809326842, 1.000000000000000000, 0.9898214418809326842, 1.000000000000000000, 0.9898214418809326842, 1.000000000000000000, 0.9898214418809326842, 1.000000000000000000, 0.9898214418809326842, 1.000000000000000000, 0.9898214418809326842, 1.000000000000000000, 0.9898214418809326842, 1.000000000000000000, 0.9898214418809326842, 1.000000000000000000, 0.9898214418809326842, 1.000000000000000000, 0.9898214418809326842, 1.000000000000000000, 0.9898214418809326842, 1.000000000000000000, 0.9898214418809326842, 1.000000000000000000, 0.9898214418809326842, 1.000000000000000000, 0.9898214418809326842, 1.000000000000000000, 0.9898214418809326842, 1.000000000000000000, 0.9898214418809326842, 1.000000000000000000, 0.9898214418809326842, 1.000000000000000000, 0.9898214418809326842, 1.000000000000000000, 0.9898214418809326842, 1.000000000000000000, 0.9898214418809326842, 1.000000000000000000, 0.9898214418809326842, 1.000000000000000000, 0.9898214418809326842, 1.000000000000000000, 0.9898214418809326842, 1.000000000000000000, 0.9898214418809326842, 1.000000000000000000, 0.9898214418809326842, 1.000000000000000000, 0.9898214418809326842, 1.000000000000000000, 0.9898214418809326842, 1.000000000000000000, 0.9898214418809326842, 1.000000000000000000, 0.9898214418809326842, 1.000000000000000000, 0.9898214418809326842, 1.000000000000000000, 0.9898214418809326842, 1.000000000000000000, 0.9898214418809326842, 1.000000000000000000, 0.9898214418809326842, 1.000000000000000000, 0.9898214418809326842, 1.000000000000000000, 0.9898214418809326842, 1.000000000000000000, 0.9898214418809326842, 1.000000000000000000, 0.9898214418809326842, 1.000000000000000000, 0.9898214418809326842, 1.000000000000000000, 0.9898214418809326842, 1.000000000000000000, 0.9898214418809326842, 1.000000000000000000, 0.9898214418809326842, 1.000000000000000000, 0.9898214418809326842, 1.000000000000000000, 0.9898214418809326842, 1.000000000000000000, 0.9898214418809326842, 1.000000000000000000, 0.9898214418809326842, 1.000000000000000000, 0.9898214418809326842, 1.000000000000000000, 0.9898214418809326842, 1.000000000000000000, 0.9898214418809326842, 1.000000000000000000, 0.9898214418809326842, 1.000000000000000000, 0.9898214418809326842, 1.000000000000000000, 0.9898214418809326842, 1.000000000000000000, 0.9898214418809326842, 1.000000000000000000, 0.9898214418809326842, 1.000000000000000000, 0.9898214418809326842, 1.000000000000000000, 0.9898214418809326842, 1.000000000000000000, 0.9898214418809326842, 1.000000000000000000, 0.9898214418809326842, 1.000000000000000000, 0.9898214418809326842, 1.000000000000000000, 0.9898214418809326842, 1.000000000000000000, 0.9898214418809326842, 1.000000000000000000, 0.9898214418809326842, 1.000000000000000000, 0.9898214418809326842, 1.000000000000000000, 0.9898214418809326842, 1.000000000000000000, 0.9898214418809326842, 1.000000000000000000, 0.9898214418809326842, 1.000000000000000000, 0.9898214418809326842, 1.000000000000000000, 0.9898214418809326842, 1.000000000000000000, 0.9898214418809326842, 1.000000000000000000, 0.9898214418809326842, 1.000000000000000000, 0.9898214418809326842, 1.000000000000000000, 0.9898214418809326842, 1.000000000000000000, 0.9898214418809326842, 1.000000000000000000, 0.9898214418809326842, 1.000000000000000000, 0.9898214418809326842, 1.000000000000000000, 0.9898214418809326842, 1.000000000000000000, 0.9898214418809326842, 1.000000000000000000, 0.9898214418809326842, 1.000000000000000000, 0.9898214418809326842, 1.000000000000000000, 0.9898214418809326842, 1.000000000000000000, 0.9898214418809326842, 1.000000000000000000, 0.9898214418809326842, 1.000000000000000000, 0.9898214418809326842, 1.000000000000000000, 0.9898214418809326842, 1.000000000000000000, 0.9898214418809326842, 1.000000000000000000, 0.9898214418809326842, 1.000000000000000000, 0.9898214418809326842, 1.000000000000000000, 0.9898214418809326842, 1.000000000000000000, 0.9898214418809326842, 1.000000000000000000, 0.9898214418809326842, 1.000000000000000000, 0.9898214418809326842, 1.000000000000000000, 0.9898214418809326842, 1.000000000000000000, 0.9898214418809326842, 1.000000000000000000, 0.9898214418809326842, 1.000000000000000000, 0.9898214418809326842, 1.000000000000000000, 0.9898214418809326842, 1.000000000000000000, 0.9898214418809326842, 1.000000000000000000, 0.9898214418809326842, 1.000000000000000000, 0.9898214418809326842, 1.000000000000000000, 0.9898214418809326842, 1.000000000000000000, 0.9898214418809326842, 1.000000000000000000, 0.9898214418809326842, 1.000000000000000000, 0.9898214418809326842, 1.000000000000000000, 0.9898214418809326842, 1.000000000000000000, 0.9898214418809326842, 1.000000000000000000, 0.9898214418809326842, 1.000000000000000000, 0.9898214418809326842, 1.000000000000000000, 0.9898214418809326842, 1.000000000000000000, 0.9898214418809326842, 1.000000000000000000, 0.9898214418809326842, 1.000000000000000000, 0.9898214418809326842, 1.000000000000000000, 0.9898214418809326842, 1.000000000000000000, 0.9898214418809326842, 1.000000000000000000, 0.9898214418809326842, 1.000000000000000000, 0.9898214418809326842, 1.000000000000000000, 0.9898214418809326842, 1.000000000000000000, 0.9898214418809326842, 1.000000000000000000, 0.9898214418809326842, 1.000000000000000000, 0.9898214418809326842, 1.000000000000000000, 0.9898214418809326842, 1.000000000000000000, 0.9898214418809326842, 1.000000000000000000, 0.9898214418809326842, 1.000000000000000000, 0.9898214418809326842, 1.000000000000000000, 0.9898214418809326842, 1.000000000000000000, 0.9898214418809326842, 1.000000000000000000, 0.9898214418809326842, 1.000000000000000000, 0.9898214418809326842, 1.000000000000000000, 0.9898214418809326842, 1.000000000000000000, 0.9898214418809326842, 1.000000000000000000, 0.9898214418809326842, 1.000000000000000000, 0.9898214418809326842, 1.000000000000000000, 0.9898214418809326842, 1.000000000000000000, 0.9898214418809326842, 1.000000000000000000, 0.9898214418809326842, 1.000000000000000000, 0.9898214418809326842, 1.000000000000000000, 0.9898214418809326842, 1.000000000000000000, 0.9898214418809326842, 1.000000000000000000, 0.9898214418809326842, 1.000000000000000000, 0.9898214418809326842, 1.000000000000000000, 0.9898214418809326842, 1.000000000000000000, 0.9898214418809326842, 1.000000000000000000, 0.9898214418809326842, 1.000000000000000000, 0.9898214418809326842, 1.000000000000000000, 0.9898214418809326842, 1.000000000000000000, 0.9898214418809326842, 1.000000000000000000, 0.9898214418809326842, 1.000000000000000000, 0.9898214418809326842, 1.000000000000000000, 0.9898214418809326842, 1.000000000000000000, 0.9898214418809326842, 1.000000000000000000, 0.9898214418809326842, 1.000000000000000000, 0.9898214418809326842, 1.000000000000000000, 0.9898214418809326842, 1.000000000000000000, 0.9898214418809326842, 1.000000000000000000, 0.9898214418809326842, 1.000000000000000000, 0.9898214418809326842, 1.000000000000000000, 0.9898214418809326842, 1.000000000000000000, 0.9898214418809326842, 1.000000000000000000, 0.9898214418809326842, 1.000000000000000000, 0.9898214418809326842, 1.000000000000000000, 0.9898214418809326842, 1.000000000000000000, 0.9898214418809326842, 1.000000000000000000, 0.9898214418809326842, 1.000000000000000000, 0.9898214418809326842, 1.000000000000000000, 0.9898214418809326842, 1.000000000000000000, 0.9898214418809326842, 1.000000000000000000, 0.9898214418809326842, 1.000000000000000000, 0.9898214418809326842, 1.000000000000000000, 0.9898214418809326842, 1.000000000000000000, 0.9898214418809326842, 1.000000000000000000, 0.9898214418809326842, 1.000000000000000000, 0.9898214418809326842, 1.000000000000000000, 0.9898214418809326842, 1.000000000000000000, 0.9898214418809326842, 1.000000000000000000, 0.9898214418809326842, 1.000000000000000000, 0.9898214418809326842, 1.000000000000000000, 0.9898214418809326842, 1.000000000000000000, 0.9898214418809326842, 1.000000000000000000, 0.9898214418809326842, 1.000000000000000000, 0.9898214418809326842, 1.000000000000000000, 0.9898214418809326842, 1.000000000000000000, 0.9898214418809326842, 1.000000000000000000, 0.9898214418809326842, 1.000000000000000000, 0.9898214418809326842, 1.000000000000000000, 0.9898214418809326842, 1.000000000000000000, 0.9898214418809326842, 1.000000000000000000, 0.9898214418809326842, 1.000000000000000000, 0.9898214418809326842, 1.000000000000000000, 0.9898214418809326842, 1.000000000000000000, 0.9898214418809326842, 1.000000000000000000, 0.9898214418809326842, 1.000000000000000000, 0.9898214418809326842, 1.000000000000000000, 0.9898214418809326842, 1.000000000000000000, 0.9898214418809326842, 1.000000000000000000, 0.9898214418809326842, 1.000000000000000000, 0.9898214418809326842, 1.000000000000000000, 0.9898214418809326842, 1.000000000000000000, 0.9898214418809326842, 1.000000000000000000, 0.9898214418809326842, 1.000000000000000000, 0.9898214418809326842, 1.000000000000000000, 0.9898214418809326842, 1.000000000000000000, 0.9898214418809326842, 1.000000000000000000, 0.9898214418809326842, 1.000000000000000000, 0.9898214418809326842, 1.000000000000000000, 0.9898214418809326842, 1.000000000000000000, 0.9898214418809326842, 1.000000000000000000, 0.9898214418809326842, 1.000000000000000000, 0.9898214418809326842, 1.000000000000000000, 0.9898214418809326842, 1.000000000000000000, 0.9898214418809326842, 1.000000000000000000, 0.9898214418809326842, 1.000000000000000000, 0.9898214418809326842, 1.000000000000000000, 0.9898214418809326842, 1.000000000000000000, 0.9898214418809326842, 1.000000000000000000, 0.9898214418809326842, 1.000000000000000000, 0.9898214418809326842, 1.000000000000000000, 0.9898214418809326842, 1.000000000000000000, 0.9898214418809326842, 1.000000000000000000, 0.9898214418809326842, 1.000000000000000000, 0.9898214418809326842, 1.000000000000000000, 0.9898214418809326842, 1.000000000000000000, 0.9898214418809326842, 1.000000000000000000, 0.9898214418809326842, 1.000000000000000000, 0.9898214418809326842, 1.000000000000000000, 0.9898214418809326842, 1.000000000000000000, 0.9898214418809326842, 1.000000000000000000, 0.9898214418809326842, 1.000000000000000000, 0.9898214418809326842, 1.000000000000000000, 0.9898214418809326842, 1.000000000000000000, 0.9898214418809326842, 1.000000000000000000, 0.9898214418809326842, 1.000000000000000000, 0.9898214418809326842, 1.000000000000000000, 0.9898214418809326842, 1.000000000000000000, 0.9898214418809326842, 1.000000000000000000, 0.9898214418809326842, 1.000000000000000000, 0.9898214418809326842, 1.000000000000000000, 0.9898214418809326842, 1.000000000000000000, 0.9898214418809326842, 1.000000000000000000, 0.9898214418809326842, 1.000000000000000000, 0.9898214418809326842, 1.000000000000000000, 0.9898214418809326842, 1.000000000000000000, 0.9898214418809326842, 1.000000000000000000, 0.9898214418809326842, 1.000000000000000000, 0.9898214418809326842, 1.000000000000000000, 0.9898214418809326842, 1.000000000000000000, 0.9898214418809326842, 1.000000000000000000, 0.9898214418809326842, 1.000000000000000000, 0.9898214418809326842, 1.000000000000000000, 0.9898214418809326842, 1.000000000000000000, 0.9898214418809326842, 1.000000000000000000, 0.9898214418809326842, 1.000000000000000000, 0.9898214418809326842, 1.000000000000000000, 0.9898214418809326842, 1.000000000000000000, 0.9898214418809326842, 1.000000000000000000, 0.9898214418809326842, 1.000000000000000000, 0.9898214418809326842, 1.000000000000000000, 0.9898214418809326842, 1.000000000000000000, 0.9898214418809326842, 1.000000000000000000, 0.9898214418809326842, 1.000000000000000000, 0.9898214418809326842, 1.000000000000000000, 0.9898214418809326842, 1.000000000000000000, 0.9898214418809326842, 1.000000000000000000, 0.9898214418809326842, 1.000000000000000000, 0.9898214418809326842, 1.000000000000000000, 0.9898214418809326842, 1.000000000000000000, 0.9898214418809326842, 1.000000000000000000, 0.9898214418809326842, 1.000000000000000000, 0.9898214418809326842, 1.000000000000000000, 0.9898214418809326842, 1.000000000000000000, 0.9898214418809326842, 1.000000000000000000, 0.9898214418809326842, 1.000000000000000000, 0.9898214418809326842, 1.000000000000000000, 0.9898214418809326842, 1.000000000000000000, 0.9898214418809326842, 1.000000000000000000, 0.9898214418809326842, 1.000000000000000000, 0.9898214418809326842, 1.000000000000000000, 0.9898214418809326842, 1.000000000000000000, 0.9898214418809326842, 1.000000000000000000, 0.9898214418809326842, 1.000000000000000000, 0.9898214418809326842, 1.000000000000000000, 0.9898214418809326842, 1.000000000000000000, 0.9898214418809326842, 1.000000000000000000, 0.9898214418809326842, 1.000000000000000000, 0.9898214418809326842, 1.000000000000000000, 0.9898214418809326842, 1.000000000000000000, 0.9898214418809326842, 1.000000000000000000, 0.9898214418809326842, 1.000000000000000000, 0.9898214418809326842, 1.000000000000000000, 0.9898214418809326842, 1.000000000000000000, 0.9898214418809326842, 1.000000000000000000, 0.9898214418809326842, 1.000000000000000000, 0.9898214418809326842, 1.000000000000000000, 0.9961809353924466759, 0.9952277490961531914),
 ( 0.3333333333333333703, 0.3299404806269776169, 0.3333333333333333703, 0.3299404806269776169, 0.3333333333333333703, 0.3299404806269776169, 0.3333333333333333703, 0.3299404806269776169, 0.3333333333333333703, 0.3299404806269776169, 0.3333333333333333703, 0.3299404806269776169, 0.3333333333333333703, 0.3299404806269776169, 0.3333333333333333703, 0.3299404806269776169, 0.3333333333333333703, 0.3299404806269776169, 0.3333333333333333703, 0.3299404806269776169, 0.3333333333333333703, 0.3299404806269776169, 0.3333333333333333703, 0.3299404806269776169, 0.3333333333333333703, 0.3299404806269776169, 0.3333333333333333703, 0.3299404806269776169, 0.3333333333333333703, 0.3299404806269776169, 0.3333333333333333703, 0.3299404806269776169, 0.3333333333333333703, 0.3299404806269776169, 0.3333333333333333703, 0.3299404806269776169, 0.3333333333333333703, 0.3299404806269776169, 0.3333333333333333703, 0.3299404806269776169, 0.3333333333333333703, 0.3299404806269776169, 0.3333333333333333703, 0.3299404806269776169, 0.3333333333333333703, 0.3299404806269776169, 0.3333333333333333703, 0.3299404806269776169, 0.3333333333333333703, 0.3299404806269776169, 0.3333333333333333703, 0.3299404806269776169, 0.3333333333333333703, 0.3299404806269776169, 0.3333333333333333703, 0.3299404806269776169, 0.3333333333333333703, 0.3299404806269776169, 0.3333333333333333703, 0.3299404806269776169, 0.3333333333333333703, 0.3299404806269776169, 0.3333333333333333703, 0.3299404806269776169, 0.3333333333333333703, 0.3299404806269776169, 0.3333333333333333703, 0.3299404806269776169, 0.3333333333333333703, 0.3299404806269776169, 0.3333333333333333703, 0.3299404806269776169, 0.3333333333333333703, 0.3299404806269776169, 0.3333333333333333703, 0.3299404806269776169, 0.3333333333333333703, 0.3299404806269776169, 0.3333333333333333703, 0.3299404806269776169, 0.3333333333333333703, 0.3299404806269776169, 0.3333333333333333703, 0.3299404806269776169, 0.3333333333333333703, 0.3299404806269776169, 0.3333333333333333703, 0.3299404806269776169, 0.3333333333333333703, 0.3299404806269776169, 0.3333333333333333703, 0.3299404806269776169, 0.3333333333333333703, 0.3299404806269776169, 0.3333333333333333703, 0.3299404806269776169, 0.3333333333333333703, 0.3299404806269776169, 0.3333333333333333703, 0.3299404806269776169, 0.3333333333333333703, 0.3299404806269776169, 0.3333333333333333703, 0.3299404806269776169, 0.3333333333333333703, 0.3299404806269776169, 0.3333333333333333703, 0.3299404806269776169, 0.3333333333333333703, 0.3299404806269776169, 0.3333333333333333703, 0.3299404806269776169, 0.3333333333333333703, 0.3299404806269776169, 0.3333333333333333703, 0.3299404806269776169, 0.3333333333333333703, 0.3299404806269776169, 0.3333333333333333703, 0.3299404806269776169, 0.3333333333333333703, 0.3299404806269776169, 0.3333333333333333703, 0.3299404806269776169, 0.3333333333333333703, 0.3299404806269776169, 0.3333333333333333703, 0.3299404806269776169, 0.3333333333333333703, 0.3299404806269776169, 0.3333333333333333703, 0.3299404806269776169, 0.3333333333333333703, 0.3299404806269776169, 0.3333333333333333703, 0.3299404806269776169, 0.3333333333333333703, 0.3299404806269776169, 0.3333333333333333703, 0.3299404806269776169, 0.3333333333333333703, 0.3299404806269776169, 0.3333333333333333703, 0.3299404806269776169, 0.3333333333333333703, 0.3299404806269776169, 0.3333333333333333703, 0.3299404806269776169, 0.3333333333333333703, 0.3299404806269776169, 0.3333333333333333703, 0.3299404806269776169, 0.3333333333333333703, 0.3299404806269776169, 0.3333333333333333703, 0.3299404806269776169, 0.3333333333333333703, 0.3299404806269776169, 0.3333333333333333703, 0.3299404806269776169, 0.3333333333333333703, 0.3299404806269776169, 0.3333333333333333703, 0.3299404806269776169, 0.3333333333333333703, 0.3299404806269776169, 0.3333333333333333703, 0.3299404806269776169, 0.3333333333333333703, 0.3299404806269776169, 0.3333333333333333703, 0.3299404806269776169, 0.3333333333333333703, 0.3299404806269776169, 0.3333333333333333703, 0.3299404806269776169, 0.3333333333333333703, 0.3299404806269776169, 0.3333333333333333703, 0.3299404806269776169, 0.3333333333333333703, 0.3299404806269776169, 0.3333333333333333703, 0.3299404806269776169, 0.3333333333333333703, 0.3299404806269776169, 0.3333333333333333703, 0.3299404806269776169, 0.3333333333333333703, 0.3299404806269776169, 0.3333333333333333703, 0.3299404806269776169, 0.3333333333333333703, 0.3299404806269776169, 0.3333333333333333703, 0.3299404806269776169, 0.3333333333333333703, 0.3299404806269776169, 0.3333333333333333703, 0.3299404806269776169, 0.3333333333333333703, 0.3299404806269776169, 0.3333333333333333703, 0.3299404806269776169, 0.3333333333333333703, 0.3299404806269776169, 0.3333333333333333703, 0.3299404806269776169, 0.3333333333333333703, 0.3299404806269776169, 0.3333333333333333703, 0.3299404806269776169, 0.3333333333333333703, 0.3299404806269776169, 0.3333333333333333703, 0.3299404806269776169, 0.3333333333333333703, 0.3299404806269776169, 0.3333333333333333703, 0.3299404806269776169, 0.3333333333333333703, 0.3299404806269776169, 0.3333333333333333703, 0.3299404806269776169, 0.3333333333333333703, 0.3299404806269776169, 0.3333333333333333703, 0.3299404806269776169, 0.3333333333333333703, 0.3299404806269776169, 0.3333333333333333703, 0.3299404806269776169, 0.3333333333333333703, 0.3299404806269776169, 0.3333333333333333703, 0.3299404806269776169, 0.3333333333333333703, 0.3299404806269776169, 0.3333333333333333703, 0.3299404806269776169, 0.3333333333333333703, 0.3299404806269776169, 0.3333333333333333703, 0.3299404806269776169, 0.3333333333333333703, 0.3299404806269776169, 0.3333333333333333703, 0.3299404806269776169, 0.3333333333333333703, 0.3299404806269776169, 0.3333333333333333703, 0.3299404806269776169, 0.3333333333333333703, 0.3299404806269776169, 0.3333333333333333703, 0.3299404806269776169, 0.3333333333333333703, 0.3299404806269776169, 0.3333333333333333703, 0.3299404806269776169, 0.3333333333333333703, 0.3299404806269776169, 0.3333333333333333703, 0.3299404806269776169, 0.3333333333333333703, 0.3299404806269776169, 0.3333333333333333703, 0.3299404806269776169, 0.3333333333333333703, 0.3299404806269776169, 0.3333333333333333703, 0.3299404806269776169, 0.3333333333333333703, 0.3299404806269776169, 0.3333333333333333703, 0.3299404806269776169, 0.3333333333333333703, 0.3299404806269776169, 0.3333333333333333703, 0.3299404806269776169, 0.3333333333333333703, 0.3299404806269776169, 0.3333333333333333703, 0.3299404806269776169, 0.3333333333333333703, 0.3299404806269776169, 0.3333333333333333703, 0.3299404806269776169, 0.3333333333333333703, 0.3299404806269776169, 0.3333333333333333703, 0.3299404806269776169, 0.3333333333333333703, 0.3299404806269776169, 0.3333333333333333703, 0.3299404806269776169, 0.3333333333333333703, 0.3299404806269776169, 0.3333333333333333703, 0.3299404806269776169, 0.3333333333333333703, 0.3299404806269776169, 0.3333333333333333703, 0.3299404806269776169, 0.3333333333333333703, 0.3299404806269776169, 0.3333333333333333703, 0.3299404806269776169, 0.3333333333333333703, 0.3299404806269776169, 0.3333333333333333703, 0.3299404806269776169, 0.3333333333333333703, 0.3299404806269776169, 0.3333333333333333703, 0.3299404806269776169, 0.3333333333333333703, 0.3299404806269776169, 0.3333333333333333703, 0.3299404806269776169, 0.3333333333333333703, 0.3299404806269776169, 0.3333333333333333703, 0.3299404806269776169, 0.3333333333333333703, 0.3299404806269776169, 0.3333333333333333703, 0.3299404806269776169, 0.3333333333333333703, 0.3299404806269776169, 0.3333333333333333703, 0.3299404806269776169, 0.3333333333333333703, 0.3299404806269776169, 0.3333333333333333703, 0.3299404806269776169, 0.3333333333333333703, 0.3299404806269776169, 0.3333333333333333703, 0.3299404806269776169, 0.3333333333333333703, 0.3299404806269776169, 0.3333333333333333703, 0.3299404806269776169, 0.3333333333333333703, 0.3299404806269776169, 0.3333333333333333703, 0.3299404806269776169, 0.3333333333333333703, 0.3299404806269776169, 0.3333333333333333703, 0.3299404806269776169, 0.3333333333333333703, 0.3299404806269776169, 0.3333333333333333703, 0.3299404806269776169, 0.3333333333333333703, 0.3299404806269776169, 0.3333333333333333703, 0.3299404806269776169, 0.3333333333333333703, 0.3299404806269776169, 0.3333333333333333703, 0.3299404806269776169, 0.3333333333333333703, 0.3299404806269776169, 0.3333333333333333703, 0.3299404806269776169, 0.3333333333333333703, 0.3299404806269776169, 0.3333333333333333703, 0.3299404806269776169, 0.3333333333333333703, 0.3299404806269776169, 0.3333333333333333703, 0.3299404806269776169, 0.3333333333333333703, 0.3299404806269776169, 0.3333333333333333703, 0.3299404806269776169, 0.3333333333333333703, 0.3299404806269776169, 0.3333333333333333703, 0.3299404806269776169, 0.3333333333333333703, 0.3299404806269776169, 0.3333333333333333703, 0.3299404806269776169, 0.3333333333333333703, 0.3299404806269776169, 0.3333333333333333703, 0.3299404806269776169, 0.3333333333333333703, 0.3299404806269776169, 0.3333333333333333703, 0.3299404806269776169, 0.3333333333333333703, 0.3299404806269776169, 0.3333333333333333703, 0.3299404806269776169, 0.3333333333333333703, 0.3299404806269776169, 0.3333333333333333703, 0.3299404806269776169, 0.3333333333333333703, 0.3299404806269776169, 0.3333333333333333703, 0.3299404806269776169, 0.3333333333333333703, 0.3299404806269776169, 0.3333333333333333703, 0.3299404806269776169, 0.3333333333333333703, 0.3299404806269776169, 0.3333333333333333703, 0.3299404806269776169, 0.3333333333333333703, 0.3299404806269776169, 0.3333333333333333703, 0.3299404806269776169, 0.3333333333333333703, 0.3299404806269776169, 0.3333333333333333703, 0.3299404806269776169, 0.3333333333333333703, 0.3299404806269776169, 0.3333333333333333703, 0.3299404806269776169, 0.3333333333333333703, 0.3299404806269776169, 0.3333333333333333703, 0.3299404806269776169, 0.3333333333333333703, 0.3299404806269776169, 0.3333333333333333703, 0.3299404806269776169, 0.3333333333333333703, 0.3299404806269776169, 0.3333333333333333703, 0.3299404806269776169, 0.3333333333333333703, 0.3299404806269776169, 0.3333333333333333703, 0.3299404806269776169, 0.3333333333333333703, 0.3299404806269776169, 0.3333333333333333703, 0.3299404806269776169, 0.3333333333333333703, 0.3299404806269776169, 0.3333333333333333703, 0.3299404806269776169, 0.3333333333333333703, 0.3299404806269776169, 0.3333333333333333703, 0.3299404806269776169, 0.3333333333333333703, 0.3299404806269776169, 0.3333333333333333703, 0.3299404806269776169, 0.3333333333333333703, 0.3299404806269776169, 0.3333333333333333703, 0.3299404806269776169, 0.3333333333333333703, 0.3299404806269776169, 0.3333333333333333703, 0.3299404806269776169, 0.3333333333333333703, 0.3299404806269776169, 0.3333333333333333703, 0.3299404806269776169, 0.3333333333333333703, 0.3299404806269776169, 0.3333333333333333703, 0.3299404806269776169, 0.3333333333333333703, 0.3299404806269776169, 0.3333333333333333703, 0.3299404806269776169, 0.3333333333333333703, 0.3299404806269776169, 0.3333333333333333703, 0.3299404806269776169, 0.3333333333333333703, 0.3299404806269776169, 0.3333333333333333703, 0.3299404806269776169, 0.3333333333333333703, 0.3299404806269776169, 0.3333333333333333703, 0.3299404806269776169, 0.3333333333333333703, 0.3299404806269776169, 0.3333333333333333703, 0.3299404806269776169, 0.3333333333333333703, 0.3299404806269776169, 0.3333333333333333703, 0.3299404806269776169, 0.3333333333333333703, 0.3299404806269776169, 0.3333333333333333703, 0.3299404806269776169, 0.3333333333333333703, 0.3299404806269776169, 0.3333333333333333703, 0.3299404806269776169, 0.3333333333333333703, 0.3299404806269776169, 0.3333333333333333703, 0.3299404806269776169, 0.3333333333333333703, 0.3299404806269776169, 0.3333333333333333703, 0.3299404806269776169, 0.3333333333333333703, 0.3299404806269776169, 0.3333333333333333703, 0.3299404806269776169, 0.3333333333333333703, 0.3299404806269776169, 0.3333333333333333703, 0.3299404806269776169, 0.3333333333333333703, 0.3299404806269776169, 0.3333333333333333703, 0.3299404806269776169, 0.3333333333333333703, 0.3299404806269776169, 0.3333333333333333703, 0.3299404806269776169, 0.3333333333333333703, 0.3299404806269776169, 0.3333333333333333703, 0.3299404806269776169, 0.3333333333333333703, 0.3299404806269776169, 0.3333333333333333703, 0.3299404806269776169, 0.3333333333333333703, 0.3299404806269776169, 0.3333333333333333703, 0.3299404806269776169, 0.3333333333333333703, 0.3299404806269776169, 0.3333333333333333703, 0.3299404806269776169, 0.3333333333333333703, 0.3299404806269776169, 0.3333333333333333703, 0.3299404806269776169, 0.3333333333333333703, 0.3299404806269776169, 0.3333333333333333703, 0.3299404806269776169, 0.3333333333333333703, 0.3299404806269776169, 0.3333333333333333703, 0.3299404806269776169, 0.3333333333333333703, 0.3299404806269776169, 0.3333333333333333703, 0.3299404806269776169, 0.3333333333333333703, 0.3299404806269776169, 0.3333333333333333703, 0.3299404806269776169, 0.3333333333333333703, 0.3299404806269776169, 0.3333333333333333703, 0.3299404806269776169, 0.3333333333333333703, 0.3299404806269776169, 0.3333333333333333703, 0.3299404806269776169, 0.3333333333333333703, 0.3299404806269776169, 0.3333333333333333703, 0.3299404806269776169, 0.3333333333333333703, 0.3299404806269776169, 0.3333333333333333703, 0.3299404806269776169, 0.3333333333333333703, 0.3299404806269776169, 0.3333333333333333703, 0.3299404806269776169, 0.3333333333333333703, 0.3299404806269776169, 0.3333333333333333703, 0.3299404806269776169, 0.3333333333333333703, 0.3299404806269776169, 0.3333333333333333703, 0.3299404806269776169, 0.3333333333333333703, 0.3299404806269776169, 0.3333333333333333703, 0.3299404806269776169, 0.3333333333333333703, 0.3299404806269776169, 0.3333333333333333703, 0.3299404806269776169, 0.3333333333333333703, 0.3299404806269776169, 0.3333333333333333703, 0.3299404806269776169, 0.3333333333333333703, 0.3299404806269776169, 0.3333333333333333703, 0.3299404806269776169, 0.3333333333333333703, 0.3299404806269776169, 0.3333333333333333703, 0.3299404806269776169, 0.3333333333333333703, 0.3299404806269776169, 0.3333333333333333703, 0.3299404806269776169, 0.3333333333333333703, 0.3299404806269776169, 0.3333333333333333703, 0.3299404806269776169, 0.3333333333333333703, 0.3299404806269776169, 0.3333333333333333703, 0.3299404806269776169, 0.3333333333333333703, 0.3299404806269776169, 0.3333333333333333703, 0.3299404806269776169, 0.3333333333333333703, 0.3299404806269776169, 0.3333333333333333703, 0.3299404806269776169, 0.3333333333333333703, 0.3299404806269776169, 0.3333333333333333703, 0.3299404806269776169, 0.3333333333333333703, 0.3299404806269776169, 0.3333333333333333703, 0.3299404806269776169, 0.3333333333333333703, 0.3299404806269776169, 0.3333333333333333703, 0.3299404806269776169, 0.3333333333333333703, 0.3299404806269776169, 0.3333333333333333703, 0.3299404806269776169, 0.3333333333333333703, 0.3299404806269776169, 0.3333333333333333703, 0.3299404806269776169, 0.3333333333333333703, 0.3299404806269776169, 0.3333333333333333703, 0.3299404806269776169, 0.3333333333333333703, 0.3299404806269776169, 0.3333333333333333703, 0.3299404806269776169, 0.3333333333333333703, 0.3299404806269776169, 0.3333333333333333703, 0.3299404806269776169, 0.3333333333333333703, 0.3299404806269776169, 0.3333333333333333703, 0.3299404806269776169, 0.3333333333333333703, 0.3299404806269776169, 0.3333333333333333703, 0.3299404806269776169, 0.3333333333333333703, 0.3299404806269776169, 0.3333333333333333703, 0.3299404806269776169, 0.3333333333333333703, 0.3299404806269776169, 0.3333333333333333703, 0.3299404806269776169, 0.3333333333333333703, 0.3299404806269776169, 0.3333333333333333703, 0.3299404806269776169, 0.3333333333333333703, 0.3299404806269776169, 0.3333333333333333703, 0.3299404806269776169, 0.3333333333333333703, 0.3299404806269776169, 0.3333333333333333703, 0.3299404806269776169, 0.3333333333333333703, 0.3299404806269776169, 0.3333333333333333703, 0.3299404806269776169, 0.3333333333333333703, 0.3299404806269776169, 0.3333333333333333703, 0.3299404806269776169, 0.3333333333333333703, 0.3299404806269776169, 0.3333333333333333703, 0.3299404806269776169, 0.3333333333333333703, 0.3299404806269776169, 0.3333333333333333703, 0.3299404806269776169, 0.3333333333333333703, 0.3299404806269776169, 0.3333333333333333703, 0.3299404806269776169, 0.3333333333333333703, 0.3299404806269776169, 0.3333333333333333703, 0.3299404806269776169, 0.3333333333333333703, 0.3299404806269776169, 0.3333333333333333703, 0.3299404806269776169, 0.3333333333333333703, 0.3299404806269776169, 0.3333333333333333703, 0.3299404806269776169, 0.3333333333333333703, 0.3299404806269776169, 0.3333333333333333703, 0.3299404806269776169, 0.3333333333333333703, 0.3299404806269776169, 0.3333333333333333703, 0.3299404806269776169, 0.3333333333333333703, 0.3299404806269776169, 0.3333333333333333703, 0.3299404806269776169, 0.3333333333333333703, 0.3299404806269776169, 0.3333333333333333703, 0.3299404806269776169, 0.3333333333333333703, 0.3299404806269776169, 0.3333333333333333703, 0.3299404806269776169, 0.3333333333333333703, 0.3299404806269776169, 0.3333333333333333703, 0.3299404806269776169, 0.3333333333333333703, 0.3299404806269776169, 0.3333333333333333703, 0.3299404806269776169, 0.3333333333333333703, 0.3299404806269776169, 0.3333333333333333703, 0.3299404806269776169, 0.3333333333333333703, 0.3299404806269776169, 0.3333333333333333703, 0.3299404806269776169, 0.3333333333333333703, 0.3299404806269776169, 0.3333333333333333703, 0.3299404806269776169, 0.3333333333333333703, 0.3299404806269776169, 0.3333333333333333703, 0.3299404806269776169, 0.3333333333333333703, 0.3299404806269776169, 0.3333333333333333703, 0.3299404806269776169, 0.3333333333333333703, 0.3299404806269776169, 0.3333333333333333703, 0.3299404806269776169, 0.3333333333333333703, 0.3299404806269776169, 0.3333333333333333703, 0.3299404806269776169, 0.3333333333333333703, 0.3299404806269776169, 0.3333333333333333703, 0.3299404806269776169, 0.3333333333333333703, 0.3299404806269776169, 0.3333333333333333703, 0.3299404806269776169, 0.3333333333333333703, 0.3299404806269776169, 0.3333333333333333703, 0.3299404806269776169, 0.3333333333333333703, 0.3299404806269776169, 0.3333333333333333703, 0.3299404806269776169, 0.3333333333333333703, 0.3299404806269776169, 0.3333333333333333703, 0.3299404806269776169, 0.3333333333333333703, 0.3299404806269776169, 0.3333333333333333703, 0.3299404806269776169, 0.3333333333333333703, 0.3299404806269776169, 0.3333333333333333703, 0.3299404806269776169, 0.3333333333333333703, 0.3299404806269776169, 0.3333333333333333703, 0.3299404806269776169, 0.3333333333333333703, 0.3299404806269776169, 0.3333333333333333703, 0.3299404806269776169, 0.3333333333333333703, 0.3299404806269776169, 0.3333333333333333703, 0.3299404806269776169, 0.3333333333333333703, 0.3299404806269776169, 0.3333333333333333703, 0.3299404806269776169, 0.3333333333333333703, 0.3299404806269776169, 0.3333333333333333703, 0.3299404806269776169, 0.3333333333333333703, 0.3299404806269776169, 0.3333333333333333703, 0.3299404806269776169, 0.3333333333333333703, 0.3299404806269776169, 0.3333333333333333703, 0.3299404806269776169, 0.3333333333333333703, 0.3299404806269776169, 0.3333333333333333703, 0.3299404806269776169, 0.3333333333333333703, 0.3299404806269776169, 0.3333333333333333703, 0.3299404806269776169, 0.3333333333333333703, 0.3299404806269776169, 0.3333333333333333703, 0.3299404806269776169, 0.3333333333333333703, 0.3299404806269776169, 0.3333333333333333703, 0.3299404806269776169, 0.3333333333333333703, 0.3299404806269776169, 0.3333333333333333703, 0.3299404806269776169, 0.3333333333333333703, 0.3320603117974822438, 0.3317425830320511193),
 ( 0.3333333333333333703, 0.3299404806269776169, 0.3333333333333333703, 0.3299404806269776169, 0.3333333333333333703, 0.3299404806269776169, 0.3333333333333333703, 0.3299404806269776169, 0.3333333333333333703, 0.3299404806269776169, 0.3333333333333333703, 0.3299404806269776169, 0.3333333333333333703, 0.3299404806269776169, 0.3333333333333333703, 0.3299404806269776169, 0.3333333333333333703, 0.3299404806269776169, 0.3333333333333333703, 0.3299404806269776169, 0.3333333333333333703, 0.3299404806269776169, 0.3333333333333333703, 0.3299404806269776169, 0.3333333333333333703, 0.3299404806269776169, 0.3333333333333333703, 0.3299404806269776169, 0.3333333333333333703, 0.3299404806269776169, 0.3333333333333333703, 0.3299404806269776169, 0.3333333333333333703, 0.3299404806269776169, 0.3333333333333333703, 0.3299404806269776169, 0.3333333333333333703, 0.3299404806269776169, 0.3333333333333333703, 0.3299404806269776169, 0.3333333333333333703, 0.3299404806269776169, 0.3333333333333333703, 0.3299404806269776169, 0.3333333333333333703, 0.3299404806269776169, 0.3333333333333333703, 0.3299404806269776169, 0.3333333333333333703, 0.3299404806269776169, 0.3333333333333333703, 0.3299404806269776169, 0.3333333333333333703, 0.3299404806269776169, 0.3333333333333333703, 0.3299404806269776169, 0.3333333333333333703, 0.3299404806269776169, 0.3333333333333333703, 0.3299404806269776169, 0.3333333333333333703, 0.3299404806269776169, 0.3333333333333333703, 0.3299404806269776169, 0.3333333333333333703, 0.3299404806269776169, 0.3333333333333333703, 0.3299404806269776169, 0.3333333333333333703, 0.3299404806269776169, 0.3333333333333333703, 0.3299404806269776169, 0.3333333333333333703, 0.3299404806269776169, 0.3333333333333333703, 0.3299404806269776169, 0.3333333333333333703, 0.3299404806269776169, 0.3333333333333333703, 0.3299404806269776169, 0.3333333333333333703, 0.3299404806269776169, 0.3333333333333333703, 0.3299404806269776169, 0.3333333333333333703, 0.3299404806269776169, 0.3333333333333333703, 0.3299404806269776169, 0.3333333333333333703, 0.3299404806269776169, 0.3333333333333333703, 0.3299404806269776169, 0.3333333333333333703, 0.3299404806269776169, 0.3333333333333333703, 0.3299404806269776169, 0.3333333333333333703, 0.3299404806269776169, 0.3333333333333333703, 0.3299404806269776169, 0.3333333333333333703, 0.3299404806269776169, 0.3333333333333333703, 0.3299404806269776169, 0.3333333333333333703, 0.3299404806269776169, 0.3333333333333333703, 0.3299404806269776169, 0.3333333333333333703, 0.3299404806269776169, 0.3333333333333333703, 0.3299404806269776169, 0.3333333333333333703, 0.3299404806269776169, 0.3333333333333333703, 0.3299404806269776169, 0.3333333333333333703, 0.3299404806269776169, 0.3333333333333333703, 0.3299404806269776169, 0.3333333333333333703, 0.3299404806269776169, 0.3333333333333333703, 0.3299404806269776169, 0.3333333333333333703, 0.3299404806269776169, 0.3333333333333333703, 0.3299404806269776169, 0.3333333333333333703, 0.3299404806269776169, 0.3333333333333333703, 0.3299404806269776169, 0.3333333333333333703, 0.3299404806269776169, 0.3333333333333333703, 0.3299404806269776169, 0.3333333333333333703, 0.3299404806269776169, 0.3333333333333333703, 0.3299404806269776169, 0.3333333333333333703, 0.3299404806269776169, 0.3333333333333333703, 0.3299404806269776169, 0.3333333333333333703, 0.3299404806269776169, 0.3333333333333333703, 0.3299404806269776169, 0.3333333333333333703, 0.3299404806269776169, 0.3333333333333333703, 0.3299404806269776169, 0.3333333333333333703, 0.3299404806269776169, 0.3333333333333333703, 0.3299404806269776169, 0.3333333333333333703, 0.3299404806269776169, 0.3333333333333333703, 0.3299404806269776169, 0.3333333333333333703, 0.3299404806269776169, 0.3333333333333333703, 0.3299404806269776169, 0.3333333333333333703, 0.3299404806269776169, 0.3333333333333333703, 0.3299404806269776169, 0.3333333333333333703, 0.3299404806269776169, 0.3333333333333333703, 0.3299404806269776169, 0.3333333333333333703, 0.3299404806269776169, 0.3333333333333333703, 0.3299404806269776169, 0.3333333333333333703, 0.3299404806269776169, 0.3333333333333333703, 0.3299404806269776169, 0.3333333333333333703, 0.3299404806269776169, 0.3333333333333333703, 0.3299404806269776169, 0.3333333333333333703, 0.3299404806269776169, 0.3333333333333333703, 0.3299404806269776169, 0.3333333333333333703, 0.3299404806269776169, 0.3333333333333333703, 0.3299404806269776169, 0.3333333333333333703, 0.3299404806269776169, 0.3333333333333333703, 0.3299404806269776169, 0.3333333333333333703, 0.3299404806269776169, 0.3333333333333333703, 0.3299404806269776169, 0.3333333333333333703, 0.3299404806269776169, 0.3333333333333333703, 0.3299404806269776169, 0.3333333333333333703, 0.3299404806269776169, 0.3333333333333333703, 0.3299404806269776169, 0.3333333333333333703, 0.3299404806269776169, 0.3333333333333333703, 0.3299404806269776169, 0.3333333333333333703, 0.3299404806269776169, 0.3333333333333333703, 0.3299404806269776169, 0.3333333333333333703, 0.3299404806269776169, 0.3333333333333333703, 0.3299404806269776169, 0.3333333333333333703, 0.3299404806269776169, 0.3333333333333333703, 0.3299404806269776169, 0.3333333333333333703, 0.3299404806269776169, 0.3333333333333333703, 0.3299404806269776169, 0.3333333333333333703, 0.3299404806269776169, 0.3333333333333333703, 0.3299404806269776169, 0.3333333333333333703, 0.3299404806269776169, 0.3333333333333333703, 0.3299404806269776169, 0.3333333333333333703, 0.3299404806269776169, 0.3333333333333333703, 0.3299404806269776169, 0.3333333333333333703, 0.3299404806269776169, 0.3333333333333333703, 0.3299404806269776169, 0.3333333333333333703, 0.3299404806269776169, 0.3333333333333333703, 0.3299404806269776169, 0.3333333333333333703, 0.3299404806269776169, 0.3333333333333333703, 0.3299404806269776169, 0.3333333333333333703, 0.3299404806269776169, 0.3333333333333333703, 0.3299404806269776169, 0.3333333333333333703, 0.3299404806269776169, 0.3333333333333333703, 0.3299404806269776169, 0.3333333333333333703, 0.3299404806269776169, 0.3333333333333333703, 0.3299404806269776169, 0.3333333333333333703, 0.3299404806269776169, 0.3333333333333333703, 0.3299404806269776169, 0.3333333333333333703, 0.3299404806269776169, 0.3333333333333333703, 0.3299404806269776169, 0.3333333333333333703, 0.3299404806269776169, 0.3333333333333333703, 0.3299404806269776169, 0.3333333333333333703, 0.3299404806269776169, 0.3333333333333333703, 0.3299404806269776169, 0.3333333333333333703, 0.3299404806269776169, 0.3333333333333333703, 0.3299404806269776169, 0.3333333333333333703, 0.3299404806269776169, 0.3333333333333333703, 0.3299404806269776169, 0.3333333333333333703, 0.3299404806269776169, 0.3333333333333333703, 0.3299404806269776169, 0.3333333333333333703, 0.3299404806269776169, 0.3333333333333333703, 0.3299404806269776169, 0.3333333333333333703, 0.3299404806269776169, 0.3333333333333333703, 0.3299404806269776169, 0.3333333333333333703, 0.3299404806269776169, 0.3333333333333333703, 0.3299404806269776169, 0.3333333333333333703, 0.3299404806269776169, 0.3333333333333333703, 0.3299404806269776169, 0.3333333333333333703, 0.3299404806269776169, 0.3333333333333333703, 0.3299404806269776169, 0.3333333333333333703, 0.3299404806269776169, 0.3333333333333333703, 0.3299404806269776169, 0.3333333333333333703, 0.3299404806269776169, 0.3333333333333333703, 0.3299404806269776169, 0.3333333333333333703, 0.3299404806269776169, 0.3333333333333333703, 0.3299404806269776169, 0.3333333333333333703, 0.3299404806269776169, 0.3333333333333333703, 0.3299404806269776169, 0.3333333333333333703, 0.3299404806269776169, 0.3333333333333333703, 0.3299404806269776169, 0.3333333333333333703, 0.3299404806269776169, 0.3333333333333333703, 0.3299404806269776169, 0.3333333333333333703, 0.3299404806269776169, 0.3333333333333333703, 0.3299404806269776169, 0.3333333333333333703, 0.3299404806269776169, 0.3333333333333333703, 0.3299404806269776169, 0.3333333333333333703, 0.3299404806269776169, 0.3333333333333333703, 0.3299404806269776169, 0.3333333333333333703, 0.3299404806269776169, 0.3333333333333333703, 0.3299404806269776169, 0.3333333333333333703, 0.3299404806269776169, 0.3333333333333333703, 0.3299404806269776169, 0.3333333333333333703, 0.3299404806269776169, 0.3333333333333333703, 0.3299404806269776169, 0.3333333333333333703, 0.3299404806269776169, 0.3333333333333333703, 0.3299404806269776169, 0.3333333333333333703, 0.3299404806269776169, 0.3333333333333333703, 0.3299404806269776169, 0.3333333333333333703, 0.3299404806269776169, 0.3333333333333333703, 0.3299404806269776169, 0.3333333333333333703, 0.3299404806269776169, 0.3333333333333333703, 0.3299404806269776169, 0.3333333333333333703, 0.3299404806269776169, 0.3333333333333333703, 0.3299404806269776169, 0.3333333333333333703, 0.3299404806269776169, 0.3333333333333333703, 0.3299404806269776169, 0.3333333333333333703, 0.3299404806269776169, 0.3333333333333333703, 0.3299404806269776169, 0.3333333333333333703, 0.3299404806269776169, 0.3333333333333333703, 0.3299404806269776169, 0.3333333333333333703, 0.3299404806269776169, 0.3333333333333333703, 0.3299404806269776169, 0.3333333333333333703, 0.3299404806269776169, 0.3333333333333333703, 0.3299404806269776169, 0.3333333333333333703, 0.3299404806269776169, 0.3333333333333333703, 0.3299404806269776169, 0.3333333333333333703, 0.3299404806269776169, 0.3333333333333333703, 0.3299404806269776169, 0.3333333333333333703, 0.3299404806269776169, 0.3333333333333333703, 0.3299404806269776169, 0.3333333333333333703, 0.3299404806269776169, 0.3333333333333333703, 0.3299404806269776169, 0.3333333333333333703, 0.3299404806269776169, 0.3333333333333333703, 0.3299404806269776169, 0.3333333333333333703, 0.3299404806269776169, 0.3333333333333333703, 0.3299404806269776169, 0.3333333333333333703, 0.3299404806269776169, 0.3333333333333333703, 0.3299404806269776169, 0.3333333333333333703, 0.3299404806269776169, 0.3333333333333333703, 0.3299404806269776169, 0.3333333333333333703, 0.3299404806269776169, 0.3333333333333333703, 0.3299404806269776169, 0.3333333333333333703, 0.3299404806269776169, 0.3333333333333333703, 0.3299404806269776169, 0.3333333333333333703, 0.3299404806269776169, 0.3333333333333333703, 0.3299404806269776169, 0.3333333333333333703, 0.3299404806269776169, 0.3333333333333333703, 0.3299404806269776169, 0.3333333333333333703, 0.3299404806269776169, 0.3333333333333333703, 0.3299404806269776169, 0.3333333333333333703, 0.3299404806269776169, 0.3333333333333333703, 0.3299404806269776169, 0.3333333333333333703, 0.3299404806269776169, 0.3333333333333333703, 0.3299404806269776169, 0.3333333333333333703, 0.3299404806269776169, 0.3333333333333333703, 0.3299404806269776169, 0.3333333333333333703, 0.3299404806269776169, 0.3333333333333333703, 0.3299404806269776169, 0.3333333333333333703, 0.3299404806269776169, 0.3333333333333333703, 0.3299404806269776169, 0.3333333333333333703, 0.3299404806269776169, 0.3333333333333333703, 0.3299404806269776169, 0.3333333333333333703, 0.3299404806269776169, 0.3333333333333333703, 0.3299404806269776169, 0.3333333333333333703, 0.3299404806269776169, 0.3333333333333333703, 0.3299404806269776169, 0.3333333333333333703, 0.3299404806269776169, 0.3333333333333333703, 0.3299404806269776169, 0.3333333333333333703, 0.3299404806269776169, 0.3333333333333333703, 0.3299404806269776169, 0.3333333333333333703, 0.3299404806269776169, 0.3333333333333333703, 0.3299404806269776169, 0.3333333333333333703, 0.3299404806269776169, 0.3333333333333333703, 0.3299404806269776169, 0.3333333333333333703, 0.3299404806269776169, 0.3333333333333333703, 0.3299404806269776169, 0.3333333333333333703, 0.3299404806269776169, 0.3333333333333333703, 0.3299404806269776169, 0.3333333333333333703, 0.3299404806269776169, 0.3333333333333333703, 0.3299404806269776169, 0.3333333333333333703, 0.3299404806269776169, 0.3333333333333333703, 0.3299404806269776169, 0.3333333333333333703, 0.3299404806269776169, 0.3333333333333333703, 0.3299404806269776169, 0.3333333333333333703, 0.3299404806269776169, 0.3333333333333333703, 0.3299404806269776169, 0.3333333333333333703, 0.3299404806269776169, 0.3333333333333333703, 0.3299404806269776169, 0.3333333333333333703, 0.3299404806269776169, 0.3333333333333333703, 0.3299404806269776169, 0.3333333333333333703, 0.3299404806269776169, 0.3333333333333333703, 0.3299404806269776169, 0.3333333333333333703, 0.3299404806269776169, 0.3333333333333333703, 0.3299404806269776169, 0.3333333333333333703, 0.3299404806269776169, 0.3333333333333333703, 0.3299404806269776169, 0.3333333333333333703, 0.3299404806269776169, 0.3333333333333333703, 0.3299404806269776169, 0.3333333333333333703, 0.3299404806269776169, 0.3333333333333333703, 0.3299404806269776169, 0.3333333333333333703, 0.3299404806269776169, 0.3333333333333333703, 0.3299404806269776169, 0.3333333333333333703, 0.3299404806269776169, 0.3333333333333333703, 0.3299404806269776169, 0.3333333333333333703, 0.3299404806269776169, 0.3333333333333333703, 0.3299404806269776169, 0.3333333333333333703, 0.3299404806269776169, 0.3333333333333333703, 0.3299404806269776169, 0.3333333333333333703, 0.3299404806269776169, 0.3333333333333333703, 0.3299404806269776169, 0.3333333333333333703, 0.3299404806269776169, 0.3333333333333333703, 0.3299404806269776169, 0.3333333333333333703, 0.3299404806269776169, 0.3333333333333333703, 0.3299404806269776169, 0.3333333333333333703, 0.3299404806269776169, 0.3333333333333333703, 0.3299404806269776169, 0.3333333333333333703, 0.3299404806269776169, 0.3333333333333333703, 0.3299404806269776169, 0.3333333333333333703, 0.3299404806269776169, 0.3333333333333333703, 0.3299404806269776169, 0.3333333333333333703, 0.3299404806269776169, 0.3333333333333333703, 0.3299404806269776169, 0.3333333333333333703, 0.3299404806269776169, 0.3333333333333333703, 0.3299404806269776169, 0.3333333333333333703, 0.3299404806269776169, 0.3333333333333333703, 0.3299404806269776169, 0.3333333333333333703, 0.3299404806269776169, 0.3333333333333333703, 0.3299404806269776169, 0.3333333333333333703, 0.3299404806269776169, 0.3333333333333333703, 0.3299404806269776169, 0.3333333333333333703, 0.3299404806269776169, 0.3333333333333333703, 0.3299404806269776169, 0.3333333333333333703, 0.3299404806269776169, 0.3333333333333333703, 0.3299404806269776169, 0.3333333333333333703, 0.3299404806269776169, 0.3333333333333333703, 0.3299404806269776169, 0.3333333333333333703, 0.3299404806269776169, 0.3333333333333333703, 0.3299404806269776169, 0.3333333333333333703, 0.3299404806269776169, 0.3333333333333333703, 0.3299404806269776169, 0.3333333333333333703, 0.3299404806269776169, 0.3333333333333333703, 0.3299404806269776169, 0.3333333333333333703, 0.3299404806269776169, 0.3333333333333333703, 0.3299404806269776169, 0.3333333333333333703, 0.3299404806269776169, 0.3333333333333333703, 0.3299404806269776169, 0.3333333333333333703, 0.3299404806269776169, 0.3333333333333333703, 0.3299404806269776169, 0.3333333333333333703, 0.3299404806269776169, 0.3333333333333333703, 0.3299404806269776169, 0.3333333333333333703, 0.3299404806269776169, 0.3333333333333333703, 0.3299404806269776169, 0.3333333333333333703, 0.3299404806269776169, 0.3333333333333333703, 0.3299404806269776169, 0.3333333333333333703, 0.3299404806269776169, 0.3333333333333333703, 0.3299404806269776169, 0.3333333333333333703, 0.3299404806269776169, 0.3333333333333333703, 0.3299404806269776169, 0.3333333333333333703, 0.3299404806269776169, 0.3333333333333333703, 0.3299404806269776169, 0.3333333333333333703, 0.3299404806269776169, 0.3333333333333333703, 0.3299404806269776169, 0.3333333333333333703, 0.3299404806269776169, 0.3333333333333333703, 0.3299404806269776169, 0.3333333333333333703, 0.3299404806269776169, 0.3333333333333333703, 0.3299404806269776169, 0.3333333333333333703, 0.3299404806269776169, 0.3333333333333333703, 0.3299404806269776169, 0.3333333333333333703, 0.3299404806269776169, 0.3333333333333333703, 0.3299404806269776169, 0.3333333333333333703, 0.3299404806269776169, 0.3333333333333333703, 0.3299404806269776169, 0.3333333333333333703, 0.3299404806269776169, 0.3333333333333333703, 0.3299404806269776169, 0.3333333333333333703, 0.3299404806269776169, 0.3333333333333333703, 0.3299404806269776169, 0.3333333333333333703, 0.3299404806269776169, 0.3333333333333333703, 0.3299404806269776169, 0.3333333333333333703, 0.3299404806269776169, 0.3333333333333333703, 0.3299404806269776169, 0.3333333333333333703, 0.3299404806269776169, 0.3333333333333333703, 0.3299404806269776169, 0.3333333333333333703, 0.3299404806269776169, 0.3333333333333333703, 0.3299404806269776169, 0.3333333333333333703, 0.3299404806269776169, 0.3333333333333333703, 0.3299404806269776169, 0.3333333333333333703, 0.3299404806269776169, 0.3333333333333333703, 0.3299404806269776169, 0.3333333333333333703, 0.3299404806269776169, 0.3333333333333333703, 0.3299404806269776169, 0.3333333333333333703, 0.3299404806269776169, 0.3333333333333333703, 0.3299404806269776169, 0.3333333333333333703, 0.3299404806269776169, 0.3333333333333333703, 0.3299404806269776169, 0.3333333333333333703, 0.3299404806269776169, 0.3333333333333333703, 0.3299404806269776169, 0.3333333333333333703, 0.3299404806269776169, 0.3333333333333333703, 0.3299404806269776169, 0.3333333333333333703, 0.3299404806269776169, 0.3333333333333333703, 0.3299404806269776169, 0.3333333333333333703, 0.3299404806269776169, 0.3333333333333333703, 0.3299404806269776169, 0.3333333333333333703, 0.3299404806269776169, 0.3333333333333333703, 0.3299404806269776169, 0.3333333333333333703, 0.3299404806269776169, 0.3333333333333333703, 0.3299404806269776169, 0.3333333333333333703, 0.3299404806269776169, 0.3333333333333333703, 0.3299404806269776169, 0.3333333333333333703, 0.3299404806269776169, 0.3333333333333333703, 0.3299404806269776169, 0.3333333333333333703, 0.3299404806269776169, 0.3333333333333333703, 0.3299404806269776169, 0.3333333333333333703, 0.3299404806269776169, 0.3333333333333333703, 0.3299404806269776169, 0.3333333333333333703, 0.3299404806269776169, 0.3333333333333333703, 0.3299404806269776169, 0.3333333333333333703, 0.3299404806269776169, 0.3333333333333333703, 0.3299404806269776169, 0.3333333333333333703, 0.3299404806269776169, 0.3333333333333333703, 0.3299404806269776169, 0.3333333333333333703, 0.3299404806269776169, 0.3333333333333333703, 0.3299404806269776169, 0.3333333333333333703, 0.3299404806269776169, 0.3333333333333333703, 0.3299404806269776169, 0.3333333333333333703, 0.3299404806269776169, 0.3333333333333333703, 0.3299404806269776169, 0.3333333333333333703, 0.3299404806269776169, 0.3333333333333333703, 0.3299404806269776169, 0.3333333333333333703, 0.3299404806269776169, 0.3333333333333333703, 0.3299404806269776169, 0.3333333333333333703, 0.3299404806269776169, 0.3333333333333333703, 0.3299404806269776169, 0.3333333333333333703, 0.3299404806269776169, 0.3333333333333333703, 0.3299404806269776169, 0.3333333333333333703, 0.3299404806269776169, 0.3333333333333333703, 0.3299404806269776169, 0.3333333333333333703, 0.3299404806269776169, 0.3333333333333333703, 0.3299404806269776169, 0.3333333333333333703, 0.3299404806269776169, 0.3333333333333333703, 0.3299404806269776169, 0.3333333333333333703, 0.3299404806269776169, 0.3333333333333333703, 0.3299404806269776169, 0.3333333333333333703, 0.3299404806269776169, 0.3333333333333333703, 0.3299404806269776169, 0.3333333333333333703, 0.3299404806269776169, 0.3333333333333333703, 0.3299404806269776169, 0.3333333333333333703, 0.3299404806269776169, 0.3333333333333333703, 0.3299404806269776169, 0.3333333333333333703, 0.3299404806269776169, 0.3333333333333333703, 0.3299404806269776169, 0.3333333333333333703, 0.3299404806269776169, 0.3333333333333333703, 0.3299404806269776169, 0.3333333333333333703, 0.3299404806269776169, 0.3333333333333333703, 0.3299404806269776169, 0.3333333333333333703, 0.3320603117974822438, 0.3317425830320511193),
 ( 1.000000000000000000, 0.9898214418809326842, 1.000000000000000000, 0.9898214418809326842, 1.000000000000000000, 0.9898214418809326842, 1.000000000000000000, 0.9898214418809326842, 1.000000000000000000, 0.9898214418809326842, 1.000000000000000000, 0.9898214418809326842, 1.000000000000000000, 0.9898214418809326842, 1.000000000000000000, 0.9898214418809326842, 1.000000000000000000, 0.9898214418809326842, 1.000000000000000000, 0.9898214418809326842, 1.000000000000000000, 0.9898214418809326842, 1.000000000000000000, 0.9898214418809326842, 1.000000000000000000, 0.9898214418809326842, 1.000000000000000000, 0.9898214418809326842, 1.000000000000000000, 0.9898214418809326842, 1.000000000000000000, 0.9898214418809326842, 1.000000000000000000, 0.9898214418809326842, 1.000000000000000000, 0.9898214418809326842, 1.000000000000000000, 0.9898214418809326842, 1.000000000000000000, 0.9898214418809326842, 1.000000000000000000, 0.9898214418809326842, 1.000000000000000000, 0.9898214418809326842, 1.000000000000000000, 0.9898214418809326842, 1.000000000000000000, 0.9898214418809326842, 1.000000000000000000, 0.9898214418809326842, 1.000000000000000000, 0.9898214418809326842, 1.000000000000000000, 0.9898214418809326842, 1.000000000000000000, 0.9898214418809326842, 1.000000000000000000, 0.9898214418809326842, 1.000000000000000000, 0.9898214418809326842, 1.000000000000000000, 0.9898214418809326842, 1.000000000000000000, 0.9898214418809326842, 1.000000000000000000, 0.9898214418809326842, 1.000000000000000000, 0.9898214418809326842, 1.000000000000000000, 0.9898214418809326842, 1.000000000000000000, 0.9898214418809326842, 1.000000000000000000, 0.9898214418809326842, 1.000000000000000000, 0.9898214418809326842, 1.000000000000000000, 0.9898214418809326842, 1.000000000000000000, 0.9898214418809326842, 1.000000000000000000, 0.9898214418809326842, 1.000000000000000000, 0.9898214418809326842, 1.000000000000000000, 0.9898214418809326842, 1.000000000000000000, 0.9898214418809326842, 1.000000000000000000, 0.9898214418809326842, 1.000000000000000000, 0.9898214418809326842, 1.000000000000000000, 0.9898214418809326842, 1.000000000000000000, 0.9898214418809326842, 1.000000000000000000, 0.9898214418809326842, 1.000000000000000000, 0.9898214418809326842, 1.000000000000000000, 0.9898214418809326842, 1.000000000000000000, 0.9898214418809326842, 1.000000000000000000, 0.9898214418809326842, 1.000000000000000000, 0.9898214418809326842, 1.000000000000000000, 0.9898214418809326842, 1.000000000000000000, 0.9898214418809326842, 1.000000000000000000, 0.9898214418809326842, 1.000000000000000000, 0.9898214418809326842, 1.000000000000000000, 0.9898214418809326842, 1.000000000000000000, 0.9898214418809326842, 1.000000000000000000, 0.9898214418809326842, 1.000000000000000000, 0.9898214418809326842, 1.000000000000000000, 0.9898214418809326842, 1.000000000000000000, 0.9898214418809326842, 1.000000000000000000, 0.9898214418809326842, 1.000000000000000000, 0.9898214418809326842, 1.000000000000000000, 0.9898214418809326842, 1.000000000000000000, 0.9898214418809326842, 1.000000000000000000, 0.9898214418809326842, 1.000000000000000000, 0.9898214418809326842, 1.000000000000000000, 0.9898214418809326842, 1.000000000000000000, 0.9898214418809326842, 1.000000000000000000, 0.9898214418809326842, 1.000000000000000000, 0.9898214418809326842, 1.000000000000000000, 0.9898214418809326842, 1.000000000000000000, 0.9898214418809326842, 1.000000000000000000, 0.9898214418809326842, 1.000000000000000000, 0.9898214418809326842, 1.000000000000000000, 0.9898214418809326842, 1.000000000000000000, 0.9898214418809326842, 1.000000000000000000, 0.9898214418809326842, 1.000000000000000000, 0.9898214418809326842, 1.000000000000000000, 0.9898214418809326842, 1.000000000000000000, 0.9898214418809326842, 1.000000000000000000, 0.9898214418809326842, 1.000000000000000000, 0.9898214418809326842, 1.000000000000000000, 0.9898214418809326842, 1.000000000000000000, 0.9898214418809326842, 1.000000000000000000, 0.9898214418809326842, 1.000000000000000000, 0.9898214418809326842, 1.000000000000000000, 0.9898214418809326842, 1.000000000000000000, 0.9898214418809326842, 1.000000000000000000, 0.9898214418809326842, 1.000000000000000000, 0.9898214418809326842, 1.000000000000000000, 0.9898214418809326842, 1.000000000000000000, 0.9898214418809326842, 1.000000000000000000, 0.9898214418809326842, 1.000000000000000000, 0.9898214418809326842, 1.000000000000000000, 0.9898214418809326842, 1.000000000000000000, 0.9898214418809326842, 1.000000000000000000, 0.9898214418809326842, 1.000000000000000000, 0.9898214418809326842, 1.000000000000000000, 0.9898214418809326842, 1.000000000000000000, 0.9898214418809326842, 1.000000000000000000, 0.9898214418809326842, 1.000000000000000000, 0.9898214418809326842, 1.000000000000000000, 0.9898214418809326842, 1.000000000000000000, 0.9898214418809326842, 1.000000000000000000, 0.9898214418809326842, 1.000000000000000000, 0.9898214418809326842, 1.000000000000000000, 0.9898214418809326842, 1.000000000000000000, 0.9898214418809326842, 1.000000000000000000, 0.9898214418809326842, 1.000000000000000000, 0.9898214418809326842, 1.000000000000000000, 0.9898214418809326842, 1.000000000000000000, 0.9898214418809326842, 1.000000000000000000, 0.9898214418809326842, 1.000000000000000000, 0.9898214418809326842, 1.000000000000000000, 0.9898214418809326842, 1.000000000000000000, 0.9898214418809326842, 1.000000000000000000, 0.9898214418809326842, 1.000000000000000000, 0.9898214418809326842, 1.000000000000000000, 0.9898214418809326842, 1.000000000000000000, 0.9898214418809326842, 1.000000000000000000, 0.9898214418809326842, 1.000000000000000000, 0.9898214418809326842, 1.000000000000000000, 0.9898214418809326842, 1.000000000000000000, 0.9898214418809326842, 1.000000000000000000, 0.9898214418809326842, 1.000000000000000000, 0.9898214418809326842, 1.000000000000000000, 0.9898214418809326842, 1.000000000000000000, 0.9898214418809326842, 1.000000000000000000, 0.9898214418809326842, 1.000000000000000000, 0.9898214418809326842, 1.000000000000000000, 0.9898214418809326842, 1.000000000000000000, 0.9898214418809326842, 1.000000000000000000, 0.9898214418809326842, 1.000000000000000000, 0.9898214418809326842, 1.000000000000000000, 0.9898214418809326842, 1.000000000000000000, 0.9898214418809326842, 1.000000000000000000, 0.9898214418809326842, 1.000000000000000000, 0.9898214418809326842, 1.000000000000000000, 0.9898214418809326842, 1.000000000000000000, 0.9898214418809326842, 1.000000000000000000, 0.9898214418809326842, 1.000000000000000000, 0.9898214418809326842, 1.000000000000000000, 0.9898214418809326842, 1.000000000000000000, 0.9898214418809326842, 1.000000000000000000, 0.9898214418809326842, 1.000000000000000000, 0.9898214418809326842, 1.000000000000000000, 0.9898214418809326842, 1.000000000000000000, 0.9898214418809326842, 1.000000000000000000, 0.9898214418809326842, 1.000000000000000000, 0.9898214418809326842, 1.000000000000000000, 0.9898214418809326842, 1.000000000000000000, 0.9898214418809326842, 1.000000000000000000, 0.9898214418809326842, 1.000000000000000000, 0.9898214418809326842, 1.000000000000000000, 0.9898214418809326842, 1.000000000000000000, 0.9898214418809326842, 1.000000000000000000, 0.9898214418809326842, 1.000000000000000000, 0.9898214418809326842, 1.000000000000000000, 0.9898214418809326842, 1.000000000000000000, 0.9898214418809326842, 1.000000000000000000, 0.9898214418809326842, 1.000000000000000000, 0.9898214418809326842, 1.000000000000000000, 0.9898214418809326842, 1.000000000000000000, 0.9898214418809326842, 1.000000000000000000, 0.9898214418809326842, 1.000000000000000000, 0.9898214418809326842, 1.000000000000000000, 0.9898214418809326842, 1.000000000000000000, 0.9898214418809326842, 1.000000000000000000, 0.9898214418809326842, 1.000000000000000000, 0.9898214418809326842, 1.000000000000000000, 0.9898214418809326842, 1.000000000000000000, 0.9898214418809326842, 1.000000000000000000, 0.9898214418809326842, 1.000000000000000000, 0.9898214418809326842, 1.000000000000000000, 0.9898214418809326842, 1.000000000000000000, 0.9898214418809326842, 1.000000000000000000, 0.9898214418809326842, 1.000000000000000000, 0.9898214418809326842, 1.000000000000000000, 0.9898214418809326842, 1.000000000000000000, 0.9898214418809326842, 1.000000000000000000, 0.9898214418809326842, 1.000000000000000000, 0.9898214418809326842, 1.000000000000000000, 0.9898214418809326842, 1.000000000000000000, 0.9898214418809326842, 1.000000000000000000, 0.9898214418809326842, 1.000000000000000000, 0.9898214418809326842, 1.000000000000000000, 0.9898214418809326842, 1.000000000000000000, 0.9898214418809326842, 1.000000000000000000, 0.9898214418809326842, 1.000000000000000000, 0.9898214418809326842, 1.000000000000000000, 0.9898214418809326842, 1.000000000000000000, 0.9898214418809326842, 1.000000000000000000, 0.9898214418809326842, 1.000000000000000000, 0.9898214418809326842, 1.000000000000000000, 0.9898214418809326842, 1.000000000000000000, 0.9898214418809326842, 1.000000000000000000, 0.9898214418809326842, 1.000000000000000000, 0.9898214418809326842, 1.000000000000000000, 0.9898214418809326842, 1.000000000000000000, 0.9898214418809326842, 1.000000000000000000, 0.9898214418809326842, 1.000000000000000000, 0.9898214418809326842, 1.000000000000000000, 0.9898214418809326842, 1.000000000000000000, 0.9898214418809326842, 1.000000000000000000, 0.9898214418809326842, 1.000000000000000000, 0.9898214418809326842, 1.000000000000000000, 0.9898214418809326842, 1.000000000000000000, 0.9898214418809326842, 1.000000000000000000, 0.9898214418809326842, 1.000000000000000000, 0.9898214418809326842, 1.000000000000000000, 0.9898214418809326842, 1.000000000000000000, 0.9898214418809326842, 1.000000000000000000, 0.9898214418809326842, 1.000000000000000000, 0.9898214418809326842, 1.000000000000000000, 0.9898214418809326842, 1.000000000000000000, 0.9898214418809326842, 1.000000000000000000, 0.9898214418809326842, 1.000000000000000000, 0.9898214418809326842, 1.000000000000000000, 0.9898214418809326842, 1.000000000000000000, 0.9898214418809326842, 1.000000000000000000, 0.9898214418809326842, 1.000000000000000000, 0.9898214418809326842, 1.000000000000000000, 0.9898214418809326842, 1.000000000000000000, 0.9898214418809326842, 1.000000000000000000, 0.9898214418809326842, 1.000000000000000000, 0.9898214418809326842, 1.000000000000000000, 0.9898214418809326842, 1.000000000000000000, 0.9898214418809326842, 1.000000000000000000, 0.9898214418809326842, 1.000000000000000000, 0.9898214418809326842, 1.000000000000000000, 0.9898214418809326842, 1.000000000000000000, 0.9898214418809326842, 1.000000000000000000, 0.9898214418809326842, 1.000000000000000000, 0.9898214418809326842, 1.000000000000000000, 0.9898214418809326842, 1.000000000000000000, 0.9898214418809326842, 1.000000000000000000, 0.9898214418809326842, 1.000000000000000000, 0.9898214418809326842, 1.000000000000000000, 0.9898214418809326842, 1.000000000000000000, 0.9898214418809326842, 1.000000000000000000, 0.9898214418809326842, 1.000000000000000000, 0.9898214418809326842, 1.000000000000000000, 0.9898214418809326842, 1.000000000000000000, 0.9898214418809326842, 1.000000000000000000, 0.9898214418809326842, 1.000000000000000000, 0.9898214418809326842, 1.000000000000000000, 0.9898214418809326842, 1.000000000000000000, 0.9898214418809326842, 1.000000000000000000, 0.9898214418809326842, 1.000000000000000000, 0.9898214418809326842, 1.000000000000000000, 0.9898214418809326842, 1.000000000000000000, 0.9898214418809326842, 1.000000000000000000, 0.9898214418809326842, 1.000000000000000000, 0.9898214418809326842, 1.000000000000000000, 0.9898214418809326842, 1.000000000000000000, 0.9898214418809326842, 1.000000000000000000, 0.9898214418809326842, 1.000000000000000000, 0.9898214418809326842, 1.000000000000000000, 0.9898214418809326842, 1.000000000000000000, 0.9898214418809326842, 1.000000000000000000, 0.9898214418809326842, 1.000000000000000000, 0.9898214418809326842, 1.000000000000000000, 0.9898214418809326842, 1.000000000000000000, 0.9898214418809326842, 1.000000000000000000, 0.9898214418809326842, 1.000000000000000000, 0.9898214418809326842, 1.000000000000000000, 0.9898214418809326842, 1.000000000000000000, 0.9898214418809326842, 1.000000000000000000, 0.9898214418809326842, 1.000000000000000000, 0.9898214418809326842, 1.000000000000000000, 0.9898214418809326842, 1.000000000000000000, 0.9898214418809326842, 1.000000000000000000, 0.9898214418809326842, 1.000000000000000000, 0.9898214418809326842, 1.000000000000000000, 0.9898214418809326842, 1.000000000000000000, 0.9898214418809326842, 1.000000000000000000, 0.9898214418809326842, 1.000000000000000000, 0.9898214418809326842, 1.000000000000000000, 0.9898214418809326842, 1.000000000000000000, 0.9898214418809326842, 1.000000000000000000, 0.9898214418809326842, 1.000000000000000000, 0.9898214418809326842, 1.000000000000000000, 0.9898214418809326842, 1.000000000000000000, 0.9898214418809326842, 1.000000000000000000, 0.9898214418809326842, 1.000000000000000000, 0.9898214418809326842, 1.000000000000000000, 0.9898214418809326842, 1.000000000000000000, 0.9898214418809326842, 1.000000000000000000, 0.9898214418809326842, 1.000000000000000000, 0.9898214418809326842, 1.000000000000000000, 0.9898214418809326842, 1.000000000000000000, 0.9898214418809326842, 1.000000000000000000, 0.9898214418809326842, 1.000000000000000000, 0.9898214418809326842, 1.000000000000000000, 0.9898214418809326842, 1.000000000000000000, 0.9898214418809326842, 1.000000000000000000, 0.9898214418809326842, 1.000000000000000000, 0.9898214418809326842, 1.000000000000000000, 0.9898214418809326842, 1.000000000000000000, 0.9898214418809326842, 1.000000000000000000, 0.9898214418809326842, 1.000000000000000000, 0.9898214418809326842, 1.000000000000000000, 0.9898214418809326842, 1.000000000000000000, 0.9898214418809326842, 1.000000000000000000, 0.9898214418809326842, 1.000000000000000000, 0.9898214418809326842, 1.000000000000000000, 0.9898214418809326842, 1.000000000000000000, 0.9898214418809326842, 1.000000000000000000, 0.9898214418809326842, 1.000000000000000000, 0.9898214418809326842, 1.000000000000000000, 0.9898214418809326842, 1.000000000000000000, 0.9898214418809326842, 1.000000000000000000, 0.9898214418809326842, 1.000000000000000000, 0.9898214418809326842, 1.000000000000000000, 0.9898214418809326842, 1.000000000000000000, 0.9898214418809326842, 1.000000000000000000, 0.9898214418809326842, 1.000000000000000000, 0.9898214418809326842, 1.000000000000000000, 0.9898214418809326842, 1.000000000000000000, 0.9898214418809326842, 1.000000000000000000, 0.9898214418809326842, 1.000000000000000000, 0.9898214418809326842, 1.000000000000000000, 0.9898214418809326842, 1.000000000000000000, 0.9898214418809326842, 1.000000000000000000, 0.9898214418809326842, 1.000000000000000000, 0.9898214418809326842, 1.000000000000000000, 0.9898214418809326842, 1.000000000000000000, 0.9898214418809326842, 1.000000000000000000, 0.9898214418809326842, 1.000000000000000000, 0.9898214418809326842, 1.000000000000000000, 0.9898214418809326842, 1.000000000000000000, 0.9898214418809326842, 1.000000000000000000, 0.9898214418809326842, 1.000000000000000000, 0.9898214418809326842, 1.000000000000000000, 0.9898214418809326842, 1.000000000000000000, 0.9898214418809326842, 1.000000000000000000, 0.9898214418809326842, 1.000000000000000000, 0.9898214418809326842, 1.000000000000000000, 0.9898214418809326842, 1.000000000000000000, 0.9898214418809326842, 1.000000000000000000, 0.9898214418809326842, 1.000000000000000000, 0.9898214418809326842, 1.000000000000000000, 0.9898214418809326842, 1.000000000000000000, 0.9898214418809326842, 1.000000000000000000, 0.9898214418809326842, 1.000000000000000000, 0.9898214418809326842, 1.000000000000000000, 0.9898214418809326842, 1.000000000000000000, 0.9898214418809326842, 1.000000000000000000, 0.9898214418809326842, 1.000000000000000000, 0.9898214418809326842, 1.000000000000000000, 0.9898214418809326842, 1.000000000000000000, 0.9898214418809326842, 1.000000000000000000, 0.9898214418809326842, 1.000000000000000000, 0.9898214418809326842, 1.000000000000000000, 0.9898214418809326842, 1.000000000000000000, 0.9898214418809326842, 1.000000000000000000, 0.9898214418809326842, 1.000000000000000000, 0.9898214418809326842, 1.000000000000000000, 0.9898214418809326842, 1.000000000000000000, 0.9898214418809326842, 1.000000000000000000, 0.9898214418809326842, 1.000000000000000000, 0.9898214418809326842, 1.000000000000000000, 0.9898214418809326842, 1.000000000000000000, 0.9898214418809326842, 1.000000000000000000, 0.9898214418809326842, 1.000000000000000000, 0.9898214418809326842, 1.000000000000000000, 0.9898214418809326842, 1.000000000000000000, 0.9898214418809326842, 1.000000000000000000, 0.9898214418809326842, 1.000000000000000000, 0.9898214418809326842, 1.000000000000000000, 0.9898214418809326842, 1.000000000000000000, 0.9898214418809326842, 1.000000000000000000, 0.9898214418809326842, 1.000000000000000000, 0.9898214418809326842, 1.000000000000000000, 0.9898214418809326842, 1.000000000000000000, 0.9898214418809326842, 1.000000000000000000, 0.9898214418809326842, 1.000000000000000000, 0.9898214418809326842, 1.000000000000000000, 0.9898214418809326842, 1.000000000000000000, 0.9898214418809326842, 1.000000000000000000, 0.9898214418809326842, 1.000000000000000000, 0.9898214418809326842, 1.000000000000000000, 0.9898214418809326842, 1.000000000000000000, 0.9898214418809326842, 1.000000000000000000, 0.9898214418809326842, 1.000000000000000000, 0.9898214418809326842, 1.000000000000000000, 0.9898214418809326842, 1.000000000000000000, 0.9898214418809326842, 1.000000000000000000, 0.9898214418809326842, 1.000000000000000000, 0.9898214418809326842, 1.000000000000000000, 0.9898214418809326842, 1.000000000000000000, 0.9898214418809326842, 1.000000000000000000, 0.9898214418809326842, 1.000000000000000000, 0.9898214418809326842, 1.000000000000000000, 0.9898214418809326842, 1.000000000000000000, 0.9898214418809326842, 1.000000000000000000, 0.9898214418809326842, 1.000000000000000000, 0.9898214418809326842, 1.000000000000000000, 0.9898214418809326842, 1.000000000000000000, 0.9898214418809326842, 1.000000000000000000, 0.9898214418809326842, 1.000000000000000000, 0.9898214418809326842, 1.000000000000000000, 0.9898214418809326842, 1.000000000000000000, 0.9898214418809326842, 1.000000000000000000, 0.9898214418809326842, 1.000000000000000000, 0.9898214418809326842, 1.000000000000000000, 0.9898214418809326842, 1.000000000000000000, 0.9898214418809326842, 1.000000000000000000, 0.9898214418809326842, 1.000000000000000000, 0.9898214418809326842, 1.000000000000000000, 0.9898214418809326842, 1.000000000000000000, 0.9898214418809326842, 1.000000000000000000, 0.9898214418809326842, 1.000000000000000000, 0.9898214418809326842, 1.000000000000000000, 0.9898214418809326842, 1.000000000000000000, 0.9898214418809326842, 1.000000000000000000, 0.9898214418809326842, 1.000000000000000000, 0.9898214418809326842, 1.000000000000000000, 0.9898214418809326842, 1.000000000000000000, 0.9898214418809326842, 1.000000000000000000, 0.9898214418809326842, 1.000000000000000000, 0.9898214418809326842, 1.000000000000000000, 0.9898214418809326842, 1.000000000000000000, 0.9898214418809326842, 1.000000000000000000, 0.9898214418809326842, 1.000000000000000000, 0.9898214418809326842, 1.000000000000000000, 0.9961809353924466759, 0.9952277490961531914) ) ) 
 REPRESENTATION_ITEM ( '' )  SURFACE ( )  );
#25891=CARTESIAN_POINT ( 'NONE',  ( 745.1769319972822814, -161.8055962898689870, 346.2694204179732083 ) ) ;
#25896=CARTESIAN_POINT ( 'NONE',  ( 792.1044303154645831, -252.4527844766015789, 317.8323909638837677 ) ) ;
#25897=CARTESIAN_POINT ( 'NONE',  ( 805.1927285166399315, -256.8164208402379245, 341.8018195045277707 ) ) ;
#25901=CARTESIAN_POINT ( 'NONE',  ( 755.0488828828309806, 6.194403710130517382, 344.1219089521771934 ) ) ;
#25904=CARTESIAN_POINT ( 'NONE',  ( 808.0189434323515343, -182.0891481129654323, 319.0252816721025511 ) ) ;
#25905=CARTESIAN_POINT ( 'NONE',  ( 804.4086373105744769, -265.6454272087889876, 333.3843516231986541 ) ) ;
#25906=CARTESIAN_POINT ( 'NONE',  ( 790.8726784830453198, -394.7146871989591546, 362.5472867521010585 ) ) ;
#25909=CARTESIAN_POINT ( 'NONE',  ( 748.3538107759620743, -208.7146871989596946, 355.8262568251490165 ) ) ;
#25914=CARTESIAN_POINT ( 'NONE',  ( 805.1016975059191054, -270.8965053807777394, 343.0745993439771837 ) ) ;
#25921=CARTESIAN_POINT ( 'NONE',  ( 768.9521613784389729, -177.8272453906074304, 373.2346286133773106 ) ) ;
#25926=CARTESIAN_POINT ( 'NONE',  ( 808.3070685750230950, -18.99823902205683979, 361.1904061080339261 ) ) ;
#25927=VECTOR ( 'NONE', #45309, 1000.000000000000000 ) ;
#25932=CARTESIAN_POINT ( 'NONE',  ( 754.8072714833581358, -28.81642084023863148, 338.1981804954720587 ) ) ;
#25933=CARTESIAN_POINT ( 'NONE',  ( 797.8822607201568644, -270.5545181178798657, 370.1134526219340160 ) ) ;
#25935=CARTESIAN_POINT ( 'NONE',  ( 814.9108240113580450, -256.2709662947834204, 337.5031285880265273 ) ) ;
#25939=CARTESIAN_POINT ( 'NONE',  ( 797.6776695296629214, -355.5436935675103882, 357.6776695296636603 ) ) ;
#25940=CARTESIAN_POINT ( 'NONE',  ( 793.0897708529556667, -102.5545181178804057, 361.3366627262616362 ) ) ;
#25944=CARTESIAN_POINT ( 'NONE',  ( 804.6798772138708955, -399.7255117493283478, 334.6312213355107019 ) ) ;
#25945=ORIENTED_EDGE ( 'NONE', *, *, #36798, .T. ) ;
#25947=CARTESIAN_POINT ( 'NONE',  ( 764.8639956371174549, -152.0891481129655460, 319.7806653035542013 ) ) ;
#25950=CARTESIAN_POINT ( 'NONE',  ( 810.1134526219336749, -440.5328690171407970, 357.8822607201570349 ) ) ;
#25952=CARTESIAN_POINT ( 'NONE',  ( 781.7834795799800531, -346.8164208402376971, 315.0636971347436202 ) ) ;
#25955=CARTESIAN_POINT ( 'NONE',  ( 756.3353852180819104, -437.9073299311463074, 331.1735550268788302 ) ) ;
#25962=CARTESIAN_POINT ( 'NONE',  ( 799.2566176426618085, -456.0090635724247932, 324.0069404352559559 ) ) ;
#25963=CARTESIAN_POINT ( 'NONE',  ( 758.8095938919642549, -224.0891481129653187, 311.6929314249763365 ) ) ;
#25964=CARTESIAN_POINT ( 'NONE',  ( 759.2295555964440155, -160.1692326535053326, 353.9708237608231229 ) ) ;
#25971=CARTESIAN_POINT ( 'NONE',  ( 793.5525998758768083, -79.09997266333503774, 372.6845335610516941 ) ) ;
#25977=DIRECTION ( 'NONE',  ( -1.000000000000000000, 0.000000000000000000, 0.000000000000000000 ) ) ;
#25979=CARTESIAN_POINT ( 'NONE',  ( 780.5236548040995785, -404.7363362996975980, 314.9735926884559944 ) ) ;
#25984=CARTESIAN_POINT ( 'NONE',  ( 799.9636004259356241, -190.9181544815164955, 311.2241431872006956 ) ) ;
#25986=CARTESIAN_POINT ( 'NONE',  ( 813.1304606946830518, -161.9073299311472454, 352.3570229623690580 ) ) ;
#25990=CARTESIAN_POINT ( 'NONE',  ( 791.9812246680005501, -212.6346026584198796, 361.9419747391813189 ) ) ;
#25991=CARTESIAN_POINT ( 'NONE',  ( 766.9102291470427417, -18.55451811788065797, 318.6633372737382501 ) ) ;
#25995=CARTESIAN_POINT ( 'NONE',  ( 768.8385539511368734, -23.26014174441484883, 306.4236121716840557 ) ) ;
#25998=CARTESIAN_POINT ( 'NONE',  ( 794.9819416627830151, -36.99823902205679360, 319.9864689768909898 ) ) ;
#26001=CARTESIAN_POINT ( 'NONE',  ( 776.2433038121456548, -348.8965053807774552, 374.8207195650711014 ) ) ;
#26003=CARTESIAN_POINT ( 'NONE',  ( 795.6651683502461765, -418.7146871989590409, 371.3240766477733814 ) ) ;
#26005=CARTESIAN_POINT ( 'NONE',  ( 771.2633955100217236, -335.9073299311468190, 363.4237431249939618 ) ) ;
#26013=CARTESIAN_POINT ( 'NONE',  ( 800.2193346964447755, -42.99823902205675807, 355.1360043628815788 ) ) ;
#26014=CARTESIAN_POINT ( 'NONE',  ( 783.0745993439762742, -368.1908817542433212, 365.1016975059196739 ) ) ;
#26016=CARTESIAN_POINT ( 'NONE',  ( 782.4968714119720516, -418.8164208402374129, 305.0891759886411023 ) ) ;
#26018=CARTESIAN_POINT ( 'NONE',  ( 776.2433038121456548, -324.8965053807775121, 374.8207195650711014 ) ) ;
#26019=CARTESIAN_POINT ( 'NONE',  ( 746.0683387631852383, -91.44195992623282621, 331.3260364891676204 ) ) ;
#26025=CARTESIAN_POINT ( 'NONE',  ( 772.4837098697144029, -431.3618753856918033, 374.5518280994205611 ) ) ;
#26031=ADVANCED_FACE ( 'NONE', ( #40810 ), #5245, .F. ) ;
#26032=CARTESIAN_POINT ( 'NONE',  ( 759.0159684113467620, -304.9181544815161828, 325.8855110935213020 ) ) ;
#26033=CARTESIAN_POINT ( 'NONE',  ( 762.3223304703356007, -175.5436935675108998, 322.3223304703362828 ) ) ;
#26036=CARTESIAN_POINT ( 'NONE',  ( 773.3843516231979720, -325.4419599262320162, 364.4086373105754433 ) ) ;
#26037=CARTESIAN_POINT ( 'NONE',  ( 795.8262568251477660, -70.37269993606230400, 308.3538107759623585 ) ) ;
#26040=CARTESIAN_POINT ( 'NONE',  ( 792.1044303154645831, -132.4527844766018916, 317.8323909638837677 ) ) ;
#26042=VERTEX_POINT ( 'NONE', #30647 ) ;
#26046=CARTESIAN_POINT ( 'NONE',  ( 766.0291762391763086, -10.91815448151704793, 360.7704444035551319 ) ) ;
#26049=CARTESIAN_POINT ( 'NONE',  ( 786.6156483768007774, -385.4419599262319593, 315.5913626894246136 ) ) ;
#26051=CARTESIAN_POINT ( 'NONE',  ( 766.7756240680305382, -86.53286901714194812, 361.5560724626415663 ) ) ;
#26056=CARTESIAN_POINT ( 'NONE',  ( 766.5853460496234675, -253.9874144716868329, 372.3518521366060554 ) ) ;
#26057=CARTESIAN_POINT ( 'NONE',  ( 802.1676090361155502, -62.63460265842032726, 327.8955696845344505 ) ) ;
#26060=CARTESIAN_POINT ( 'NONE',  ( 778.2165204200184689, -238.8164208402379813, 364.9363028652563230 ) ) ;
#26067=CARTESIAN_POINT ( 'NONE',  ( 808.0189434323515343, -278.0891481129651197, 319.0252816721025511 ) ) ;
#26068=CARTESIAN_POINT ( 'NONE',  ( 788.7631598425961101, -25.44195992623301450, 305.7194118038759143 ) ) ;
#26074=CARTESIAN_POINT ( 'NONE',  ( 764.8639956371174549, -224.0891481129653187, 319.7806653035542013 ) ) ;
#26078=CARTESIAN_POINT ( 'NONE',  ( 804.7487373415286811, -331.5436935675104451, 364.7487373415288516 ) ) ;
#26081=CARTESIAN_POINT ( 'NONE',  ( 765.8855110935204493, -358.1692326535047641, 319.0159684113471599 ) ) ;
#26085=CARTESIAN_POINT ( 'NONE',  ( 793.0897708529556667, -198.5545181178800647, 361.3366627262616362 ) ) ;
#26086=CARTESIAN_POINT ( 'NONE',  ( 804.4286716492782716, -65.36187538569306810, 345.3141322388244703 ) ) ;
#26090=CARTESIAN_POINT ( 'NONE',  ( 804.9511171171677688, -221.8055962898687881, 335.8780910478229202 ) ) ;
#26094=CARTESIAN_POINT ( 'NONE',  ( 772.4837098697144029, -431.3618753856918033, 374.5518280994205611 ) ) ;
#26095=DIRECTION ( 'NONE',  ( -0.000000000000000000, 1.000000000000000000, -0.000000000000000000 ) ) ;
#26099=EDGE_CURVE ( 'NONE', #14626, #18157, #31826, .T. ) ;
#26100=CARTESIAN_POINT ( 'NONE',  ( 763.0537975583475827, -48.45278447660219712, 371.0346526505627480 ) ) ;
#26101=CARTESIAN_POINT ( 'NONE',  ( 751.9810565676468741, -122.0891481129656171, 360.9747183278973921 ) ) ;
#26104=CARTESIAN_POINT ( 'NONE',  ( 749.5768839229115201, -396.5545181178794678, 358.0661480581553064 ) ) ;
#26106=CARTESIAN_POINT ( 'NONE',  ( 755.2512626584698410, -367.5436935675102745, 315.2512626584710915 ) ) ;
#26108=CARTESIAN_POINT ( 'NONE',  ( 780.5290396650775619, 11.64894916467595642, 365.2837595273619513 ) ) ;
#26113=ADVANCED_FACE ( 'NONE', ( #19124 ), #33212, .T. ) ;
#26114=CARTESIAN_POINT ( 'NONE',  ( 754.0944755984390895, -135.6237781080508853, 364.1009440267246760 ) ) ;
#26115=CARTESIAN_POINT ( 'NONE',  ( 804.9363028652555840, -424.2709662947829088, 338.2165204200192079 ) ) ;
#26117=CARTESIAN_POINT ( 'NONE',  ( 747.3154664389472828, -163.9874144716871456, 326.4474001241230781 ) ) ;
#26121=CARTESIAN_POINT ( 'NONE',  ( 792.1044303154645831, -132.4527844766018916, 317.8323909638837677 ) ) ;
#26123=CARTESIAN_POINT ( 'NONE',  ( 767.8955696845333705, -264.4527844766016074, 362.1676090361162323 ) ) ;
#26124=CARTESIAN_POINT ( 'NONE',  ( 756.3353852180820240, -269.9073299311469327, 331.1735550268787733 ) ) ;
#26127=CARTESIAN_POINT ( 'NONE',  ( 801.3366627262608972, 15.46713098285775878, 353.0897708529566899 ) ) ;
#26132=CIRCLE ( 'NONE', #13617, 30.00000000000008171 ) ;
#26133=CARTESIAN_POINT ( 'NONE',  ( 777.4774526936600978, -202.2709662947835341, 304.7301800767028226 ) ) ;
#26134=CARTESIAN_POINT ( 'NONE',  ( 796.9571628226829034, -287.4636090269708575, 321.2382568024804641 ) ) ;
#26135=CARTESIAN_POINT ( 'NONE',  ( 756.1348686366196716, -401.2601417444137155, 347.5531968255698416 ) ) ;
#26144=CARTESIAN_POINT ( 'NONE',  ( 755.8398074228967971, -259.4419599262322436, 333.4516893846970333 ) ) ;
#26146=DIRECTION ( 'NONE',  ( -0.7014439490181308967, 0.1263042864341425708, 0.7014439490181749726 ) ) ;
#26152=VECTOR ( 'NONE', #39085, 1000.000000000000000 ) ;
#26153=CARTESIAN_POINT ( 'NONE',  ( 762.1177392798416577, -162.5545181178802352, 309.8865473780659272 ) ) ;
#26163=CIRCLE ( 'NONE', #35797, 30.00000000000008171 ) ;
#26165=CARTESIAN_POINT ( 'NONE',  ( 758.0580252608178853, -30.45278447660226817, 328.0187753319985404 ) ) ;
#26167=CARTESIAN_POINT ( 'NONE',  ( 805.6418435158337843, -293.4636090269707438, 363.8556311672236916 ) ) ;
#26168=CARTESIAN_POINT ( 'NONE',  ( 751.6929314249748586, -270.9982390220561115, 318.8095938919659034 ) ) ;
#26173=CARTESIAN_POINT ( 'NONE',  ( 764.8639956371174549, -368.0891481129647786, 319.7806653035542013 ) ) ;
#26174=CARTESIAN_POINT ( 'NONE',  ( 755.5913626894240451, -133.6454272087893571, 346.6156483768012890 ) ) ;
#26178=CARTESIAN_POINT ( 'NONE',  ( 803.4237431249931660, -399.1800572038738437, 331.2633955100225194 ) ) ;
#26183=CARTESIAN_POINT ( 'NONE',  ( 756.5762568750052424, -147.1800572038746395, 348.7366044899774238 ) ) ;
#26188=CARTESIAN_POINT ( 'NONE',  ( 759.7806653035534055, -366.9982390220556567, 324.8639956371180801 ) ) ;
#26191=CARTESIAN_POINT ( 'NONE',  ( 767.8955696845333705, -432.4527844766008684, 362.1676090361162323 ) ) ;
#26193=CARTESIAN_POINT ( 'NONE',  ( 792.3570229623691148, -69.18005720387488111, 373.1304606946836770 ) ) ;
#26195=AXIS2_PLACEMENT_3D ( 'NONE', #21177, #3635, #17722 ) ;
#26200=CARTESIAN_POINT ( 'NONE',  ( 801.9419747391806368, 5.547215523397618142, 351.9812246680014027 ) ) ;
#26201=CARTESIAN_POINT ( 'NONE',  ( 744.7301800767019131, -220.8164208402379529, 337.4774526936615757 ) ) ;
#26202=CARTESIAN_POINT ( 'NONE',  ( 784.0799538623451781, -155.8055962898689586, 364.6971507214555572 ) ) ;
#26210=CARTESIAN_POINT ( 'NONE',  ( 797.8822607201568644, -54.55451811788054783, 370.1134526219340160 ) ) ;
#26211=DIRECTION ( 'NONE',  ( -1.000000000000000000, -0.000000000000000000, -0.000000000000000000 ) ) ;
#26219=CARTESIAN_POINT ( 'NONE',  ( 798.5707757039680246, -413.4636090269704027, 356.7845633553585003 ) ) ;
#26222=CARTESIAN_POINT ( 'NONE',  ( 787.5531968255692163, -237.8272453906072599, 316.1348686366205811 ) ) ;
#26226=CARTESIAN_POINT ( 'NONE',  ( 807.2620300519052989, -168.0090635724256458, 318.0141637701419768 ) ) ;
#26228=CARTESIAN_POINT ( 'NONE',  ( 777.5031285880264704, -142.8164208402382656, 374.9108240113588408 ) ) ;
#26232=DIRECTION ( 'NONE',  ( 0.000000000000000000, 0.000000000000000000, 1.000000000000000000 ) ) ;
#26233=CARTESIAN_POINT ( 'NONE',  ( 778.2165204200184689, -238.8164208402379813, 364.9363028652563230 ) ) ;
#26234=CARTESIAN_POINT ( 'NONE',  ( 758.4439275373578084, -12.55451811788067751, 353.2243759319684386 ) ) ;
#26240=CARTESIAN_POINT ( 'NONE',  ( 780.5290396650775619, -60.35105083532383219, 365.2837595273619513 ) ) ;
#26241=ORIENTED_EDGE ( 'NONE', *, *, #28951, .T. ) ;
#26244=CARTESIAN_POINT ( 'NONE',  ( 759.9864689768902508, -26.08914811296592262, 354.9819416627836404 ) ) ;
#26247=CARTESIAN_POINT ( 'NONE',  ( 813.9316612368132837, -343.4419599262320162, 348.6739635108323228 ) ) ;
#26250=CARTESIAN_POINT ( 'NONE',  ( 795.1360043628807261, -332.0891481129649492, 360.2193346964456282 ) ) ;
#26258=CARTESIAN_POINT ( 'NONE',  ( 762.1405469898971887, -73.54369356751118403, 357.8594530101015607 ) ) ;
#26259=CARTESIAN_POINT ( 'NONE',  ( 804.4086373105744769, -361.6454272087887603, 333.3843516231986541 ) ) ;
#26261=CARTESIAN_POINT ( 'NONE',  ( 810.7187646348534145, -426.4527844766010389, 356.7737145352016341 ) ) ;
#26263=CARTESIAN_POINT ( 'NONE',  ( 788.7631598425961101, -313.4419599262320730, 305.7194118038759143 ) ) ;
#26267=CARTESIAN_POINT ( 'NONE',  ( 767.7687537140311633, -431.9073299311464211, 372.7932403749916830 ) ) ;
#26270=DIRECTION ( 'NONE',  ( -1.000000000000000000, 0.000000000000000000, 0.000000000000000000 ) ) ;
#26275=CARTESIAN_POINT ( 'NONE',  ( 790.9844846989617508, -310.3726999360616219, 317.2208543904092721 ) ) ;
#26276=CARTESIAN_POINT ( 'NONE',  ( 792.1044303154645831, -180.4527844766017211, 317.8323909638837677 ) ) ;
#26280=CARTESIAN_POINT ( 'NONE',  ( 810.4231160770870019, -72.55451811788049099, 321.9338519418446936 ) ) ;
#26283=CARTESIAN_POINT ( 'NONE',  ( 803.6646147819161570, -137.9073299311473875, 348.8264449731210561 ) ) ;
#26287=CARTESIAN_POINT ( 'NONE',  ( 801.5560724626406000, -0.5545181178807169209, 326.7756240680316182 ) ) ;
#26290=CARTESIAN_POINT ( 'NONE',  ( 786.6156483768007774, -409.4419599262317320, 315.5913626894246136 ) ) ;
#26296=CARTESIAN_POINT ( 'NONE',  ( 746.7653713866222915, -257.2601417444141134, 351.0478386215610271 ) ) ;
#26297=CARTESIAN_POINT ( 'NONE',  ( 781.8018195045267476, -46.27096629478403855, 365.1927285166407273 ) ) ;
#26300=CARTESIAN_POINT ( 'NONE',  ( 759.7806653035534055, -222.9982390220561399, 324.8639956371180801 ) ) ;
#26311=CARTESIAN_POINT ( 'NONE',  ( 751.6929314249750860, -318.9982390220558841, 318.8095938919659034 ) ) ;
#26312=CARTESIAN_POINT ( 'NONE',  ( 783.7566961878529810, -24.89650538077847486, 305.1792804349288417 ) ) ;
#26317=CARTESIAN_POINT ( 'NONE',  ( 803.4237431249931660, -207.1800572038744406, 331.2633955100225194 ) ) ;
#26321=CARTESIAN_POINT ( 'NONE',  ( 747.2067596250078623, -339.1800572038740142, 352.2312462859687230 ) ) ;
#26322=CARTESIAN_POINT ( 'NONE',  ( 799.9999999999993179, -512.9681489794448908, 350.0000000000000000 ) ) ;
#26325=CARTESIAN_POINT ( 'NONE',  ( 763.8424801807145741, -186.0090635724255890, 320.5453621957614700 ) ) ;
#26326=CARTESIAN_POINT ( 'NONE',  ( 762.1405469898971887, -73.54369356751118403, 357.8594530101015607 ) ) ;
#26330=CARTESIAN_POINT ( 'NONE',  ( 763.2154366446407039, -261.6237781080504305, 321.4292242960311228 ) ) ;
#26334=CARTESIAN_POINT ( 'NONE',  ( 782.5225473063381969, -430.2709662947827383, 375.2698199232970637 ) ) ;
#26339=CARTESIAN_POINT ( 'NONE',  ( 814.5518280994195948, -39.72551174932951312, 332.4837098697145734 ) ) ;
#26340=CARTESIAN_POINT ( 'NONE',  ( 772.5602148656447525, -153.7255117493291721, 305.7998596910095443 ) ) ;
#26343=CARTESIAN_POINT ( 'NONE',  ( 744.7301800767019131, -364.8164208402374697, 337.4774526936615757 ) ) ;
#26345=CARTESIAN_POINT ( 'NONE',  ( 804.6798772138708955, -447.7255117493280636, 334.6312213355107019 ) ) ;
#26348=CARTESIAN_POINT ( 'NONE',  ( 786.2056067578752163, -131.8055962898690439, 374.4686193811670023 ) ) ;
#26349=CARTESIAN_POINT ( 'NONE',  ( 771.1735550268780344, -441.1800572038736163, 316.3353852180828198 ) ) ;
#26354=CARTESIAN_POINT ( 'NONE',  ( 794.9819416627830151, -132.9982390220564810, 319.9864689768909898 ) ) ;
#26357=CARTESIAN_POINT ( 'NONE',  ( 781.7834795799800531, -274.8164208402378108, 315.0636971347436202 ) ) ;
#26358=CARTESIAN_POINT ( 'NONE',  ( 755.5713283507202505, -245.3618753856925139, 334.6858677611754729 ) ) ;
#26361=CARTESIAN_POINT ( 'NONE',  ( 800.0135310231082713, -446.0891481129646081, 325.0180583372163028 ) ) ;
#26367=CARTESIAN_POINT ( 'NONE',  ( 813.1304606946831655, -233.9073299311470464, 352.3570229623691716 ) ) ;
#26368=CARTESIAN_POINT ( 'NONE',  ( 804.4086373105744769, -289.6454272087889308, 333.3843516231986541 ) ) ;
#26369=CARTESIAN_POINT ( 'NONE',  ( 761.2382568024794409, -399.6237781080500326, 356.9571628226838129 ) ) ;
#26370=ORIENTED_EDGE ( 'NONE', *, *, #12353, .T. ) ;
#26376=CARTESIAN_POINT ( 'NONE',  ( 794.1144889064781864, -250.1692326535050199, 360.9840315886528401 ) ) ;
#26378=CARTESIAN_POINT ( 'NONE',  ( 758.7867965644027208, 16.45630643248849267, 318.7867965644036872 ) ) ;
#26384=CARTESIAN_POINT ( 'NONE',  ( 812.3518521366052028, -193.0999726633346256, 326.5853460496235243 ) ) ;
#26390=CARTESIAN_POINT ( 'NONE',  ( 754.9967657858570647, -49.54369356751129061, 365.0032342141425374 ) ) ;
#26394=CARTESIAN_POINT ( 'NONE',  ( 778.1981804954714335, -34.27096629478407408, 314.8072714833589885 ) ) ;
#26396=CARTESIAN_POINT ( 'NONE',  ( 744.6391490659812007, -278.7363362996980527, 338.7502325331110455 ) ) ;
#26397=CARTESIAN_POINT ( 'NONE',  ( 800.9747183278959710, -252.9982390220560831, 311.9810565676471583 ) ) ;
#26401=CARTESIAN_POINT ( 'NONE',  ( 804.9363028652555840, -352.2709662947830225, 338.2165204200192079 ) ) ;
#26402=CARTESIAN_POINT ( 'NONE',  ( 755.3028492785439312, -111.2817908451530968, 335.9200461376539693 ) ) ;
#26405=EDGE_CURVE ( 'NONE', #41138, #26699, #16716, .T. ) ;
#26407=CARTESIAN_POINT ( 'NONE',  ( 800.2193346964447755, -402.9982390220555430, 355.1360043628815788 ) ) ;
#26408=ORIENTED_EDGE ( 'NONE', *, *, #42804, .T. ) ;
#26411=CARTESIAN_POINT ( 'NONE',  ( 778.2165204200184689, -166.8164208402382087, 364.9363028652563230 ) ) ;
#26412=CARTESIAN_POINT ( 'NONE',  ( 762.1405469898973024, -169.5436935675108998, 357.8594530101016176 ) ) ;
#26416=CARTESIAN_POINT ( 'NONE',  ( 762.3223304703356007, -343.5436935675103314, 322.3223304703362828 ) ) ;
#26422=CARTESIAN_POINT ( 'NONE',  ( 801.1904061080338124, -68.08914811296577341, 368.3070685750236066 ) ) ;
#26423=ORIENTED_EDGE ( 'NONE', *, *, #8949, .T. ) ;
#26428=CARTESIAN_POINT ( 'NONE',  ( 751.9810565676468741, -266.0891481129651197, 360.9747183278973921 ) ) ;
#26429=CARTESIAN_POINT ( 'NONE',  ( 802.7791456095903868, -172.7146871989598083, 329.0155153010375102 ) ) ;
#26432=CARTESIAN_POINT ( 'NONE',  ( 814.8230680027162407, -413.8055962898681059, 333.7305795820267917 ) ) ;
#26438=CARTESIAN_POINT ( 'NONE',  ( 757.7880784355613741, -90.00906357242590161, 312.4576283171834916 ) ) ;
#26447=CARTESIAN_POINT ( 'NONE',  ( 790.0220218866281812, -391.0999726633340288, 363.2186876482849129 ) ) ;
#26449=CARTESIAN_POINT ( 'NONE',  ( 804.8461984189677878, -242.1908817542435770, 336.9566956441385628 ) ) ;
#26453=CARTESIAN_POINT ( 'NONE',  ( 745.5313806188320314, -183.2817908451528695, 333.7943932421247268 ) ) ;
#26455=CARTESIAN_POINT ( 'NONE',  ( 787.5162901302840055, -155.3618753856927128, 305.4481719005792684 ) ) ;
#26458=CARTESIAN_POINT ( 'NONE',  ( 797.6776695296629214, -259.5436935675106156, 357.6776695296636603 ) ) ;
#26459=CARTESIAN_POINT ( 'NONE',  ( 779.4763451958990572, -32.73633629969879877, 365.0264073115438919 ) ) ;
#26465=CARTESIAN_POINT ( 'NONE',  ( 754.9735926884551418, -90.35105083532373271, 340.5236548041000333 ) ) ;
#26466=CARTESIAN_POINT ( 'NONE',  ( 804.9363028652555840, -304.2709662947832499, 338.2165204200192079 ) ) ;
#26469=CARTESIAN_POINT ( 'NONE',  ( 767.8955696845333705, -72.45278447660213317, 362.1676090361162323 ) ) ;
#26472=CARTESIAN_POINT ( 'NONE',  ( 747.3154664389472828, -355.9874144716865203, 326.4474001241230781 ) ) ;
#26474=CARTESIAN_POINT ( 'NONE',  ( 768.8385539511368734, -431.2601417444136018, 306.4236121716840557 ) ) ;
#26475=CARTESIAN_POINT ( 'NONE',  ( 774.6858677611749044, -369.7255117493284615, 315.5713283507209894 ) ) ;
#26483=CARTESIAN_POINT ( 'NONE',  ( 768.0187753319979720, -80.63460265842029173, 318.0580252608186242 ) ) ;
#26484=CARTESIAN_POINT ( 'NONE',  ( 804.8461984189677878, -410.1908817542430370, 336.9566956441385628 ) ) ;
#26485=CARTESIAN_POINT ( 'NONE',  ( 792.2312462859673587, -443.9073299311464780, 307.2067596250082602 ) ) ;
#26486=DIRECTION ( 'NONE',  ( 0.000000000000000000, 0.000000000000000000, -1.000000000000000000 ) ) ;
#26487=CARTESIAN_POINT ( 'NONE',  ( 747.3154664389472828, -331.9874144716865203, 326.4474001241230781 ) ) ;
#26488=CARTESIAN_POINT ( 'NONE',  ( 761.9338519418445230, -110.5328690171418629, 370.4231160770881957 ) ) ;
#26492=CARTESIAN_POINT ( 'NONE',  ( 808.0189434323515343, -422.0891481129647218, 319.0252816721025511 ) ) ;
#26499=CARTESIAN_POINT ( 'NONE',  ( 804.8461984189677878, -314.1908817542433781, 336.9566956441385628 ) ) ;
#26503=CARTESIAN_POINT ( 'NONE',  ( 766.4474001241216001, -91.09997266333496668, 307.3154664389482491 ) ) ;
#26506=CARTESIAN_POINT ( 'NONE',  ( 774.6858677611749044, -153.7255117493291721, 315.5713283507209894 ) ) ;
#26507=ORIENTED_EDGE ( 'NONE', *, *, #138, .F. ) ;
#26510=CARTESIAN_POINT ( 'NONE',  ( 759.0159684113467620, -16.91815448151702839, 325.8855110935213020 ) ) ;
#26513=CARTESIAN_POINT ( 'NONE',  ( 773.3843516231979720, -397.4419599262317320, 364.4086373105754433 ) ) ;
#26519=CARTESIAN_POINT ( 'NONE',  ( 791.1614460488616487, -251.2601417444141134, 373.5763878283158874 ) ) ;
#26520=CARTESIAN_POINT ( 'NONE',  ( 778.2165204200184689, -70.81642084023850714, 364.9363028652563230 ) ) ;
#26524=CARTESIAN_POINT ( 'NONE',  ( 804.9363028652555840, -232.2709662947834488, 338.2165204200192079 ) ) ;
#26528=EDGE_LOOP ( 'NONE', ( #40145, #27654 ) ) ;
#26531=CARTESIAN_POINT ( 'NONE',  ( 792.3570229623691148, -309.1800572038740711, 373.1304606946836770 ) ) ;
#26532=CARTESIAN_POINT ( 'NONE',  ( 745.1769319972822814, -41.80559628986934229, 346.2694204179732083 ) ) ;
#26537=CARTESIAN_POINT ( 'NONE',  ( 756.3353852180819104, -197.9073299311472169, 331.1735550268788302 ) ) ;
#26540=CARTESIAN_POINT ( 'NONE',  ( 772.4837098697144029, -335.3618753856920307, 374.5518280994205611 ) ) ;
#26542=CARTESIAN_POINT ( 'NONE',  ( 779.9999999999992042, -462.9681489794448339, 339.9999999999999432 ) ) ;
#26544=CARTESIAN_POINT ( 'NONE',  ( 755.1538015810308480, -206.1908817542437191, 343.0433043558613804 ) ) ;
#26545=CARTESIAN_POINT ( 'NONE',  ( 792.1044303154645831, -84.45278447660206211, 317.8323909638837677 ) ) ;
#26549=CARTESIAN_POINT ( 'NONE',  ( 800.7704444035546203, -268.1692326535049347, 326.0291762391768771 ) ) ;
#26552=CARTESIAN_POINT ( 'NONE',  ( 800.9747183278959710, -444.9982390220554862, 311.9810565676471583 ) ) ;
#26556=CARTESIAN_POINT ( 'NONE',  ( 814.9108240113580450, -88.27096629478390355, 337.5031285880265273 ) ) ;
#26557=CARTESIAN_POINT ( 'NONE',  ( 808.0189434323515343, -134.0891481129655745, 319.0252816721025511 ) ) ;
#26561=CARTESIAN_POINT ( 'NONE',  ( 813.1304606946830518, -353.9073299311467053, 352.3570229623690580 ) ) ;
#26563=CARTESIAN_POINT ( 'NONE',  ( 763.2154366446407039, 26.37622189194863509, 321.4292242960311228 ) ) ;
#26566=CARTESIAN_POINT ( 'NONE',  ( 768.8385539511368734, -119.2601417444145397, 306.4236121716840557 ) ) ;
#26567=CARTESIAN_POINT ( 'NONE',  ( 779.9999999999992042, -452.9681489794448339, 339.9999999999999432 ) ) ;
#26571=CARTESIAN_POINT ( 'NONE',  ( 803.6646147819161570, -113.9073299311474301, 348.8264449731210561 ) ) ;
#26573=CARTESIAN_POINT ( 'NONE',  ( 781.7834795799800531, -298.8164208402377540, 315.0636971347436202 ) ) ;
#26574=CARTESIAN_POINT ( 'NONE',  ( 781.7834795799800531, -274.8164208402378108, 315.0636971347436202 ) ) ;
#26577=CARTESIAN_POINT ( 'NONE',  ( 804.6798772138708955, -447.7255117493280636, 334.6312213355107019 ) ) ;
#26581=CARTESIAN_POINT ( 'NONE',  ( 808.3070685750232087, -210.9982390220562252, 361.1904061080339829 ) ) ;
#26582=CARTESIAN_POINT ( 'NONE',  ( 804.4086373105744769, -313.6454272087888171, 333.3843516231986541 ) ) ;
#26583=CARTESIAN_POINT ( 'NONE',  ( 764.0069404352550464, -399.0783235625955285, 359.2566176426627180 ) ) ;
#26591=CARTESIAN_POINT ( 'NONE',  ( 794.1144889064781864, -298.1692326535049347, 360.9840315886528401 ) ) ;
#26593=DIRECTION ( 'NONE',  ( 0.000000000000000000, 1.000000000000000000, 0.000000000000000000 ) ) ;
#26594=CARTESIAN_POINT ( 'NONE',  ( 762.3223304703356007, 16.45630643248849267, 322.3223304703362828 ) ) ;
#26597=CARTESIAN_POINT ( 'NONE',  ( 810.4231160770870019, -192.5545181178801215, 321.9338519418446936 ) ) ;
#26603=CARTESIAN_POINT ( 'NONE',  ( 751.6929314249748586, -30.99823902205680071, 318.8095938919659034 ) ) ;
#26607=CARTESIAN_POINT ( 'NONE',  ( 781.7834795799800531, -58.81642084023854267, 315.0636971347436202 ) ) ;
#26608=CARTESIAN_POINT ( 'NONE',  ( 812.3518521366052028, -313.0999726633342561, 326.5853460496235243 ) ) ;
#26609=CARTESIAN_POINT ( 'NONE',  ( 805.0032342141412300, -253.5436935675104735, 314.9967657858571783 ) ) ;
#26614=CARTESIAN_POINT ( 'NONE',  ( 804.6798772138708955, -351.7255117493284047, 334.6312213355107019 ) ) ;
#26616=CARTESIAN_POINT ( 'NONE',  ( 759.0159684113467620, -112.9181544815167229, 325.8855110935213020 ) ) ;
#26619=DIRECTION ( 'NONE',  ( 0.000000000000000000, 0.000000000000000000, 1.000000000000000000 ) ) ;
#26620=CARTESIAN_POINT ( 'NONE',  ( 771.2368401574024119, -133.4419599262326699, 374.2805881961240857 ) ) ;
#26621=CARTESIAN_POINT ( 'NONE',  ( 781.8018195045266339, -382.2709662947828519, 365.1927285166406705 ) ) ;
#26624=CARTESIAN_POINT ( 'NONE',  ( 768.0187753319979720, -176.6346026584199933, 318.0580252608186242 ) ) ;
#26625=CARTESIAN_POINT ( 'NONE',  ( 771.2633955100217236, -143.9073299311473590, 363.4237431249939618 ) ) ;
#26627=CARTESIAN_POINT ( 'NONE',  ( 799.9999999999993179, 205.0000000000000568, 339.9999999999999432 ) ) ;
#26629=ORIENTED_EDGE ( 'NONE', *, *, #14281, .T. ) ;
#26630=CARTESIAN_POINT ( 'NONE',  ( 756.3353852180819104, -341.9073299311465917, 331.1735550268788302 ) ) ;
#26635=CARTESIAN_POINT ( 'NONE',  ( 746.8695393053151292, -101.9073299311474869, 327.6429770376306578 ) ) ;
#26637=ORIENTED_EDGE ( 'NONE', *, *, #8659, .F. ) ;
#26641=CARTESIAN_POINT ( 'NONE',  ( 745.4481719005789273, -243.7255117493287742, 347.5162901302853129 ) ) ;
#26642=CARTESIAN_POINT ( 'NONE',  ( 764.0069404352550464, -207.0783235625960685, 359.2566176426627180 ) ) ;
#26650=CARTESIAN_POINT ( 'NONE',  ( 744.6391490659812007, -86.73633629969862113, 338.7502325331110455 ) ) ;
#26660=CARTESIAN_POINT ( 'NONE',  ( 769.9779781133707957, -451.0999726633339151, 316.7813123517150871 ) ) ;
#26665=CARTESIAN_POINT ( 'NONE',  ( 802.9823548866075953, -241.0999726633345119, 330.0799878456151077 ) ) ;
#26669=CARTESIAN_POINT ( 'NONE',  ( 802.2119215644370342, -198.0090635724255606, 367.5423716828165084 ) ) ;
#26671=CARTESIAN_POINT ( 'NONE',  ( 814.5518280994195948, -159.7255117493291436, 332.4837098697145734 ) ) ;
#26676=CARTESIAN_POINT ( 'NONE',  ( 765.0180583372156207, -240.9982390220561683, 360.0135310231089534 ) ) ;
#26677=CARTESIAN_POINT ( 'NONE',  ( 779.4763451958990572, -8.736336299698871599, 365.0264073115438919 ) ) ;
#26682=CARTESIAN_POINT ( 'NONE',  ( 795.9930595647434757, -99.07832356259642381, 320.7433823573372820 ) ) ;
#26686=CARTESIAN_POINT ( 'NONE',  ( 774.6858677611749044, -57.72551174932945628, 315.5713283507209894 ) ) ;
#26689=CARTESIAN_POINT ( 'NONE',  ( 815.1787889125755555, -390.8965053807772279, 343.7953271457877804 ) ) ;
#26691=CARTESIAN_POINT ( 'NONE',  ( 744.7301800767019131, -4.816420840238714085, 337.4774526936615757 ) ) ;
#26694=CARTESIAN_POINT ( 'NONE',  ( 805.1927285166397041, -376.8164208402375834, 341.8018195045277707 ) ) ;
#26699=VERTEX_POINT ( 'NONE', #21394 ) ;
#26701=CARTESIAN_POINT ( 'NONE',  ( 758.0580252608178853, -78.45278447660211896, 328.0187753319985404 ) ) ;
#26702=CARTESIAN_POINT ( 'NONE',  ( 755.5913626894240451, -397.6454272087885329, 346.6156483768012890 ) ) ;
#26703=CARTESIAN_POINT ( 'NONE',  ( 744.7301800767020268, -436.8164208402372992, 337.4774526936615189 ) ) ;
#26705=CARTESIAN_POINT ( 'NONE',  ( 778.7502325331095108, -312.3510508353230080, 304.6391490659818828 ) ) ;
#26709=CARTESIAN_POINT ( 'NONE',  ( 795.8262568251477660, 1.627300063937458408, 308.3538107759623585 ) ) ;
#26717=CARTESIAN_POINT ( 'NONE',  ( 758.4439275373578084, -324.5545181178796952, 353.2243759319684386 ) ) ;
#26720=CARTESIAN_POINT ( 'NONE',  ( 746.4236121716829757, -303.8272453906071178, 328.8385539511384650 ) ) ;
#26723=CARTESIAN_POINT ( 'NONE',  ( 749.5768839229115201, -84.55451811788046257, 358.0661480581553064 ) ) ;
#26726=CARTESIAN_POINT ( 'NONE',  ( 774.6312213355099630, -143.3618753856927697, 364.6798772138717482 ) ) ;
#26730=CARTESIAN_POINT ( 'NONE',  ( 801.5560724626406000, -48.55451811788057626, 326.7756240680316182 ) ) ;
#26732=DIRECTION ( 'NONE',  ( -0.000000000000000000, 1.000000000000000000, -0.000000000000000000 ) ) ;
#26733=CARTESIAN_POINT ( 'NONE',  ( 793.2243759319678702, -434.5328690171407970, 318.4439275373583200 ) ) ;
#26738=CARTESIAN_POINT ( 'NONE',  ( 756.1443688327750579, -261.6237781080504305, 314.3581564841659315 ) ) ;
#26739=CARTESIAN_POINT ( 'NONE',  ( 774.6312213355098493, -95.36187538569296862, 364.6798772138717482 ) ) ;
#26742=CARTESIAN_POINT ( 'NONE',  ( 791.9812246680005501, -284.6346026584196807, 361.9419747391813189 ) ) ;
#26745=DIRECTION ( 'NONE',  ( 0.000000000000000000, 0.000000000000000000, -1.000000000000000000 ) ) ;
#26747=EDGE_LOOP ( 'NONE', ( #488, #5217, #15129, #9375 ) ) ;
#26749=CARTESIAN_POINT ( 'NONE',  ( 811.0346526505617248, -326.6346026584194533, 323.0537975583478101 ) ) ;
#26750=CARTESIAN_POINT ( 'NONE',  ( 761.9338519418445230, -230.5328690171415076, 370.4231160770881957 ) ) ;
#26751=CARTESIAN_POINT ( 'NONE',  ( 752.4576283171824116, -45.07832356259660145, 317.7880784355627952 ) ) ;
#26756=CARTESIAN_POINT ( 'NONE',  ( 765.0180583372156207, -216.9982390220562252, 360.0135310231089534 ) ) ;
#26760=CARTESIAN_POINT ( 'NONE',  ( 780.7518514355283514, 16.45630643248848912, 313.9393219192966740 ) ) ;
#26762=CARTESIAN_POINT ( 'NONE',  ( 786.5483106153019435, -175.6454272087892718, 364.1601925771022366 ) ) ;
#26763=CARTESIAN_POINT ( 'NONE',  ( 764.8639956371174549, -80.08914811296574499, 319.7806653035542013 ) ) ;
#26768=CARTESIAN_POINT ( 'NONE',  ( 802.7791456095903868, -268.7146871989595525, 329.0155153010375102 ) ) ;
#26771=CARTESIAN_POINT ( 'NONE',  ( 805.0032342141412300, -445.5436935675098766, 314.9967657858571783 ) ) ;
#26775=CARTESIAN_POINT ( 'NONE',  ( 772.5602148656447525, -81.72551174932937101, 305.7998596910095443 ) ) ;
#26776=CARTESIAN_POINT ( 'NONE',  ( 777.4774526936600978, -154.2709662947836478, 304.7301800767027657 ) ) ;
#26782=CARTESIAN_POINT ( 'NONE',  ( 808.0189434323515343, -398.0891481129647218, 319.0252816721025511 ) ) ;
#26783=CARTESIAN_POINT ( 'NONE',  ( 813.1304606946831655, -17.90732993114776406, 352.3570229623691716 ) ) ;
#26785=CARTESIAN_POINT ( 'NONE',  ( 757.2208543904082489, 7.285312801039605546, 350.9844846989624330 ) ) ;
#26788=CARTESIAN_POINT ( 'NONE',  ( 801.9858362298568863, -123.0783235625963385, 312.7379699480935642 ) ) ;
#26793=CARTESIAN_POINT ( 'NONE',  ( 804.6798772138708955, -159.7255117493291436, 334.6312213355107019 ) ) ;
#26795=CARTESIAN_POINT ( 'NONE',  ( 762.1405469898973024, -289.5436935675105019, 357.8594530101016176 ) ) ;
#26799=CARTESIAN_POINT ( 'NONE',  ( 799.4546378042377910, -33.07832356259662987, 356.1575198192848006 ) ) ;
#26803=CARTESIAN_POINT ( 'NONE',  ( 811.0346526505617248, -230.6346026584197944, 323.0537975583478101 ) ) ;
#26804=CARTESIAN_POINT ( 'NONE',  ( 755.3028492785439312, -303.2817908451525000, 335.9200461376539693 ) ) ;
#26805=CARTESIAN_POINT ( 'NONE',  ( 795.9930595647434757, -411.0783235625954717, 320.7433823573372820 ) ) ;
#26814=CARTESIAN_POINT ( 'NONE',  ( 801.3366627262608972, -296.5328690171411949, 353.0897708529566899 ) ) ;
#26815=DIRECTION ( 'NONE',  ( 0.000000000000000000, 1.000000000000000000, 1.110223024625155554E-15 ) ) ;
#26820=CARTESIAN_POINT ( 'NONE',  ( 805.6418435158337843, -197.4636090269709996, 363.8556311672236916 ) ) ;
#26824=CARTESIAN_POINT ( 'NONE',  ( 814.9108240113580450, -40.27096629478405987, 337.5031285880265273 ) ) ;
#26829=CARTESIAN_POINT ( 'NONE',  ( 774.6858677611749044, -57.72551174932945628, 315.5713283507209894 ) ) ;
#26830=CARTESIAN_POINT ( 'NONE',  ( 781.2370466360911223, -308.7363362996979390, 304.9990715423533629 ) ) ;
#26831=CARTESIAN_POINT ( 'NONE',  ( 815.2698199232961542, -280.8164208402378677, 342.5225473063383106 ) ) ;
#26835=CARTESIAN_POINT ( 'NONE',  ( 758.0580252608178853, -366.4527844766012095, 328.0187753319985404 ) ) ;
#26836=CARTESIAN_POINT ( 'NONE',  ( 805.2837595273609850, -122.7363362996985074, 340.5290396650784714 ) ) ;
#26838=CARTESIAN_POINT ( 'NONE',  ( 748.3538107759620743, -40.71468719896024879, 355.8262568251490165 ) ) ;
#26839=CARTESIAN_POINT ( 'NONE',  ( 785.3141322388236176, -357.7255117493285184, 364.4286716492789537 ) ) ;
#26842=CARTESIAN_POINT ( 'NONE',  ( 783.7566961878529810, -144.8965053807781089, 305.1792804349288417 ) ) ;
#26843=CARTESIAN_POINT ( 'NONE',  ( 758.0580252608178853, -390.4527844766011526, 328.0187753319985404 ) ) ;
#26847=CARTESIAN_POINT ( 'NONE',  ( 774.6312213355099630, -191.3618753856925991, 364.6798772138717482 ) ) ;
#26848=CARTESIAN_POINT ( 'NONE',  ( 803.4237431249931660, -183.1800572038744974, 331.2633955100225194 ) ) ;
#26852=CARTESIAN_POINT ( 'NONE',  ( 797.8594530101008786, -373.5436935675101040, 322.1405469898980982 ) ) ;
#26855=CARTESIAN_POINT ( 'NONE',  ( 763.2262854647970016, -128.6346026584201354, 309.2812353651462445 ) ) ;
#26858=AXIS2_PLACEMENT_3D ( 'NONE', #23153, #34241, #6075 ) ;
#26864=CARTESIAN_POINT ( 'NONE',  ( 782.5225473063381969, -238.2709662947833920, 375.2698199232970637 ) ) ;
#26865=CARTESIAN_POINT ( 'NONE',  ( 776.9566956441375396, -180.8965053807779952, 364.8461984189686405 ) ) ;
#26866=CARTESIAN_POINT ( 'NONE',  ( 793.3938497862117174, -453.0432664090020580, 372.3358127763068524 ) ) ;
#26868=EDGE_CURVE ( 'NONE', #19781, #24420, #30028, .T. ) ;
#26877=CARTESIAN_POINT ( 'NONE',  ( 799.9636004259356241, -118.9181544815167229, 311.2241431872006956 ) ) ;
#26882=CARTESIAN_POINT ( 'NONE',  ( 787.4999999999992042, -512.9681489794448908, 329.9999999999999432 ) ) ;
#26887=CARTESIAN_POINT ( 'NONE',  ( 775.8780910478218402, -441.2817908451521021, 364.9511171171680530 ) ) ;
#26895=CARTESIAN_POINT ( 'NONE',  ( 809.0717654672305343, -220.9181544815164102, 360.1688906516309885 ) ) ;
#26897=CARTESIAN_POINT ( 'NONE',  ( 751.9810565676468741, -170.0891481129654608, 360.9747183278973921 ) ) ;
#26900=CARTESIAN_POINT ( 'NONE',  ( 797.8594530101008786, -253.5436935675104735, 322.1405469898980982 ) ) ;
#26902=CARTESIAN_POINT ( 'NONE',  ( 787.5531968255692163, -45.82724539060783542, 316.1348686366205811 ) ) ;
#26907=CARTESIAN_POINT ( 'NONE',  ( 764.0069404352550464, -87.07832356259646645, 359.2566176426627180 ) ) ;
#26910=CARTESIAN_POINT ( 'NONE',  ( 765.0180583372156207, -72.99823902205667991, 360.0135310231089534 ) ) ;
#26914=CARTESIAN_POINT ( 'NONE',  ( 748.3538107759620743, -376.7146871989592682, 355.8262568251490165 ) ) ;
#26917=CARTESIAN_POINT ( 'NONE',  ( 758.8095938919642549, 15.91085188703394238, 311.6929314249763365 ) ) ;
#26920=CARTESIAN_POINT ( 'NONE',  ( 756.5762568750052424, -387.1800572038738437, 348.7366044899774238 ) ) ;
#26929=CARTESIAN_POINT ( 'NONE',  ( 802.1676090361156639, -86.63460265842023489, 327.8955696845344505 ) ) ;
#26930=CARTESIAN_POINT ( 'NONE',  ( 805.2837595273609850, -410.7363362996976548, 340.5290396650784714 ) ) ;
#26931=CARTESIAN_POINT ( 'NONE',  ( 793.2243759319678702, -98.53286901714187707, 318.4439275373583200 ) ) ;
#26933=CARTESIAN_POINT ( 'NONE',  ( 782.4968714119720516, -442.8164208402372992, 305.0891759886411023 ) ) ;
#26935=CARTESIAN_POINT ( 'NONE',  ( 756.1443688327750579, -357.6237781080501463, 314.3581564841659315 ) ) ;
#26942=CARTESIAN_POINT ( 'NONE',  ( 802.2119215644370342, -6.009063572426154742, 367.5423716828165084 ) ) ;
#26951=CARTESIAN_POINT ( 'NONE',  ( 769.0155153010367712, -346.3726999360614514, 362.7791456095907279 ) ) ;
#26952=CARTESIAN_POINT ( 'NONE',  ( 767.8955696845333705, -192.4527844766016926, 362.1676090361162323 ) ) ;
#26954=CARTESIAN_POINT ( 'NONE',  ( 766.4474001241216001, -307.0999726633343130, 307.3154664389482491 ) ) ;
#26958=CARTESIAN_POINT ( 'NONE',  ( 809.0717654672305343, -100.9181544815167513, 360.1688906516309885 ) ) ;
#26964=CARTESIAN_POINT ( 'NONE',  ( 778.1981804954714335, -154.2709662947836478, 314.8072714833589885 ) ) ;
#26966=CARTESIAN_POINT ( 'NONE',  ( 755.8990559732751535, -419.4636090269702891, 365.9055244015606831 ) ) ;
#26969=CARTESIAN_POINT ( 'NONE',  ( 802.9823548866075953, -49.09997266333511590, 330.0799878456151077 ) ) ;
#26971=CARTESIAN_POINT ( 'NONE',  ( 787.4999999999992042, -512.9681489794448908, 339.9999999999999432 ) ) ;
#26972=CARTESIAN_POINT ( 'NONE',  ( 755.0488828828309806, -425.8055962898680491, 344.1219089521771934 ) ) ;
#26978=CARTESIAN_POINT ( 'NONE',  ( 748.3538107759620743, -280.7146871989594956, 355.8262568251490165 ) ) ;
#26979=CARTESIAN_POINT ( 'NONE',  ( 762.3223304703356007, -79.54369356751119824, 322.3223304703362828 ) ) ;
#26984=CARTESIAN_POINT ( 'NONE',  ( 800.0135310231082713, -254.0891481129652334, 325.0180583372163028 ) ) ;
#26988=ORIENTED_EDGE ( 'NONE', *, *, #23239, .F. ) ;
#26991=AXIS2_PLACEMENT_3D ( 'NONE', #2145, #44407, #36805 ) ;
#26994=CARTESIAN_POINT ( 'NONE',  ( 755.2512626584698410, -319.5436935675104451, 315.2512626584710915 ) ) ;
#26995=CARTESIAN_POINT ( 'NONE',  ( 746.7653713866222915, -209.2601417444142839, 351.0478386215610271 ) ) ;
#26996=CARTESIAN_POINT ( 'NONE',  ( 815.1787889125755555, -54.89650538077837183, 343.7953271457877804 ) ) ;
#27001=CARTESIAN_POINT ( 'NONE',  ( 774.6858677611749044, -201.7255117493290015, 315.5713283507209894 ) ) ;
#27004=CARTESIAN_POINT ( 'NONE',  ( 808.0189434323515343, -350.0891481129648923, 319.0252816721025511 ) ) ;
#27006=CARTESIAN_POINT ( 'NONE',  ( 776.3558828440975503, 16.45630643248848557, 314.5934542695748064 ) ) ;
#27008=CARTESIAN_POINT ( 'NONE',  ( 766.9102291470427417, -210.5545181178800647, 318.6633372737382501 ) ) ;
#27009=CARTESIAN_POINT ( 'NONE',  ( 762.1405469898971887, -97.54369356751112718, 357.8594530101015607 ) ) ;
#27013=CARTESIAN_POINT ( 'NONE',  ( 799.4546378042377910, -273.0783235625958696, 356.1575198192848006 ) ) ;
#27017=CARTESIAN_POINT ( 'NONE',  ( 796.7737145352015204, -452.6346026584191691, 370.7187646348536987 ) ) ;
#27022=CARTESIAN_POINT ( 'NONE',  ( 787.4397851343537695, -93.72551174932934259, 374.2001403089903988 ) ) ;
#27023=CARTESIAN_POINT ( 'NONE',  ( 767.6429770376289525, -153.1800572038746395, 306.8695393053162093 ) ) ;
#27027=CARTESIAN_POINT ( 'NONE',  ( 781.2370466360911223, -404.7363362996975980, 304.9990715423533629 ) ) ;
#27030=CARTESIAN_POINT ( 'NONE',  ( 796.7737145352015204, -380.6346026584192828, 370.7187646348536987 ) ) ;
#27031=CARTESIAN_POINT ( 'NONE',  ( 763.0537975583476964, -0.4527844766023629286, 371.0346526505628617 ) ) ;
#27034=CARTESIAN_POINT ( 'NONE',  ( 800.7704444035546203, -4.169232653505813069, 326.0291762391768771 ) ) ;
#27037=CARTESIAN_POINT ( 'NONE',  ( 786.2056067578752163, -155.8055962898689586, 374.4686193811670023 ) ) ;
#27038=CARTESIAN_POINT ( 'NONE',  ( 797.8594530101009923, 10.45630643248851044, 322.1405469898982119 ) ) ;
#27039=CARTESIAN_POINT ( 'NONE',  ( 813.2346286133761168, -173.2601417444143692, 328.9521613784389160 ) ) ;
#27043=CARTESIAN_POINT ( 'NONE',  ( 797.8594530101008786, -181.5436935675108145, 322.1405469898980982 ) ) ;
#27045=CARTESIAN_POINT ( 'NONE',  ( 771.2633955100217236, -287.9073299311468759, 363.4237431249939618 ) ) ;
#27046=CARTESIAN_POINT ( 'NONE',  ( 788.8264449731201466, -309.1800572038740711, 363.6646147819170665 ) ) ;
#27049=CARTESIAN_POINT ( 'NONE',  ( 755.8398074228967971, -19.44195992623303937, 333.4516893846970333 ) ) ;
#27056=CARTESIAN_POINT ( 'NONE',  ( 805.0032342141413437, -229.5436935675107009, 314.9967657858572352 ) ) ;
#27057=CARTESIAN_POINT ( 'NONE',  ( 773.4516893846965786, -307.6454272087888171, 315.8398074228977066 ) ) ;
#27058=CARTESIAN_POINT ( 'NONE',  ( 795.9930595647434757, -435.0783235625953580, 320.7433823573372820 ) ) ;
#27067=CARTESIAN_POINT ( 'NONE',  ( 775.9200461376533440, -311.8055962898685038, 315.3028492785443291 ) ) ;
#27068=CARTESIAN_POINT ( 'NONE',  ( 792.0613484971601110, -458.0032201311295807, 367.4685979341032294 ) ) ;
#27071=CARTESIAN_POINT ( 'NONE',  ( 755.5913626894240451, -109.6454272087894566, 346.6156483768012890 ) ) ;
#27078=CARTESIAN_POINT ( 'NONE',  ( 746.8695393053150156, -29.90732993114771787, 327.6429770376306010 ) ) ;
#27081=CARTESIAN_POINT ( 'NONE',  ( 799.9999999999993179, -512.9681489794448908, 309.9999999999998863 ) ) ;
#27082=CARTESIAN_POINT ( 'NONE',  ( 791.0478386215596629, -333.8272453906070041, 306.7653713866226326 ) ) ;
#27084=CARTESIAN_POINT ( 'NONE',  ( 751.6929314249748586, -294.9982390220560546, 318.8095938919659034 ) ) ;
#27089=CARTESIAN_POINT ( 'NONE',  ( 755.5713283507202505, -389.3618753856919739, 334.6858677611754729 ) ) ;
#27090=CARTESIAN_POINT ( 'NONE',  ( 769.0155153010367712, -130.3726999360621619, 362.7791456095907279 ) ) ;
#27092=CARTESIAN_POINT ( 'NONE',  ( 793.4146539503750546, -49.98741447168749374, 307.6481478633938877 ) ) ;
#27093=CARTESIAN_POINT ( 'NONE',  ( 781.7834795799800531, -370.8164208402375834, 315.0636971347436202 ) ) ;
#27097=CARTESIAN_POINT ( 'NONE',  ( 768.8385539511368734, -143.2601417444144829, 306.4236121716840557 ) ) ;
#27098=CARTESIAN_POINT ( 'NONE',  ( 792.1044303154645831, -444.4527844766009821, 317.8323909638837677 ) ) ;
#27102=CARTESIAN_POINT ( 'NONE',  ( 778.2165204200184689, -190.8164208402381234, 364.9363028652563230 ) ) ;
#27103=CARTESIAN_POINT ( 'NONE',  ( 774.6312213355098493, -191.3618753856926276, 364.6798772138717482 ) ) ;
#27107=CARTESIAN_POINT ( 'NONE',  ( 800.2193346964447755, -378.9982390220555999, 355.1360043628815788 ) ) ;
#27111=CARTESIAN_POINT ( 'NONE',  ( 744.7301800767020268, -124.8164208402383366, 337.4774526936615189 ) ) ;
#27117=CARTESIAN_POINT ( 'NONE',  ( 796.7737145352015204, -260.6346026584197375, 370.7187646348536987 ) ) ;
#27118=CARTESIAN_POINT ( 'NONE',  ( 801.3366627262608972, -200.5328690171415644, 353.0897708529566899 ) ) ;
#27128=CARTESIAN_POINT ( 'NONE',  ( 771.3260364891663130, -91.64542720878951343, 306.0683387631859773 ) ) ;
#27137=CARTESIAN_POINT ( 'NONE',  ( 772.4468031744293057, -441.8272453906066630, 363.8651313633793620 ) ) ;
#27138=CARTESIAN_POINT ( 'NONE',  ( 804.1009440267234822, -359.4636090269705164, 314.0944755984392600 ) ) ;
#27145=CARTESIAN_POINT ( 'NONE',  ( 795.8262568251477660, -214.3726999360618493, 308.3538107759623585 ) ) ;
#27147=CARTESIAN_POINT ( 'NONE',  ( 814.5518280994195948, -183.7255117493290015, 332.4837098697145734 ) ) ;
#27150=CARTESIAN_POINT ( 'NONE',  ( 803.4237431249931660, -255.1800572038742700, 331.2633955100225194 ) ) ;
#27151=CARTESIAN_POINT ( 'NONE',  ( 766.0291762391763086, -58.91815448151690759, 360.7704444035551319 ) ) ;
#27155=CARTESIAN_POINT ( 'NONE',  ( 761.2382568024794409, -87.62377810805102740, 356.9571628226838129 ) ) ;
#27156=CARTESIAN_POINT ( 'NONE',  ( 791.9812246680005501, -308.6346026584195670, 361.9419747391813189 ) ) ;
#27160=CARTESIAN_POINT ( 'NONE',  ( 791.9812246680005501, -68.63460265842033436, 361.9419747391813189 ) ) ;
#27163=CARTESIAN_POINT ( 'NONE',  ( 783.7566961878529810, -384.8965053807772847, 305.1792804349288417 ) ) ;
#27165=CARTESIAN_POINT ( 'NONE',  ( 803.6646147819161570, -305.9073299311467622, 348.8264449731210561 ) ) ;
#27166=CARTESIAN_POINT ( 'NONE',  ( 803.8556311672234642, -441.6237781080499190, 365.6418435158340117 ) ) ;
#27169=CARTESIAN_POINT ( 'NONE',  ( 804.9363028652555840, -376.2709662947829656, 338.2165204200192079 ) ) ;
#27175=CARTESIAN_POINT ( 'NONE',  ( 805.1927285166397041, -88.81642084023842187, 341.8018195045277707 ) ) ;
#27176=CARTESIAN_POINT ( 'NONE',  ( 766.0291762391763086, -394.9181544815158418, 360.7704444035551319 ) ) ;
#27177=CARTESIAN_POINT ( 'NONE',  ( 805.1016975059191054, -102.8965053807782368, 343.0745993439771837 ) ) ;
#27179=DIRECTION ( 'NONE',  ( -1.000000000000000000, -0.000000000000000000, 0.000000000000000000 ) ) ;
#27180=CARTESIAN_POINT ( 'NONE',  ( 810.1134526219336749, -344.5328690171410813, 357.8822607201570349 ) ) ;
#27185=CARTESIAN_POINT ( 'NONE',  ( 754.3581564841646241, 6.536390973028352924, 316.1443688327762516 ) ) ;
#27190=CARTESIAN_POINT ( 'NONE',  ( 798.5707757039680246, -341.4636090269705733, 356.7845633553585003 ) ) ;
#27194=CARTESIAN_POINT ( 'NONE',  ( 810.4231160770870019, -96.55451811788039151, 321.9338519418446936 ) ) ;
#27199=CARTESIAN_POINT ( 'NONE',  ( 771.1735550268778070, -153.1800572038746395, 316.3353852180827630 ) ) ;
#27201=CARTESIAN_POINT ( 'NONE',  ( 773.7305795820266212, -417.2817908451522158, 374.8230680027170365 ) ) ;
#27204=CARTESIAN_POINT ( 'NONE',  ( 796.9571628226829034, -47.46360902697148987, 321.2382568024804641 ) ) ;
#27206=CARTESIAN_POINT ( 'NONE',  ( 759.9999999999992042, 205.0000000000000568, 339.9999999999999432 ) ) ;
#27207=CARTESIAN_POINT ( 'NONE',  ( 786.6156483768007774, -433.4419599262316183, 315.5913626894246136 ) ) ;
#27208=ORIENTED_EDGE ( 'NONE', *, *, #11193, .T. ) ;
#27211=CARTESIAN_POINT ( 'NONE',  ( 772.4999999999993179, -462.9681489794448339, 370.0000000000000568 ) ) ;
#27212=CARTESIAN_POINT ( 'NONE',  ( 811.6461892240364477, -292.7146871989594956, 324.1737431748509835 ) ) ;
#27213=CARTESIAN_POINT ( 'NONE',  ( 797.8594530101009923, -85.54369356751118403, 322.1405469898982119 ) ) ;
#27216=CARTESIAN_POINT ( 'NONE',  ( 797.8594530101008786, -253.5436935675104735, 322.1405469898980982 ) ) ;
#27218=CARTESIAN_POINT ( 'NONE',  ( 790.4268473037436706, -448.2010802157933540, 366.7838603755944291 ) ) ;
#27220=ORIENTED_EDGE ( 'NONE', *, *, #2688, .F. ) ;
#27223=VECTOR ( 'NONE', #12037, 1000.000000000000000 ) ;
#27226=CARTESIAN_POINT ( 'NONE',  ( 808.3070685750232087, -330.9982390220558273, 361.1904061080339829 ) ) ;
#27227=CARTESIAN_POINT ( 'NONE',  ( 783.7566961878529810, -240.8965053807777963, 305.1792804349288417 ) ) ;
#27231=CARTESIAN_POINT ( 'NONE',  ( 791.9812246680005501, -260.6346026584197375, 361.9419747391813189 ) ) ;
#27233=CARTESIAN_POINT ( 'NONE',  ( 745.7998596910086917, -365.3618753856920875, 332.5602148656461168 ) ) ;
#27236=CARTESIAN_POINT ( 'NONE',  ( 795.0120564873543572, 16.45630643248849267, 314.4408280072604498 ) ) ;
#27238=CARTESIAN_POINT ( 'NONE',  ( 796.9571628226829034, -239.4636090269709143, 321.2382568024804641 ) ) ;
#27239=CARTESIAN_POINT ( 'NONE',  ( 804.9363028652555840, -88.27096629478390355, 338.2165204200192079 ) ) ;
#27243=CARTESIAN_POINT ( 'NONE',  ( 764.0069404352550464, -255.0783235625958980, 359.2566176426627180 ) ) ;
#27247=CARTESIAN_POINT ( 'NONE',  ( 783.7953271457878373, -8.190881754244330182, 375.1787889125761239 ) ) ;
#27251=EDGE_CURVE ( 'NONE', #10697, #34191, #15591, .T. ) ;
#27252=CARTESIAN_POINT ( 'NONE',  ( 747.2067596250078623, -99.18005720387478164, 352.2312462859687230 ) ) ;
#27253=CARTESIAN_POINT ( 'NONE',  ( 772.5602148656447525, -129.7255117493292289, 305.7998596910095443 ) ) ;
#27258=CARTESIAN_POINT ( 'NONE',  ( 762.1177392798416577, -426.5545181178794678, 309.8865473780659272 ) ) ;
#27261=CARTESIAN_POINT ( 'NONE',  ( 808.3070685750230950, -402.9982390220555430, 361.1904061080339261 ) ) ;
#27262=CARTESIAN_POINT ( 'NONE',  ( 767.6429770376291799, -9.180057203875058747, 306.8695393053162093 ) ) ;
#27263=EDGE_CURVE ( 'NONE', #28817, #1373, #13824, .T. ) ;
#27266=CARTESIAN_POINT ( 'NONE',  ( 801.3366627262608972, -8.532869017142163059, 353.0897708529566899 ) ) ;
#27269=CARTESIAN_POINT ( 'NONE',  ( 786.2056067578752163, -179.8055962898688733, 374.4686193811670023 ) ) ;
#27270=CARTESIAN_POINT ( 'NONE',  ( 795.1360043628808398, 3.910851887033986785, 360.2193346964456282 ) ) ;
#27274=CARTESIAN_POINT ( 'NONE',  ( 791.9812246680005501, -164.6346026584200217, 361.9419747391813189 ) ) ;
#27276=CARTESIAN_POINT ( 'NONE',  ( 774.6312213355099630, -287.3618753856923718, 364.6798772138717482 ) ) ;
#27279=CARTESIAN_POINT ( 'NONE',  ( 805.0264073115434940, -6.351050835323991173, 339.4763451958999099 ) ) ;
#27282=CARTESIAN_POINT ( 'NONE',  ( 751.9810565676468741, -218.0891481129653187, 360.9747183278973921 ) ) ;
#27283=CARTESIAN_POINT ( 'NONE',  ( 769.0155153010367712, -322.3726999360615082, 362.7791456095907279 ) ) ;
#27284=CARTESIAN_POINT ( 'NONE',  ( 766.7756240680305382, -422.5328690171408539, 361.5560724626415663 ) ) ;
#27290=CARTESIAN_POINT ( 'NONE',  ( 802.7791456095903868, -292.7146871989594956, 329.0155153010375102 ) ) ;
#27293=CARTESIAN_POINT ( 'NONE',  ( 754.7162404726377645, -110.7363362996985501, 339.4709603349214717 ) ) ;
#27294=CARTESIAN_POINT ( 'NONE',  ( 804.4286716492782716, 6.638124614306706306, 345.3141322388244703 ) ) ;
#27297=CARTESIAN_POINT ( 'NONE',  ( 811.3240766477731540, -196.3726999360619061, 355.6651683502462902 ) ) ;
#27300=DIRECTION ( 'NONE',  ( 1.000000000000000000, -0.000000000000000000, -0.000000000000000000 ) ) ;
#27302=CARTESIAN_POINT ( 'NONE',  ( 782.5225473063381969, -46.27096629478404566, 375.2698199232970637 ) ) ;
#27303=CARTESIAN_POINT ( 'NONE',  ( 808.5285127195401174, -452.9681489794448339, 336.5948204574517035 ) ) ;
#27306=CARTESIAN_POINT ( 'NONE',  ( 815.3608509340175488, -314.7363362996979959, 341.2497674668889545 ) ) ;
#27308=CARTESIAN_POINT ( 'NONE',  ( 814.2001403089898304, -305.3618753856922581, 347.4397851343538264 ) ) ;
#27313=CARTESIAN_POINT ( 'NONE',  ( 756.5762568750052424, -387.1800572038738437, 348.7366044899774238 ) ) ;
#27314=CARTESIAN_POINT ( 'NONE',  ( 802.5472867521000353, -172.3726999360619914, 350.8726784830461156 ) ) ;
#27316=CARTESIAN_POINT ( 'NONE',  ( 811.6461892240364477, -76.71468719896012090, 324.1737431748509835 ) ) ;
#27317=CARTESIAN_POINT ( 'NONE',  ( 755.3201227861273992, -363.7255117493284615, 345.3687786644892981 ) ) ;
#27318=CARTESIAN_POINT ( 'NONE',  ( 763.2262854647970016, 15.36539734157940629, 309.2812353651462445 ) ) ;
#27320=CARTESIAN_POINT ( 'NONE',  ( 756.5762568750052424, -435.1800572038737869, 348.7366044899774238 ) ) ;
#27321=VERTEX_POINT ( 'NONE', #37979 ) ;
#27324=CARTESIAN_POINT ( 'NONE',  ( 788.7366044899766848, -179.9073299311472454, 316.5762568750059813 ) ) ;
#27325=CARTESIAN_POINT ( 'NONE',  ( 762.3223304703356007, -175.5436935675108998, 322.3223304703362828 ) ) ;
#27329=CARTESIAN_POINT ( 'NONE',  ( 785.3687786644884454, -395.3618753856918602, 315.3201227861279676 ) ) ;
#27333=CARTESIAN_POINT ( 'NONE',  ( 811.0346526505617248, -110.6346026584201923, 323.0537975583478101 ) ) ;
#27339=CARTESIAN_POINT ( 'NONE',  ( 783.0433043558608688, -192.8965053807779668, 315.1538015810313027 ) ) ;
#27340=DIRECTION ( 'NONE',  ( -1.000000000000000000, -0.000000000000000000, 0.000000000000000000 ) ) ;
#27346=DIRECTION ( 'NONE',  ( 0.000000000000000000, 0.000000000000000000, -1.000000000000000000 ) ) ;
#27348=CARTESIAN_POINT ( 'NONE',  ( 786.2694204179717872, -93.28179084515315367, 305.1769319972829067 ) ) ;
#27355=CARTESIAN_POINT ( 'NONE',  ( 805.2837595273609850, -434.7363362996975980, 340.5290396650784714 ) ) ;
#27362=CARTESIAN_POINT ( 'NONE',  ( 778.7629533639073998, -224.7363362996982232, 375.0009284576466371 ) ) ;
#27364=CARTESIAN_POINT ( 'NONE',  ( 745.0891759886404770, -172.2709662947836478, 342.4968714119734159 ) ) ;
#27367=CARTESIAN_POINT ( 'NONE',  ( 759.9864689768902508, -290.0891481129650629, 354.9819416627836404 ) ) ;
#27368=CARTESIAN_POINT ( 'NONE',  ( 755.1538015810308480, -62.19088175424416676, 343.0433043558613804 ) ) ;
#27372=CARTESIAN_POINT ( 'NONE',  ( 754.8983024940795303, -114.8965053807782226, 336.9254006560228163 ) ) ;
#27373=CARTESIAN_POINT ( 'NONE',  ( 804.6798772138708955, -327.7255117493285184, 334.6312213355107019 ) ) ;
#27377=CARTESIAN_POINT ( 'NONE',  ( 785.3687786644884454, -83.36187538569296862, 315.3201227861279676 ) ) ;
#27380=CARTESIAN_POINT ( 'NONE',  ( 803.8556311672234642, -369.6237781080500895, 365.6418435158340117 ) ) ;
#27382=CARTESIAN_POINT ( 'NONE',  ( 762.3223304703356007, -295.5436935675105588, 322.3223304703362828 ) ) ;
#27383=CARTESIAN_POINT ( 'NONE',  ( 814.5518280994195948, 8.274488250670337663, 332.4837098697145734 ) ) ;
#27386=CARTESIAN_POINT ( 'NONE',  ( 755.3201227861273992, -387.7255117493283478, 345.3687786644892981 ) ) ;
#27392=CARTESIAN_POINT ( 'NONE',  ( 757.8323909638827445, -98.63460265842024910, 352.1044303154654358 ) ) ;
#27393=CARTESIAN_POINT ( 'NONE',  ( 760.7433823573367135, -420.0090635724249069, 355.9930595647440441 ) ) ;
#27396=CARTESIAN_POINT ( 'NONE',  ( 815.0009284576459549, -366.3510508353228374, 338.7629533639073429 ) ) ;
#27397=CARTESIAN_POINT ( 'NONE',  ( 749.8865473780648472, -116.5328690171418202, 322.1177392798429082 ) ) ;
#27401=CARTESIAN_POINT ( 'NONE',  ( 812.7932403749906598, -447.1800572038736732, 327.7687537140311633 ) ) ;
#27403=CARTESIAN_POINT ( 'NONE',  ( 799.9999999999993179, -512.9681489794448908, 370.0000000000000000 ) ) ;
#27408=CARTESIAN_POINT ( 'NONE',  ( 804.6971507214547046, -315.2817908451525000, 344.0799538623459739 ) ) ;
#27410=CARTESIAN_POINT ( 'NONE',  ( 802.2119215644370342, -318.0090635724251911, 367.5423716828165084 ) ) ;
#27414=CARTESIAN_POINT ( 'NONE',  ( 802.2119215644370342, -102.0090635724258448, 367.5423716828165084 ) ) ;
#27418=CARTESIAN_POINT ( 'NONE',  ( 767.8955696845333705, -168.4527844766018347, 362.1676090361162323 ) ) ;
#27420=CARTESIAN_POINT ( 'NONE',  ( 815.3608509340175488, -434.7363362996975980, 341.2497674668889545 ) ) ;
#27423=CARTESIAN_POINT ( 'NONE',  ( 783.0745993439762742, -56.19088175424417386, 365.1016975059196739 ) ) ;
#27426=CARTESIAN_POINT ( 'NONE',  ( 760.5453621957607311, -429.0783235625953580, 323.8424801807151425 ) ) ;
#27429=CARTESIAN_POINT ( 'NONE',  ( 811.6461892240364477, -268.7146871989595525, 324.1737431748509835 ) ) ;
#27430=CARTESIAN_POINT ( 'NONE',  ( 755.3201227861273992, -75.72551174932938522, 345.3687786644892981 ) ) ;
#27433=CARTESIAN_POINT ( 'NONE',  ( 802.1676090361156639, -278.6346026584196807, 327.8955696845344505 ) ) ;
#27436=VERTEX_POINT ( 'NONE', #16961 ) ;
#27440=CARTESIAN_POINT ( 'NONE',  ( 782.4968714119720516, -346.8164208402376971, 305.0891759886411023 ) ) ;
#27441=CARTESIAN_POINT ( 'NONE',  ( 793.4146539503750546, -241.9874144716869182, 307.6481478633938877 ) ) ;
#27447=CARTESIAN_POINT ( 'NONE',  ( 803.6646147819161570, -233.9073299311470180, 348.8264449731210561 ) ) ;
#27449=CARTESIAN_POINT ( 'NONE',  ( 745.7998596910086917, -341.3618753856922012, 332.5602148656461168 ) ) ;
#27455=CARTESIAN_POINT ( 'NONE',  ( 804.1105419155481968, -219.8272453906073167, 347.6308680596136469 ) ) ;
#27456=CARTESIAN_POINT ( 'NONE',  ( 762.3223304703356007, -103.5436935675111272, 322.3223304703362828 ) ) ;
#27460=CARTESIAN_POINT ( 'NONE',  ( 783.0433043558608688, -288.8965053807775121, 315.1538015810313027 ) ) ;
#27463=CARTESIAN_POINT ( 'NONE',  ( 813.5763878283155464, -3.827245390607979303, 351.1614460488615350 ) ) ;
#27465=CARTESIAN_POINT ( 'NONE',  ( 745.4481719005789273, -75.72551174932937101, 347.5162901302853129 ) ) ;
#27466=CARTESIAN_POINT ( 'NONE',  ( 767.7687537140311633, -167.9073299311473022, 372.7932403749916830 ) ) ;
#27468=CARTESIAN_POINT ( 'NONE',  ( 779.9999999999992042, 126.4563064324884465, 329.9999999999999432 ) ) ;
#27471=CARTESIAN_POINT ( 'NONE',  ( 750.9282345327678740, -400.9181544815159555, 319.8311093483690115 ) ) ;
#27475=CARTESIAN_POINT ( 'NONE',  ( 782.4968714119720516, -394.8164208402374697, 305.0891759886411023 ) ) ;
#27476=CARTESIAN_POINT ( 'NONE',  ( 814.2001403089898304, -17.36187538569322086, 347.4397851343538264 ) ) ;
#27478=CARTESIAN_POINT ( 'NONE',  ( 799.4546378042377910, -33.07832356259662987, 356.1575198192848006 ) ) ;
#27481=CARTESIAN_POINT ( 'NONE',  ( 751.2241431872005251, -184.1692326535052757, 359.9636004259367610 ) ) ;
#27482=CARTESIAN_POINT ( 'NONE',  ( 778.2165204200184689, 1.183579159761269040, 364.9363028652563230 ) ) ;
#27487=CARTESIAN_POINT ( 'NONE',  ( 802.1676090361156639, -158.6346026584199933, 327.8955696845344505 ) ) ;
#27489=CARTESIAN_POINT ( 'NONE',  ( 771.2633955100217236, -287.9073299311468759, 363.4237431249939618 ) ) ;
#27492=CARTESIAN_POINT ( 'NONE',  ( 756.7813123517142913, -19.98741447168758256, 329.9779781133712504 ) ) ;
#27495=CARTESIAN_POINT ( 'NONE',  ( 808.3070685750232087, -258.9982390220561115, 361.1904061080339829 ) ) ;
#27497=CARTESIAN_POINT ( 'NONE',  ( 793.0897708529556667, -342.5545181178796952, 361.3366627262616362 ) ) ;
#27498=CARTESIAN_POINT ( 'NONE',  ( 790.8726784830453198, -442.7146871989589840, 362.5472867521010585 ) ) ;
#27502=EDGE_LOOP ( 'NONE', ( #16238, #37044 ) ) ;
#27503=( GEOMETRIC_REPRESENTATION_CONTEXT ( 3 ) GLOBAL_UNCERTAINTY_ASSIGNED_CONTEXT ( ( #1918 ) ) GLOBAL_UNIT_ASSIGNED_CONTEXT ( ( #28708, #14857, #969 ) ) REPRESENTATION_CONTEXT ( 'NONE', 'WORKASPACE' ) );
#27504=CARTESIAN_POINT ( 'NONE',  ( 800.7704444035546203, -292.1692326535048210, 326.0291762391768771 ) ) ;
#27507=CARTESIAN_POINT ( 'NONE',  ( 783.0745993439762742, -128.1908817542439465, 365.1016975059196739 ) ) ;
#27508=CARTESIAN_POINT ( 'NONE',  ( 778.1981804954714335, -10.27096629478414691, 314.8072714833589885 ) ) ;
#27511=CARTESIAN_POINT ( 'NONE',  ( 752.7379699480933368, -228.0090635724254753, 361.9858362298580232 ) ) ;
#27515=CARTESIAN_POINT ( 'NONE',  ( 814.2001403089898304, -89.36187538569299704, 347.4397851343538264 ) ) ;
#27516=CARTESIAN_POINT ( 'NONE',  ( 809.5171784329539832, -452.9681489794445497, 335.1922280983832252 ) ) ;
#27520=CARTESIAN_POINT ( 'NONE',  ( 776.2046728542105711, -308.1908817542434349, 304.8212110874238761 ) ) ;
#27523=CARTESIAN_POINT ( 'NONE',  ( 810.7187646348534145, -306.4527844766013800, 356.7737145352016341 ) ) ;
#27527=CARTESIAN_POINT ( 'NONE',  ( 791.9812246680005501, -404.6346026584193396, 361.9419747391813189 ) ) ;
#27528=CARTESIAN_POINT ( 'NONE',  ( 763.0428371773158460, -155.4636090269711417, 358.7617431975195359 ) ) ;
#27531=CARTESIAN_POINT ( 'NONE',  ( 800.1688906516307043, -58.16923265350564520, 369.0717654672308186 ) ) ;
#27532=CARTESIAN_POINT ( 'NONE',  ( 804.4286716492782716, -377.3618753856920875, 345.3141322388244703 ) ) ;
#27534=CARTESIAN_POINT ( 'NONE',  ( 755.2512626584698410, 16.45630643248848912, 315.2512626584710915 ) ) ;
#27535=CARTESIAN_POINT ( 'NONE',  ( 749.8865473780648472, -140.5328690171417634, 322.1177392798429082 ) ) ;
#27536=CARTESIAN_POINT ( 'NONE',  ( 774.6858677611749044, -417.7255117493283478, 315.5713283507209894 ) ) ;
#27540=CARTESIAN_POINT ( 'NONE',  ( 801.9419747391806368, -210.4527844766016926, 351.9812246680014027 ) ) ;
#27541=CARTESIAN_POINT ( 'NONE',  ( 805.1927285166399315, -184.8164208402381234, 341.8018195045277707 ) ) ;
#27544=LINE ( 'NONE', #41648, #42634 ) ;
#27546=CARTESIAN_POINT ( 'NONE',  ( 778.2165204200184689, -406.8164208402375266, 364.9363028652563230 ) ) ;
#27551=CARTESIAN_POINT ( 'NONE',  ( 748.9653473494365699, -146.6346026584200786, 356.9462024416520762 ) ) ;
#27558=CARTESIAN_POINT ( 'NONE',  ( 761.2382568024794409, -183.6237781080507148, 356.9571628226838129 ) ) ;
#27570=CARTESIAN_POINT ( 'NONE',  ( 773.7305795820266212, -129.2817908451530400, 374.8230680027170365 ) ) ;
#27577=CARTESIAN_POINT ( 'NONE',  ( 798.5707757039680246, -437.4636090269703459, 356.7845633553585003 ) ) ;
#27578=CARTESIAN_POINT ( 'NONE',  ( 799.9636004259356241, -358.9181544815160123, 311.2241431872006956 ) ) ;
#27583=CARTESIAN_POINT ( 'NONE',  ( 802.1676090361156639, 9.365397341579420498, 327.8955696845344505 ) ) ;
#27586=CARTESIAN_POINT ( 'NONE',  ( 747.6481478633932056, -229.0999726633345404, 353.4146539503763620 ) ) ;
#27588=CARTESIAN_POINT ( 'NONE',  ( 755.2512626584698410, -199.5436935675108430, 315.2512626584710915 ) ) ;
#27591=CARTESIAN_POINT ( 'NONE',  ( 771.1735550268778070, -273.1800572038742985, 316.3353852180827630 ) ) ;
#27592=CARTESIAN_POINT ( 'NONE',  ( 759.0159684113467620, -64.91815448151686496, 325.8855110935213020 ) ) ;
#27596=CARTESIAN_POINT ( 'NONE',  ( 799.4546378042377910, -129.0783235625963243, 356.1575198192848006 ) ) ;
#27597=CARTESIAN_POINT ( 'NONE',  ( 756.5762568750052424, -339.1800572038740142, 348.7366044899774238 ) ) ;
#27598=ORIENTED_EDGE ( 'NONE', *, *, #17400, .F. ) ;
#27600=CARTESIAN_POINT ( 'NONE',  ( 805.1927285166397041, -88.81642084023842187, 341.8018195045277707 ) ) ;
#27601=AXIS2_PLACEMENT_3D ( 'NONE', #23592, #40934, #30298 ) ;
#27604=CARTESIAN_POINT ( 'NONE',  ( 759.8311093483677041, -382.1692326535045936, 310.9282345327691814 ) ) ;
#27606=CARTESIAN_POINT ( 'NONE',  ( 802.1676090361156639, -278.6346026584196807, 327.8955696845344505 ) ) ;
#27609=CARTESIAN_POINT ( 'NONE',  ( 764.8639956371174549, -392.0891481129648355, 319.7806653035542013 ) ) ;
#27616=CARTESIAN_POINT ( 'NONE',  ( 774.6312213355099630, -119.3618753856928691, 364.6798772138717482 ) ) ;
#27617=CARTESIAN_POINT ( 'NONE',  ( 765.8855110935204493, -94.16923265350555994, 319.0159684113471599 ) ) ;
#27619=CYLINDRICAL_SURFACE ( 'NONE', #40962, 10.00000000000000888 ) ;
#27620=CARTESIAN_POINT ( 'NONE',  ( 771.2368401574024119, -349.4419599262320162, 374.2805881961240857 ) ) ;
#27625=CARTESIAN_POINT ( 'NONE',  ( 757.7880784355613741, 5.990936427573807954, 312.4576283171834916 ) ) ;
#27632=CARTESIAN_POINT ( 'NONE',  ( 780.5236548040995785, -332.7363362996979390, 314.9735926884559944 ) ) ;
#27634=CARTESIAN_POINT ( 'NONE',  ( 745.1792804349281596, -302.1908817542433781, 343.7566961878542884 ) ) ;
#27638=AXIS2_PLACEMENT_3D ( 'NONE', #37990, #38220, #25248 ) ;
#27639=CARTESIAN_POINT ( 'NONE',  ( 815.3608509340175488, -98.73633629969859271, 341.2497674668889545 ) ) ;
#27643=CARTESIAN_POINT ( 'NONE',  ( 802.1676090361156639, -182.6346026584199649, 327.8955696845344505 ) ) ;
#27645=CARTESIAN_POINT ( 'NONE',  ( 810.4231160770870019, -408.5545181178794110, 321.9338519418446936 ) ) ;
#27650=CARTESIAN_POINT ( 'NONE',  ( 761.4292242960306112, -41.46360902697149697, 323.2154366446414429 ) ) ;
#27653=CARTESIAN_POINT ( 'NONE',  ( 748.3538107759620743, 7.285312801039605546, 355.8262568251490165 ) ) ;
#27654=ORIENTED_EDGE ( 'NONE', *, *, #39704, .F. ) ;
#27659=CARTESIAN_POINT ( 'NONE',  ( 751.2241431872005251, -280.1692326535049347, 359.9636004259367610 ) ) ;
#27660=CARTESIAN_POINT ( 'NONE',  ( 774.6858677611749044, -105.7255117493293000, 315.5713283507209894 ) ) ;
#27664=CARTESIAN_POINT ( 'NONE',  ( 778.1981804954714335, -274.2709662947833067, 314.8072714833589885 ) ) ;
#27667=AXIS2_PLACEMENT_3D ( 'NONE', #26567, #6480, #41359 ) ;
#27674=CARTESIAN_POINT ( 'NONE',  ( 767.6429770376291799, -369.1800572038739006, 306.8695393053162093 ) ) ;
#27675=CARTESIAN_POINT ( 'NONE',  ( 748.3538107759620743, -256.7146871989595525, 355.8262568251490165 ) ) ;
#27676=CARTESIAN_POINT ( 'NONE',  ( 813.2346286133761168, -53.26014174441475291, 328.9521613784389160 ) ) ;
#27681=CARTESIAN_POINT ( 'NONE',  ( 797.8594530101008786, -229.5436935675106440, 322.1405469898980982 ) ) ;
#27683=CARTESIAN_POINT ( 'NONE',  ( 749.2812353651451076, -366.4527844766012095, 323.2262854647983090 ) ) ;
#27684=AXIS2_PLACEMENT_3D ( 'NONE', #38009, #34535, #45395 ) ;
#27688=CARTESIAN_POINT ( 'NONE',  ( 779.9999999999992042, 16.45630643248849267, 350.0000000000000000 ) ) ;
#27689=CARTESIAN_POINT ( 'NONE',  ( 786.5483106153019435, -223.6454272087891013, 364.1601925771022366 ) ) ;
#27690=CARTESIAN_POINT ( 'NONE',  ( 756.3353852180819104, -125.9073299311474159, 331.1735550268788302 ) ) ;
#27695=CARTESIAN_POINT ( 'NONE',  ( 805.0264073115434940, -294.3510508353230648, 339.4763451958999099 ) ) ;
#27698=CARTESIAN_POINT ( 'NONE',  ( 764.1737431748507561, -10.37269993606250473, 371.6461892240376415 ) ) ;
#27700=CARTESIAN_POINT ( 'NONE',  ( 772.5602148656447525, -177.7255117493290868, 305.7998596910095443 ) ) ;
#27701=CARTESIAN_POINT ( 'NONE',  ( 801.9419747391806368, -90.45278447660209054, 351.9812246680014027 ) ) ;
#27707=CARTESIAN_POINT ( 'NONE',  ( 757.7880784355613741, -402.0090635724250205, 312.4576283171834916 ) ) ;
#27710=CARTESIAN_POINT ( 'NONE',  ( 767.7687537140311633, -407.9073299311465348, 372.7932403749916830 ) ) ;
#27711=CARTESIAN_POINT ( 'NONE',  ( 801.1904061080338124, -20.08914811296593328, 368.3070685750236066 ) ) ;
#27713=CARTESIAN_POINT ( 'NONE',  ( 787.6308680596127942, -11.26014174441488258, 364.1105419155492768 ) ) ;
#27716=CARTESIAN_POINT ( 'NONE',  ( 746.0683387631852383, -187.4419599262325278, 331.3260364891676204 ) ) ;
#27717=CARTESIAN_POINT ( 'NONE',  ( 759.7806653035535192, -30.99823902205680781, 324.8639956371181370 ) ) ;
#27718=CARTESIAN_POINT ( 'NONE',  ( 791.1614460488616487, -179.2601417444143692, 373.5763878283158874 ) ) ;
#27722=CARTESIAN_POINT ( 'NONE',  ( 762.3223304703356007, -151.5436935675109851, 322.3223304703362828 ) ) ;
#27724=VECTOR ( 'NONE', #38477, 1000.000000000000000 ) ;
#27726=CARTESIAN_POINT ( 'NONE',  ( 774.6312213355098493, -287.3618753856923718, 364.6798772138717482 ) ) ;
#27728=ORIENTED_EDGE ( 'NONE', *, *, #28642, .F. ) ;
#27729=CARTESIAN_POINT ( 'NONE',  ( 784.0799538623451781, -11.80559628986942577, 364.6971507214555572 ) ) ;
#27731=CARTESIAN_POINT ( 'NONE',  ( 772.4837098697145166, -263.3618753856924286, 374.5518280994205611 ) ) ;
#27732=CARTESIAN_POINT ( 'NONE',  ( 790.0220218866281812, -343.0999726633342561, 363.2186876482849129 ) ) ;
#27733=CARTESIAN_POINT ( 'NONE',  ( 801.9858362298568863, 20.92167643740319605, 312.7379699480935642 ) ) ;
#27737=ORIENTED_EDGE ( 'NONE', *, *, #21115, .T. ) ;
#27739=CARTESIAN_POINT ( 'NONE',  ( 766.7756240680305382, -326.5328690171411381, 361.5560724626415663 ) ) ;
#27742=CARTESIAN_POINT ( 'NONE',  ( 769.0155153010367712, -106.3726999360621903, 362.7791456095907279 ) ) ;
#27743=CARTESIAN_POINT ( 'NONE',  ( 771.2633955100217236, 0.09267006885218045942, 363.4237431249939618 ) ) ;
#27748=CARTESIAN_POINT ( 'NONE',  ( 804.1009440267234822, -239.4636090269709143, 314.0944755984392600 ) ) ;
#27749=CARTESIAN_POINT ( 'NONE',  ( 800.7704444035546203, -196.1692326535052473, 326.0291762391768771 ) ) ;
#27754=CARTESIAN_POINT ( 'NONE',  ( 782.5225473063381969, -70.27096629478397460, 375.2698199232970637 ) ) ;
#27758=CARTESIAN_POINT ( 'NONE',  ( 781.2370466360911223, -356.7363362996978253, 304.9990715423533629 ) ) ;
#27760=CARTESIAN_POINT ( 'NONE',  ( 772.5602148656447525, -297.7255117493286889, 305.7998596910095443 ) ) ;
#27765=CARTESIAN_POINT ( 'NONE',  ( 801.9419747391806368, -378.4527844766011526, 351.9812246680014027 ) ) ;
#27766=CARTESIAN_POINT ( 'NONE',  ( 761.4292242960306112, -161.4636090269711133, 323.2154366446414429 ) ) ;
#27769=CARTESIAN_POINT ( 'NONE',  ( 752.4576283171824116, -69.07832356259653750, 317.7880784355627952 ) ) ;
#27770=CARTESIAN_POINT ( 'NONE',  ( 771.2633955100217236, -383.9073299311466485, 363.4237431249939618 ) ) ;
#27771=CYLINDRICAL_SURFACE ( 'NONE', #9983, 30.00000000000008171 ) ;
#27772=CARTESIAN_POINT ( 'NONE',  ( 768.0187753319979720, -416.6346026584192259, 318.0580252608186242 ) ) ;
#27779=CARTESIAN_POINT ( 'NONE',  ( 800.0135310231082713, -230.0891481129652618, 325.0180583372163028 ) ) ;
#27780=CARTESIAN_POINT ( 'NONE',  ( 801.9419747391806368, -186.4527844766017779, 351.9812246680014027 ) ) ;
#27781=VECTOR ( 'NONE', #4801, 1000.000000000000000 ) ;
#27785=CARTESIAN_POINT ( 'NONE',  ( 803.6646147819161570, -377.9073299311466485, 348.8264449731210561 ) ) ;
#27790=CARTESIAN_POINT ( 'NONE',  ( 767.6429770376291799, -153.1800572038746111, 306.8695393053162093 ) ) ;
#27792=CARTESIAN_POINT ( 'NONE',  ( 773.7943932421234194, -191.8055962898689017, 305.5313806188329409 ) ) ;
#27799=CARTESIAN_POINT ( 'NONE',  ( 795.9930595647434757, -243.0783235625959833, 320.7433823573372820 ) ) ;
#27802=ORIENTED_EDGE ( 'NONE', *, *, #3160, .F. ) ;
#27808=CARTESIAN_POINT ( 'NONE',  ( 814.2805881961230625, -121.6454272087894282, 331.2368401574024119 ) ) ;
#27816=CARTESIAN_POINT ( 'NONE',  ( 802.2119215644370342, -390.0090635724249069, 367.5423716828165084 ) ) ;
#27825=CARTESIAN_POINT ( 'NONE',  ( 786.2694204179717872, -237.2817908451526421, 305.1769319972829067 ) ) ;
#27827=CARTESIAN_POINT ( 'NONE',  ( 777.4774526936600978, -202.2709662947834772, 304.7301800767027657 ) ) ;
#27832=CARTESIAN_POINT ( 'NONE',  ( 805.1927285166397041, -280.8164208402378677, 341.8018195045277707 ) ) ;
#27833=CARTESIAN_POINT ( 'NONE',  ( 766.9102291470427417, -66.55451811788050520, 318.6633372737382501 ) ) ;
#27837=CARTESIAN_POINT ( 'NONE',  ( 801.3366627262608972, -128.5328690171417634, 353.0897708529566899 ) ) ;
#27838=CARTESIAN_POINT ( 'NONE',  ( 795.1360043628807261, -332.0891481129649492, 360.2193346964456282 ) ) ;
#27842=CARTESIAN_POINT ( 'NONE',  ( 765.0180583372156207, -96.99823902205660886, 360.0135310231089534 ) ) ;
#27845=CARTESIAN_POINT ( 'NONE',  ( 811.6461892240364477, -412.7146871989590409, 324.1737431748509835 ) ) ;
#27847=CARTESIAN_POINT ( 'NONE',  ( 794.9819416627830151, -276.9982390220559978, 319.9864689768909898 ) ) ;
#27851=CARTESIAN_POINT ( 'NONE',  ( 804.4286716492782716, -401.3618753856920307, 345.3141322388244703 ) ) ;
#27859=CARTESIAN_POINT ( 'NONE',  ( 759.9864689768902508, -122.0891481129656171, 354.9819416627836404 ) ) ;
#27860=CARTESIAN_POINT ( 'NONE',  ( 805.2837595273609850, -434.7363362996975980, 340.5290396650784714 ) ) ;
#27861=CARTESIAN_POINT ( 'NONE',  ( 790.8726784830453198, -106.7146871989600498, 362.5472867521010585 ) ) ;
#27864=CARTESIAN_POINT ( 'NONE',  ( 747.3154664389472828, -355.9874144716865203, 326.4474001241230781 ) ) ;
#27865=ORIENTED_EDGE ( 'NONE', *, *, #20953, .F. ) ;
#27869=CARTESIAN_POINT ( 'NONE',  ( 815.3608509340175488, -50.73633629969874193, 341.2497674668889545 ) ) ;
#27877=CARTESIAN_POINT ( 'NONE',  ( 754.7162404726377645, -350.7363362996978253, 339.4709603349214717 ) ) ;
#27878=CARTESIAN_POINT ( 'NONE',  ( 745.5313806188320314, -351.2817908451523294, 333.7943932421247268 ) ) ;
#27880=DIRECTION ( 'NONE',  ( 0.000000000000000000, 0.000000000000000000, -1.000000000000000000 ) ) ;
#27882=CARTESIAN_POINT ( 'NONE',  ( 811.3240766477731540, -124.3726999360621619, 355.6651683502462902 ) ) ;
#27886=CARTESIAN_POINT ( 'NONE',  ( 764.8639956371174549, -176.0891481129653755, 319.7806653035542013 ) ) ;
#27887=CARTESIAN_POINT ( 'NONE',  ( 812.3518521366052028, -409.0999726633340288, 326.5853460496235243 ) ) ;
#27893=CARTESIAN_POINT ( 'NONE',  ( 801.9858362298568863, -3.078323562596726681, 312.7379699480935642 ) ) ;
#27898=CARTESIAN_POINT ( 'NONE',  ( 752.4576283171824116, -309.0783235625957559, 317.7880784355627952 ) ) ;
#27899=CARTESIAN_POINT ( 'NONE',  ( 765.0180583372156207, -120.9982390220565378, 360.0135310231089534 ) ) ;
#27901=CARTESIAN_POINT ( 'NONE',  ( 791.9812246680005501, -308.6346026584195670, 361.9419747391813189 ) ) ;
#27907=CARTESIAN_POINT ( 'NONE',  ( 800.0135310231082713, -14.08914811296595460, 325.0180583372163028 ) ) ;
#27909=CARTESIAN_POINT ( 'NONE',  ( 814.9108240113580450, -376.2709662947829656, 337.5031285880265273 ) ) ;
#27910=CARTESIAN_POINT ( 'NONE',  ( 745.1769319972822814, -257.8055962898686744, 346.2694204179732083 ) ) ;
#27915=CARTESIAN_POINT ( 'NONE',  ( 756.3353852180819104, -245.9073299311469896, 331.1735550268788302 ) ) ;
#27918=CARTESIAN_POINT ( 'NONE',  ( 814.9108240113580450, -400.2709662947828519, 337.5031285880265273 ) ) ;
#27923=CARTESIAN_POINT ( 'NONE',  ( 784.1219089521767955, -237.2817908451526421, 315.0488828828318333 ) ) ;
#27924=CARTESIAN_POINT ( 'NONE',  ( 757.8323909638827445, -122.6346026584201354, 352.1044303154654358 ) ) ;
#27928=CARTESIAN_POINT ( 'NONE',  ( 761.2382568024794409, -303.6237781080503169, 356.9571628226838129 ) ) ;
#27930=CARTESIAN_POINT ( 'NONE',  ( 776.2046728542105711, -20.19088175424429110, 304.8212110874238761 ) ) ;
#27932=CARTESIAN_POINT ( 'NONE',  ( 755.3201227861273992, -75.72551174932937101, 345.3687786644892981 ) ) ;
#27935=CARTESIAN_POINT ( 'NONE',  ( 748.6759233522253680, -400.3726999360612808, 324.3348316497537098 ) ) ;
#27938=CARTESIAN_POINT ( 'NONE',  ( 805.0264073115434940, -366.3510508353228374, 339.4763451958999099 ) ) ;
#27939=CARTESIAN_POINT ( 'NONE',  ( 746.8695393053151292, -53.90732993114765037, 327.6429770376306578 ) ) ;
#27941=CARTESIAN_POINT ( 'NONE',  ( 805.0264073115434940, -6.351050835323991173, 339.4763451958999099 ) ) ;
#27945=CARTESIAN_POINT ( 'NONE',  ( 788.7631598425961101, -169.4419599262325562, 305.7194118038759143 ) ) ;
#27946=CARTESIAN_POINT ( 'NONE',  ( 804.4286716492782716, -17.36187538569322086, 345.3141322388244703 ) ) ;
#27950=CARTESIAN_POINT ( 'NONE',  ( 792.1044303154645831, -204.4527844766016926, 317.8323909638837677 ) ) ;
#27952=CARTESIAN_POINT ( 'NONE',  ( 771.1735550268780344, -321.1800572038740711, 316.3353852180828198 ) ) ;
#27955=CARTESIAN_POINT ( 'NONE',  ( 769.1273215169530886, -46.71468719896022748, 317.4527132478988847 ) ) ;
#27957=CARTESIAN_POINT ( 'NONE',  ( 767.6429770376291799, -273.1800572038742985, 306.8695393053162093 ) ) ;
#27958=CARTESIAN_POINT ( 'NONE',  ( 804.6971507214547046, -339.2817908451524431, 344.0799538623459739 ) ) ;
#27959=CARTESIAN_POINT ( 'NONE',  ( 778.7502325331095108, 23.64894916467591912, 304.6391490659818828 ) ) ;
#27964=CARTESIAN_POINT ( 'NONE',  ( 782.4968714119720516, -250.8164208402379245, 305.0891759886411023 ) ) ;
#27965=CARTESIAN_POINT ( 'NONE',  ( 805.1016975059191054, -342.8965053807773984, 343.0745993439771837 ) ) ;
#27967=CARTESIAN_POINT ( 'NONE',  ( 755.8894580844503253, -111.8272453906076151, 332.3691319403863531 ) ) ;
#27968=CARTESIAN_POINT ( 'NONE',  ( 771.1735550268778070, -9.180057203875058747, 316.3353852180827630 ) ) ;
#27972=CARTESIAN_POINT ( 'NONE',  ( 814.4686193811664907, -243.2817908451526705, 346.2056067578752732 ) ) ;
#27974=CARTESIAN_POINT ( 'NONE',  ( 801.3366627262608972, -176.5328690171416213, 353.0897708529566899 ) ) ;
#27978=CARTESIAN_POINT ( 'NONE',  ( 763.0537975583475827, -24.45278447660229304, 371.0346526505627480 ) ) ;
#27979=CARTESIAN_POINT ( 'NONE',  ( 751.6929314249748586, -78.99823902205662307, 318.8095938919659034 ) ) ;
#27980=CARTESIAN_POINT ( 'NONE',  ( 809.1994704715707485, -452.9681489794448908, 335.3884333643831042 ) ) ;
#27983=CARTESIAN_POINT ( 'NONE',  ( 797.8822607201568644, -342.5545181178796952, 370.1134526219340160 ) ) ;
#27985=CARTESIAN_POINT ( 'NONE',  ( 746.8695393053150156, -317.9073299311468190, 327.6429770376306010 ) ) ;
#27989=CARTESIAN_POINT ( 'NONE',  ( 800.2193346964447755, -378.9982390220555999, 355.1360043628815788 ) ) ;
#27990=CARTESIAN_POINT ( 'NONE',  ( 802.9823548866075953, -145.0999726633347677, 330.0799878456151077 ) ) ;
#27993=CARTESIAN_POINT ( 'NONE',  ( 793.4146539503750546, -73.98741447168741558, 307.6481478633938877 ) ) ;
#27994=CARTESIAN_POINT ( 'NONE',  ( 785.3141322388236176, -405.7255117493283478, 364.4286716492789537 ) ) ;
#27997=CARTESIAN_POINT ( 'NONE',  ( 756.3353852180819104, -437.9073299311463074, 331.1735550268788302 ) ) ;
#28003=CARTESIAN_POINT ( 'NONE',  ( 755.3201227861273992, -243.7255117493287742, 345.3687786644892981 ) ) ;
#28004=CARTESIAN_POINT ( 'NONE',  ( 785.3141322388236176, -213.7255117493289731, 364.4286716492789537 ) ) ;
#28008=CARTESIAN_POINT ( 'NONE',  ( 788.8264449731200330, -381.1800572038737869, 363.6646147819171233 ) ) ;
#28011=CARTESIAN_POINT ( 'NONE',  ( 751.6929314249750860, -150.9982390220564241, 318.8095938919659034 ) ) ;
#28013=CARTESIAN_POINT ( 'NONE',  ( 810.1134526219336749, -200.5328690171415644, 357.8822607201570349 ) ) ;
#28018=CARTESIAN_POINT ( 'NONE',  ( 776.9566956441375396, -228.8965053807778816, 364.8461984189686405 ) ) ;
#28028=CARTESIAN_POINT ( 'NONE',  ( 802.2119215644370342, -126.0090635724257737, 367.5423716828165084 ) ) ;
#28036=CARTESIAN_POINT ( 'NONE',  ( 745.7194118038753459, -373.6454272087887034, 348.7631598425976449 ) ) ;
#28040=CARTESIAN_POINT ( 'NONE',  ( 805.1927285166397041, 7.183579159761247723, 341.8018195045277707 ) ) ;
#28042=CARTESIAN_POINT ( 'NONE',  ( 771.3260364891663130, -235.6454272087890729, 306.0683387631859773 ) ) ;
#28044=CARTESIAN_POINT ( 'NONE',  ( 772.4837098697144029, -191.3618753856925991, 374.5518280994205611 ) ) ;
#28047=CARTESIAN_POINT ( 'NONE',  ( 805.1927285166397041, -304.8164208402376403, 341.8018195045277707 ) ) ;
#28048=CARTESIAN_POINT ( 'NONE',  ( 790.9844846989617508, -94.37269993606224716, 317.2208543904092721 ) ) ;
#28054=CARTESIAN_POINT ( 'NONE',  ( 754.9735926884551418, -138.3510508353236048, 340.5236548041000333 ) ) ;
#28055=CARTESIAN_POINT ( 'NONE',  ( 756.3353852180819104, -317.9073299311468190, 331.1735550268788302 ) ) ;
#28058=CARTESIAN_POINT ( 'NONE',  ( 795.1360043628807261, -92.08914811296568814, 360.2193346964456282 ) ) ;
#28060=DIRECTION ( 'NONE',  ( 0.000000000000000000, 0.000000000000000000, -1.000000000000000000 ) ) ;
#28061=CARTESIAN_POINT ( 'NONE',  ( 813.2346286133761168, -413.2601417444136018, 328.9521613784389160 ) ) ;
#28062=ORIENTED_EDGE ( 'NONE', *, *, #30074, .F. ) ;
#28063=CARTESIAN_POINT ( 'NONE',  ( 792.1044303154645831, -300.4527844766012663, 317.8323909638837677 ) ) ;
#28065=CARTESIAN_POINT ( 'NONE',  ( 762.1405469898971887, -409.5436935675101040, 357.8594530101015607 ) ) ;
#28071=CARTESIAN_POINT ( 'NONE',  ( 764.8639956371174549, -128.0891481129655176, 319.7806653035542013 ) ) ;
#28072=CARTESIAN_POINT ( 'NONE',  ( 759.0159684113467620, -424.9181544815158986, 325.8855110935213020 ) ) ;
#28073=CARTESIAN_POINT ( 'NONE',  ( 770.0799878456142551, -109.9874144716873019, 362.9823548866085616 ) ) ;
#28075=LINE ( 'NONE', #24154, #40258 ) ;
#28076=CARTESIAN_POINT ( 'NONE',  ( 752.4576283171824116, -405.0783235625954148, 317.7880784355627952 ) ) ;
#28082=CARTESIAN_POINT ( 'NONE',  ( 760.0363995740630116, -34.91815448151697154, 368.7758568127991907 ) ) ;
#28092=CARTESIAN_POINT ( 'NONE',  ( 799.2566176426618085, -360.0090635724250774, 324.0069404352559559 ) ) ;
#28093=CARTESIAN_POINT ( 'NONE',  ( 749.5768839229115201, -324.5545181178796952, 358.0661480581553064 ) ) ;
#28097=CARTESIAN_POINT ( 'NONE',  ( 807.2620300519052989, -144.0090635724257027, 318.0141637701419768 ) ) ;
#28102=CARTESIAN_POINT ( 'NONE',  ( 801.9419747391806368, -186.4527844766017779, 351.9812246680014027 ) ) ;
#28104=CARTESIAN_POINT ( 'NONE',  ( 752.7379699480933368, -444.0090635724249069, 361.9858362298580232 ) ) ;
#28110=CARTESIAN_POINT ( 'NONE',  ( 813.2346286133761168, -5.260141744414903897, 328.9521613784389160 ) ) ;
#28112=CARTESIAN_POINT ( 'NONE',  ( 778.2165204200184689, -262.8164208402379245, 364.9363028652563230 ) ) ;
#28116=CARTESIAN_POINT ( 'NONE',  ( 759.8311093483677041, -310.1692326535048778, 310.9282345327691814 ) ) ;
#28117=CARTESIAN_POINT ( 'NONE',  ( 804.6798772138710092, -135.7255117493291721, 334.6312213355106451 ) ) ;
#28119=CARTESIAN_POINT ( 'NONE',  ( 762.1405469898971887, -313.5436935675102745, 357.8594530101015607 ) ) ;
#28125=EDGE_CURVE ( 'NONE', #37078, #29447, #5141, .T. ) ;
#28126=CARTESIAN_POINT ( 'NONE',  ( 795.1360043628807261, -20.08914811296592973, 360.2193346964456282 ) ) ;
#28128=CARTESIAN_POINT ( 'NONE',  ( 749.2812353651451076, -366.4527844766012095, 323.2262854647983090 ) ) ;
#28129=CARTESIAN_POINT ( 'NONE',  ( 771.2368401574024119, -253.4419599262323572, 374.2805881961240857 ) ) ;
#28131=CARTESIAN_POINT ( 'NONE',  ( 746.0683387631852383, -67.44195992623289726, 331.3260364891676204 ) ) ;
#28136=CARTESIAN_POINT ( 'NONE',  ( 800.0135310231082713, -230.0891481129652618, 325.0180583372163028 ) ) ;
#28137=CARTESIAN_POINT ( 'NONE',  ( 792.2312462859673587, -395.9073299311465348, 307.2067596250082602 ) ) ;
#28144=CARTESIAN_POINT ( 'NONE',  ( 779.4763451958990572, -272.7363362996981095, 365.0264073115438919 ) ) ;
#28145=CARTESIAN_POINT ( 'NONE',  ( 791.9812246680005501, -116.6346026584201780, 361.9419747391813189 ) ) ;
#28151=CARTESIAN_POINT ( 'NONE',  ( 755.8398074228967971, -307.4419599262320730, 333.4516893846970333 ) ) ;
#28153=CARTESIAN_POINT ( 'NONE',  ( 746.4236121716829757, -39.82724539060786384, 328.8385539511384650 ) ) ;
#28155=CARTESIAN_POINT ( 'NONE',  ( 746.8695393053150156, -173.9073299311472169, 327.6429770376306010 ) ) ;
#28156=CARTESIAN_POINT ( 'NONE',  ( 800.0135310231082713, -86.08914811296573077, 325.0180583372163028 ) ) ;
#28159=CARTESIAN_POINT ( 'NONE',  ( 762.1177392798416577, -450.5545181178793541, 309.8865473780659272 ) ) ;
#28162=CARTESIAN_POINT ( 'NONE',  ( 754.8983024940795303, -354.8965053807774552, 336.9254006560228163 ) ) ;
#28163=CARTESIAN_POINT ( 'NONE',  ( 759.0252816721024374, -48.99823902205675807, 368.0189434323527280 ) ) ;
#28165=CARTESIAN_POINT ( 'NONE',  ( 775.9200461376533440, -47.80559628986931386, 315.3028492785443291 ) ) ;
#28168=CARTESIAN_POINT ( 'NONE',  ( 805.9055244015594326, -195.6237781080506863, 315.8990559732753240 ) ) ;
#28169=CARTESIAN_POINT ( 'NONE',  ( 805.1927285166399315, -16.81642084023867412, 341.8018195045277707 ) ) ;
#28172=CARTESIAN_POINT ( 'NONE',  ( 801.9419747391806368, -210.4527844766016926, 351.9812246680014027 ) ) ;
#28174=CARTESIAN_POINT ( 'NONE',  ( 802.1676090361155502, -326.6346026584194533, 327.8955696845344505 ) ) ;
#28177=ORIENTED_EDGE ( 'NONE', *, *, #2078, .T. ) ;
#28178=CARTESIAN_POINT ( 'NONE',  ( 758.6633372737375112, -68.53286901714197654, 326.9102291470432533 ) ) ;
#28180=CARTESIAN_POINT ( 'NONE',  ( 767.7687537140311633, -239.9073299311470748, 372.7932403749916830 ) ) ;
#28181=CARTESIAN_POINT ( 'NONE',  ( 768.8385539511368734, 0.7398582555850804487, 306.4236121716840557 ) ) ;
#28186=CARTESIAN_POINT ( 'NONE',  ( 812.7932403749906598, -279.1800572038741848, 327.7687537140311633 ) ) ;
#28188=CARTESIAN_POINT ( 'NONE',  ( 801.3366627262608972, -344.5328690171410813, 353.0897708529566899 ) ) ;
#28190=CARTESIAN_POINT ( 'NONE',  ( 804.1105419155481968, -147.8272453906075157, 347.6308680596136469 ) ) ;
#28191=CARTESIAN_POINT ( 'NONE',  ( 803.6646147819161570, -17.90732993114776406, 348.8264449731210561 ) ) ;
#28195=CARTESIAN_POINT ( 'NONE',  ( 783.7953271457878373, -224.1908817542436623, 375.1787889125761239 ) ) ;
#28196=CARTESIAN_POINT ( 'NONE',  ( 755.0488828828309806, -185.8055962898689302, 344.1219089521771934 ) ) ;
#28200=CARTESIAN_POINT ( 'NONE',  ( 777.4774526936600978, -10.27096629478414691, 304.7301800767027657 ) ) ;
#28201=CARTESIAN_POINT ( 'NONE',  ( 754.9967657858570647, -73.54369356751118403, 365.0032342141425374 ) ) ;
#28205=CARTESIAN_POINT ( 'NONE',  ( 764.1737431748507561, -346.3726999360614514, 371.6461892240376415 ) ) ;
#28206=DIRECTION ( 'NONE',  ( 0.000000000000000000, 1.000000000000000000, 0.000000000000000000 ) ) ;
#28207=CARTESIAN_POINT ( 'NONE',  ( 787.4397851343537695, -333.7255117493286320, 374.2001403089903988 ) ) ;
#28211=CARTESIAN_POINT ( 'NONE',  ( 756.3353852180819104, -413.9073299311465348, 331.1735550268788302 ) ) ;
#28212=CARTESIAN_POINT ( 'NONE',  ( 783.0745993439762742, -152.1908817542438612, 365.1016975059196739 ) ) ;
#28215=CARTESIAN_POINT ( 'NONE',  ( 748.3538107759620743, -112.7146871989600356, 355.8262568251490165 ) ) ;
#28216=CARTESIAN_POINT ( 'NONE',  ( 758.0580252608178853, -390.4527844766011526, 328.0187753319985404 ) ) ;
#28222=CARTESIAN_POINT ( 'NONE',  ( 762.1405469898971887, -241.5436935675106156, 357.8594530101015607 ) ) ;
#28223=CARTESIAN_POINT ( 'NONE',  ( 785.3687786644885591, -227.3618753856925423, 315.3201227861280813 ) ) ;
#28226=CARTESIAN_POINT ( 'NONE',  ( 805.0032342141412300, 10.45630643248850866, 314.9967657858571783 ) ) ;
#28229=CARTESIAN_POINT ( 'NONE',  ( 800.2193346964447755, -426.9982390220554862, 355.1360043628815788 ) ) ;
#28232=CARTESIAN_POINT ( 'NONE',  ( 772.4837098697145166, -143.3618753856927697, 374.5518280994205611 ) ) ;
#28238=CARTESIAN_POINT ( 'NONE',  ( 760.5453621957607311, -213.0783235625960401, 323.8424801807151425 ) ) ;
#28239=CARTESIAN_POINT ( 'NONE',  ( 758.7867965644027208, 16.45630643248849267, 318.7867965644036872 ) ) ;
#28256=CARTESIAN_POINT ( 'NONE',  ( 755.3201227861273992, -3.725511749329622813, 345.3687786644892981 ) ) ;
#28259=CARTESIAN_POINT ( 'NONE',  ( 795.8262568251477660, -262.3726999360617924, 308.3538107759623585 ) ) ;
#28261=CARTESIAN_POINT ( 'NONE',  ( 812.7932403749906598, -207.1800572038744406, 327.7687537140311633 ) ) ;
#28264=CARTESIAN_POINT ( 'NONE',  ( 803.4237431249931660, -279.1800572038741848, 331.2633955100225194 ) ) ;
#28265=CARTESIAN_POINT ( 'NONE',  ( 800.9840315886518738, -100.9181544815167513, 354.1144889064786412 ) ) ;
#28270=CARTESIAN_POINT ( 'NONE',  ( 784.0799538623451781, -131.8055962898690439, 364.6971507214555572 ) ) ;
#28271=CARTESIAN_POINT ( 'NONE',  ( 771.1735550268778070, -369.1800572038739574, 316.3353852180827630 ) ) ;
#28274=CARTESIAN_POINT ( 'NONE',  ( 755.3201227861273992, -99.72551174932928575, 345.3687786644892981 ) ) ;
#28277=CARTESIAN_POINT ( 'NONE',  ( 786.2056067578752163, -419.8055962898681059, 374.4686193811670023 ) ) ;
#28280=CARTESIAN_POINT ( 'NONE',  ( 792.1044303154645831, -324.4527844766013231, 317.8323909638837677 ) ) ;
#28284=CARTESIAN_POINT ( 'NONE',  ( 778.2165204200184689, -406.8164208402375266, 364.9363028652563230 ) ) ;
#28291=CARTESIAN_POINT ( 'NONE',  ( 763.8424801807145741, -426.0090635724247932, 320.5453621957614700 ) ) ;
#28292=CARTESIAN_POINT ( 'NONE',  ( 805.0264073115434940, -126.3510508353236048, 339.4763451958999099 ) ) ;
#28296=CARTESIAN_POINT ( 'NONE',  ( 795.6651683502461765, -394.7146871989591546, 371.3240766477733814 ) ) ;
#28301=CARTESIAN_POINT ( 'NONE',  ( 748.6759233522253680, -16.37269993606248519, 324.3348316497537098 ) ) ;
#28310=CARTESIAN_POINT ( 'NONE',  ( 783.0745993439762742, -368.1908817542433212, 365.1016975059196739 ) ) ;
#28311=CARTESIAN_POINT ( 'NONE',  ( 783.7953271457878373, -344.1908817542433212, 375.1787889125761239 ) ) ;
#28316=CARTESIAN_POINT ( 'NONE',  ( 764.1737431748507561, -154.3726999360620198, 371.6461892240376415 ) ) ;
#28318=CARTESIAN_POINT ( 'NONE',  ( 755.2512626584698410, -127.5436935675110561, 315.2512626584710915 ) ) ;
#28322=CARTESIAN_POINT ( 'NONE',  ( 771.1735550268778070, -201.1800572038744690, 316.3353852180827630 ) ) ;
#28324=CARTESIAN_POINT ( 'NONE',  ( 796.9571628226829034, 0.5363909730283709099, 321.2382568024804641 ) ) ;
#28328=CARTESIAN_POINT ( 'NONE',  ( 795.6651683502461765, 13.28531280103958423, 371.3240766477733814 ) ) ;
#28332=CARTESIAN_POINT ( 'NONE',  ( 813.9316612368132837, -295.4419599262320730, 348.6739635108323228 ) ) ;
#28333=CARTESIAN_POINT ( 'NONE',  ( 767.8955696845334842, -120.4527844766019768, 362.1676090361161755 ) ) ;
#28335=AXIS2_PLACEMENT_3D ( 'NONE', #45467, #2962, #13826 ) ;
#28337=CARTESIAN_POINT ( 'NONE',  ( 778.2165204200184689, -310.8164208402377540, 364.9363028652563230 ) ) ;
#28339=VECTOR ( 'NONE', #30601, 1000.000000000000000 ) ;
#28341=CARTESIAN_POINT ( 'NONE',  ( 810.7187646348534145, -66.45278447660216159, 356.7737145352016341 ) ) ;
#28347=CARTESIAN_POINT ( 'NONE',  ( 767.8955696845333705, -24.45278447660229304, 362.1676090361162323 ) ) ;
#28349=CARTESIAN_POINT ( 'NONE',  ( 751.9810565676468741, -386.0891481129647786, 360.9747183278973921 ) ) ;
#28350=CARTESIAN_POINT ( 'NONE',  ( 803.8556311672234642, -273.6237781080504305, 365.6418435158340117 ) ) ;
#28351=CARTESIAN_POINT ( 'NONE',  ( 815.1787889125755555, -78.89650538077832209, 343.7953271457877804 ) ) ;
#28359=CARTESIAN_POINT ( 'NONE',  ( 812.7932403749906598, -399.1800572038738437, 327.7687537140311633 ) ) ;
#28367=CARTESIAN_POINT ( 'NONE',  ( 790.9844846989617508, -262.3726999360617924, 317.2208543904092721 ) ) ;
#28368=CARTESIAN_POINT ( 'NONE',  ( 804.9363028652555840, -112.2709662947838325, 338.2165204200192079 ) ) ;
#28369=EDGE_LOOP ( 'NONE', ( #23629, #27208, #34034, #16192 ) ) ;
#28372=CARTESIAN_POINT ( 'NONE',  ( 803.8651313633788504, -293.2601417444139429, 332.4468031744301015 ) ) ;
#28375=CARTESIAN_POINT ( 'NONE',  ( 811.3240766477731540, -52.37269993606237506, 355.6651683502462902 ) ) ;
#28377=CIRCLE ( 'NONE', #18804, 30.00000000000002842 ) ;
#28378=CARTESIAN_POINT ( 'NONE',  ( 745.0891759886404770, -172.2709662947836478, 342.4968714119734159 ) ) ;
#28379=CARTESIAN_POINT ( 'NONE',  ( 797.8594530101008786, -85.54369356751118403, 322.1405469898980982 ) ) ;
#28383=CARTESIAN_POINT ( 'NONE',  ( 745.5313806188320314, -447.2817908451521021, 333.7943932421247268 ) ) ;
#28386=CARTESIAN_POINT ( 'NONE',  ( 801.3366627262608972, -368.5328690171409676, 353.0897708529566899 ) ) ;
#28387=CARTESIAN_POINT ( 'NONE',  ( 758.8095938919644823, -32.08914811296589420, 311.6929314249762797 ) ) ;
#28391=CARTESIAN_POINT ( 'NONE',  ( 804.9511171171677688, -53.80559628986930676, 335.8780910478229202 ) ) ;
#28395=CARTESIAN_POINT ( 'NONE',  ( 793.4146539503750546, -193.9874144716870319, 307.6481478633938877 ) ) ;
#28396=CARTESIAN_POINT ( 'NONE',  ( 755.0636971347428243, -4.270966294784170003, 341.7834795799807353 ) ) ;
#28398=CARTESIAN_POINT ( 'NONE',  ( 766.7756240680305382, -374.5328690171410813, 361.5560724626415663 ) ) ;
#28402=CARTESIAN_POINT ( 'NONE',  ( 795.1360043628807261, -188.0891481129653187, 360.2193346964456282 ) ) ;
#28404=CARTESIAN_POINT ( 'NONE',  ( 762.3223304703356007, -343.5436935675103314, 322.3223304703362828 ) ) ;
#28410=CARTESIAN_POINT ( 'NONE',  ( 799.4546378042377910, -57.07832356259658013, 356.1575198192848006 ) ) ;
#28413=CARTESIAN_POINT ( 'NONE',  ( 772.5602148656447525, -249.7255117493288594, 305.7998596910095443 ) ) ;
#28414=CARTESIAN_POINT ( 'NONE',  ( 745.1769319972822814, 6.194403710130517382, 346.2694204179732083 ) ) ;
#28419=CARTESIAN_POINT ( 'NONE',  ( 787.5162901302840055, -275.3618753856923149, 305.4481719005792684 ) ) ;
#28421=CARTESIAN_POINT ( 'NONE',  ( 793.9708237608222134, -214.9181544815164386, 319.2295555964448681 ) ) ;
#28422=CARTESIAN_POINT ( 'NONE',  ( 779.4709603349208464, -336.3510508353228943, 314.7162404726379918 ) ) ;
#28424=CARTESIAN_POINT ( 'NONE',  ( 801.5560724626406000, -168.5545181178802352, 326.7756240680316182 ) ) ;
#28425=CARTESIAN_POINT ( 'NONE',  ( 756.5762568750052424, -3.180057203875080063, 348.7366044899774238 ) ) ;
#28430=CARTESIAN_POINT ( 'NONE',  ( 815.3608509340175488, -218.7363362996982232, 341.2497674668889545 ) ) ;
#28431=CARTESIAN_POINT ( 'NONE',  ( 794.1144889064781864, -370.1692326535045936, 360.9840315886528401 ) ) ;
#28432=CARTESIAN_POINT ( 'NONE',  ( 757.2208543904082489, -184.7146871989598083, 350.9844846989624330 ) ) ;
#28435=CARTESIAN_POINT ( 'NONE',  ( 802.1676090361156639, 9.365397341579420498, 327.8955696845344505 ) ) ;
#28439=CARTESIAN_POINT ( 'NONE',  ( 813.1304606946830518, -17.90732993114776406, 352.3570229623690580 ) ) ;
#28440=CARTESIAN_POINT ( 'NONE',  ( 787.5162901302840055, -83.36187538569296862, 305.4481719005792684 ) ) ;
#28441=DIRECTION ( 'NONE',  ( 0.000000000000000000, 0.000000000000000000, -1.000000000000000000 ) ) ;
#28445=CARTESIAN_POINT ( 'NONE',  ( 799.9636004259356241, -358.9181544815160123, 311.2241431872006956 ) ) ;
#28447=CARTESIAN_POINT ( 'NONE',  ( 748.9653473494363425, -338.6346026584195101, 356.9462024416521331 ) ) ;
#28452=CARTESIAN_POINT ( 'NONE',  ( 756.5762568750052424, -435.1800572038737869, 348.7366044899774238 ) ) ;
#28453=CARTESIAN_POINT ( 'NONE',  ( 755.3028492785439312, -207.2817908451527842, 335.9200461376539693 ) ) ;
#28456=CARTESIAN_POINT ( 'NONE',  ( 812.6845335610512393, -103.9874144716873161, 353.5525998758768651 ) ) ;
#28457=CARTESIAN_POINT ( 'NONE',  ( 788.7366044899766848, -419.9073299311465348, 316.5762568750059813 ) ) ;
#28463=CARTESIAN_POINT ( 'NONE',  ( 778.1981804954714335, -226.2709662947834204, 314.8072714833589885 ) ) ;
#28464=CARTESIAN_POINT ( 'NONE',  ( 804.9363028652555840, -232.2709662947834488, 338.2165204200192079 ) ) ;
#28469=CARTESIAN_POINT ( 'NONE',  ( 759.7806653035534055, -414.9982390220555430, 324.8639956371180801 ) ) ;
#28474=CARTESIAN_POINT ( 'NONE',  ( 814.2001403089898304, -161.3618753856927697, 347.4397851343538264 ) ) ;
#28475=CARTESIAN_POINT ( 'NONE',  ( 769.9779781133707957, -283.0999726633344267, 316.7813123517150871 ) ) ;
#28476=CARTESIAN_POINT ( 'NONE',  ( 757.2208543904082489, -376.7146871989592682, 350.9844846989624330 ) ) ;
#28483=CARTESIAN_POINT ( 'NONE',  ( 798.7617431975189675, -243.6237781080504590, 323.0428371773161871 ) ) ;
#28494=CARTESIAN_POINT ( 'NONE',  ( 791.0478386215596629, -141.8272453906075157, 306.7653713866226326 ) ) ;
#28500=CARTESIAN_POINT ( 'NONE',  ( 750.9282345327678740, -376.9181544815159555, 319.8311093483690115 ) ) ;
#28505=CARTESIAN_POINT ( 'NONE',  ( 800.0135310231082713, -14.08914811296595460, 325.0180583372163028 ) ) ;
#28507=CARTESIAN_POINT ( 'NONE',  ( 760.0363995740630116, -250.9181544815163534, 368.7758568127991907 ) ) ;
#28509=CARTESIAN_POINT ( 'NONE',  ( 777.5031285880264704, -214.8164208402380666, 374.9108240113588408 ) ) ;
#28513=CARTESIAN_POINT ( 'NONE',  ( 794.9819416627830151, -324.9982390220559409, 319.9864689768909898 ) ) ;
#28515=CARTESIAN_POINT ( 'NONE',  ( 796.9571628226829034, -95.46360902697132644, 321.2382568024804641 ) ) ;
#28516=CARTESIAN_POINT ( 'NONE',  ( 800.9840315886518738, -76.91815448151683654, 354.1144889064786412 ) ) ;
#28520=CARTESIAN_POINT ( 'NONE',  ( 805.1016975059191054, -150.8965053807781089, 343.0745993439771837 ) ) ;
#28521=CARTESIAN_POINT ( 'NONE',  ( 803.4237431249931660, -351.1800572038740142, 331.2633955100225194 ) ) ;
#28523=AXIS2_PLACEMENT_3D ( 'NONE', #10309, #35246, #38042 ) ;
#28525=CARTESIAN_POINT ( 'NONE',  ( 757.8323909638827445, -146.6346026584200217, 352.1044303154654358 ) ) ;
#28528=CARTESIAN_POINT ( 'NONE',  ( 759.8311093483677041, -430.1692326535043094, 310.9282345327691814 ) ) ;
#28530=CARTESIAN_POINT ( 'NONE',  ( 781.8018195045266339, -310.2709662947832499, 365.1927285166406705 ) ) ;
#28534=CARTESIAN_POINT ( 'NONE',  ( 791.9812246680005501, -404.6346026584193396, 361.9419747391813189 ) ) ;
#28538=ORIENTED_EDGE ( 'NONE', *, *, #5460, .T. ) ;
#28541=CARTESIAN_POINT ( 'NONE',  ( 766.9102291470427417, -450.5545181178793541, 318.6633372737382501 ) ) ;
#28542=CARTESIAN_POINT ( 'NONE',  ( 755.0488828828309806, -137.8055962898690154, 344.1219089521771934 ) ) ;
#28544=CARTESIAN_POINT ( 'NONE',  ( 767.9999999999992042, 178.9475563372491251, 320.0000000000000000 ) ) ;
#28546=CARTESIAN_POINT ( 'NONE',  ( 778.7502325331095108, -384.3510508353227806, 304.6391490659818828 ) ) ;
#28547=ORIENTED_EDGE ( 'NONE', *, *, #26868, .F. ) ;
#28552=CARTESIAN_POINT ( 'NONE',  ( 781.2370466360911223, -20.73633629969883430, 304.9990715423533629 ) ) ;
#28562=CARTESIAN_POINT ( 'NONE',  ( 798.5707757039680246, -365.4636090269705164, 356.7845633553585003 ) ) ;
#28563=CARTESIAN_POINT ( 'NONE',  ( 810.4231160770870019, -336.5545181178796952, 321.9338519418446936 ) ) ;
#28568=CARTESIAN_POINT ( 'NONE',  ( 747.6481478633932056, -157.0999726633347962, 353.4146539503763620 ) ) ;
#28570=CARTESIAN_POINT ( 'NONE',  ( 772.5602148656447525, -105.7255117493293000, 305.7998596910095443 ) ) ;
#28575=CARTESIAN_POINT ( 'NONE',  ( 805.1927285166397041, -208.8164208402380666, 341.8018195045277707 ) ) ;
#28576=CARTESIAN_POINT ( 'NONE',  ( 804.1105419155481968, -3.827245390607979303, 347.6308680596136469 ) ) ;
#28581=CARTESIAN_POINT ( 'NONE',  ( 771.2368401574024119, -13.44195992623305713, 374.2805881961240857 ) ) ;
#28582=VERTEX_POINT ( 'NONE', #7871 ) ;
#28586=CARTESIAN_POINT ( 'NONE',  ( 745.1769319972822814, -305.8055962898684470, 346.2694204179732083 ) ) ;
#28587=CARTESIAN_POINT ( 'NONE',  ( 781.8018195045267476, -118.2709662947838041, 365.1927285166407273 ) ) ;
#28590=CARTESIAN_POINT ( 'NONE',  ( 754.8072714833581358, -316.8164208402377540, 338.1981804954720587 ) ) ;
#28593=CARTESIAN_POINT ( 'NONE',  ( 745.0891759886404770, -76.27096629478394618, 342.4968714119734159 ) ) ;
#28598=CARTESIAN_POINT ( 'NONE',  ( 785.3687786644884454, -35.36187538569316047, 315.3201227861279676 ) ) ;
#28600=CARTESIAN_POINT ( 'NONE',  ( 815.2698199232962679, -400.8164208402374697, 342.5225473063383674 ) ) ;
#28601=CARTESIAN_POINT ( 'NONE',  ( 749.8865473780648472, -284.5328690171412518, 322.1177392798429082 ) ) ;
#28602=CARTESIAN_POINT ( 'NONE',  ( 748.3538107759620743, -88.71468719896009247, 355.8262568251490165 ) ) ;
#28609=CARTESIAN_POINT ( 'NONE',  ( 796.7737145352015204, -380.6346026584192828, 370.7187646348536987 ) ) ;
#28615=EDGE_CURVE ( 'NONE', #30209, #25624, #23283, .T. ) ;
#28616=CARTESIAN_POINT ( 'NONE',  ( 763.0428371773158460, -251.4636090269709143, 358.7617431975195359 ) ) ;
#28617=CARTESIAN_POINT ( 'NONE',  ( 794.9819416627830151, -156.9982390220564241, 319.9864689768909898 ) ) ;
#28621=CARTESIAN_POINT ( 'NONE',  ( 772.3691319403857278, -311.2601417444139429, 315.8894580844506663 ) ) ;
#28624=CARTESIAN_POINT ( 'NONE',  ( 812.3518521366052028, -49.09997266333511590, 326.5853460496235243 ) ) ;
#28625=CARTESIAN_POINT ( 'NONE',  ( 759.9864689768902508, -194.0891481129654039, 354.9819416627836404 ) ) ;
#28629=CARTESIAN_POINT ( 'NONE',  ( 788.7366044899766848, -83.90732993114754379, 316.5762568750059813 ) ) ;
#28630=DIRECTION ( 'NONE',  ( 0.000000000000000000, 1.000000000000000000, 1.110223024625155554E-15 ) ) ;
#28632=CARTESIAN_POINT ( 'NONE',  ( 814.4686193811664907, -459.2817908451519884, 346.2056067578752732 ) ) ;
#28634=CARTESIAN_POINT ( 'NONE',  ( 757.2208543904082489, -376.7146871989592682, 350.9844846989624330 ) ) ;
#28635=CARTESIAN_POINT ( 'NONE',  ( 800.9747183278959710, -60.99823902205671544, 311.9810565676471583 ) ) ;
#28637=CARTESIAN_POINT ( 'NONE',  ( 802.7791456095903868, -52.71468719896020616, 329.0155153010375102 ) ) ;
#28640=CARTESIAN_POINT ( 'NONE',  ( 803.8556311672234642, -201.6237781080506863, 365.6418435158340117 ) ) ;
#28641=CARTESIAN_POINT ( 'NONE',  ( 800.0135310231082713, -14.08914811296595460, 325.0180583372163028 ) ) ;
#28642=EDGE_CURVE ( 'NONE', #17401, #37455, #40414, .T. ) ;
#28645=CARTESIAN_POINT ( 'NONE',  ( 785.3141322388236176, -213.7255117493289731, 364.4286716492789537 ) ) ;
#28647=CARTESIAN_POINT ( 'NONE',  ( 754.8072714833583632, -316.8164208402377540, 338.1981804954721156 ) ) ;
#28651=CARTESIAN_POINT ( 'NONE',  ( 773.3843516231979720, -37.44195992623299674, 364.4086373105754433 ) ) ;
#28654=CARTESIAN_POINT ( 'NONE',  ( 814.9108240113580450, -304.2709662947832499, 337.5031285880265273 ) ) ;
#28655=CARTESIAN_POINT ( 'NONE',  ( 758.0141637701419768, 8.921676437403235127, 367.2620300519063790 ) ) ;
#28660=CARTESIAN_POINT ( 'NONE',  ( 745.0891759886404770, -292.2709662947831930, 342.4968714119734159 ) ) ;
#28661=ADVANCED_FACE ( 'NONE', ( #15476 ), #5279, .T. ) ;
#28663=CARTESIAN_POINT ( 'NONE',  ( 790.8726784830453198, -346.7146871989592682, 362.5472867521010585 ) ) ;
#28666=CARTESIAN_POINT ( 'NONE',  ( 802.5472867521000353, -172.3726999360619914, 350.8726784830461156 ) ) ;
#28667=CARTESIAN_POINT ( 'NONE',  ( 802.1676090361156639, -38.63460265842041252, 327.8955696845344505 ) ) ;
#28671=CARTESIAN_POINT ( 'NONE',  ( 776.2046728542105711, -260.1908817542435486, 304.8212110874238761 ) ) ;
#28672=CARTESIAN_POINT ( 'NONE',  ( 756.7813123517142913, -187.9874144716870603, 329.9779781133712504 ) ) ;
#28674=CARTESIAN_POINT ( 'NONE',  ( 791.9812246680005501, 3.365397341579444479, 361.9419747391813189 ) ) ;
#28678=CARTESIAN_POINT ( 'NONE',  ( 745.4481719005789273, -27.72551174932954510, 347.5162901302853129 ) ) ;
#28679=CARTESIAN_POINT ( 'NONE',  ( 801.1904061080336987, -92.08914811296568814, 368.3070685750235498 ) ) ;
#28684=CARTESIAN_POINT ( 'NONE',  ( 744.6391490659812007, -350.7363362996978253, 338.7502325331110455 ) ) ;
#28686=CARTESIAN_POINT ( 'NONE',  ( 814.5518280994195948, -327.7255117493285184, 332.4837098697145734 ) ) ;
#28690=CARTESIAN_POINT ( 'NONE',  ( 768.0187753319979720, -440.6346026584191122, 318.0580252608186242 ) ) ;
#28691=CARTESIAN_POINT ( 'NONE',  ( 776.9254006560222479, -188.1908817542437760, 314.8983024940802125 ) ) ;
#28694=CARTESIAN_POINT ( 'NONE',  ( 793.4146539503750546, -97.98741447168734453, 307.6481478633938877 ) ) ;
#28695=CARTESIAN_POINT ( 'NONE',  ( 774.6858677611749044, -417.7255117493283478, 315.5713283507209894 ) ) ;
#28701=CARTESIAN_POINT ( 'NONE',  ( 785.3141322388236176, -213.7255117493289731, 364.4286716492789537 ) ) ;
#28702=CARTESIAN_POINT ( 'NONE',  ( 781.7834795799800531, -226.8164208402380098, 315.0636971347436202 ) ) ;
#28706=CARTESIAN_POINT ( 'NONE',  ( 791.9812246680005501, -428.6346026584192259, 361.9419747391813189 ) ) ;
#28708=( LENGTH_UNIT ( ) NAMED_UNIT ( * ) SI_UNIT ( .MILLI., .METRE. ) );
#28710=CARTESIAN_POINT ( 'NONE',  ( 759.0252816721024374, -168.9982390220563673, 368.0189434323527280 ) ) ;
#28711=CARTESIAN_POINT ( 'NONE',  ( 761.4292242960306112, -257.4636090269708575, 323.2154366446414429 ) ) ;
#28712=CARTESIAN_POINT ( 'NONE',  ( 760.5453621957607311, -381.0783235625954717, 323.8424801807151425 ) ) ;
#28713=ORIENTED_EDGE ( 'NONE', *, *, #19085, .F. ) ;
#28715=CARTESIAN_POINT ( 'NONE',  ( 813.2346286133761168, -197.2601417444143124, 328.9521613784389160 ) ) ;
#28722=CARTESIAN_POINT ( 'NONE',  ( 800.7704444035546203, -244.1692326535050768, 326.0291762391768771 ) ) ;
#28729=ORIENTED_EDGE ( 'NONE', *, *, #14961, .F. ) ;
#28731=CARTESIAN_POINT ( 'NONE',  ( 771.3260364891663130, -163.6454272087893003, 306.0683387631859773 ) ) ;
#28736=CARTESIAN_POINT ( 'NONE',  ( 795.8262568251477660, -382.3726999360613945, 308.3538107759623585 ) ) ;
#28740=CARTESIAN_POINT ( 'NONE',  ( 757.8323909638827445, -26.63460265842045871, 352.1044303154654358 ) ) ;
#28741=CARTESIAN_POINT ( 'NONE',  ( 804.1009440267234822, -263.4636090269708006, 314.0944755984392600 ) ) ;
#28743=CARTESIAN_POINT ( 'NONE',  ( 759.0252816721024374, -216.9982390220562252, 368.0189434323527280 ) ) ;
#28746=CARTESIAN_POINT ( 'NONE',  ( 785.3141322388236176, -309.7255117493287457, 364.4286716492789537 ) ) ;
#28747=CARTESIAN_POINT ( 'NONE',  ( 779.4763451958990572, -80.73633629969864955, 365.0264073115438919 ) ) ;
#28748=CARTESIAN_POINT ( 'NONE',  ( 769.9779781133707957, -91.09997266333496668, 316.7813123517150871 ) ) ;
#28753=CARTESIAN_POINT ( 'NONE',  ( 761.2382568024794409, -159.6237781080508285, 356.9571628226838129 ) ) ;
#28754=CARTESIAN_POINT ( 'NONE',  ( 785.3687786644884454, -347.3618753856922012, 315.3201227861279676 ) ) ;
#28757=CARTESIAN_POINT ( 'NONE',  ( 771.1735550268778070, -129.1800572038746111, 316.3353852180827630 ) ) ;
#28760=CARTESIAN_POINT ( 'NONE',  ( 773.7943932421234194, -431.8055962898681059, 305.5313806188329409 ) ) ;
#28762=CARTESIAN_POINT ( 'NONE',  ( 797.6776695296629214, -331.5436935675104451, 357.6776695296636603 ) ) ;
#28766=CARTESIAN_POINT ( 'NONE',  ( 762.3223304703356007, -439.5436935675101040, 322.3223304703362828 ) ) ;
#28772=CARTESIAN_POINT ( 'NONE',  ( 768.0187753319979720, -8.634602658420517329, 318.0580252608186242 ) ) ;
#28773=CARTESIAN_POINT ( 'NONE',  ( 814.9108240113580450, -232.2709662947834488, 337.5031285880265273 ) ) ;
#28774=CARTESIAN_POINT ( 'NONE',  ( 776.9566956441375396, -108.8965053807782084, 364.8461984189686405 ) ) ;
#28777=CARTESIAN_POINT ( 'NONE',  ( 807.5423716828161105, -393.0783235625954717, 362.2119215644372048 ) ) ;
#28782=CARTESIAN_POINT ( 'NONE',  ( 768.9521613784389729, -33.82724539060788516, 373.2346286133773106 ) ) ;
#28790=CARTESIAN_POINT ( 'NONE',  ( 804.6971507214547046, -363.2817908451523294, 344.0799538623459739 ) ) ;
#28791=CARTESIAN_POINT ( 'NONE',  ( 778.7629533639073998, -320.7363362996979390, 375.0009284576466371 ) ) ;
#28795=CARTESIAN_POINT ( 'NONE',  ( 786.2694204179717872, -141.2817908451530400, 305.1769319972829067 ) ) ;
#28797=CARTESIAN_POINT ( 'NONE',  ( 812.7932403749906598, -111.1800572038747532, 327.7687537140311633 ) ) ;
#28801=CARTESIAN_POINT ( 'NONE',  ( 803.6646147819161570, -209.9073299311470748, 348.8264449731210561 ) ) ;
#28802=CARTESIAN_POINT ( 'NONE',  ( 793.9708237608222134, 1.081845518482914104, 319.2295555964448681 ) ) ;
#28806=CARTESIAN_POINT ( 'NONE',  ( 764.3348316497523456, -46.71468719896022748, 308.6759233522265617 ) ) ;
#28809=CARTESIAN_POINT ( 'NONE',  ( 754.8072714833581358, -28.81642084023863148, 338.1981804954720587 ) ) ;
#28811=CARTESIAN_POINT ( 'NONE',  ( 815.0009284576459549, -294.3510508353230648, 338.7629533639073429 ) ) ;
#28812=CARTESIAN_POINT ( 'NONE',  ( 797.8594530101009923, -157.5436935675109282, 322.1405469898982119 ) ) ;
#28814=CARTESIAN_POINT ( 'NONE',  ( 797.8594530101008786, -349.5436935675102745, 322.1405469898980982 ) ) ;
#28816=CARTESIAN_POINT ( 'NONE',  ( 796.7737145352015204, -68.63460265842033436, 370.7187646348536987 ) ) ;
#28817=VERTEX_POINT ( 'NONE', #16133 ) ;
#28821=CARTESIAN_POINT ( 'NONE',  ( 774.6312213355099630, -71.36187538569302546, 364.6798772138717482 ) ) ;
#28822=CARTESIAN_POINT ( 'NONE',  ( 755.8894580844503253, -327.8272453906069472, 332.3691319403863531 ) ) ;
#28824=CARTESIAN_POINT ( 'NONE',  ( 792.2312462859673587, -395.9073299311465348, 307.2067596250082602 ) ) ;
#28825=CARTESIAN_POINT ( 'NONE',  ( 758.0141637701419768, -279.0783235625958127, 367.2620300519063790 ) ) ;
#28826=CARTESIAN_POINT ( 'NONE',  ( 751.2241431872005251, -64.16923265350563099, 359.9636004259367610 ) ) ;
#28834=CARTESIAN_POINT ( 'NONE',  ( 814.2001403089898304, -377.3618753856920875, 347.4397851343538264 ) ) ;
#28837=DIRECTION ( 'NONE',  ( -1.000000000000000000, -0.000000000000000000, 0.000000000000000000 ) ) ;
#28839=CARTESIAN_POINT ( 'NONE',  ( 757.0176451133909268, -277.0999726633344267, 349.9200121543848354 ) ) ;
#28840=CARTESIAN_POINT ( 'NONE',  ( 800.0135310231082713, -158.0891481129655176, 325.0180583372163028 ) ) ;
#28844=CARTESIAN_POINT ( 'NONE',  ( 801.3366627262608972, -320.5328690171411949, 353.0897708529566899 ) ) ;
#28846=CARTESIAN_POINT ( 'NONE',  ( 809.0717654672305343, -52.91815448151692891, 360.1688906516309885 ) ) ;
#28848=CARTESIAN_POINT ( 'NONE',  ( 763.0537975583475827, -192.4527844766016926, 371.0346526505627480 ) ) ;
#28849=CARTESIAN_POINT ( 'NONE',  ( 771.2633955100217236, -119.9073299311474443, 363.4237431249939618 ) ) ;
#28852=CARTESIAN_POINT ( 'NONE',  ( 815.3608509340175488, -434.7363362996975980, 341.2497674668889545 ) ) ;
#28855=CARTESIAN_POINT ( 'NONE',  ( 756.7813123517142913, -355.9874144716865203, 329.9779781133712504 ) ) ;
#28856=CARTESIAN_POINT ( 'NONE',  ( 814.9108240113580450, -64.27096629478397460, 337.5031285880265273 ) ) ;
#28858=CARTESIAN_POINT ( 'NONE',  ( 757.2208543904082489, -40.71468719896024879, 350.9844846989624330 ) ) ;
#28861=CARTESIAN_POINT ( 'NONE',  ( 813.2346286133761168, -197.2601417444143124, 328.9521613784389160 ) ) ;
#28862=CARTESIAN_POINT ( 'NONE',  ( 765.0180583372156207, -48.99823902205675807, 360.0135310231089534 ) ) ;
#28865=CARTESIAN_POINT ( 'NONE',  ( 768.0187753319979720, -200.6346026584199365, 318.0580252608186242 ) ) ;
#28868=CARTESIAN_POINT ( 'NONE',  ( 755.0636971347428243, -340.2709662947831362, 341.7834795799807353 ) ) ;
#28870=DIRECTION ( 'NONE',  ( -0.000000000000000000, 1.000000000000000000, -0.000000000000000000 ) ) ;
#28872=CARTESIAN_POINT ( 'NONE',  ( 803.8651313633788504, -53.26014174441475291, 332.4468031744301015 ) ) ;
#28875=CARTESIAN_POINT ( 'NONE',  ( 767.7687537140311633, -287.9073299311468759, 372.7932403749916830 ) ) ;
#28876=CARTESIAN_POINT ( 'NONE',  ( 795.6651683502461765, 13.28531280103958423, 371.3240766477733814 ) ) ;
#28882=CARTESIAN_POINT ( 'NONE',  ( 808.0189434323515343, -302.0891481129650629, 319.0252816721025511 ) ) ;
#28885=CARTESIAN_POINT ( 'NONE',  ( 763.2154366446407039, -357.6237781080501463, 321.4292242960311228 ) ) ;
#28887=CARTESIAN_POINT ( 'NONE',  ( 757.0176451133909268, -157.0999726633347962, 349.9200121543848354 ) ) ;
#28888=CARTESIAN_POINT ( 'NONE',  ( 778.1981804954714335, -58.27096629478398171, 314.8072714833589885 ) ) ;
#28892=CARTESIAN_POINT ( 'NONE',  ( 748.6759233522253680, -256.3726999360617924, 324.3348316497537098 ) ) ;
#28893=CARTESIAN_POINT ( 'NONE',  ( 755.8398074228967971, -211.4419599262324709, 333.4516893846970333 ) ) ;
#28897=CARTESIAN_POINT ( 'NONE',  ( 787.5531968255692163, -453.8272453906066630, 316.1348686366205811 ) ) ;
#28900=CARTESIAN_POINT ( 'NONE',  ( 749.2812353651451076, -6.452784476602343666, 323.2262854647983090 ) ) ;
#28901=ADVANCED_FACE ( 'NONE', ( #6653 ), #41773, .T. ) ;
#28902=CARTESIAN_POINT ( 'NONE',  ( 744.7301800767019131, -100.8164208402383792, 337.4774526936615757 ) ) ;
#28903=FACE_OUTER_BOUND ( 'NONE', #20098, .T. ) ;
#28906=CARTESIAN_POINT ( 'NONE',  ( 747.6481478633932056, -397.0999726633340288, 353.4146539503763620 ) ) ;
#28908=CARTESIAN_POINT ( 'NONE',  ( 811.0346526505616112, -326.6346026584193396, 323.0537975583477532 ) ) ;
#28911=CARTESIAN_POINT ( 'NONE',  ( 792.1044303154645831, -444.4527844766009821, 317.8323909638837677 ) ) ;
#28912=AXIS2_PLACEMENT_3D ( 'NONE', #33, #27300, #2819 ) ;
#28913=CARTESIAN_POINT ( 'NONE',  ( 798.5707757039680246, -173.4636090269710849, 356.7845633553585003 ) ) ;
#28916=CARTESIAN_POINT ( 'NONE',  ( 771.2368401574024119, -85.44195992623282621, 374.2805881961240857 ) ) ;
#28920=CARTESIAN_POINT ( 'NONE',  ( 761.9338519418445230, -158.5328690171417065, 370.4231160770881957 ) ) ;
#28925=ADVANCED_FACE ( 'NONE', ( #23957 ), #45698, .T. ) ;
#28927=CARTESIAN_POINT ( 'NONE',  ( 755.3201227861273992, -267.7255117493286320, 345.3687786644892981 ) ) ;
#28928=CARTESIAN_POINT ( 'NONE',  ( 762.1405469898973024, -241.5436935675106440, 357.8594530101016176 ) ) ;
#28931=CARTESIAN_POINT ( 'NONE',  ( 758.0580252608178853, -438.4527844766009821, 328.0187753319985404 ) ) ;
#28932=ORIENTED_EDGE ( 'NONE', *, *, #1261, .F. ) ;
#28935=CARTESIAN_POINT ( 'NONE',  ( 748.9653473494365699, -170.6346026584199933, 356.9462024416520762 ) ) ;
#28936=CARTESIAN_POINT ( 'NONE',  ( 775.8780910478218402, -249.2817908451526421, 364.9511171171680530 ) ) ;
#28939=CARTESIAN_POINT ( 'NONE',  ( 744.9990715423526808, -234.3510508353232638, 341.2370466360926002 ) ) ;
#28944=CARTESIAN_POINT ( 'NONE',  ( 773.3843516231979720, -253.4419599262323572, 364.4086373105754433 ) ) ;
#28945=LINE ( 'NONE', #1882, #43285 ) ;
#28951=EDGE_CURVE ( 'NONE', #30414, #8827, #20577, .T. ) ;
#28952=CARTESIAN_POINT ( 'NONE',  ( 755.8990559732751535, -179.4636090269710849, 365.9055244015606831 ) ) ;
#28959=CARTESIAN_POINT ( 'NONE',  ( 767.6429770376289525, -9.180057203875058747, 306.8695393053162093 ) ) ;
#28960=CARTESIAN_POINT ( 'NONE',  ( 759.9999999999992042, -512.9681489794448908, 370.0000000000000000 ) ) ;
#28963=CARTESIAN_POINT ( 'NONE',  ( 803.4237431249931660, -15.18005720387504631, 331.2633955100225194 ) ) ;
#28964=CARTESIAN_POINT ( 'NONE',  ( 781.2370466360911223, -284.7363362996979390, 304.9990715423533629 ) ) ;
#28966=CARTESIAN_POINT ( 'NONE',  ( 777.5031285880264704, -238.8164208402379813, 374.9108240113588408 ) ) ;
#28969=CARTESIAN_POINT ( 'NONE',  ( 779.9999999999992042, 126.4563064324884465, 350.0000000000000000 ) ) ;
#28970=CARTESIAN_POINT ( 'NONE',  ( 755.0636971347428243, -316.2709662947832499, 341.7834795799807353 ) ) ;
#28973=CARTESIAN_POINT ( 'NONE',  ( 766.9102291470427417, -90.55451811788041994, 318.6633372737382501 ) ) ;
#28978=CARTESIAN_POINT ( 'NONE',  ( 790.8726784830453198, -154.7146871989598935, 362.5472867521010585 ) ) ;
#28979=CARTESIAN_POINT ( 'NONE',  ( 800.0135310231082713, -374.0891481129647786, 325.0180583372163028 ) ) ;
#28985=CARTESIAN_POINT ( 'NONE',  ( 793.9861285913068514, -442.9180389616178672, 372.1637643035757606 ) ) ;
#28987=CARTESIAN_POINT ( 'NONE',  ( 762.1405469898971887, -313.5436935675102745, 357.8594530101015607 ) ) ;
#28989=CARTESIAN_POINT ( 'NONE',  ( 791.9812246680005501, -428.6346026584192259, 361.9419747391813189 ) ) ;
#28996=CARTESIAN_POINT ( 'NONE',  ( 795.1360043628807261, 3.910851887033985896, 360.2193346964456282 ) ) ;
#28997=CARTESIAN_POINT ( 'NONE',  ( 759.2295555964440155, -112.1692326535054889, 353.9708237608231229 ) ) ;
#29000=CARTESIAN_POINT ( 'NONE',  ( 751.2241431872005251, -376.1692326535046504, 359.9636004259367610 ) ) ;
#29007=CARTESIAN_POINT ( 'NONE',  ( 745.1792804349281596, -62.19088175424416676, 343.7566961878542884 ) ) ;
#29015=CARTESIAN_POINT ( 'NONE',  ( 761.4292242960306112, -401.4636090269704027, 323.2154366446414429 ) ) ;
#29020=CARTESIAN_POINT ( 'NONE',  ( 797.8822607201568644, -150.5545181178802352, 370.1134526219340160 ) ) ;
#29022=CARTESIAN_POINT ( 'NONE',  ( 805.0032342141412300, -109.5436935675110988, 314.9967657858571783 ) ) ;
#29026=CARTESIAN_POINT ( 'NONE',  ( 771.2633955100217236, -215.9073299311471317, 363.4237431249939618 ) ) ;
#29027=CARTESIAN_POINT ( 'NONE',  ( 764.1737431748507561, -442.3726999360611103, 371.6461892240376415 ) ) ;
#29031=CARTESIAN_POINT ( 'NONE',  ( 746.0683387631852383, -19.44195992623303937, 331.3260364891676204 ) ) ;
#29035=CARTESIAN_POINT ( 'NONE',  ( 771.1735550268778070, -9.180057203875058747, 316.3353852180827630 ) ) ;
#29038=CARTESIAN_POINT ( 'NONE',  ( 744.8212110874229666, -330.8965053807774552, 336.2046728542121627 ) ) ;
#29039=CARTESIAN_POINT ( 'NONE',  ( 755.5713283507202505, -149.3618753856928265, 334.6858677611754729 ) ) ;
#29042=CARTESIAN_POINT ( 'NONE',  ( 786.2056067578752163, -419.8055962898681059, 374.4686193811670023 ) ) ;
#29044=CARTESIAN_POINT ( 'NONE',  ( 762.3223304703356007, -343.5436935675103314, 322.3223304703362828 ) ) ;
#29051=CARTESIAN_POINT ( 'NONE',  ( 765.0180583372156207, -48.99823902205675807, 360.0135310231089534 ) ) ;
#29052=CARTESIAN_POINT ( 'NONE',  ( 761.4292242960306112, -377.4636090269704596, 323.2154366446414429 ) ) ;
#29054=CARTESIAN_POINT ( 'NONE',  ( 808.3070685750232087, -378.9982390220557136, 361.1904061080339829 ) ) ;
#29055=CARTESIAN_POINT ( 'NONE',  ( 771.2368401574024119, -301.4419599262320730, 374.2805881961240857 ) ) ;
#29056=CARTESIAN_POINT ( 'NONE',  ( 798.0661480581538854, -74.53286901714196233, 309.5768839229118043 ) ) ;
#29063=CARTESIAN_POINT ( 'NONE',  ( 772.5602148656447525, -441.7255117493282910, 305.7998596910095443 ) ) ;
#29069=CARTESIAN_POINT ( 'NONE',  ( 769.9779781133707957, -283.0999726633344267, 316.7813123517150871 ) ) ;
#29070=CARTESIAN_POINT ( 'NONE',  ( 800.2193346964447755, -162.9982390220563673, 355.1360043628815788 ) ) ;
#29075=CARTESIAN_POINT ( 'NONE',  ( 757.2208543904082489, -328.7146871989592682, 350.9844846989624330 ) ) ;
#29076=DIRECTION ( 'NONE',  ( -0.000000000000000000, 1.000000000000000000, -0.000000000000000000 ) ) ;
#29077=CARTESIAN_POINT ( 'NONE',  ( 814.8207195650702488, -26.19088175424427334, 336.2433038121456548 ) ) ;
#29079=CARTESIAN_POINT ( 'NONE',  ( 800.2193346964447755, -114.9982390220565236, 355.1360043628815788 ) ) ;
#29083=CARTESIAN_POINT ( 'NONE',  ( 815.3608509340175488, -458.7363362996973706, 341.2497674668889545 ) ) ;
#29085=DIRECTION ( 'NONE',  ( -1.000000000000000000, -0.000000000000000000, 0.000000000000000000 ) ) ;
#29086=CARTESIAN_POINT ( 'NONE',  ( 759.2295555964440155, -400.1692326535045936, 353.9708237608231229 ) ) ;
#29093=CARTESIAN_POINT ( 'NONE',  ( 751.2241431872005251, -232.1692326535051620, 359.9636004259367610 ) ) ;
#29094=CARTESIAN_POINT ( 'NONE',  ( 785.3687786644885591, -35.36187538569316047, 315.3201227861280813 ) ) ;
#29097=CARTESIAN_POINT ( 'NONE',  ( 755.0636971347428243, -220.2709662947834772, 341.7834795799807353 ) ) ;
#29100=CARTESIAN_POINT ( 'NONE',  ( 805.1927285166399315, -352.8164208402375266, 341.8018195045277707 ) ) ;
#29105=CARTESIAN_POINT ( 'NONE',  ( 811.0346526505617248, -278.6346026584196807, 323.0537975583478101 ) ) ;
#29106=CARTESIAN_POINT ( 'NONE',  ( 749.8865473780648472, 3.467130982857797417, 322.1177392798429082 ) ) ;
#29112=CARTESIAN_POINT ( 'NONE',  ( 796.9462024416508257, -324.4527844766013231, 308.9653473494370246 ) ) ;
#29114=DIRECTION ( 'NONE',  ( 0.000000000000000000, -1.000000000000000000, 0.000000000000000000 ) ) ;
#29115=CARTESIAN_POINT ( 'NONE',  ( 805.2837595273609850, -218.7363362996982232, 340.5290396650784714 ) ) ;
#29118=CARTESIAN_POINT ( 'NONE',  ( 775.8780910478218402, -153.2817908451529831, 364.9511171171680530 ) ) ;
#29119=CARTESIAN_POINT ( 'NONE',  ( 757.8323909638827445, -50.63460265842036989, 352.1044303154654358 ) ) ;
#29123=CARTESIAN_POINT ( 'NONE',  ( 750.9282345327678740, -280.9181544815162965, 319.8311093483690115 ) ) ;
#29124=CARTESIAN_POINT ( 'NONE',  ( 794.1144889064781864, -226.1692326535051052, 360.9840315886528401 ) ) ;
#29126=CARTESIAN_POINT ( 'NONE',  ( 778.2165204200184689, 1.183579159761269040, 364.9363028652563230 ) ) ;
#29129=CARTESIAN_POINT ( 'NONE',  ( 814.9108240113580450, -40.27096629478405987, 337.5031285880265273 ) ) ;
#29130=CARTESIAN_POINT ( 'NONE',  ( 763.0537975583475827, -96.45278447660203369, 371.0346526505627480 ) ) ;
#29132=VECTOR ( 'NONE', #31165, 1000.000000000000000 ) ;
#29135=CARTESIAN_POINT ( 'NONE',  ( 744.6391490659812007, -374.7363362996978253, 338.7502325331110455 ) ) ;
#29137=CARTESIAN_POINT ( 'NONE',  ( 772.5602148656447525, -345.7255117493285184, 305.7998596910095443 ) ) ;
#29141=CARTESIAN_POINT ( 'NONE',  ( 755.0636971347428243, -412.2709662947829088, 341.7834795799807353 ) ) ;
#29142=CARTESIAN_POINT ( 'NONE',  ( 769.0155153010367712, -202.3726999360618777, 362.7791456095907279 ) ) ;
#29145=CARTESIAN_POINT ( 'NONE',  ( 756.1443688327750579, -93.62377810805098477, 314.3581564841659315 ) ) ;
#29146=CARTESIAN_POINT ( 'NONE',  ( 759.9864689768902508, -434.0891481129646081, 354.9819416627836404 ) ) ;
#29150=ORIENTED_EDGE ( 'NONE', *, *, #3233, .F. ) ;
#29154=CARTESIAN_POINT ( 'NONE',  ( 771.2633955100217236, -263.9073299311469327, 363.4237431249939618 ) ) ;
#29155=CARTESIAN_POINT ( 'NONE',  ( 754.8072714833583632, -268.8164208402378677, 338.1981804954721156 ) ) ;
#29158=CARTESIAN_POINT ( 'NONE',  ( 803.2186876482843445, 16.01258552831230375, 350.0220218866286928 ) ) ;
#29160=CARTESIAN_POINT ( 'NONE',  ( 796.7737145352015204, -188.6346026584199365, 370.7187646348536987 ) ) ;
#29162=CARTESIAN_POINT ( 'NONE',  ( 804.8461984189677878, -266.1908817542435486, 336.9566956441385628 ) ) ;
#29165=CARTESIAN_POINT ( 'NONE',  ( 749.8865473780648472, -212.5328690171415076, 322.1177392798429082 ) ) ;
#29167=VECTOR ( 'NONE', #35536, 1000.000000000000000 ) ;
#29172=CARTESIAN_POINT ( 'NONE',  ( 784.0799538623451781, -275.8055962898685038, 364.6971507214555572 ) ) ;
#29180=CARTESIAN_POINT ( 'NONE',  ( 809.0717654672305343, -172.9181544815165239, 360.1688906516309885 ) ) ;
#29184=CARTESIAN_POINT ( 'NONE',  ( 779.9999999999992042, -452.9681489794448339, 339.9999999999999432 ) ) ;
#29188=CARTESIAN_POINT ( 'NONE',  ( 815.2698199232961542, -16.81642084023866701, 342.5225473063383106 ) ) ;
#29193=CARTESIAN_POINT ( 'NONE',  ( 756.5762568750052424, -3.180057203875080063, 348.7366044899774238 ) ) ;
#29194=CARTESIAN_POINT ( 'NONE',  ( 813.5763878283155464, -291.8272453906071746, 351.1614460488615350 ) ) ;
#29196=CARTESIAN_POINT ( 'NONE',  ( 800.9747183278959710, -228.9982390220561683, 311.9810565676471583 ) ) ;
#29202=CARTESIAN_POINT ( 'NONE',  ( 757.8323909638827445, -314.6346026584194533, 352.1044303154654358 ) ) ;
#29204=CARTESIAN_POINT ( 'NONE',  ( 799.2566176426618085, -96.00906357242585898, 324.0069404352559559 ) ) ;
#29209=CARTESIAN_POINT ( 'NONE',  ( 786.6156483768007774, -145.4419599262326699, 315.5913626894246136 ) ) ;
#29210=CARTESIAN_POINT ( 'NONE',  ( 767.8955696845333705, -360.4527844766010958, 362.1676090361162323 ) ) ;
#29211=EDGE_LOOP ( 'NONE', ( #30936, #31834, #43506, #7683 ) ) ;
#29213=CARTESIAN_POINT ( 'NONE',  ( 781.7834795799800531, -154.8164208402382371, 315.0636971347436202 ) ) ;
#29217=CARTESIAN_POINT ( 'NONE',  ( 788.7631598425961101, -433.4419599262316183, 305.7194118038759143 ) ) ;
#29220=CARTESIAN_POINT ( 'NONE',  ( 767.8955696845333705, -336.4527844766012095, 362.1676090361162323 ) ) ;
#29225=CARTESIAN_POINT ( 'NONE',  ( 792.1044303154645831, -444.4527844766009821, 317.8323909638837677 ) ) ;
#29233=CARTESIAN_POINT ( 'NONE',  ( 774.6312213355099630, 0.6381246143067236254, 364.6798772138717482 ) ) ;
#29234=CARTESIAN_POINT ( 'NONE',  ( 763.2154366446407039, -165.6237781080507716, 321.4292242960311228 ) ) ;
#29237=CARTESIAN_POINT ( 'NONE',  ( 793.4146539503750546, -409.9874144716863498, 307.6481478633938877 ) ) ;
#29238=EDGE_LOOP ( 'NONE', ( #33685, #9186, #28177, #7341 ) ) ;
#29242=CARTESIAN_POINT ( 'NONE',  ( 764.1737431748507561, -58.37269993606236085, 371.6461892240376415 ) ) ;
#29250=DIRECTION ( 'NONE',  ( 0.000000000000000000, 0.000000000000000000, 1.000000000000000000 ) ) ;
#29253=CARTESIAN_POINT ( 'NONE',  ( 804.6971507214547046, -387.2817908451522726, 344.0799538623459739 ) ) ;
#29258=CARTESIAN_POINT ( 'NONE',  ( 746.4236121716829757, -183.8272453906074020, 328.8385539511384650 ) ) ;
#29260=CARTESIAN_POINT ( 'NONE',  ( 812.7932403749906598, -135.1800572038746679, 327.7687537140311633 ) ) ;
#29262=EDGE_CURVE ( 'NONE', #40029, #25691, #42712, .T. ) ;
#29265=CARTESIAN_POINT ( 'NONE',  ( 804.9363028652555840, -232.2709662947834488, 338.2165204200192079 ) ) ;
#29266=CARTESIAN_POINT ( 'NONE',  ( 759.0159684113467620, -16.91815448151702839, 325.8855110935213020 ) ) ;
#29271=CARTESIAN_POINT ( 'NONE',  ( 783.7566961878529810, -24.89650538077847486, 305.1792804349288417 ) ) ;
#29274=CARTESIAN_POINT ( 'NONE',  ( 768.0187753319979720, -8.634602658420517329, 318.0580252608186242 ) ) ;
#29276=CARTESIAN_POINT ( 'NONE',  ( 745.1769319972822814, -353.8055962898683333, 346.2694204179732083 ) ) ;
#29277=CARTESIAN_POINT ( 'NONE',  ( 774.6312213355098493, -167.3618753856927412, 364.6798772138717482 ) ) ;
#29279=CARTESIAN_POINT ( 'NONE',  ( 756.1443688327750579, -429.6237781080499190, 314.3581564841659315 ) ) ;
#29282=CARTESIAN_POINT ( 'NONE',  ( 805.1927285166397041, -352.8164208402374129, 341.8018195045277707 ) ) ;
#29292=CARTESIAN_POINT ( 'NONE',  ( 757.8323909638827445, -50.63460265842036989, 352.1044303154654358 ) ) ;
#29293=CARTESIAN_POINT ( 'NONE',  ( 755.8894580844503253, -375.8272453906069472, 332.3691319403863531 ) ) ;
#29296=CARTESIAN_POINT ( 'NONE',  ( 763.0537975583476964, -408.4527844766009821, 371.0346526505628617 ) ) ;
#29297=CARTESIAN_POINT ( 'NONE',  ( 768.8385539511368734, -287.2601417444140566, 306.4236121716840557 ) ) ;
#29298=CARTESIAN_POINT ( 'NONE',  ( 813.9316612368132837, -103.4419599262327836, 348.6739635108323228 ) ) ;
#29304=CARTESIAN_POINT ( 'NONE',  ( 746.8695393053150156, -413.9073299311465348, 327.6429770376306010 ) ) ;
#29311=CARTESIAN_POINT ( 'NONE',  ( 761.4292242960306112, -305.4636090269706870, 323.2154366446414429 ) ) ;
#29312=CARTESIAN_POINT ( 'NONE',  ( 755.3201227861273992, -147.7255117493291152, 345.3687786644892981 ) ) ;
#29313=ORIENTED_EDGE ( 'NONE', *, *, #8380, .T. ) ;
#29315=CARTESIAN_POINT ( 'NONE',  ( 770.0799878456142551, -325.9874144716865771, 362.9823548866085616 ) ) ;
#29317=CARTESIAN_POINT ( 'NONE',  ( 749.5768839229115201, -60.55451811788051941, 358.0661480581553064 ) ) ;
#29321=CARTESIAN_POINT ( 'NONE',  ( 772.5602148656447525, -201.7255117493290015, 305.7998596910095443 ) ) ;
#29322=CARTESIAN_POINT ( 'NONE',  ( 759.9864689768902508, -122.0891481129656171, 354.9819416627836404 ) ) ;
#29325=CARTESIAN_POINT ( 'NONE',  ( 802.5472867521000353, -4.372699936062523385, 350.8726784830461156 ) ) ;
#29328=CARTESIAN_POINT ( 'NONE',  ( 758.6633372737375112, -380.5328690171409676, 326.9102291470432533 ) ) ;
#29335=CARTESIAN_POINT ( 'NONE',  ( 815.0009284576459549, -246.3510508353232638, 338.7629533639073429 ) ) ;
#29336=CARTESIAN_POINT ( 'NONE',  ( 785.3687786644885591, -59.36187538569307520, 315.3201227861280813 ) ) ;
#29338=CARTESIAN_POINT ( 'NONE',  ( 762.1405469898971887, -217.5436935675107293, 357.8594530101015607 ) ) ;
#29344=CARTESIAN_POINT ( 'NONE',  ( 777.4774526936600978, -298.2709662947831930, 304.7301800767028226 ) ) ;
#29345=CARTESIAN_POINT ( 'NONE',  ( 800.1688906516307043, -34.16923265350572336, 369.0717654672308186 ) ) ;
#29352=CARTESIAN_POINT ( 'NONE',  ( 763.2262854647970016, -320.6346026584195670, 309.2812353651462445 ) ) ;
#29354=CARTESIAN_POINT ( 'NONE',  ( 799.4546378042377910, -369.0783235625956422, 356.1575198192848006 ) ) ;
#29356=CARTESIAN_POINT ( 'NONE',  ( 799.2566176426618085, -192.0090635724255606, 324.0069404352559559 ) ) ;
#29357=CARTESIAN_POINT ( 'NONE',  ( 774.6858677611749044, -57.72551174932945628, 315.5713283507209894 ) ) ;
#29363=CARTESIAN_POINT ( 'NONE',  ( 789.9200121543843807, -217.9874144716870035, 317.0176451133914384 ) ) ;
#29366=CARTESIAN_POINT ( 'NONE',  ( 759.7806653035534055, -6.998239022056885972, 324.8639956371180801 ) ) ;
#29369=CARTESIAN_POINT ( 'NONE',  ( 748.9653473494363425, -50.63460265842036989, 356.9462024416521331 ) ) ;
#29370=CARTESIAN_POINT ( 'NONE',  ( 787.4397851343537695, -93.72551174932934259, 374.2001403089903988 ) ) ;
#29371=DIRECTION ( 'NONE',  ( -1.000000000000000000, -0.000000000000000000, 0.000000000000000000 ) ) ;
#29372=CARTESIAN_POINT ( 'NONE',  ( 767.9999999999992042, 240.0000000000000853, 360.0000000000000000 ) ) ;
#29373=CARTESIAN_POINT ( 'NONE',  ( 783.7953271457878373, -392.1908817542432075, 375.1787889125761239 ) ) ;
#29375=CARTESIAN_POINT ( 'NONE',  ( 763.2262854647970016, -368.6346026584193964, 309.2812353651462445 ) ) ;
#29377=CARTESIAN_POINT ( 'NONE',  ( 754.8983024940795303, 5.103494619221427442, 336.9254006560228163 ) ) ;
#29378=CARTESIAN_POINT ( 'NONE',  ( 796.1575198192839480, -174.0090635724256742, 359.4546378042384163 ) ) ;
#29381=CARTESIAN_POINT ( 'NONE',  ( 758.0141637701419768, -135.0783235625962959, 367.2620300519063790 ) ) ;
#29382=CARTESIAN_POINT ( 'NONE',  ( 803.4237431249931660, -423.1800572038737300, 331.2633955100225194 ) ) ;
#29387=CARTESIAN_POINT ( 'NONE',  ( 762.3223304703356007, -247.5436935675106724, 322.3223304703362828 ) ) ;
#29388=CARTESIAN_POINT ( 'NONE',  ( 762.1405469898973024, -265.5436935675106156, 357.8594530101016176 ) ) ;
#29389=DIRECTION ( 'NONE',  ( 0.000000000000000000, 0.000000000000000000, 1.000000000000000000 ) ) ;
#29391=CARTESIAN_POINT ( 'NONE',  ( 793.2243759319678702, 21.46713098285774279, 318.4439275373583200 ) ) ;
#29394=CARTESIAN_POINT ( 'NONE',  ( 767.6429770376291799, -177.1800572038744974, 306.8695393053162093 ) ) ;
#29395=CARTESIAN_POINT ( 'NONE',  ( 755.1538015810308480, -278.1908817542434917, 343.0433043558613804 ) ) ;
#29398=CARTESIAN_POINT ( 'NONE',  ( 773.7943932421234194, -215.8055962898687881, 305.5313806188329409 ) ) ;
#29400=EDGE_LOOP ( 'NONE', ( #31760, #4367 ) ) ;
#29403=CARTESIAN_POINT ( 'NONE',  ( 802.7791456095903868, -268.7146871989595525, 329.0155153010375102 ) ) ;
#29405=CARTESIAN_POINT ( 'NONE',  ( 759.9999999999992042, 205.0000000000000568, 339.9999999999999432 ) ) ;
#29411=CARTESIAN_POINT ( 'NONE',  ( 802.2119215644370342, -174.0090635724256742, 367.5423716828165084 ) ) ;
#29415=CARTESIAN_POINT ( 'NONE',  ( 759.9999999999992042, -512.9681489794448908, 309.9999999999998863 ) ) ;
#29420=CARTESIAN_POINT ( 'NONE',  ( 759.9864689768902508, -50.08914811296584446, 354.9819416627836404 ) ) ;
#29421=CARTESIAN_POINT ( 'NONE',  ( 760.0363995740630116, -298.9181544815161828, 368.7758568127991907 ) ) ;
#29423=CARTESIAN_POINT ( 'NONE',  ( 815.2698199232961542, -256.8164208402379245, 342.5225473063383106 ) ) ;
#29426=CARTESIAN_POINT ( 'NONE',  ( 765.0180583372156207, -336.9982390220558273, 360.0135310231089534 ) ) ;
#29427=CARTESIAN_POINT ( 'NONE',  ( 754.7162404726377645, -86.73633629969862113, 339.4709603349214717 ) ) ;
#29430=PLANE ( 'NONE',  #23287 ) ;
#29431=CARTESIAN_POINT ( 'NONE',  ( 789.9200121543843807, -169.9874144716871172, 317.0176451133914384 ) ) ;
#29432=CARTESIAN_POINT ( 'NONE',  ( 788.8264449731200330, -381.1800572038737869, 363.6646147819171233 ) ) ;
#29435=CARTESIAN_POINT ( 'NONE',  ( 800.2193346964447755, -162.9982390220563673, 355.1360043628815788 ) ) ;
#29438=CARTESIAN_POINT ( 'NONE',  ( 812.7932403749906598, 8.819942796124882634, 327.7687537140311633 ) ) ;
#29440=CARTESIAN_POINT ( 'NONE',  ( 801.9419747391806368, -354.4527844766012095, 351.9812246680014027 ) ) ;
#29444=CARTESIAN_POINT ( 'NONE',  ( 755.0636971347428243, -436.2709662947827951, 341.7834795799807353 ) ) ;
#29445=EDGE_CURVE ( 'NONE', #27321, #18957, #40936, .T. ) ;
#29447=VERTEX_POINT ( 'NONE', #16348 ) ;
#29451=CARTESIAN_POINT ( 'NONE',  ( 792.1044303154645831, 11.54721552339760038, 317.8323909638837677 ) ) ;
#29452=CARTESIAN_POINT ( 'NONE',  ( 780.5290396650775619, -156.3510508353235480, 365.2837595273619513 ) ) ;
#29460=CARTESIAN_POINT ( 'NONE',  ( 814.4686193811664907, -75.28179084515321051, 346.2056067578752732 ) ) ;
#29468=CARTESIAN_POINT ( 'NONE',  ( 805.2837595273609850, -386.7363362996977116, 340.5290396650784714 ) ) ;
#29474=CARTESIAN_POINT ( 'NONE',  ( 754.3581564841646241, -185.4636090269710280, 316.1443688327762516 ) ) ;
#29477=CARTESIAN_POINT ( 'NONE',  ( 763.2262854647970016, -152.6346026584200786, 309.2812353651462445 ) ) ;
#29481=EDGE_CURVE ( 'NONE', #755, #8326, #37233, .T. ) ;
#29482=CARTESIAN_POINT ( 'NONE',  ( 805.1927285166397041, -232.8164208402379245, 341.8018195045277707 ) ) ;
#29483=CARTESIAN_POINT ( 'NONE',  ( 790.9844846989617508, -22.37269993606246743, 317.2208543904092721 ) ) ;
#29487=CARTESIAN_POINT ( 'NONE',  ( 754.0944755984390895, -39.62377810805116951, 364.1009440267246760 ) ) ;
#29490=CARTESIAN_POINT ( 'NONE',  ( 765.0180583372156207, -24.99823902205683268, 360.0135310231089534 ) ) ;
#29493=CARTESIAN_POINT ( 'NONE',  ( 800.1688906516307043, -346.1692326535047641, 369.0717654672308186 ) ) ;
#29495=CARTESIAN_POINT ( 'NONE',  ( 764.3348316497523456, -430.7146871989590409, 308.6759233522265617 ) ) ;
#29497=CARTESIAN_POINT ( 'NONE',  ( 802.1676090361156639, -350.6346026584192828, 327.8955696845344505 ) ) ;
#29505=CARTESIAN_POINT ( 'NONE',  ( 792.1044303154645831, -60.45278447660215448, 317.8323909638837677 ) ) ;
#29506=CARTESIAN_POINT ( 'NONE',  ( 800.9840315886518738, -364.9181544815158986, 354.1144889064786412 ) ) ;
#29508=CARTESIAN_POINT ( 'NONE',  ( 814.5518280994195948, -423.7255117493282341, 332.4837098697145166 ) ) ;
#29509=CARTESIAN_POINT ( 'NONE',  ( 812.6845335610512393, -319.9874144716866340, 353.5525998758768651 ) ) ;
#29510=EDGE_CURVE ( 'NONE', #3360, #25515, #12165, .T. ) ;
#29511=CARTESIAN_POINT ( 'NONE',  ( 759.8311093483677041, -94.16923265350555994, 310.9282345327691814 ) ) ;
#29517=CARTESIAN_POINT ( 'NONE',  ( 792.2312462859673587, -419.9073299311465348, 307.2067596250082602 ) ) ;
#29523=CARTESIAN_POINT ( 'NONE',  ( 769.9779781133707957, -307.0999726633343130, 316.7813123517150871 ) ) ;
#29524=CARTESIAN_POINT ( 'NONE',  ( 788.7366044899766848, -155.9073299311473306, 316.5762568750059813 ) ) ;
#29527=CARTESIAN_POINT ( 'NONE',  ( 784.0799538623451781, -323.8055962898684470, 364.6971507214555572 ) ) ;
#29529=CARTESIAN_POINT ( 'NONE',  ( 783.7953271457878373, -80.19088175424411702, 375.1787889125761239 ) ) ;
#29532=CARTESIAN_POINT ( 'NONE',  ( 759.0252816721024374, -192.9982390220562820, 368.0189434323527280 ) ) ;
#29533=CARTESIAN_POINT ( 'NONE',  ( 757.8323909638827445, -122.6346026584201354, 352.1044303154654358 ) ) ;
#29537=CARTESIAN_POINT ( 'NONE',  ( 761.4292242960306112, -17.46360902697157513, 323.2154366446414429 ) ) ;
#29540=CARTESIAN_POINT ( 'NONE',  ( 756.7813123517142913, -379.9874144716865203, 329.9779781133712504 ) ) ;
#29542=CARTESIAN_POINT ( 'NONE',  ( 796.7845633553578182, -81.62377810805104161, 358.5707757039688204 ) ) ;
#29547=CARTESIAN_POINT ( 'NONE',  ( 814.8230680027162407, -245.8055962898686460, 333.7305795820267917 ) ) ;
#29548=CARTESIAN_POINT ( 'NONE',  ( 788.8264449731201466, -45.18005720387493795, 363.6646147819170665 ) ) ;
#29551=CARTESIAN_POINT ( 'NONE',  ( 754.8072714833581358, -220.8164208402379529, 338.1981804954720587 ) ) ;
#29555=CARTESIAN_POINT ( 'NONE',  ( 799.9999999999993179, 205.0000000000000568, 339.9999999999999432 ) ) ;
#29560=CARTESIAN_POINT ( 'NONE',  ( 748.9653473494365699, -290.6346026584196238, 356.9462024416520762 ) ) ;
#29561=CARTESIAN_POINT ( 'NONE',  ( 813.2346286133761168, -29.26014174441482751, 328.9521613784389160 ) ) ;
#29567=CARTESIAN_POINT ( 'NONE',  ( 777.4774526936600978, -322.2709662947830225, 304.7301800767027657 ) ) ;
#29568=PLANE ( 'NONE',  #17452 ) ;
#29569=CARTESIAN_POINT ( 'NONE',  ( 758.6633372737375112, -356.5328690171410813, 326.9102291470432533 ) ) ;
#29570=LINE ( 'NONE', #42808, #24067 ) ;
#29572=CARTESIAN_POINT ( 'NONE',  ( 772.4468031744293057, -177.8272453906074304, 363.8651313633793620 ) ) ;
#29573=CARTESIAN_POINT ( 'NONE',  ( 804.6798772138708955, -63.72551174932939233, 334.6312213355107019 ) ) ;
#29577=CARTESIAN_POINT ( 'NONE',  ( 761.2382568024794409, -231.6237781080504874, 356.9571628226838129 ) ) ;
#29580=CARTESIAN_POINT ( 'NONE',  ( 758.8095938919642549, -416.0891481129645513, 311.6929314249763365 ) ) ;
#29584=CARTESIAN_POINT ( 'NONE',  ( 745.7998596910086917, -53.36187538569310362, 332.5602148656461168 ) ) ;
#29585=CARTESIAN_POINT ( 'NONE',  ( 759.0252816721024374, -96.99823902205660886, 368.0189434323527280 ) ) ;
#29588=CARTESIAN_POINT ( 'NONE',  ( 757.7880784355613741, -378.0090635724250774, 312.4576283171834916 ) ) ;
#29590=CARTESIAN_POINT ( 'NONE',  ( 751.9810565676468741, -362.0891481129648923, 360.9747183278973921 ) ) ;
#29592=CARTESIAN_POINT ( 'NONE',  ( 787.6308680596127942, 12.73985825558503926, 364.1105419155492768 ) ) ;
#29595=CARTESIAN_POINT ( 'NONE',  ( 805.9055244015594326, -123.6237781080508569, 315.8990559732753240 ) ) ;
#29600=CARTESIAN_POINT ( 'NONE',  ( 802.1676090361156639, -134.6346026584201070, 327.8955696845344505 ) ) ;
#29602=CARTESIAN_POINT ( 'NONE',  ( 794.9819416627830151, -252.9982390220560831, 319.9864689768909898 ) ) ;
#29603=CARTESIAN_POINT ( 'NONE',  ( 802.1676090361155502, -254.6346026584197091, 327.8955696845344505 ) ) ;
#29604=DIRECTION ( 'NONE',  ( 0.000000000000000000, 1.000000000000000000, 0.000000000000000000 ) ) ;
#29606=CARTESIAN_POINT ( 'NONE',  ( 800.7704444035546203, 19.83076734649410966, 326.0291762391768771 ) ) ;
#29609=CARTESIAN_POINT ( 'NONE',  ( 792.2312462859673587, -179.9073299311472454, 307.2067596250082602 ) ) ;
#29610=CARTESIAN_POINT ( 'NONE',  ( 761.4292242960306112, -305.4636090269706870, 323.2154366446414429 ) ) ;
#29611=CARTESIAN_POINT ( 'NONE',  ( 776.9566956441375396, -396.8965053807772847, 364.8461984189686405 ) ) ;
#29618=CARTESIAN_POINT ( 'NONE',  ( 800.7704444035546203, -268.1692326535049347, 326.0291762391768771 ) ) ;
#29628=CARTESIAN_POINT ( 'NONE',  ( 813.1304606946830518, -17.90732993114776406, 352.3570229623690580 ) ) ;
#29633=CARTESIAN_POINT ( 'NONE',  ( 778.1981804954714335, -58.27096629478398171, 314.8072714833589885 ) ) ;
#29634=CARTESIAN_POINT ( 'NONE',  ( 814.4686193811664907, -291.2817908451525000, 346.2056067578752732 ) ) ;
#29635=CARTESIAN_POINT ( 'NONE',  ( 782.4968714119720516, -250.8164208402379245, 305.0891759886411023 ) ) ;
#29639=CARTESIAN_POINT ( 'NONE',  ( 759.7806653035534055, -366.9982390220556567, 324.8639956371180801 ) ) ;
#29640=CARTESIAN_POINT ( 'NONE',  ( 755.8894580844503253, -135.8272453906076009, 332.3691319403863531 ) ) ;
#29644=CARTESIAN_POINT ( 'NONE',  ( 812.6845335610512393, -127.9874144716872308, 353.5525998758768651 ) ) ;
#29645=CARTESIAN_POINT ( 'NONE',  ( 759.7806653035534055, -390.9982390220557136, 324.8639956371180801 ) ) ;
#29648=CARTESIAN_POINT ( 'NONE',  ( 759.9864689768902508, -170.0891481129654608, 354.9819416627836404 ) ) ;
#29653=ORIENTED_EDGE ( 'NONE', *, *, #3849, .T. ) ;
#29654=CARTESIAN_POINT ( 'NONE',  ( 805.1927285166397041, -352.8164208402374129, 341.8018195045277707 ) ) ;
#29656=CARTESIAN_POINT ( 'NONE',  ( 804.4286716492782716, -449.3618753856918602, 345.3141322388244703 ) ) ;
#29658=CARTESIAN_POINT ( 'NONE',  ( 751.9810565676468741, -98.08914811296568814, 360.9747183278973921 ) ) ;
#29660=AXIS2_PLACEMENT_3D ( 'NONE', #30354, #34046, #44446 ) ;
#29664=CARTESIAN_POINT ( 'NONE',  ( 755.0636971347428243, -4.270966294784170003, 341.7834795799807353 ) ) ;
#29665=CARTESIAN_POINT ( 'NONE',  ( 772.3691319403857278, -167.2601417444143976, 315.8894580844506663 ) ) ;
#29669=ADVANCED_FACE ( 'NONE', ( #1570, #29748 ), #8752, .F. ) ;
#29672=CARTESIAN_POINT ( 'NONE',  ( 802.2119215644370342, -78.00906357242591582, 367.5423716828165084 ) ) ;
#29679=LINE ( 'NONE', #15597, #3172 ) ;
#29681=CARTESIAN_POINT ( 'NONE',  ( 793.0897708529556667, -414.5545181178795247, 361.3366627262616362 ) ) ;
#29684=CARTESIAN_POINT ( 'NONE',  ( 755.8894580844503253, -231.8272453906072315, 332.3691319403863531 ) ) ;
#29687=CARTESIAN_POINT ( 'NONE',  ( 812.3518521366052028, -193.0999726633346256, 326.5853460496235243 ) ) ;
#29689=CARTESIAN_POINT ( 'NONE',  ( 812.7932403749906598, -159.1800572038746111, 327.7687537140311633 ) ) ;
#29693=CARTESIAN_POINT ( 'NONE',  ( 791.9812246680005501, -260.6346026584197375, 361.9419747391813189 ) ) ;
#29694=CARTESIAN_POINT ( 'NONE',  ( 784.1219089521767955, -21.28179084515337749, 315.0488828828318333 ) ) ;
#29700=CARTESIAN_POINT ( 'NONE',  ( 764.0069404352550464, -39.07832356259662276, 359.2566176426627180 ) ) ;
#29704=CARTESIAN_POINT ( 'NONE',  ( 803.6646147819161570, -17.90732993114776406, 348.8264449731210561 ) ) ;
#29707=CARTESIAN_POINT ( 'NONE',  ( 759.8311093483677041, -334.1692326535047073, 310.9282345327691814 ) ) ;
#29709=CARTESIAN_POINT ( 'NONE',  ( 755.5713283507202505, -341.3618753856922012, 334.6858677611754729 ) ) ;
#29713=ORIENTED_EDGE ( 'NONE', *, *, #18266, .T. ) ;
#29717=CARTESIAN_POINT ( 'NONE',  ( 795.1360043628807261, -68.08914811296575920, 360.2193346964456282 ) ) ;
#29718=CARTESIAN_POINT ( 'NONE',  ( 784.1219089521767955, -357.2817908451523294, 315.0488828828318333 ) ) ;
#29719=CARTESIAN_POINT ( 'NONE',  ( 751.6929314249750860, -414.9982390220555430, 318.8095938919659034 ) ) ;
#29721=CARTESIAN_POINT ( 'NONE',  ( 746.0683387631852383, -307.4419599262320730, 331.3260364891676204 ) ) ;
#29722=CARTESIAN_POINT ( 'NONE',  ( 793.4146539503750546, -97.98741447168734453, 307.6481478633938877 ) ) ;
#29726=CARTESIAN_POINT ( 'NONE',  ( 814.9108240113580450, -424.2709662947829088, 337.5031285880265273 ) ) ;
#29732=CARTESIAN_POINT ( 'NONE',  ( 793.9708237608222134, -286.9181544815161828, 319.2295555964448681 ) ) ;
#29736=CARTESIAN_POINT ( 'NONE',  ( 750.9282345327678740, -88.91815448151682233, 319.8311093483690115 ) ) ;
#29740=CARTESIAN_POINT ( 'NONE',  ( 771.1735550268778070, -105.1800572038747248, 316.3353852180827630 ) ) ;
#29746=CARTESIAN_POINT ( 'NONE',  ( 798.5707757039680246, -29.46360902697153250, 356.7845633553585003 ) ) ;
#29748=FACE_OUTER_BOUND ( 'NONE', #31318, .T. ) ;
#29749=CARTESIAN_POINT ( 'NONE',  ( 780.5290396650775619, -396.3510508353228374, 365.2837595273619513 ) ) ;
#29756=CARTESIAN_POINT ( 'NONE',  ( 754.0944755984390895, -255.6237781080504874, 364.1009440267246760 ) ) ;
#29757=CARTESIAN_POINT ( 'NONE',  ( 778.1981804954715471, -58.27096629478398881, 314.8072714833591021 ) ) ;
#29761=CARTESIAN_POINT ( 'NONE',  ( 800.0135310231082713, -230.0891481129652618, 325.0180583372163028 ) ) ;
#29771=CARTESIAN_POINT ( 'NONE',  ( 787.5162901302840055, -323.3618753856922581, 305.4481719005793252 ) ) ;
#29772=CARTESIAN_POINT ( 'NONE',  ( 746.0683387631852383, -19.44195992623303937, 331.3260364891676204 ) ) ;
#29776=VECTOR ( 'NONE', #15823, 1000.000000000000000 ) ;
#29780=CARTESIAN_POINT ( 'NONE',  ( 759.7806653035534055, -222.9982390220561399, 324.8639956371180801 ) ) ;
#29782=VERTEX_POINT ( 'NONE', #41761 ) ;
#29783=CARTESIAN_POINT ( 'NONE',  ( 748.9653473494363425, -338.6346026584195101, 356.9462024416521331 ) ) ;
#29784=DIRECTION ( 'NONE',  ( 0.000000000000000000, 0.000000000000000000, 1.000000000000000000 ) ) ;
#29787=CARTESIAN_POINT ( 'NONE',  ( 779.4763451958990572, -176.7363362996983369, 365.0264073115438919 ) ) ;
#29788=CARTESIAN_POINT ( 'NONE',  ( 795.1360043628807261, -92.08914811296568814, 360.2193346964456282 ) ) ;
#29792=CARTESIAN_POINT ( 'NONE',  ( 789.9200121543843807, -265.9874144716867477, 317.0176451133914384 ) ) ;
#29797=CARTESIAN_POINT ( 'NONE',  ( 814.9108240113580450, -424.2709662947829088, 337.5031285880265273 ) ) ;
#29802=CARTESIAN_POINT ( 'NONE',  ( 805.0032342141412300, -37.54369356751132614, 314.9967657858571783 ) ) ;
#29803=CARTESIAN_POINT ( 'NONE',  ( 792.3570229623688874, -141.1800572038746395, 373.1304606946836202 ) ) ;
#29807=CARTESIAN_POINT ( 'NONE',  ( 796.9462024416508257, -372.4527844766010958, 308.9653473494370246 ) ) ;
#29810=CARTESIAN_POINT ( 'NONE',  ( 769.1273215169530886, 25.28531280103955226, 317.4527132478988847 ) ) ;
#29814=CARTESIAN_POINT ( 'NONE',  ( 746.7653713866222915, -137.2601417444144829, 351.0478386215610271 ) ) ;
#29816=CARTESIAN_POINT ( 'NONE',  ( 748.3538107759620743, -160.7146871989598651, 355.8262568251490165 ) ) ;
#29820=CARTESIAN_POINT ( 'NONE',  ( 781.8018195045266339, -118.2709662947837899, 365.1927285166406705 ) ) ;
#29822=CARTESIAN_POINT ( 'NONE',  ( 768.0187753319979720, -272.6346026584196807, 318.0580252608186242 ) ) ;
#29823=CARTESIAN_POINT ( 'NONE',  ( 759.9864689768902508, -266.0891481129651197, 354.9819416627836404 ) ) ;
#29826=CARTESIAN_POINT ( 'NONE',  ( 754.8983024940795303, 5.103494619221427442, 336.9254006560228163 ) ) ;
#29831=CARTESIAN_POINT ( 'NONE',  ( 746.8695393053151292, -221.9073299311471033, 327.6429770376306578 ) ) ;
#29832=CARTESIAN_POINT ( 'NONE',  ( 759.0159684113467620, -304.9181544815161828, 325.8855110935213020 ) ) ;
#29833=CARTESIAN_POINT ( 'NONE',  ( 796.7845633553578182, -393.6237781080500326, 358.5707757039688204 ) ) ;
#29840=CARTESIAN_POINT ( 'NONE',  ( 756.7813123517142913, -259.9874144716869182, 329.9779781133712504 ) ) ;
#29848=CARTESIAN_POINT ( 'NONE',  ( 776.2046728542105711, -212.1908817542436623, 304.8212110874238761 ) ) ;
#29857=CARTESIAN_POINT ( 'NONE',  ( 756.3353852180819104, -53.90732993114765037, 331.1735550268788302 ) ) ;
#29858=AXIS2_PLACEMENT_3D ( 'NONE', #19356, #22818, #33442 ) ;
#29859=CARTESIAN_POINT ( 'NONE',  ( 809.0717654672305343, -292.9181544815162397, 360.1688906516309885 ) ) ;
#29860=CARTESIAN_POINT ( 'NONE',  ( 747.2067596250078623, -267.1800572038742985, 352.2312462859687230 ) ) ;
#29866=CARTESIAN_POINT ( 'NONE',  ( 759.7806653035534055, -342.9982390220557136, 324.8639956371180801 ) ) ;
#29867=CARTESIAN_POINT ( 'NONE',  ( 766.9102291470427417, -114.5545181178803631, 318.6633372737382501 ) ) ;
#29871=CARTESIAN_POINT ( 'NONE',  ( 803.6646147819161570, -401.9073299311463643, 348.8264449731210561 ) ) ;
#29875=CARTESIAN_POINT ( 'NONE',  ( 758.0580252608178853, -150.4527844766018916, 328.0187753319985404 ) ) ;
#29880=CARTESIAN_POINT ( 'NONE',  ( 771.1735550268778070, -369.1800572038739574, 316.3353852180827630 ) ) ;
#29881=VECTOR ( 'NONE', #10424, 1000.000000000000000 ) ;
#29884=CARTESIAN_POINT ( 'NONE',  ( 808.3070685750232087, -90.99823902205662307, 361.1904061080339829 ) ) ;
#29890=CARTESIAN_POINT ( 'NONE',  ( 804.7487373415286811, -259.5436935675106156, 364.7487373415288516 ) ) ;
#29891=CARTESIAN_POINT ( 'NONE',  ( 793.2243759319678702, -170.5328690171416781, 318.4439275373583200 ) ) ;
#29900=CARTESIAN_POINT ( 'NONE',  ( 754.3581564841646241, -113.4636090269712554, 316.1443688327762516 ) ) ;
#29909=CARTESIAN_POINT ( 'NONE',  ( 769.9779781133707957, -403.0999726633339719, 316.7813123517150871 ) ) ;
#29913=CARTESIAN_POINT ( 'NONE',  ( 766.9102291470427417, -234.5545181178799794, 318.6633372737382501 ) ) ;
#29917=CARTESIAN_POINT ( 'NONE',  ( 781.2370466360911223, -188.7363362996983085, 304.9990715423533629 ) ) ;
#29919=CARTESIAN_POINT ( 'NONE',  ( 808.3070685750230950, -138.9982390220563957, 361.1904061080339261 ) ) ;
#29923=CARTESIAN_POINT ( 'NONE',  ( 755.0636971347428243, -244.2709662947834204, 341.7834795799807353 ) ) ;
#29924=CARTESIAN_POINT ( 'NONE',  ( 755.1538015810308480, -38.19088175424422360, 343.0433043558613804 ) ) ;
#29930=CARTESIAN_POINT ( 'NONE',  ( 793.2243759319678702, -74.53286901714196233, 318.4439275373583200 ) ) ;
#29934=CARTESIAN_POINT ( 'NONE',  ( 800.2193346964447755, -66.99823902205672255, 355.1360043628815788 ) ) ;
#29937=CARTESIAN_POINT ( 'NONE',  ( 791.1614460488616487, -347.2601417444138860, 373.5763878283158874 ) ) ;
#29940=CARTESIAN_POINT ( 'NONE',  ( 754.8072714833581358, -364.8164208402374697, 338.1981804954720587 ) ) ;
#29948=CARTESIAN_POINT ( 'NONE',  ( 802.1676090361156639, -110.6346026584201638, 327.8955696845344505 ) ) ;
#29949=CARTESIAN_POINT ( 'NONE',  ( 802.9823548866075953, -409.0999726633340288, 330.0799878456151077 ) ) ;
#29950=VECTOR ( 'NONE', #3339, 1000.000000000000000 ) ;
#29952=CARTESIAN_POINT ( 'NONE',  ( 767.7687537140311633, -431.9073299311464211, 372.7932403749916830 ) ) ;
#29954=CARTESIAN_POINT ( 'NONE',  ( 744.8212110874229666, -330.8965053807774552, 336.2046728542121627 ) ) ;
#29958=CARTESIAN_POINT ( 'NONE',  ( 751.9810565676468741, -434.0891481129646081, 360.9747183278973921 ) ) ;
#29959=AXIS2_PLACEMENT_3D ( 'NONE', #16826, #37133, #5734 ) ;
#29967=CARTESIAN_POINT ( 'NONE',  ( 799.2566176426618085, -312.0090635724251911, 324.0069404352559559 ) ) ;
#29969=CARTESIAN_POINT ( 'NONE',  ( 755.8990559732751535, -275.4636090269708575, 365.9055244015606831 ) ) ;
#29972=CARTESIAN_POINT ( 'NONE',  ( 752.7379699480933368, -84.00906357242590161, 361.9858362298580232 ) ) ;
#29975=CARTESIAN_POINT ( 'NONE',  ( 802.1676090361156639, -158.6346026584199933, 327.8955696845344505 ) ) ;
#29979=CARTESIAN_POINT ( 'NONE',  ( 758.4439275373578084, -12.55451811788067751, 353.2243759319684386 ) ) ;
#29982=CARTESIAN_POINT ( 'NONE',  ( 803.8651313633788504, -389.2601417444136018, 332.4468031744301015 ) ) ;
#29987=CARTESIAN_POINT ( 'NONE',  ( 807.5423716828161105, -249.0783235625959549, 362.2119215644372048 ) ) ;
#29988=CARTESIAN_POINT ( 'NONE',  ( 755.0636971347428243, -100.2709662947838609, 341.7834795799807353 ) ) ;
#29991=CARTESIAN_POINT ( 'NONE',  ( 759.7806653035534055, -246.9982390220560546, 324.8639956371180801 ) ) ;
#29995=ORIENTED_EDGE ( 'NONE', *, *, #17132, .F. ) ;
#29999=CARTESIAN_POINT ( 'NONE',  ( 746.8695393053151292, -341.9073299311466485, 327.6429770376306578 ) ) ;
#30001=CARTESIAN_POINT ( 'NONE',  ( 773.7943932421234194, -47.80559628986931386, 305.5313806188329409 ) ) ;
#30006=CARTESIAN_POINT ( 'NONE',  ( 804.4286716492782716, -209.3618753856926276, 345.3141322388244703 ) ) ;
#30009=CARTESIAN_POINT ( 'NONE',  ( 751.9810565676468741, -338.0891481129649492, 360.9747183278973921 ) ) ;
#30015=CARTESIAN_POINT ( 'NONE',  ( 800.9840315886518738, -196.9181544815164386, 354.1144889064786412 ) ) ;
#30016=CARTESIAN_POINT ( 'NONE',  ( 756.5762568750052424, -99.18005720387478164, 348.7366044899774238 ) ) ;
#30020=CARTESIAN_POINT ( 'NONE',  ( 794.1144889064781864, -250.1692326535050199, 360.9840315886528401 ) ) ;
#30024=CARTESIAN_POINT ( 'NONE',  ( 777.5031285880264704, -430.8164208402374129, 374.9108240113588408 ) ) ;
#30025=CARTESIAN_POINT ( 'NONE',  ( 795.2725662613897839, 16.45630643248849267, 314.1785221222716586 ) ) ;
#30028=CIRCLE ( 'NONE', #25626, 10.00000000000000888 ) ;
#30029=CARTESIAN_POINT ( 'NONE',  ( 777.5031285880264704, -46.81642084023858530, 374.9108240113588408 ) ) ;
#30030=CARTESIAN_POINT ( 'NONE',  ( 763.2262854647970016, -152.6346026584200786, 309.2812353651462445 ) ) ;
#30036=CARTESIAN_POINT ( 'NONE',  ( 814.9108240113580450, -376.2709662947829656, 337.5031285880265273 ) ) ;
#30038=CARTESIAN_POINT ( 'NONE',  ( 795.9930595647434757, 20.92167643740319605, 320.7433823573372820 ) ) ;
#30042=CARTESIAN_POINT ( 'NONE',  ( 813.2346286133761168, -149.2601417444144261, 328.9521613784389160 ) ) ;
#30043=CARTESIAN_POINT ( 'NONE',  ( 804.6798772138710092, 8.274488250670337663, 334.6312213355106451 ) ) ;
#30044=CARTESIAN_POINT ( 'NONE',  ( 793.4146539503750546, -169.9874144716871172, 307.6481478633938877 ) ) ;
#30047=CARTESIAN_POINT ( 'NONE',  ( 788.8264449731200330, -117.1800572038746964, 363.6646147819171233 ) ) ;
#30049=CARTESIAN_POINT ( 'NONE',  ( 774.6858677611749044, -297.7255117493286889, 315.5713283507209894 ) ) ;
#30050=CARTESIAN_POINT ( 'NONE',  ( 771.1735550268780344, -273.1800572038742985, 316.3353852180828198 ) ) ;
#30053=CARTESIAN_POINT ( 'NONE',  ( 765.8855110935204493, 1.830767346494167391, 319.0159684113471599 ) ) ;
#30059=CARTESIAN_POINT ( 'NONE',  ( 804.7487373415286811, -235.5436935675107293, 364.7487373415288516 ) ) ;
#30061=CARTESIAN_POINT ( 'NONE',  ( 780.5236548040995785, -284.7363362996979390, 314.9735926884559944 ) ) ;
#30062=CARTESIAN_POINT ( 'NONE',  ( 786.6156483768007774, -409.4419599262317320, 315.5913626894246136 ) ) ;
#30070=CARTESIAN_POINT ( 'NONE',  ( 805.1016975059191054, -294.8965053807775689, 343.0745993439771837 ) ) ;
#30074=EDGE_CURVE ( 'NONE', #37455, #24474, #43859, .T. ) ;
#30078=CARTESIAN_POINT ( 'NONE',  ( 744.6391490659812007, -206.7363362996982801, 338.7502325331110455 ) ) ;
#30083=CARTESIAN_POINT ( 'NONE',  ( 772.5602148656447525, -33.72551174932952733, 305.7998596910095443 ) ) ;
#30086=CARTESIAN_POINT ( 'NONE',  ( 762.3223304703356007, -55.54369356751127640, 322.3223304703362828 ) ) ;
#30088=CARTESIAN_POINT ( 'NONE',  ( 762.1177392798416577, -306.5545181178797520, 309.8865473780659272 ) ) ;
#30090=CARTESIAN_POINT ( 'NONE',  ( 777.4774526936600978, -250.2709662947832783, 304.7301800767027657 ) ) ;
#30094=CARTESIAN_POINT ( 'NONE',  ( 792.1044303154645831, -372.4527844766010958, 317.8323909638837677 ) ) ;
#30095=CARTESIAN_POINT ( 'NONE',  ( 775.8780910478218402, -129.2817908451530400, 364.9511171171680530 ) ) ;
#30099=CARTESIAN_POINT ( 'NONE',  ( 756.5762568750052424, -411.1800572038738437, 348.7366044899774238 ) ) ;
#30102=CARTESIAN_POINT ( 'NONE',  ( 754.8072714833581358, -172.8164208402381234, 338.1981804954720587 ) ) ;
#30103=CARTESIAN_POINT ( 'NONE',  ( 803.6646147819162707, -161.9073299311472738, 348.8264449731211130 ) ) ;
#30108=CARTESIAN_POINT ( 'NONE',  ( 774.6858677611749044, -345.7255117493285184, 315.5713283507209894 ) ) ;
#30112=CARTESIAN_POINT ( 'NONE',  ( 772.5602148656447525, -105.7255117493293000, 305.7998596910095443 ) ) ;
#30119=CARTESIAN_POINT ( 'NONE',  ( 772.4837098697144029, -263.3618753856924855, 374.5518280994205611 ) ) ;
#30120=CARTESIAN_POINT ( 'NONE',  ( 755.8398074228967971, -211.4419599262324709, 333.4516893846970333 ) ) ;
#30122=CARTESIAN_POINT ( 'NONE',  ( 779.9999999999992042, -452.9681489794448339, 309.9999999999998863 ) ) ;
#30128=CARTESIAN_POINT ( 'NONE',  ( 791.0478386215596629, -117.8272453906076151, 306.7653713866226326 ) ) ;
#30137=CARTESIAN_POINT ( 'NONE',  ( 755.8894580844503253, -423.8272453906067199, 332.3691319403863531 ) ) ;
#30138=CARTESIAN_POINT ( 'NONE',  ( 812.3518521366052028, -361.0999726633341425, 326.5853460496235243 ) ) ;
#30142=CARTESIAN_POINT ( 'NONE',  ( 779.9999999999992042, -462.9681489794448339, 370.0000000000000568 ) ) ;
#30144=CARTESIAN_POINT ( 'NONE',  ( 814.4686193811664907, -171.2817908451529263, 346.2056067578752732 ) ) ;
#30146=CARTESIAN_POINT ( 'NONE',  ( 763.0537975583475827, -144.4527844766018632, 371.0346526505627480 ) ) ;
#30149=CARTESIAN_POINT ( 'NONE',  ( 764.8639956371174549, -248.0891481129651481, 319.7806653035542013 ) ) ;
#30150=CARTESIAN_POINT ( 'NONE',  ( 759.0159684113467620, -40.91815448151695023, 325.8855110935213020 ) ) ;
#30156=CARTESIAN_POINT ( 'NONE',  ( 801.3366627262608972, -80.53286901714194812, 353.0897708529566899 ) ) ;
#30159=CARTESIAN_POINT ( 'NONE',  ( 754.8072714833581358, -52.81642084023856398, 338.1981804954720587 ) ) ;
#30162=CARTESIAN_POINT ( 'NONE',  ( 754.0944755984390895, -375.6237781080501463, 364.1009440267246760 ) ) ;
#30164=CARTESIAN_POINT ( 'NONE',  ( 756.3353852180819104, -269.9073299311468190, 331.1735550268788302 ) ) ;
#30165=CARTESIAN_POINT ( 'NONE',  ( 747.2067596250078623, -3.180057203875080063, 352.2312462859687230 ) ) ;
#30167=CARTESIAN_POINT ( 'NONE',  ( 757.8323909638827445, -362.6346026584194533, 352.1044303154654358 ) ) ;
#30170=ORIENTED_EDGE ( 'NONE', *, *, #18455, .F. ) ;
#30174=CARTESIAN_POINT ( 'NONE',  ( 788.8264449731200330, -93.18005720387481006, 363.6646147819171233 ) ) ;
#30175=CARTESIAN_POINT ( 'NONE',  ( 796.1575198192839480, -390.0090635724249069, 359.4546378042384163 ) ) ;
#30176=CARTESIAN_POINT ( 'NONE',  ( 796.9462024416508257, -420.4527844766009821, 308.9653473494370246 ) ) ;
#30178=CARTESIAN_POINT ( 'NONE',  ( 793.4146539503750546, -337.9874144716865771, 307.6481478633938877 ) ) ;
#30179=CARTESIAN_POINT ( 'NONE',  ( 752.4576283171824116, -93.07832356259645223, 317.7880784355627952 ) ) ;
#30184=CARTESIAN_POINT ( 'NONE',  ( 793.3938497862117174, -453.0432664090020012, 372.3358127763067955 ) ) ;
#30189=CARTESIAN_POINT ( 'NONE',  ( 789.7124813865536908, -452.9681489794450613, 363.0370378529873960 ) ) ;
#30191=CARTESIAN_POINT ( 'NONE',  ( 800.9840315886518738, -340.9181544815160123, 354.1144889064786412 ) ) ;
#30192=CARTESIAN_POINT ( 'NONE',  ( 803.4237431249931660, -183.1800572038744974, 331.2633955100225194 ) ) ;
#30194=CARTESIAN_POINT ( 'NONE',  ( 776.2046728542105711, -284.1908817542434917, 304.8212110874238761 ) ) ;
#30197=CARTESIAN_POINT ( 'NONE',  ( 814.2805881961230625, -73.64542720878957027, 331.2368401574024119 ) ) ;
#30201=CARTESIAN_POINT ( 'NONE',  ( 797.8594530101008786, -157.5436935675108998, 322.1405469898980982 ) ) ;
#30205=CARTESIAN_POINT ( 'NONE',  ( 755.8894580844503253, -15.82724539060794200, 332.3691319403863531 ) ) ;
#30208=CARTESIAN_POINT ( 'NONE',  ( 754.8983024940795303, -426.8965053807771142, 336.9254006560228163 ) ) ;
#30209=VERTEX_POINT ( 'NONE', #35960 ) ;
#30212=CARTESIAN_POINT ( 'NONE',  ( 808.7758568127978833, -268.1692326535049347, 320.0363995740631822 ) ) ;
#30213=CARTESIAN_POINT ( 'NONE',  ( 755.0636971347428243, -76.27096629478394618, 341.7834795799807353 ) ) ;
#30218=CARTESIAN_POINT ( 'NONE',  ( 794.9819416627830151, -276.9982390220559978, 319.9864689768909898 ) ) ;
#30223=CARTESIAN_POINT ( 'NONE',  ( 787.4397851343537695, -309.7255117493287457, 374.2001403089903988 ) ) ;
#30224=CARTESIAN_POINT ( 'NONE',  ( 771.2368401574024119, -229.4419599262323572, 374.2805881961240857 ) ) ;
#30225=CARTESIAN_POINT ( 'NONE',  ( 812.6845335610512393, -31.98741447168754348, 353.5525998758768651 ) ) ;
#30230=CARTESIAN_POINT ( 'NONE',  ( 774.6312213355099630, -215.3618753856925423, 364.6798772138717482 ) ) ;
#30234=CARTESIAN_POINT ( 'NONE',  ( 787.3558975768202117, 16.45630643248848557, 313.9911135047267408 ) ) ;
#30236=CARTESIAN_POINT ( 'NONE',  ( 757.4527132478984868, -184.3726999360619629, 329.1273215169538844 ) ) ;
#30237=CARTESIAN_POINT ( 'NONE',  ( 756.5762568750052424, -75.18005720387485269, 348.7366044899774238 ) ) ;
#30241=CARTESIAN_POINT ( 'NONE',  ( 805.1016975059191054, -270.8965053807777394, 343.0745993439771837 ) ) ;
#30244=CARTESIAN_POINT ( 'NONE',  ( 796.9462024416508257, -444.4527844766009821, 308.9653473494370246 ) ) ;
#30248=CARTESIAN_POINT ( 'NONE',  ( 745.7998596910086917, -77.36187538569302546, 332.5602148656461168 ) ) ;
#30249=CARTESIAN_POINT ( 'NONE',  ( 777.5031285880264704, -142.8164208402382656, 374.9108240113588408 ) ) ;
#30254=CARTESIAN_POINT ( 'NONE',  ( 777.4774526936600978, -394.2709662947827951, 304.7301800767027657 ) ) ;
#30255=CARTESIAN_POINT ( 'NONE',  ( 755.2512626584698410, -7.543693567511430942, 315.2512626584710915 ) ) ;
#30257=CARTESIAN_POINT ( 'NONE',  ( 772.3691319403857278, 24.73985825558500551, 315.8894580844506663 ) ) ;
#30260=CARTESIAN_POINT ( 'NONE',  ( 811.6461892240364477, -124.7146871989599930, 324.1737431748509835 ) ) ;
#30265=CARTESIAN_POINT ( 'NONE',  ( 755.0636971347428243, -172.2709662947836478, 341.7834795799807353 ) ) ;
#30268=CARTESIAN_POINT ( 'NONE',  ( 755.3201227861273992, -291.7255117493286320, 345.3687786644892981 ) ) ;
#30271=CARTESIAN_POINT ( 'NONE',  ( 794.1144889064781864, -10.16923265350579442, 360.9840315886528401 ) ) ;
#30275=CARTESIAN_POINT ( 'NONE',  ( 772.4837098697145166, -215.3618753856925707, 374.5518280994205611 ) ) ;
#30276=CARTESIAN_POINT ( 'NONE',  ( 755.5913626894240451, -301.6454272087889308, 346.6156483768012890 ) ) ;
#30277=CARTESIAN_POINT ( 'NONE',  ( 789.9200121543843807, -409.9874144716863498, 317.0176451133914384 ) ) ;
#30285=CARTESIAN_POINT ( 'NONE',  ( 805.0264073115434940, -294.3510508353230648, 339.4763451958999099 ) ) ;
#30295=CARTESIAN_POINT ( 'NONE',  ( 777.5031285880264704, -46.81642084023858530, 374.9108240113588408 ) ) ;
#30298=DIRECTION ( 'NONE',  ( 0.000000000000000000, 0.000000000000000000, 1.000000000000000000 ) ) ;
#30299=CARTESIAN_POINT ( 'NONE',  ( 794.9819416627830151, -60.99823902205671544, 319.9864689768909898 ) ) ;
#30301=CARTESIAN_POINT ( 'NONE',  ( 764.1737431748507561, -322.3726999360615082, 371.6461892240376415 ) ) ;
#30302=CARTESIAN_POINT ( 'NONE',  ( 755.2512626584698410, -271.5436935675106156, 315.2512626584710915 ) ) ;
#30307=CARTESIAN_POINT ( 'NONE',  ( 755.0636971347428243, -364.2709662947830793, 341.7834795799807353 ) ) ;
#30308=CARTESIAN_POINT ( 'NONE',  ( 761.4292242960306112, -137.4636090269711985, 323.2154366446414429 ) ) ;
#30310=CARTESIAN_POINT ( 'NONE',  ( 752.4576283171824116, -45.07832356259660145, 317.7880784355627952 ) ) ;
#30311=CARTESIAN_POINT ( 'NONE',  ( 801.9419747391806368, -354.4527844766012095, 351.9812246680014027 ) ) ;
#30314=CARTESIAN_POINT ( 'NONE',  ( 801.9419747391806368, -402.4527844766010389, 351.9812246680014027 ) ) ;
#30320=CARTESIAN_POINT ( 'NONE',  ( 804.6798772138708955, -183.7255117493290015, 334.6312213355107019 ) ) ;
#30321=CARTESIAN_POINT ( 'NONE',  ( 759.7806653035535192, -174.9982390220563673, 324.8639956371181370 ) ) ;
#30325=CARTESIAN_POINT ( 'NONE',  ( 759.7806653035534055, -342.9982390220557136, 324.8639956371180801 ) ) ;
#30328=CARTESIAN_POINT ( 'NONE',  ( 751.9810565676468741, -122.0891481129656171, 360.9747183278973921 ) ) ;
#30336=CARTESIAN_POINT ( 'NONE',  ( 745.7998596910086917, -245.3618753856925139, 332.5602148656461168 ) ) ;
#30337=CARTESIAN_POINT ( 'NONE',  ( 756.7813123517142913, -187.9874144716870603, 329.9779781133712504 ) ) ;
#30348=CARTESIAN_POINT ( 'NONE',  ( 745.7194118038753459, -109.6454272087894566, 348.7631598425976449 ) ) ;
#30354=CARTESIAN_POINT ( 'NONE',  ( 779.9999999999992042, 16.45630643248849267, 339.9999999999999432 ) ) ;
#30357=CARTESIAN_POINT ( 'NONE',  ( 799.2566176426618085, -432.0090635724247932, 324.0069404352559559 ) ) ;
#30366=CARTESIAN_POINT ( 'NONE',  ( 746.4236121716829757, -231.8272453906072315, 328.8385539511384650 ) ) ;
#30368=CARTESIAN_POINT ( 'NONE',  ( 763.0537975583475827, -168.4527844766018347, 371.0346526505627480 ) ) ;
#30372=CARTESIAN_POINT ( 'NONE',  ( 768.0187753319979720, -248.6346026584197659, 318.0580252608186242 ) ) ;
#30373=CARTESIAN_POINT ( 'NONE',  ( 793.9708237608222134, -46.91815448151694312, 319.2295555964448681 ) ) ;
#30377=CARTESIAN_POINT ( 'NONE',  ( 793.2243759319678702, -98.53286901714187707, 318.4439275373583200 ) ) ;
#30378=EDGE_LOOP ( 'NONE', ( #38414, #28729, #42566, #41252, #45592, #22845 ) ) ;
#30382=CARTESIAN_POINT ( 'NONE',  ( 768.0187753319979720, -56.63460265842036279, 318.0580252608186242 ) ) ;
#30385=CARTESIAN_POINT ( 'NONE',  ( 815.1787889125755555, -366.8965053807773984, 343.7953271457877804 ) ) ;
#30387=CARTESIAN_POINT ( 'NONE',  ( 762.3223304703356007, -271.5436935675106156, 322.3223304703362828 ) ) ;
#30388=CARTESIAN_POINT ( 'NONE',  ( 813.1304606946830518, 6.092670068852159559, 352.3570229623690580 ) ) ;
#30390=CARTESIAN_POINT ( 'NONE',  ( 781.8018195045266339, -382.2709662947828519, 365.1927285166406705 ) ) ;
#30397=CARTESIAN_POINT ( 'NONE',  ( 755.0636971347428243, -100.2709662947838609, 341.7834795799807353 ) ) ;
#30398=CARTESIAN_POINT ( 'NONE',  ( 793.9708237608222134, -406.9181544815157849, 319.2295555964448681 ) ) ;
#30399=CARTESIAN_POINT ( 'NONE',  ( 745.4481719005789273, -435.7255117493282341, 347.5162901302853697 ) ) ;
#30401=CARTESIAN_POINT ( 'NONE',  ( 807.5423716828161105, -369.0783235625956422, 362.2119215644372048 ) ) ;
#30406=CARTESIAN_POINT ( 'NONE',  ( 782.4968714119720516, -442.8164208402372992, 305.0891759886411023 ) ) ;
#30413=CARTESIAN_POINT ( 'NONE',  ( 790.0220218866281812, -343.0999726633342561, 363.2186876482849129 ) ) ;
#30414=VERTEX_POINT ( 'NONE', #12825 ) ;
#30415=CARTESIAN_POINT ( 'NONE',  ( 805.6418435158337843, -293.4636090269707438, 363.8556311672236916 ) ) ;
#30418=CARTESIAN_POINT ( 'NONE',  ( 749.5768839229115201, -108.5545181178803915, 358.0661480581553064 ) ) ;
#30421=CARTESIAN_POINT ( 'NONE',  ( 804.9363028652555840, -136.2709662947837330, 338.2165204200192079 ) ) ;
#30423=CARTESIAN_POINT ( 'NONE',  ( 771.3260364891663130, -403.6454272087884760, 306.0683387631859773 ) ) ;
#30426=CARTESIAN_POINT ( 'NONE',  ( 773.4516893846965786, -43.64542720878966975, 315.8398074228977066 ) ) ;
#30429=CARTESIAN_POINT ( 'NONE',  ( 796.7845633553578182, -441.6237781080499190, 358.5707757039688204 ) ) ;
#30431=CARTESIAN_POINT ( 'NONE',  ( 804.1601925771018387, -79.44195992623286884, 346.5483106153029098 ) ) ;
#30435=CARTESIAN_POINT ( 'NONE',  ( 761.9338519418445230, -278.5328690171412518, 370.4231160770881957 ) ) ;
#30436=CARTESIAN_POINT ( 'NONE',  ( 757.8323909638828582, -74.63460265842030594, 352.1044303154654358 ) ) ;
#30438=CARTESIAN_POINT ( 'NONE',  ( 804.4286716492782716, -257.3618753856924286, 345.3141322388244703 ) ) ;
#30444=CARTESIAN_POINT ( 'NONE',  ( 754.9967657858570647, -313.5436935675103882, 365.0032342141425943 ) ) ;
#30445=CARTESIAN_POINT ( 'NONE',  ( 778.7502325331095108, -216.3510508353233490, 304.6391490659818828 ) ) ;
#30450=CARTESIAN_POINT ( 'NONE',  ( 755.0636971347428243, -220.2709662947834772, 341.7834795799807353 ) ) ;
#30453=CARTESIAN_POINT ( 'NONE',  ( 782.4968714119720516, -346.8164208402376971, 305.0891759886411023 ) ) ;
#30457=CARTESIAN_POINT ( 'NONE',  ( 769.0155153010367712, -226.3726999360617924, 362.7791456095907279 ) ) ;
#30458=CARTESIAN_POINT ( 'NONE',  ( 774.6312213355099630, -95.36187538569294020, 364.6798772138717482 ) ) ;
#30463=CARTESIAN_POINT ( 'NONE',  ( 757.8323909638827445, -74.63460265842032015, 352.1044303154654358 ) ) ;
#30464=CARTESIAN_POINT ( 'NONE',  ( 783.0433043558608688, -264.8965053807776826, 315.1538015810313027 ) ) ;
#30467=CARTESIAN_POINT ( 'NONE',  ( 747.6481478633932056, -13.09997266333522248, 353.4146539503763620 ) ) ;
#30471=CARTESIAN_POINT ( 'NONE',  ( 746.8695393053150156, -77.90732993114757221, 327.6429770376306010 ) ) ;
#30472=CARTESIAN_POINT ( 'NONE',  ( 767.7687537140311633, -143.9073299311473590, 372.7932403749916830 ) ) ;
#30477=CARTESIAN_POINT ( 'NONE',  ( 745.5313806188320314, -423.2817908451521589, 333.7943932421247268 ) ) ;
#30480=CARTESIAN_POINT ( 'NONE',  ( 763.2262854647970016, -392.6346026584193396, 309.2812353651462445 ) ) ;
#30481=CARTESIAN_POINT ( 'NONE',  ( 751.6929314249750860, -6.998239022056886860, 318.8095938919659034 ) ) ;
#30483=CARTESIAN_POINT ( 'NONE',  ( 783.0433043558608688, -24.89650538077847486, 315.1538015810313027 ) ) ;
#30486=CARTESIAN_POINT ( 'NONE',  ( 776.2433038121456548, -156.8965053807780805, 374.8207195650711014 ) ) ;
#30487=CARTESIAN_POINT ( 'NONE',  ( 785.3687786644885591, 12.63812461430668677, 315.3201227861280813 ) ) ;
#30491=CARTESIAN_POINT ( 'NONE',  ( 803.4237431249931660, -159.1800572038746111, 331.2633955100225194 ) ) ;
#30493=CARTESIAN_POINT ( 'NONE',  ( 756.5762568750052424, -291.1800572038741848, 348.7366044899774238 ) ) ;
#30494=CARTESIAN_POINT ( 'NONE',  ( 771.1735550268780344, -297.1800572038741279, 316.3353852180828198 ) ) ;
#30498=CARTESIAN_POINT ( 'NONE',  ( 757.2208543904082489, -16.71468719896031985, 350.9844846989624330 ) ) ;
#30503=CARTESIAN_POINT ( 'NONE',  ( 782.5225473063383106, -238.2709662947833920, 375.2698199232970637 ) ) ;
#30504=CARTESIAN_POINT ( 'NONE',  ( 755.1538015810308480, -302.1908817542433781, 343.0433043558613804 ) ) ;
#30505=CARTESIAN_POINT ( 'NONE',  ( 789.9200121543843807, -433.9874144716862361, 317.0176451133914384 ) ) ;
#30513=CARTESIAN_POINT ( 'NONE',  ( 756.7813123517142913, -307.9874144716866340, 329.9779781133712504 ) ) ;
#30516=CARTESIAN_POINT ( 'NONE',  ( 763.8424801807145741, -114.0090635724258163, 320.5453621957614700 ) ) ;
#30526=CARTESIAN_POINT ( 'NONE',  ( 787.5162901302840055, -59.36187538569306810, 305.4481719005792684 ) ) ;
#30530=VECTOR ( 'NONE', #23188, 1000.000000000000000 ) ;
#30532=CARTESIAN_POINT ( 'NONE',  ( 802.2119215644370342, -318.0090635724251911, 367.5423716828165084 ) ) ;
#30534=CARTESIAN_POINT ( 'NONE',  ( 782.5225473063381969, -286.2709662947833635, 375.2698199232970637 ) ) ;
#30537=DIRECTION ( 'NONE',  ( 0.000000000000000000, 0.000000000000000000, -1.000000000000000000 ) ) ;
#30538=CARTESIAN_POINT ( 'NONE',  ( 795.1360043628807261, -356.0891481129647218, 360.2193346964456282 ) ) ;
#30539=CARTESIAN_POINT ( 'NONE',  ( 772.4468031744293057, -129.8272453906075725, 363.8651313633793620 ) ) ;
#30541=CARTESIAN_POINT ( 'NONE',  ( 768.8385539511368734, -71.26014174441469606, 306.4236121716840557 ) ) ;
#30542=CARTESIAN_POINT ( 'NONE',  ( 774.6858677611749044, -369.7255117493284615, 315.5713283507209894 ) ) ;
#30546=CARTESIAN_POINT ( 'NONE',  ( 744.8212110874229666, -138.8965053807781374, 336.2046728542121627 ) ) ;
#30547=CARTESIAN_POINT ( 'NONE',  ( 788.7366044899766848, -443.9073299311464780, 316.5762568750059813 ) ) ;
#30548=EDGE_LOOP ( 'NONE', ( #43194, #12344, #20777, #12401 ) ) ;
#30550=CARTESIAN_POINT ( 'NONE',  ( 771.1735550268778070, -177.1800572038744690, 316.3353852180827630 ) ) ;
#30551=CARTESIAN_POINT ( 'NONE',  ( 765.0180583372156207, -192.9982390220562820, 360.0135310231089534 ) ) ;
#30555=CARTESIAN_POINT ( 'NONE',  ( 759.9864689768902508, -410.0891481129647218, 354.9819416627836404 ) ) ;
#30558=CARTESIAN_POINT ( 'NONE',  ( 763.2262854647970016, -104.6346026584202207, 309.2812353651462445 ) ) ;
#30560=CARTESIAN_POINT ( 'NONE',  ( 751.2241431872005251, -184.1692326535052757, 359.9636004259367610 ) ) ;
#30562=VECTOR ( 'NONE', #25191, 1000.000000000000000 ) ;
#30566=CARTESIAN_POINT ( 'NONE',  ( 772.4837098697144029, -239.3618753856924570, 374.5518280994205611 ) ) ;
#30567=CARTESIAN_POINT ( 'NONE',  ( 754.9735926884551418, -186.3510508353234343, 340.5236548041000333 ) ) ;
#30578=CARTESIAN_POINT ( 'NONE',  ( 773.7305795820266212, -105.2817908451530968, 374.8230680027170365 ) ) ;
#30588=CARTESIAN_POINT ( 'NONE',  ( 786.5483106153019435, -439.6454272087884760, 364.1601925771022366 ) ) ;
#30590=CARTESIAN_POINT ( 'NONE',  ( 795.8262568251477660, -358.3726999360613945, 308.3538107759623585 ) ) ;
#30597=CARTESIAN_POINT ( 'NONE',  ( 764.1737431748507561, -202.3726999360618777, 371.6461892240376415 ) ) ;
#30599=CARTESIAN_POINT ( 'NONE',  ( 814.9108240113580450, -184.2709662947835909, 337.5031285880265273 ) ) ;
#30601=DIRECTION ( 'NONE',  ( -1.000000000000000000, -0.000000000000000000, 0.000000000000000000 ) ) ;
#30603=CARTESIAN_POINT ( 'NONE',  ( 759.9864689768902508, -266.0891481129651197, 354.9819416627836404 ) ) ;
#30605=CARTESIAN_POINT ( 'NONE',  ( 769.9779781133707957, -67.09997266333506616, 316.7813123517150871 ) ) ;
#30612=CARTESIAN_POINT ( 'NONE',  ( 780.5290396650775619, -84.35105083532374692, 365.2837595273619513 ) ) ;
#30613=CARTESIAN_POINT ( 'NONE',  ( 802.1676090361156639, -326.6346026584193396, 327.8955696845344505 ) ) ;
#30617=CARTESIAN_POINT ( 'NONE',  ( 788.8264449731200330, -69.18005720387488111, 363.6646147819171233 ) ) ;
#30620=CARTESIAN_POINT ( 'NONE',  ( 758.0141637701419768, -375.0783235625955285, 367.2620300519063790 ) ) ;
#30622=CARTESIAN_POINT ( 'NONE',  ( 756.5762568750052424, -291.1800572038741848, 348.7366044899774238 ) ) ;
#30624=CARTESIAN_POINT ( 'NONE',  ( 795.6651683502461765, -442.7146871989589840, 371.3240766477733814 ) ) ;
#30626=CARTESIAN_POINT ( 'NONE',  ( 758.0580252608178853, -366.4527844766012095, 328.0187753319985404 ) ) ;
#30629=AXIS2_PLACEMENT_3D ( 'NONE', #1496, #8443, #22288 ) ;
#30635=CARTESIAN_POINT ( 'NONE',  ( 781.7834795799800531, -82.81642084023846451, 315.0636971347436202 ) ) ;
#30636=CARTESIAN_POINT ( 'NONE',  ( 757.0176451133909268, -421.0999726633340288, 349.9200121543848354 ) ) ;
#30637=CARTESIAN_POINT ( 'NONE',  ( 756.7813123517142913, -91.98741447168737295, 329.9779781133712504 ) ) ;
#30640=CARTESIAN_POINT ( 'NONE',  ( 754.0944755984390895, -351.6237781080502032, 364.1009440267246760 ) ) ;
#30647=CARTESIAN_POINT ( 'NONE',  ( 772.4999999999993179, -462.9681489794447771, 309.9999999999998863 ) ) ;
#30654=CARTESIAN_POINT ( 'NONE',  ( 800.9840315886518738, -316.9181544815160692, 354.1144889064786412 ) ) ;
#30656=CARTESIAN_POINT ( 'NONE',  ( 781.2370466360911223, -308.7363362996979390, 304.9990715423533629 ) ) ;
#30659=CARTESIAN_POINT ( 'NONE',  ( 791.0478386215596629, -117.8272453906076151, 306.7653713866226326 ) ) ;
#30665=CARTESIAN_POINT ( 'NONE',  ( 781.8018195045266339, -142.2709662947837330, 365.1927285166406705 ) ) ;
#30667=CARTESIAN_POINT ( 'NONE',  ( 809.0717654672305343, -412.9181544815157281, 360.1688906516309885 ) ) ;
#30670=CARTESIAN_POINT ( 'NONE',  ( 763.0428371773158460, -35.46360902697151829, 358.7617431975195359 ) ) ;
#30672=DIRECTION ( 'NONE',  ( 0.000000000000000000, 0.000000000000000000, 1.000000000000000000 ) ) ;
#30673=CARTESIAN_POINT ( 'NONE',  ( 784.0799538623451781, -419.8055962898681059, 364.6971507214555572 ) ) ;
#30678=CARTESIAN_POINT ( 'NONE',  ( 746.0683387631852383, -259.4419599262322436, 331.3260364891676204 ) ) ;
#30679=CARTESIAN_POINT ( 'NONE',  ( 785.3141322388236176, -69.72551174932942786, 364.4286716492789537 ) ) ;
#30683=CARTESIAN_POINT ( 'NONE',  ( 805.1927285166397041, -256.8164208402379245, 341.8018195045277707 ) ) ;
#30693=CARTESIAN_POINT ( 'NONE',  ( 745.0891759886404770, -316.2709662947832499, 342.4968714119734159 ) ) ;
#30694=CARTESIAN_POINT ( 'NONE',  ( 815.1787889125755555, -246.8965053807777679, 343.7953271457877804 ) ) ;
#30695=CARTESIAN_POINT ( 'NONE',  ( 805.9055244015594326, -51.62377810805111267, 315.8990559732753240 ) ) ;
#30699=CARTESIAN_POINT ( 'NONE',  ( 795.1360043628807261, -260.0891481129650060, 360.2193346964456282 ) ) ;
#30701=CARTESIAN_POINT ( 'NONE',  ( 813.1304606946830518, -353.9073299311467053, 352.3570229623690580 ) ) ;
#30704=CARTESIAN_POINT ( 'NONE',  ( 779.2785047387700388, 16.45630643248848912, 314.0977342670951202 ) ) ;
#30706=CARTESIAN_POINT ( 'NONE',  ( 779.4763451958990572, -224.7363362996982232, 365.0264073115438919 ) ) ;
#30707=CARTESIAN_POINT ( 'NONE',  ( 778.1981804954714335, -82.27096629478388934, 314.8072714833589885 ) ) ;
#30710=CARTESIAN_POINT ( 'NONE',  ( 756.7813123517142913, -259.9874144716869182, 329.9779781133712504 ) ) ;
#30714=CARTESIAN_POINT ( 'NONE',  ( 791.0478386215596629, -21.82724539060792424, 306.7653713866226326 ) ) ;
#30719=CARTESIAN_POINT ( 'NONE',  ( 811.0346526505616112, -86.63460265842023489, 323.0537975583477532 ) ) ;
#30720=CARTESIAN_POINT ( 'NONE',  ( 814.9108240113580450, -160.2709662947836762, 337.5031285880265273 ) ) ;
#30725=CARTESIAN_POINT ( 'NONE',  ( 795.8262568251477660, -406.3726999360612808, 308.3538107759623585 ) ) ;
#30728=CARTESIAN_POINT ( 'NONE',  ( 813.1304606946830518, -401.9073299311463643, 352.3570229623690580 ) ) ;
#30729=CARTESIAN_POINT ( 'NONE',  ( 782.5225473063383106, -22.27096629478410605, 375.2698199232970637 ) ) ;
#30731=CARTESIAN_POINT ( 'NONE',  ( 796.7845633553578182, -9.623778108051251223, 358.5707757039688204 ) ) ;
#30734=CARTESIAN_POINT ( 'NONE',  ( 749.8865473780648472, -164.5328690171416781, 322.1177392798429082 ) ) ;
#30739=CARTESIAN_POINT ( 'NONE',  ( 768.0187753319979720, -152.6346026584200786, 318.0580252608186242 ) ) ;
#30741=CARTESIAN_POINT ( 'NONE',  ( 778.2165204200184689, -286.8164208402378677, 364.9363028652563230 ) ) ;
#30744=CARTESIAN_POINT ( 'NONE',  ( 789.9200121543843807, -25.98741447168755769, 317.0176451133914384 ) ) ;
#30748=CARTESIAN_POINT ( 'NONE',  ( 754.9967657858570647, -217.5436935675107293, 365.0032342141425943 ) ) ;
#30749=CARTESIAN_POINT ( 'NONE',  ( 754.7162404726377645, -350.7363362996978253, 339.4709603349214717 ) ) ;
#30750=CARTESIAN_POINT ( 'NONE',  ( 779.4709603349208464, -432.3510508353226669, 314.7162404726379918 ) ) ;
#30753=VECTOR ( 'NONE', #26815, 1000.000000000000000 ) ;
#30759=CARTESIAN_POINT ( 'NONE',  ( 756.7813123517142913, -283.9874144716867477, 329.9779781133712504 ) ) ;
#30760=CARTESIAN_POINT ( 'NONE',  ( 793.4578903520955464, -453.6923923018891855, 372.2744472307925321 ) ) ;
#30763=CARTESIAN_POINT ( 'NONE',  ( 779.4763451958990572, -128.7363362996984790, 365.0264073115438919 ) ) ;
#30767=CARTESIAN_POINT ( 'NONE',  ( 791.0478386215596629, -189.8272453906073736, 306.7653713866226326 ) ) ;
#30771=CARTESIAN_POINT ( 'NONE',  ( 813.1304606946830518, -41.90732993114767169, 352.3570229623690580 ) ) ;
#30772=CARTESIAN_POINT ( 'NONE',  ( 798.5757817331792694, -452.9681489794448339, 357.1584183591081683 ) ) ;
#30776=CARTESIAN_POINT ( 'NONE',  ( 810.4231160770870019, -336.5545181178796952, 321.9338519418446936 ) ) ;
#30778=CARTESIAN_POINT ( 'NONE',  ( 747.2067596250078623, -291.1800572038741848, 352.2312462859687230 ) ) ;
#30781=DIRECTION ( 'NONE',  ( -1.000000000000000000, -0.000000000000000000, -0.000000000000000000 ) ) ;
#30782=CARTESIAN_POINT ( 'NONE',  ( 778.2165204200184689, -382.8164208402374697, 364.9363028652563230 ) ) ;
#30783=CARTESIAN_POINT ( 'NONE',  ( 804.6971507214547046, -171.2817908451529263, 344.0799538623459739 ) ) ;
#30785=CARTESIAN_POINT ( 'NONE',  ( 788.7631598425961101, -49.44195992623295410, 305.7194118038759143 ) ) ;
#30786=CARTESIAN_POINT ( 'NONE',  ( 797.6776695296629214, -355.5436935675103882, 357.6776695296636603 ) ) ;
#30789=CARTESIAN_POINT ( 'NONE',  ( 800.0135310231082713, -446.0891481129646081, 325.0180583372163028 ) ) ;
#30793=CARTESIAN_POINT ( 'NONE',  ( 759.7806653035534055, -198.9982390220562252, 324.8639956371180801 ) ) ;
#30794=CARTESIAN_POINT ( 'NONE',  ( 804.6798772138710092, -207.7255117493289731, 334.6312213355106451 ) ) ;
#30796=CARTESIAN_POINT ( 'NONE',  ( 769.9999999999992042, 178.9475563372491251, 360.0000000000000000 ) ) ;
#30798=CARTESIAN_POINT ( 'NONE',  ( 768.0187753319979720, -392.6346026584193396, 318.0580252608186242 ) ) ;
#30802=CARTESIAN_POINT ( 'NONE',  ( 745.0891759886404770, -100.2709662947838609, 342.4968714119734159 ) ) ;
#30805=ORIENTED_EDGE ( 'NONE', *, *, #28125, .T. ) ;
#30808=CARTESIAN_POINT ( 'NONE',  ( 773.3843516231979720, -181.4419599262325278, 364.4086373105754433 ) ) ;
#30817=CARTESIAN_POINT ( 'NONE',  ( 813.5763878283155464, -99.82724539060768620, 351.1614460488615350 ) ) ;
#30826=CARTESIAN_POINT ( 'NONE',  ( 755.5913626894240451, -421.6454272087885329, 346.6156483768012890 ) ) ;
#30833=CARTESIAN_POINT ( 'NONE',  ( 783.7953271457878373, -224.1908817542436623, 375.1787889125761239 ) ) ;
#30835=CARTESIAN_POINT ( 'NONE',  ( 751.6929314249748586, -198.9982390220562252, 318.8095938919659034 ) ) ;
#30838=CARTESIAN_POINT ( 'NONE',  ( 785.3687786644884454, -275.3618753856923149, 315.3201227861279676 ) ) ;
#30839=CARTESIAN_POINT ( 'NONE',  ( 799.2566176426618085, -72.00906357242594424, 324.0069404352559559 ) ) ;
#30843=CARTESIAN_POINT ( 'NONE',  ( 795.9930595647434757, -75.07832356259649487, 320.7433823573372820 ) ) ;
#30844=CARTESIAN_POINT ( 'NONE',  ( 755.3201227861273992, -339.7255117493285184, 345.3687786644892981 ) ) ;
#30849=CARTESIAN_POINT ( 'NONE',  ( 794.9819416627830151, -60.99823902205671544, 319.9864689768909898 ) ) ;
#30852=CARTESIAN_POINT ( 'NONE',  ( 786.2056067578752163, -371.8055962898682765, 374.4686193811670023 ) ) ;
#30854=CARTESIAN_POINT ( 'NONE',  ( 755.3201227861273992, -291.7255117493285752, 345.3687786644892981 ) ) ;
#30858=CARTESIAN_POINT ( 'NONE',  ( 803.6646147819161570, -377.9073299311466485, 348.8264449731210561 ) ) ;
#30859=EDGE_CURVE ( 'NONE', #16721, #6763, #16614, .T. ) ;
#30865=CARTESIAN_POINT ( 'NONE',  ( 803.6646147819161570, -89.90732993114750116, 348.8264449731210561 ) ) ;
#30866=CARTESIAN_POINT ( 'NONE',  ( 800.9840315886518738, -412.9181544815157281, 354.1144889064786412 ) ) ;
#30869=CARTESIAN_POINT ( 'NONE',  ( 801.9858362298568863, -363.0783235625955854, 312.7379699480935642 ) ) ;
#30873=CARTESIAN_POINT ( 'NONE',  ( 752.7379699480933368, -12.00906357242613609, 361.9858362298580232 ) ) ;
#30881=CARTESIAN_POINT ( 'NONE',  ( 802.9823548866075953, -337.0999726633342561, 330.0799878456151077 ) ) ;
#30882=EDGE_CURVE ( 'NONE', #25691, #28582, #20211, .T. ) ;
#30884=CARTESIAN_POINT ( 'NONE',  ( 814.2805881961230625, -313.6454272087888171, 331.2368401574024119 ) ) ;
#30888=CARTESIAN_POINT ( 'NONE',  ( 814.8207195650702488, -98.19088175424404596, 336.2433038121456548 ) ) ;
#30892=CARTESIAN_POINT ( 'NONE',  ( 803.6646147819161570, -161.9073299311472454, 348.8264449731210561 ) ) ;
#30894=CARTESIAN_POINT ( 'NONE',  ( 754.3581564841646241, -425.4636090269703459, 316.1443688327762516 ) ) ;
#30898=CARTESIAN_POINT ( 'NONE',  ( 793.0897708529556667, -54.55451811788054783, 361.3366627262616362 ) ) ;
#30901=CARTESIAN_POINT ( 'NONE',  ( 776.9566956441375396, -420.8965053807772279, 364.8461984189686405 ) ) ;
#30906=CARTESIAN_POINT ( 'NONE',  ( 768.8385539511368734, -287.2601417444140566, 306.4236121716840557 ) ) ;
#30907=CARTESIAN_POINT ( 'NONE',  ( 778.2165204200184689, -94.81642084023843609, 364.9363028652563230 ) ) ;
#30910=CARTESIAN_POINT ( 'NONE',  ( 771.1735550268778070, -273.1800572038742985, 316.3353852180827630 ) ) ;
#30919=CARTESIAN_POINT ( 'NONE',  ( 777.4774526936600978, -346.2709662947830225, 304.7301800767028226 ) ) ;
#30920=CARTESIAN_POINT ( 'NONE',  ( 766.5853460496234675, -253.9874144716868329, 372.3518521366060554 ) ) ;
#30921=CARTESIAN_POINT ( 'NONE',  ( 801.9858362298568863, -51.07832356259657303, 312.7379699480935642 ) ) ;
#30926=CARTESIAN_POINT ( 'NONE',  ( 765.0180583372156207, -240.9982390220561683, 360.0135310231089534 ) ) ;
#30928=CARTESIAN_POINT ( 'NONE',  ( 751.6929314249748586, -342.9982390220557136, 318.8095938919659034 ) ) ;
#30930=EDGE_CURVE ( 'NONE', #26699, #41138, #18834, .T. ) ;
#30932=CARTESIAN_POINT ( 'NONE',  ( 781.4876528434626834, 16.45630643248849267, 313.8857452882203347 ) ) ;
#30934=CARTESIAN_POINT ( 'NONE',  ( 804.6971507214547046, -243.2817908451526705, 344.0799538623459739 ) ) ;
#30935=CARTESIAN_POINT ( 'NONE',  ( 764.8639956371174549, -104.0891481129656881, 319.7806653035542013 ) ) ;
#30936=ORIENTED_EDGE ( 'NONE', *, *, #17349, .T. ) ;
#30939=CARTESIAN_POINT ( 'NONE',  ( 773.3843516231979720, -301.4419599262320730, 364.4086373105754433 ) ) ;
#30942=CARTESIAN_POINT ( 'NONE',  ( 814.4686193811664907, -3.281790845153435221, 346.2056067578752732 ) ) ;
#30945=CARTESIAN_POINT ( 'NONE',  ( 796.9462024416508257, -84.45278447660206211, 308.9653473494370246 ) ) ;
#30946=CARTESIAN_POINT ( 'NONE',  ( 787.4397851343537695, -189.7255117493290300, 374.2001403089903988 ) ) ;
#30951=CARTESIAN_POINT ( 'NONE',  ( 793.5525998758768083, -415.0999726633340288, 372.6845335610516941 ) ) ;
#30954=CARTESIAN_POINT ( 'NONE',  ( 777.5031285880264704, -406.8164208402375266, 374.9108240113588408 ) ) ;
#30955=CARTESIAN_POINT ( 'NONE',  ( 804.7487373415286811, -19.54369356751139364, 364.7487373415288516 ) ) ;
#30958=CARTESIAN_POINT ( 'NONE',  ( 803.2186876482843445, -31.98741447168754348, 350.0220218866286928 ) ) ;
#30961=CARTESIAN_POINT ( 'NONE',  ( 764.3348316497523456, -166.7146871989598367, 308.6759233522265617 ) ) ;
#30962=CARTESIAN_POINT ( 'NONE',  ( 805.1927285166399315, 7.183579159761249500, 341.8018195045277707 ) ) ;
#30966=CARTESIAN_POINT ( 'NONE',  ( 800.2193346964447755, -162.9982390220563673, 355.1360043628815788 ) ) ;
#30968=CARTESIAN_POINT ( 'NONE',  ( 788.7366044899766848, -299.9073299311468759, 316.5762568750059813 ) ) ;
#30971=CARTESIAN_POINT ( 'NONE',  ( 775.9200461376533440, 0.1944037101305369775, 315.3028492785443291 ) ) ;
#30973=CARTESIAN_POINT ( 'NONE',  ( 782.4968714119720516, -250.8164208402379245, 305.0891759886411023 ) ) ;
#30974=CARTESIAN_POINT ( 'NONE',  ( 773.4516893846965786, -331.6454272087888171, 315.8398074228977066 ) ) ;
#30975=CARTESIAN_POINT ( 'NONE',  ( 775.9200461376533440, -431.8055962898681059, 315.3028492785443291 ) ) ;
#30979=ORIENTED_EDGE ( 'NONE', *, *, #29481, .T. ) ;
#30981=CARTESIAN_POINT ( 'NONE',  ( 802.7791456095903868, -316.7146871989593819, 329.0155153010375102 ) ) ;
#30982=LINE ( 'NONE', #45079, #30753 ) ;
#30984=CARTESIAN_POINT ( 'NONE',  ( 755.1538015810308480, -134.1908817542439181, 343.0433043558613804 ) ) ;
#30985=CARTESIAN_POINT ( 'NONE',  ( 800.2193346964447755, 5.001760977943074948, 355.1360043628815788 ) ) ;
#30988=CARTESIAN_POINT ( 'NONE',  ( 799.9636004259356241, -238.9181544815163534, 311.2241431872006956 ) ) ;
#30990=CARTESIAN_POINT ( 'NONE',  ( 799.9999999999993179, -462.9681489794448339, 309.9999999999998863 ) ) ;
#30992=CARTESIAN_POINT ( 'NONE',  ( 792.3570229623688874, -45.18005720387493085, 373.1304606946836202 ) ) ;
#30993=CARTESIAN_POINT ( 'NONE',  ( 806.2451613922657998, -452.9681489794450613, 344.7413990863497020 ) ) ;
#30996=CARTESIAN_POINT ( 'NONE',  ( 804.1009440267234822, -311.4636090269706870, 314.0944755984392600 ) ) ;
#30998=CARTESIAN_POINT ( 'NONE',  ( 779.9999999999992042, 126.4563064324884465, 339.9999999999999432 ) ) ;
#30999=CARTESIAN_POINT ( 'NONE',  ( 763.2262854647970016, -296.6346026584195670, 309.2812353651462445 ) ) ;
#31003=CARTESIAN_POINT ( 'NONE',  ( 785.3687786644884454, -395.3618753856918602, 315.3201227861279676 ) ) ;
#31004=CARTESIAN_POINT ( 'NONE',  ( 755.8894580844503253, -159.8272453906075157, 332.3691319403863531 ) ) ;
#31007=CARTESIAN_POINT ( 'NONE',  ( 815.1787889125755555, -54.89650538077837183, 343.7953271457877804 ) ) ;
#31008=CARTESIAN_POINT ( 'NONE',  ( 771.2633955100217236, -359.9073299311467053, 363.4237431249939618 ) ) ;
#31009=CARTESIAN_POINT ( 'NONE',  ( 779.9999999999992042, -462.9681489794448339, 339.9999999999999432 ) ) ;
#31011=CARTESIAN_POINT ( 'NONE',  ( 754.8072714833581358, -436.8164208402372992, 338.1981804954720587 ) ) ;
#31015=CARTESIAN_POINT ( 'NONE',  ( 785.3141322388236176, -189.7255117493290300, 364.4286716492789537 ) ) ;
#31016=CARTESIAN_POINT ( 'NONE',  ( 788.7366044899766848, -203.9073299311471885, 316.5762568750059813 ) ) ;
#31021=CARTESIAN_POINT ( 'NONE',  ( 804.4286716492782716, -401.3618753856920307, 345.3141322388244703 ) ) ;
#31024=CARTESIAN_POINT ( 'NONE',  ( 787.5162901302840055, -131.3618753856928549, 305.4481719005793252 ) ) ;
#31029=CARTESIAN_POINT ( 'NONE',  ( 799.4546378042377910, -201.0783235625961254, 356.1575198192848006 ) ) ;
#31031=CARTESIAN_POINT ( 'NONE',  ( 779.9999999999992042, -452.9681489794448339, 370.0000000000000568 ) ) ;
#31035=FACE_OUTER_BOUND ( 'NONE', #39961, .T. ) ;
#31037=CARTESIAN_POINT ( 'NONE',  ( 783.7953271457878373, -128.1908817542439465, 375.1787889125761239 ) ) ;
#31045=CARTESIAN_POINT ( 'NONE',  ( 755.3028492785439312, -423.2817908451521589, 335.9200461376539693 ) ) ;
#31049=DIRECTION ( 'NONE',  ( -0.000000000000000000, 1.000000000000000000, -0.000000000000000000 ) ) ;
#31050=CARTESIAN_POINT ( 'NONE',  ( 792.1044303154645831, 11.54721552339760038, 317.8323909638837677 ) ) ;
#31052=CARTESIAN_POINT ( 'NONE',  ( 749.5768839229115201, -228.5545181178799794, 358.0661480581553064 ) ) ;
#31054=CARTESIAN_POINT ( 'NONE',  ( 796.9462024416508257, -204.4527844766016926, 308.9653473494370246 ) ) ;
#31057=CARTESIAN_POINT ( 'NONE',  ( 804.6798772138708955, -303.7255117493287457, 334.6312213355107019 ) ) ;
#31059=CARTESIAN_POINT ( 'NONE',  ( 760.7433823573367135, -60.00906357242598688, 355.9930595647440441 ) ) ;
#31063=CARTESIAN_POINT ( 'NONE',  ( 779.4709603349208464, -120.3510508353236048, 314.7162404726379918 ) ) ;
#31064=CARTESIAN_POINT ( 'NONE',  ( 758.0580252608178853, -342.4527844766013231, 328.0187753319985404 ) ) ;
#31067=CARTESIAN_POINT ( 'NONE',  ( 755.5713283507202505, -101.3618753856929544, 334.6858677611754729 ) ) ;
#31070=CARTESIAN_POINT ( 'NONE',  ( 795.6651683502461765, -370.7146871989592114, 371.3240766477733814 ) ) ;
#31072=CARTESIAN_POINT ( 'NONE',  ( 759.9864689768902508, -290.0891481129650629, 354.9819416627836404 ) ) ;
#31075=CARTESIAN_POINT ( 'NONE',  ( 785.3687786644884454, -395.3618753856918602, 315.3201227861279676 ) ) ;
#31082=CARTESIAN_POINT ( 'NONE',  ( 804.9363028652555840, -112.2709662947838325, 338.2165204200192079 ) ) ;
#31083=CARTESIAN_POINT ( 'NONE',  ( 787.5531968255692163, -453.8272453906066630, 316.1348686366205811 ) ) ;
#31084=CARTESIAN_POINT ( 'NONE',  ( 769.1273215169530886, -94.71468719896007826, 317.4527132478988847 ) ) ;
#31085=CARTESIAN_POINT ( 'NONE',  ( 799.9999999999993179, -512.9681489794448908, 350.0000000000000000 ) ) ;
#31087=CARTESIAN_POINT ( 'NONE',  ( 791.1614460488616487, -371.2601417444136587, 373.5763878283158874 ) ) ;
#31091=CARTESIAN_POINT ( 'NONE',  ( 812.3518521366052028, -1.099972663335260226, 326.5853460496235243 ) ) ;
#31098=CARTESIAN_POINT ( 'NONE',  ( 799.2566176426618085, -336.0090635724251911, 324.0069404352559559 ) ) ;
#31099=CARTESIAN_POINT ( 'NONE',  ( 783.7953271457878373, -296.1908817542434917, 375.1787889125761239 ) ) ;
#31102=CARTESIAN_POINT ( 'NONE',  ( 754.3581564841646241, -113.4636090269712554, 316.1443688327762516 ) ) ;
#31107=CARTESIAN_POINT ( 'NONE',  ( 754.8072714833581358, -196.8164208402380950, 338.1981804954720587 ) ) ;
#31111=CARTESIAN_POINT ( 'NONE',  ( 793.5525998758768083, -439.0999726633339719, 372.6845335610516941 ) ) ;
#31114=CARTESIAN_POINT ( 'NONE',  ( 755.5913626894240451, -61.64542720878961291, 346.6156483768012890 ) ) ;
#31117=CARTESIAN_POINT ( 'NONE',  ( 802.7791456095903868, -436.7146871989589272, 329.0155153010375102 ) ) ;
#31119=CARTESIAN_POINT ( 'NONE',  ( 756.5762568750052424, -267.1800572038742985, 348.7366044899774238 ) ) ;
#31122=CARTESIAN_POINT ( 'NONE',  ( 793.4146539503750546, -265.9874144716867477, 307.6481478633938877 ) ) ;
#31123=CARTESIAN_POINT ( 'NONE',  ( 785.3141322388236176, -117.7255117493292715, 364.4286716492789537 ) ) ;
#31125=CARTESIAN_POINT ( 'NONE',  ( 759.9864689768902508, -266.0891481129651197, 354.9819416627836404 ) ) ;
#31127=CARTESIAN_POINT ( 'NONE',  ( 789.6004645510835189, -449.9487230857661757, 364.2073161732290600 ) ) ;
#31132=CARTESIAN_POINT ( 'NONE',  ( 788.8264449731200330, -21.18005720387502677, 363.6646147819171233 ) ) ;
#31134=CARTESIAN_POINT ( 'NONE',  ( 805.0032342141413437, -373.5436935675102177, 314.9967657858572352 ) ) ;
#31135=CARTESIAN_POINT ( 'NONE',  ( 781.2497674668890113, -252.3510508353232353, 375.3608509340180603 ) ) ;
#31141=CARTESIAN_POINT ( 'NONE',  ( 774.6312213355099630, -239.3618753856924570, 364.6798772138717482 ) ) ;
#31143=CARTESIAN_POINT ( 'NONE',  ( 746.8695393053150156, -365.9073299311465917, 327.6429770376306010 ) ) ;
#31146=DIRECTION ( 'NONE',  ( 0.000000000000000000, 1.000000000000000000, 0.000000000000000000 ) ) ;
#31149=CARTESIAN_POINT ( 'NONE',  ( 754.7162404726377645, -230.7363362996981664, 339.4709603349214717 ) ) ;
#31150=CARTESIAN_POINT ( 'NONE',  ( 758.0580252608178853, -102.4527844766020337, 328.0187753319985404 ) ) ;
#31154=CARTESIAN_POINT ( 'NONE',  ( 755.8398074228967971, -283.4419599262321867, 333.4516893846970333 ) ) ;
#31157=CARTESIAN_POINT ( 'NONE',  ( 773.7305795820266212, -9.281790845153418346, 374.8230680027170365 ) ) ;
#31161=CARTESIAN_POINT ( 'NONE',  ( 745.7998596910086917, -173.3618753856927128, 332.5602148656461168 ) ) ;
#31162=CARTESIAN_POINT ( 'NONE',  ( 771.1735550268778070, -81.18005720387481006, 316.3353852180827630 ) ) ;
#31165=DIRECTION ( 'NONE',  ( -0.3826814224632300032, 0.000000000000000000, -0.9238803650373347276 ) ) ;
#31167=CARTESIAN_POINT ( 'NONE',  ( 807.2620300519052989, -432.0090635724247932, 318.0141637701419768 ) ) ;
#31170=CARTESIAN_POINT ( 'NONE',  ( 749.2812353651451076, -414.4527844766010389, 323.2262854647983090 ) ) ;
#31171=CARTESIAN_POINT ( 'NONE',  ( 759.0252816721024374, -0.9982390220569063999, 368.0189434323527280 ) ) ;
#31174=CARTESIAN_POINT ( 'NONE',  ( 799.4546378042377910, -9.078323562596708030, 356.1575198192848006 ) ) ;
#31179=CARTESIAN_POINT ( 'NONE',  ( 745.1769319972822814, -185.8055962898689302, 346.2694204179732083 ) ) ;
#31180=CARTESIAN_POINT ( 'NONE',  ( 803.6646147819162707, -17.90732993114776406, 348.8264449731211130 ) ) ;
#31186=CARTESIAN_POINT ( 'NONE',  ( 781.7834795799800531, -178.8164208402381519, 315.0636971347436202 ) ) ;
#31188=CARTESIAN_POINT ( 'NONE',  ( 768.0187753319979720, -296.6346026584195670, 318.0580252608186242 ) ) ;
#31190=ORIENTED_EDGE ( 'NONE', *, *, #40721, .T. ) ;
#31191=CARTESIAN_POINT ( 'NONE',  ( 804.9511171171677688, -29.80559628986937781, 335.8780910478229202 ) ) ;
#31193=CARTESIAN_POINT ( 'NONE',  ( 744.7301800767020268, -244.8164208402379245, 337.4774526936615189 ) ) ;
#31194=CARTESIAN_POINT ( 'NONE',  ( 801.5560724626406000, -336.5545181178796952, 326.7756240680316182 ) ) ;
#31195=CARTESIAN_POINT ( 'NONE',  ( 759.8311093483677041, 25.83076734649409545, 310.9282345327691814 ) ) ;
#31202=EDGE_CURVE ( 'NONE', #24474, #37455, #15179, .T. ) ;
#31203=CARTESIAN_POINT ( 'NONE',  ( 761.2382568024794409, -327.6237781080502600, 356.9571628226838129 ) ) ;
#31206=CARTESIAN_POINT ( 'NONE',  ( 769.9779781133707957, -139.0999726633348530, 316.7813123517150871 ) ) ;
#31207=CARTESIAN_POINT ( 'NONE',  ( 755.5713283507202505, -5.361875385693257279, 334.6858677611754729 ) ) ;
#31210=DIRECTION ( 'NONE',  ( -0.000000000000000000, -1.110223024625155554E-15, 1.000000000000000000 ) ) ;
#31211=CARTESIAN_POINT ( 'NONE',  ( 760.0363995740630116, -226.9181544815163534, 368.7758568127991907 ) ) ;
#31212=CARTESIAN_POINT ( 'NONE',  ( 769.1273215169530886, -190.7146871989597798, 317.4527132478988847 ) ) ;
#31214=LINE ( 'NONE', #30990, #25927 ) ;
#31217=CARTESIAN_POINT ( 'NONE',  ( 746.8695393053150156, -77.90732993114757221, 327.6429770376306010 ) ) ;
#31221=CARTESIAN_POINT ( 'NONE',  ( 750.9282345327678740, -352.9181544815159555, 319.8311093483690115 ) ) ;
#31223=CARTESIAN_POINT ( 'NONE',  ( 772.4837098697144029, -287.3618753856923718, 374.5518280994205611 ) ) ;
#31227=CARTESIAN_POINT ( 'NONE',  ( 765.0180583372156207, -408.9982390220556567, 360.0135310231089534 ) ) ;
#31228=AXIS2_PLACEMENT_3D ( 'NONE', #19804, #5474, #9413 ) ;
#31229=CARTESIAN_POINT ( 'NONE',  ( 755.5913626894240451, -157.6454272087893287, 346.6156483768012890 ) ) ;
#31232=CARTESIAN_POINT ( 'NONE',  ( 813.2346286133761168, -53.26014174441475291, 328.9521613784389160 ) ) ;
#31233=CARTESIAN_POINT ( 'NONE',  ( 778.2165204200184689, -382.8164208402374697, 364.9363028652563230 ) ) ;
#31235=CARTESIAN_POINT ( 'NONE',  ( 777.4774526936600978, 13.72903370521577315, 304.7301800767028226 ) ) ;
#31237=CARTESIAN_POINT ( 'NONE',  ( 778.2165204200184689, -430.8164208402374129, 364.9363028652563230 ) ) ;
#31241=CARTESIAN_POINT ( 'NONE',  ( 788.8264449731200330, -189.1800572038744122, 363.6646147819171233 ) ) ;
#31242=CARTESIAN_POINT ( 'NONE',  ( 758.0580252608178853, -198.4527844766017495, 328.0187753319985404 ) ) ;
#31247=CARTESIAN_POINT ( 'NONE',  ( 797.6776695296629214, -379.5436935675102745, 357.6776695296636603 ) ) ;
#31252=CARTESIAN_POINT ( 'NONE',  ( 798.0661480581538854, -194.5328690171415644, 309.5768839229118043 ) ) ;
#31257=EDGE_CURVE ( 'NONE', #19781, #26699, #7506, .T. ) ;
#31258=CARTESIAN_POINT ( 'NONE',  ( 783.0433043558608688, -216.8965053807778816, 315.1538015810313027 ) ) ;
#31267=CARTESIAN_POINT ( 'NONE',  ( 809.0717654672305343, -124.9181544815167086, 360.1688906516309885 ) ) ;
#31274=CARTESIAN_POINT ( 'NONE',  ( 809.0717654672305343, -388.9181544815158986, 360.1688906516309885 ) ) ;
#31281=CARTESIAN_POINT ( 'NONE',  ( 807.2620300519052989, -240.0090635724253900, 318.0141637701419768 ) ) ;
#31283=CARTESIAN_POINT ( 'NONE',  ( 745.7998596910086917, -197.3618753856926560, 332.5602148656461168 ) ) ;
#31286=CARTESIAN_POINT ( 'NONE',  ( 797.6776695296629214, -283.5436935675105019, 357.6776695296636603 ) ) ;
#31287=CARTESIAN_POINT ( 'NONE',  ( 775.8780910478218402, -57.28179084515326736, 364.9511171171680530 ) ) ;
#31291=CARTESIAN_POINT ( 'NONE',  ( 789.9200121543843807, -121.9874144716872593, 317.0176451133914384 ) ) ;
#31292=CARTESIAN_POINT ( 'NONE',  ( 800.0135310231082713, -326.0891481129649492, 325.0180583372163028 ) ) ;
#31295=CARTESIAN_POINT ( 'NONE',  ( 794.9819416627830151, -84.99823902205663728, 319.9864689768909898 ) ) ;
#31298=CARTESIAN_POINT ( 'NONE',  ( 758.0141637701419768, -399.0783235625955285, 367.2620300519063790 ) ) ;
#31300=CARTESIAN_POINT ( 'NONE',  ( 781.7834795799800531, -298.8164208402377540, 315.0636971347436202 ) ) ;
#31304=CARTESIAN_POINT ( 'NONE',  ( 785.3687786644884454, -419.3618753856918033, 315.3201227861279676 ) ) ;
#31311=CARTESIAN_POINT ( 'NONE',  ( 756.3353852180819104, -125.9073299311474159, 331.1735550268788302 ) ) ;
#31312=CARTESIAN_POINT ( 'NONE',  ( 796.9571628226829034, -431.4636090269702322, 321.2382568024804641 ) ) ;
#31313=CARTESIAN_POINT ( 'NONE',  ( 794.1144889064781864, -106.1692326535054889, 360.9840315886528401 ) ) ;
#31315=CARTESIAN_POINT ( 'NONE',  ( 799.9999999999993179, -462.9681489794448339, 309.9999999999998863 ) ) ;
#31316=CARTESIAN_POINT ( 'NONE',  ( 813.9316612368132837, -343.4419599262320162, 348.6739635108323228 ) ) ;
#31318=EDGE_LOOP ( 'NONE', ( #40677, #8277, #23398, #12441 ) ) ;
#31322=CARTESIAN_POINT ( 'NONE',  ( 812.3518521366052028, -49.09997266333511590, 326.5853460496235243 ) ) ;
#31330=CARTESIAN_POINT ( 'NONE',  ( 763.8424801807145741, -354.0090635724250774, 320.5453621957614700 ) ) ;
#31331=CARTESIAN_POINT ( 'NONE',  ( 744.6391490659812007, -350.7363362996978253, 338.7502325331110455 ) ) ;
#31336=CARTESIAN_POINT ( 'NONE',  ( 799.9636004259356241, -118.9181544815167229, 311.2241431872006956 ) ) ;
#31340=CARTESIAN_POINT ( 'NONE',  ( 755.5713283507202505, -173.3618753856927128, 334.6858677611754729 ) ) ;
#31342=CARTESIAN_POINT ( 'NONE',  ( 773.7305795820266212, -441.2817908451521021, 374.8230680027170365 ) ) ;
#31348=CARTESIAN_POINT ( 'NONE',  ( 793.4146539503750546, -1.987414471687640294, 307.6481478633938877 ) ) ;
#31354=CARTESIAN_POINT ( 'NONE',  ( 810.1134526219336749, -296.5328690171411949, 357.8822607201570349 ) ) ;
#31355=CARTESIAN_POINT ( 'NONE',  ( 756.3353852180820240, -125.9073299311474159, 331.1735550268787733 ) ) ;
#31357=CARTESIAN_POINT ( 'NONE',  ( 805.1927285166397041, -304.8164208402376403, 341.8018195045277707 ) ) ;
#31366=CARTESIAN_POINT ( 'NONE',  ( 804.4286716492782716, -17.36187538569322086, 345.3141322388244703 ) ) ;
#31368=CARTESIAN_POINT ( 'NONE',  ( 767.6429770376291799, -345.1800572038739574, 306.8695393053162093 ) ) ;
#31369=CARTESIAN_POINT ( 'NONE',  ( 808.7758568127978833, -268.1692326535049347, 320.0363995740631822 ) ) ;
#31375=CARTESIAN_POINT ( 'NONE',  ( 801.9419747391806368, -234.4527844766016358, 351.9812246680014027 ) ) ;
#31377=CARTESIAN_POINT ( 'NONE',  ( 763.2262854647970016, -392.6346026584193396, 309.2812353651462445 ) ) ;
#31384=CARTESIAN_POINT ( 'NONE',  ( 783.0745993439762742, -224.1908817542436623, 365.1016975059196739 ) ) ;
#31385=CARTESIAN_POINT ( 'NONE',  ( 802.1676090361156639, -134.6346026584201070, 327.8955696845344505 ) ) ;
#31386=VERTEX_POINT ( 'NONE', #108 ) ;
#31389=CARTESIAN_POINT ( 'NONE',  ( 764.0069404352550464, -303.0783235625957559, 359.2566176426627180 ) ) ;
#31391=CARTESIAN_POINT ( 'NONE',  ( 766.4474001241216001, -19.09997266333520116, 307.3154664389482491 ) ) ;
#31394=CARTESIAN_POINT ( 'NONE',  ( 814.9108240113580450, -184.2709662947835909, 337.5031285880265273 ) ) ;
#31395=CARTESIAN_POINT ( 'NONE',  ( 778.2165204200184689, -94.81642084023843609, 364.9363028652563230 ) ) ;
#31401=CARTESIAN_POINT ( 'NONE',  ( 776.2046728542105711, -428.1908817542430938, 304.8212110874238761 ) ) ;
#31404=CARTESIAN_POINT ( 'NONE',  ( 757.2208543904082489, -352.7146871989593251, 350.9844846989624330 ) ) ;
#31405=CARTESIAN_POINT ( 'NONE',  ( 748.9653473494365699, -50.63460265842038410, 356.9462024416520762 ) ) ;
#31407=CARTESIAN_POINT ( 'NONE',  ( 758.6633372737375112, -20.53286901714212931, 326.9102291470432533 ) ) ;
#31410=CARTESIAN_POINT ( 'NONE',  ( 795.6651683502461765, -178.7146871989598083, 371.3240766477733814 ) ) ;
#31414=CARTESIAN_POINT ( 'NONE',  ( 781.7834795799800531, -202.8164208402380950, 315.0636971347436202 ) ) ;
#31418=CARTESIAN_POINT ( 'NONE',  ( 797.6776695296629214, -331.5436935675104451, 357.6776695296636603 ) ) ;
#31420=EDGE_LOOP ( 'NONE', ( #2604, #1027, #32044, #24649, #8655, #9028 ) ) ;
#31421=CARTESIAN_POINT ( 'NONE',  ( 763.2154366446407039, -45.62377810805114109, 321.4292242960311228 ) ) ;
#31424=CARTESIAN_POINT ( 'NONE',  ( 745.4481719005789273, -267.7255117493287457, 347.5162901302853697 ) ) ;
#31425=CARTESIAN_POINT ( 'NONE',  ( 787.5531968255692163, -333.8272453906070041, 316.1348686366205811 ) ) ;
#31426=CARTESIAN_POINT ( 'NONE',  ( 756.1443688327750579, 26.37622189194863509, 314.3581564841659315 ) ) ;
#31431=AXIS2_PLACEMENT_3D ( 'NONE', #45129, #2627, #6550 ) ;
#31432=CARTESIAN_POINT ( 'NONE',  ( 758.8095938919642549, -272.0891481129651197, 311.6929314249763365 ) ) ;
#31433=CARTESIAN_POINT ( 'NONE',  ( 770.0799878456142551, -325.9874144716865771, 362.9823548866085616 ) ) ;
#31436=CARTESIAN_POINT ( 'NONE',  ( 757.4527132478984868, -112.3726999360621761, 329.1273215169538844 ) ) ;
#31437=CARTESIAN_POINT ( 'NONE',  ( 774.6858677611749044, -9.725511749329603717, 315.5713283507209894 ) ) ;
#31442=CARTESIAN_POINT ( 'NONE',  ( 810.4231160770870019, -240.5545181178798941, 321.9338519418446936 ) ) ;
#31443=CARTESIAN_POINT ( 'NONE',  ( 803.8651313633788504, -173.2601417444143692, 332.4468031744301015 ) ) ;
#31449=CARTESIAN_POINT ( 'NONE',  ( 772.4837098697144029, -23.36187538569318889, 374.5518280994205611 ) ) ;
#31451=CARTESIAN_POINT ( 'NONE',  ( 796.7737145352015204, -68.63460265842033436, 370.7187646348536987 ) ) ;
#31455=CARTESIAN_POINT ( 'NONE',  ( 793.5525998758768083, -343.0999726633342561, 372.6845335610516941 ) ) ;
#31457=CARTESIAN_POINT ( 'NONE',  ( 754.9967657858570647, -289.5436935675103882, 365.0032342141425374 ) ) ;
#31461=CARTESIAN_POINT ( 'NONE',  ( 756.5762568750052424, -411.1800572038738437, 348.7366044899774238 ) ) ;
#31462=CARTESIAN_POINT ( 'NONE',  ( 772.4468031744293057, -153.8272453906075157, 363.8651313633793620 ) ) ;
#31464=CARTESIAN_POINT ( 'NONE',  ( 795.6651683502461765, -82.71468719896012090, 371.3240766477733814 ) ) ;
#31465=CARTESIAN_POINT ( 'NONE',  ( 785.3687786644885591, -395.3618753856919739, 315.3201227861280813 ) ) ;
#31467=CARTESIAN_POINT ( 'NONE',  ( 808.0189434323515343, 9.910851887033969021, 319.0252816721025511 ) ) ;
#31470=CARTESIAN_POINT ( 'NONE',  ( 771.1735550268778070, -417.1800572038736163, 316.3353852180827630 ) ) ;
#31474=ADVANCED_FACE ( 'NONE', ( #1909 ), #29430, .F. ) ;
#31476=CARTESIAN_POINT ( 'NONE',  ( 757.8323909638827445, -242.6346026584197659, 352.1044303154654358 ) ) ;
#31477=CARTESIAN_POINT ( 'NONE',  ( 759.7806653035535192, -222.9982390220561683, 324.8639956371181370 ) ) ;
#31479=CARTESIAN_POINT ( 'NONE',  ( 759.9999999999992042, -462.9681489794448339, 362.3606797749978909 ) ) ;
#31481=CARTESIAN_POINT ( 'NONE',  ( 774.6858677611749044, -393.7255117493283478, 315.5713283507209894 ) ) ;
#31483=ORIENTED_EDGE ( 'NONE', *, *, #35606, .T. ) ;
#31487=CARTESIAN_POINT ( 'NONE',  ( 812.7932403749906598, -135.1800572038746679, 327.7687537140311633 ) ) ;
#31493=CARTESIAN_POINT ( 'NONE',  ( 804.1601925771018387, -223.4419599262323857, 346.5483106153029098 ) ) ;
#31502=CARTESIAN_POINT ( 'NONE',  ( 795.8262568251477660, -142.3726999360620766, 308.3538107759623585 ) ) ;
#31508=DIRECTION ( 'NONE',  ( -0.000000000000000000, 1.000000000000000000, -0.000000000000000000 ) ) ;
#31511=CARTESIAN_POINT ( 'NONE',  ( 804.1009440267234822, -383.4636090269704596, 314.0944755984392600 ) ) ;
#31515=CARTESIAN_POINT ( 'NONE',  ( 779.9999999999992042, -462.9681489794448339, 339.9999999999999432 ) ) ;
#31516=CARTESIAN_POINT ( 'NONE',  ( 804.9363028652555840, 7.729033705215793582, 338.2165204200192079 ) ) ;
#31519=CARTESIAN_POINT ( 'NONE',  ( 754.3581564841646241, -257.4636090269708575, 316.1443688327762516 ) ) ;
#31521=CARTESIAN_POINT ( 'NONE',  ( 751.9810565676468741, -194.0891481129654039, 360.9747183278973921 ) ) ;
#31525=CARTESIAN_POINT ( 'NONE',  ( 756.3353852180819104, -293.9073299311468759, 331.1735550268788302 ) ) ;
#31526=CARTESIAN_POINT ( 'NONE',  ( 763.8424801807145741, -90.00906357242590161, 320.5453621957614700 ) ) ;
#31532=CARTESIAN_POINT ( 'NONE',  ( 790.8726784830453198, -130.7146871989599504, 362.5472867521010585 ) ) ;
#31533=CARTESIAN_POINT ( 'NONE',  ( 781.8018195045266339, -310.2709662947832499, 365.1927285166406705 ) ) ;
#31537=CARTESIAN_POINT ( 'NONE',  ( 771.1735550268778070, -81.18005720387481006, 316.3353852180827630 ) ) ;
#31540=CARTESIAN_POINT ( 'NONE',  ( 748.3538107759620743, -400.7146871989590977, 355.8262568251490165 ) ) ;
#31542=CARTESIAN_POINT ( 'NONE',  ( 795.1360043628807261, -284.0891481129650629, 360.2193346964456282 ) ) ;
#31545=CARTESIAN_POINT ( 'NONE',  ( 803.6646147819161570, -401.9073299311463643, 348.8264449731210561 ) ) ;
#31546=EDGE_CURVE ( 'NONE', #8526, #20178, #10749, .T. ) ;
#31552=CARTESIAN_POINT ( 'NONE',  ( 797.8594530101008786, -133.5436935675110135, 322.1405469898980982 ) ) ;
#31553=CARTESIAN_POINT ( 'NONE',  ( 793.0897708529556667, -438.5545181178793541, 361.3366627262616362 ) ) ;
#31554=CARTESIAN_POINT ( 'NONE',  ( 756.1348686366196716, -137.2601417444144829, 347.5531968255698416 ) ) ;
#31556=FACE_OUTER_BOUND ( 'NONE', #29211, .T. ) ;
#31557=CARTESIAN_POINT ( 'NONE',  ( 747.3154664389472828, -379.9874144716865203, 326.4474001241230781 ) ) ;
#31562=CARTESIAN_POINT ( 'NONE',  ( 746.4236121716829757, -39.82724539060786384, 328.8385539511384650 ) ) ;
#31570=CARTESIAN_POINT ( 'NONE',  ( 763.8424801807145741, -378.0090635724250774, 320.5453621957614700 ) ) ;
#31571=CARTESIAN_POINT ( 'NONE',  ( 771.3260364891663130, -331.6454272087888171, 306.0683387631859773 ) ) ;
#31574=CARTESIAN_POINT ( 'NONE',  ( 749.5768839229115201, -132.5545181178802920, 358.0661480581553064 ) ) ;
#31578=CARTESIAN_POINT ( 'NONE',  ( 774.6312213355099630, -191.3618753856925991, 364.6798772138717482 ) ) ;
#31580=CARTESIAN_POINT ( 'NONE',  ( 793.5525998758768083, -415.0999726633340288, 372.6845335610516941 ) ) ;
#31586=CARTESIAN_POINT ( 'NONE',  ( 752.4576283171824116, 2.921676437403253779, 317.7880784355627952 ) ) ;
#31587=ORIENTED_EDGE ( 'NONE', *, *, #10295, .F. ) ;
#31590=CARTESIAN_POINT ( 'NONE',  ( 813.9316612368132837, -319.4419599262320730, 348.6739635108323228 ) ) ;
#31591=CARTESIAN_POINT ( 'NONE',  ( 804.4286716492782716, -113.3618753856929260, 345.3141322388244703 ) ) ;
#31593=CARTESIAN_POINT ( 'NONE',  ( 774.6312213355099630, -287.3618753856923718, 364.6798772138717482 ) ) ;
#31595=CARTESIAN_POINT ( 'NONE',  ( 789.5584187865343893, -452.9681489794450613, 363.1011989789364520 ) ) ;
#31598=ORIENTED_EDGE ( 'NONE', *, *, #30859, .T. ) ;
#31599=CARTESIAN_POINT ( 'NONE',  ( 804.9363028652555840, -16.27096629478413092, 338.2165204200192079 ) ) ;
#31601=CARTESIAN_POINT ( 'NONE',  ( 745.4481719005789273, -363.7255117493284615, 347.5162901302853697 ) ) ;
#31602=CARTESIAN_POINT ( 'NONE',  ( 758.0141637701419768, -255.0783235625958980, 367.2620300519063790 ) ) ;
#31603=CARTESIAN_POINT ( 'NONE',  ( 800.1688906516307043, -82.16923265350558836, 369.0717654672308186 ) ) ;
#31608=CARTESIAN_POINT ( 'NONE',  ( 800.0135310231082713, -254.0891481129652334, 325.0180583372163028 ) ) ;
#31610=CARTESIAN_POINT ( 'NONE',  ( 754.9967657858570647, -385.5436935675102745, 365.0032342141425374 ) ) ;
#31613=CARTESIAN_POINT ( 'NONE',  ( 779.9999999999992042, 16.45630643248849267, 339.9999999999999432 ) ) ;
#31614=CARTESIAN_POINT ( 'NONE',  ( 799.9999999999993179, 205.0000000000000568, 339.9999999999999432 ) ) ;
#31615=CARTESIAN_POINT ( 'NONE',  ( 798.5707757039680246, -245.4636090269709143, 356.7845633553585003 ) ) ;
#31616=CARTESIAN_POINT ( 'NONE',  ( 795.1360043628807261, -116.0891481129656029, 360.2193346964456282 ) ) ;
#31620=CARTESIAN_POINT ( 'NONE',  ( 796.7845633553578182, -297.6237781080502600, 358.5707757039688204 ) ) ;
#31622=CARTESIAN_POINT ( 'NONE',  ( 814.2805881961230625, -49.64542720878965554, 331.2368401574024119 ) ) ;
#31624=CARTESIAN_POINT ( 'NONE',  ( 759.9864689768902508, -74.08914811296577341, 354.9819416627836404 ) ) ;
#31627=CARTESIAN_POINT ( 'NONE',  ( 784.1219089521767955, 2.718209154846545683, 315.0488828828318333 ) ) ;
#31630=CARTESIAN_POINT ( 'NONE',  ( 775.9200461376533440, -359.8055962898683333, 315.3028492785443291 ) ) ;
#31631=CARTESIAN_POINT ( 'NONE',  ( 800.9747183278959710, -36.99823902205679360, 311.9810565676471583 ) ) ;
#31633=CARTESIAN_POINT ( 'NONE',  ( 763.2154366446407039, -45.62377810805114109, 321.4292242960311228 ) ) ;
#31636=CARTESIAN_POINT ( 'NONE',  ( 801.9858362298568863, -195.0783235625961538, 312.7379699480935642 ) ) ;
#31637=CARTESIAN_POINT ( 'NONE',  ( 804.6798772138710092, -15.72551174932958951, 334.6312213355106451 ) ) ;
#31640=CARTESIAN_POINT ( 'NONE',  ( 803.6646147819161570, -209.9073299311470748, 348.8264449731210561 ) ) ;
#31642=CARTESIAN_POINT ( 'NONE',  ( 771.2633955100217236, -311.9073299311468759, 363.4237431249939618 ) ) ;
#31645=CARTESIAN_POINT ( 'NONE',  ( 803.2186876482843445, -55.98741447168748664, 350.0220218866286928 ) ) ;
#31647=CARTESIAN_POINT ( 'NONE',  ( 808.0189434323515343, -254.0891481129652334, 319.0252816721025511 ) ) ;
#31648=CARTESIAN_POINT ( 'NONE',  ( 744.8212110874229666, 5.103494619221427442, 336.2046728542121627 ) ) ;
#31654=CARTESIAN_POINT ( 'NONE',  ( 810.7187646348534145, -306.4527844766013800, 356.7737145352016341 ) ) ;
#31656=CARTESIAN_POINT ( 'NONE',  ( 789.9200121543843807, -337.9874144716865771, 317.0176451133914384 ) ) ;
#31658=CARTESIAN_POINT ( 'NONE',  ( 790.0220218866281812, -151.0999726633347677, 363.2186876482849129 ) ) ;
#31659=CARTESIAN_POINT ( 'NONE',  ( 804.9363028652555840, -16.27096629478413092, 338.2165204200192079 ) ) ;
#31663=CARTESIAN_POINT ( 'NONE',  ( 752.7379699480933368, -252.0090635724254184, 361.9858362298580232 ) ) ;
#31664=CARTESIAN_POINT ( 'NONE',  ( 784.0799538623451781, -179.8055962898688733, 364.6971507214555572 ) ) ;
#31668=CARTESIAN_POINT ( 'NONE',  ( 811.0346526505616112, -14.63460265842049424, 323.0537975583477532 ) ) ;
#31669=CARTESIAN_POINT ( 'NONE',  ( 809.6099558218720631, -452.9681489794449476, 335.1781210895659342 ) ) ;
#31672=CARTESIAN_POINT ( 'NONE',  ( 814.4686193811664907, -363.2817908451523294, 346.2056067578752732 ) ) ;
#31674=CARTESIAN_POINT ( 'NONE',  ( 812.7932403749906598, -327.1800572038741279, 327.7687537140311633 ) ) ;
#31679=CARTESIAN_POINT ( 'NONE',  ( 765.0180583372156207, -384.9982390220556567, 360.0135310231089534 ) ) ;
#31680=CARTESIAN_POINT ( 'NONE',  ( 804.4086373105744769, -145.6454272087893287, 333.3843516231986541 ) ) ;
#31683=CARTESIAN_POINT ( 'NONE',  ( 754.0944755984390895, -87.62377810805102740, 364.1009440267246760 ) ) ;
#31684=CARTESIAN_POINT ( 'NONE',  ( 781.7834795799800531, -394.8164208402374697, 315.0636971347436202 ) ) ;
#31685=CARTESIAN_POINT ( 'NONE',  ( 808.3070685750232087, 5.001760977943074948, 361.1904061080339829 ) ) ;
#31692=CARTESIAN_POINT ( 'NONE',  ( 788.8264449731200330, -237.1800572038742985, 363.6646147819171233 ) ) ;
#31693=CARTESIAN_POINT ( 'NONE',  ( 768.0187753319979720, -224.6346026584198228, 318.0580252608186242 ) ) ;
#31695=CARTESIAN_POINT ( 'NONE',  ( 777.5031285880264704, 1.183579159761269040, 374.9108240113588408 ) ) ;
#31698=CARTESIAN_POINT ( 'NONE',  ( 792.1044303154645831, -444.4527844766009821, 317.8323909638837677 ) ) ;
#31701=CARTESIAN_POINT ( 'NONE',  ( 792.3570229623691148, -141.1800572038746395, 373.1304606946836770 ) ) ;
#31703=CARTESIAN_POINT ( 'NONE',  ( 747.3154664389472828, -187.9874144716870603, 326.4474001241230781 ) ) ;
#31708=CARTESIAN_POINT ( 'NONE',  ( 757.2208543904082489, -232.7146871989596377, 350.9844846989624330 ) ) ;
#31717=CARTESIAN_POINT ( 'NONE',  ( 755.8990559732751535, -131.4636090269711985, 365.9055244015606831 ) ) ;
#31724=CARTESIAN_POINT ( 'NONE',  ( 764.1737431748507561, -370.3726999360613377, 371.6461892240376415 ) ) ;
#31728=CARTESIAN_POINT ( 'NONE',  ( 768.0187753319979720, -8.634602658420517329, 318.0580252608186242 ) ) ;
#31730=CARTESIAN_POINT ( 'NONE',  ( 781.2370466360911223, -260.7363362996981095, 304.9990715423533629 ) ) ;
#31732=CARTESIAN_POINT ( 'NONE',  ( 811.0346526505616112, -230.6346026584197659, 323.0537975583477532 ) ) ;
#31736=CARTESIAN_POINT ( 'NONE',  ( 781.7834795799800531, -298.8164208402377540, 315.0636971347436202 ) ) ;
#31737=CARTESIAN_POINT ( 'NONE',  ( 763.0428371773158460, -83.46360902697136908, 358.7617431975195359 ) ) ;
#31741=CARTESIAN_POINT ( 'NONE',  ( 786.6156483768007774, -121.4419599262327267, 315.5913626894246136 ) ) ;
#31742=CARTESIAN_POINT ( 'NONE',  ( 774.6858677611749044, -345.7255117493285184, 315.5713283507209894 ) ) ;
#31745=CARTESIAN_POINT ( 'NONE',  ( 804.9363028652555840, -88.27096629478390355, 338.2165204200192079 ) ) ;
#31748=CARTESIAN_POINT ( 'NONE',  ( 749.8865473780648472, -404.5328690171409107, 322.1177392798429082 ) ) ;
#31751=CARTESIAN_POINT ( 'NONE',  ( 762.3223304703356007, -319.5436935675104451, 322.3223304703362828 ) ) ;
#31752=EDGE_CURVE ( 'NONE', #19936, #24078, #32902, .T. ) ;
#31756=CARTESIAN_POINT ( 'NONE',  ( 778.1981804954714335, -418.2709662947827383, 314.8072714833589885 ) ) ;
#31760=ORIENTED_EDGE ( 'NONE', *, *, #202, .F. ) ;
#31762=CARTESIAN_POINT ( 'NONE',  ( 778.1981804954714335, -130.2709662947837899, 314.8072714833589885 ) ) ;
#31763=CARTESIAN_POINT ( 'NONE',  ( 773.4516893846965786, -427.6454272087885897, 315.8398074228977066 ) ) ;
#31764=CARTESIAN_POINT ( 'NONE',  ( 798.7617431975189675, -123.6237781080508569, 323.0428371773161871 ) ) ;
#31765=CARTESIAN_POINT ( 'NONE',  ( 779.9999999999992042, -462.9681489794448339, 339.9999999999999432 ) ) ;
#31767=CARTESIAN_POINT ( 'NONE',  ( 776.2433038121456548, -396.8965053807772847, 374.8207195650711014 ) ) ;
#31772=CARTESIAN_POINT ( 'NONE',  ( 811.3240766477731540, -28.37269993606244967, 355.6651683502462902 ) ) ;
#31781=CARTESIAN_POINT ( 'NONE',  ( 801.5560724626406000, -360.5545181178796383, 326.7756240680316182 ) ) ;
#31783=CARTESIAN_POINT ( 'NONE',  ( 757.7880784355613741, -330.0090635724251342, 312.4576283171834916 ) ) ;
#31787=CARTESIAN_POINT ( 'NONE',  ( 746.4236121716829757, -135.8272453906076009, 328.8385539511384650 ) ) ;
#31789=CARTESIAN_POINT ( 'NONE',  ( 808.3070685750230950, -90.99823902205663728, 361.1904061080339261 ) ) ;
#31794=CARTESIAN_POINT ( 'NONE',  ( 764.8639956371174549, -200.0891481129653187, 319.7806653035542013 ) ) ;
#31795=CARTESIAN_POINT ( 'NONE',  ( 794.5607502887775127, -462.9631818684622999, 371.8524697363486666 ) ) ;
#31799=CARTESIAN_POINT ( 'NONE',  ( 746.0683387631852383, 4.558040073766884248, 331.3260364891676204 ) ) ;
#31804=CARTESIAN_POINT ( 'NONE',  ( 795.6651683502461765, -322.7146871989593819, 371.3240766477733814 ) ) ;
#31805=CARTESIAN_POINT ( 'NONE',  ( 778.1981804954715471, -106.2709662947838467, 314.8072714833591021 ) ) ;
#31808=CARTESIAN_POINT ( 'NONE',  ( 768.0187753319979720, -296.6346026584195670, 318.0580252608186242 ) ) ;
#31810=CARTESIAN_POINT ( 'NONE',  ( 787.4397851343537695, -93.72551174932934259, 374.2001403089903988 ) ) ;
#31815=CARTESIAN_POINT ( 'NONE',  ( 803.6646147819161570, -17.90732993114776406, 348.8264449731210561 ) ) ;
#31817=CARTESIAN_POINT ( 'NONE',  ( 800.9747183278959710, -372.9982390220557704, 311.9810565676471583 ) ) ;
#31818=CARTESIAN_POINT ( 'NONE',  ( 744.9990715423526808, -282.3510508353230080, 341.2370466360926002 ) ) ;
#31819=CARTESIAN_POINT ( 'NONE',  ( 773.7943932421234194, -71.80559628986922860, 305.5313806188329409 ) ) ;
#31825=CARTESIAN_POINT ( 'NONE',  ( 745.4481719005789273, -387.7255117493283478, 347.5162901302853129 ) ) ;
#31826=( BOUNDED_CURVE ( )  B_SPLINE_CURVE ( 2, ( #44044, #20016, #1762, #22799, #34093, #5033, #9629 ),
 .UNSPECIFIED., .F., .T. ) 
 B_SPLINE_CURVE_WITH_KNOTS ( ( 3, 2, 2, 3 ),
 ( 0.006081874955971018626, 0.006818181818181817851, 0.009090909090909090468, 0.01033270150184909669 ),
 .UNSPECIFIED. ) 
 CURVE ( )  GEOMETRIC_REPRESENTATION_ITEM ( )  RATIONAL_B_SPLINE_CURVE ( ( 0.4977709609702910543, 0.4983514209501199721, 0.5000002209606653203, 0.4949109396520706694, 0.5000002209606653203, 0.4972194953619585855, 0.4974774836351868457 ) ) 
 REPRESENTATION_ITEM ( '' )  );
#31832=CARTESIAN_POINT ( 'NONE',  ( 773.4516893846965786, -259.6454272087890445, 315.8398074228977066 ) ) ;
#31833=CARTESIAN_POINT ( 'NONE',  ( 804.4286716492782716, -113.3618753856929260, 345.3141322388244703 ) ) ;
#31834=ORIENTED_EDGE ( 'NONE', *, *, #24906, .T. ) ;
#31836=VECTOR ( 'NONE', #45551, 1000.000000000000000 ) ;
#31838=CARTESIAN_POINT ( 'NONE',  ( 772.3691319403857278, -287.2601417444140566, 315.8894580844506663 ) ) ;
#31840=CARTESIAN_POINT ( 'NONE',  ( 814.8207195650702488, -50.19088175424420939, 336.2433038121456548 ) ) ;
#31842=CARTESIAN_POINT ( 'NONE',  ( 758.8095938919642549, -176.0891481129653755, 311.6929314249763365 ) ) ;
#31843=CARTESIAN_POINT ( 'NONE',  ( 754.8072714833581358, -76.81642084023845030, 338.1981804954720587 ) ) ;
#31845=CARTESIAN_POINT ( 'NONE',  ( 805.6418435158337843, -437.4636090269703459, 363.8556311672236916 ) ) ;
#31848=CARTESIAN_POINT ( 'NONE',  ( 773.3843516231979720, -373.4419599262319593, 364.4086373105754433 ) ) ;
#31849=CARTESIAN_POINT ( 'NONE',  ( 815.2698199232962679, -40.81642084023859951, 342.5225473063383674 ) ) ;
#31851=CARTESIAN_POINT ( 'NONE',  ( 787.6308680596127942, -59.26014174441473870, 364.1105419155492768 ) ) ;
#31854=CARTESIAN_POINT ( 'NONE',  ( 764.3348316497523456, -190.7146871989597798, 308.6759233522265617 ) ) ;
#31855=CARTESIAN_POINT ( 'NONE',  ( 755.0636971347428243, -28.27096629478409540, 341.7834795799807353 ) ) ;
#31859=CARTESIAN_POINT ( 'NONE',  ( 795.1360043628807261, -212.0891481129652902, 360.2193346964456282 ) ) ;
#31861=CARTESIAN_POINT ( 'NONE',  ( 759.9864689768902508, -338.0891481129649492, 354.9819416627836404 ) ) ;
#31865=CARTESIAN_POINT ( 'NONE',  ( 805.0264073115434940, -54.35105083532383219, 339.4763451958999099 ) ) ;
#31867=CARTESIAN_POINT ( 'NONE',  ( 763.0537975583476964, -264.4527844766016074, 371.0346526505628617 ) ) ;
#31869=CARTESIAN_POINT ( 'NONE',  ( 815.0009284576459549, 17.64894916467593688, 338.7629533639073429 ) ) ;
#31874=CARTESIAN_POINT ( 'NONE',  ( 767.7687537140311633, -287.9073299311468759, 372.7932403749916830 ) ) ;
#31876=CARTESIAN_POINT ( 'NONE',  ( 783.0433043558608688, -336.8965053807774552, 315.1538015810313027 ) ) ;
#31878=CARTESIAN_POINT ( 'NONE',  ( 787.5531968255692163, -165.8272453906074873, 316.1348686366205811 ) ) ;
#31879=CARTESIAN_POINT ( 'NONE',  ( 774.6312213355099630, -23.36187538569318889, 364.6798772138717482 ) ) ;
#31885=CARTESIAN_POINT ( 'NONE',  ( 744.6391490659812007, -230.7363362996981664, 338.7502325331110455 ) ) ;
#31886=CARTESIAN_POINT ( 'NONE',  ( 803.2186876482843445, -199.9874144716870603, 350.0220218866286928 ) ) ;
#31888=CARTESIAN_POINT ( 'NONE',  ( 785.3687786644884454, 12.63812461430668321, 315.3201227861279676 ) ) ;
#31890=CARTESIAN_POINT ( 'NONE',  ( 763.2262854647970016, -8.634602658420517329, 309.2812353651462445 ) ) ;
#31891=CARTESIAN_POINT ( 'NONE',  ( 767.6429770376289525, -81.18005720387481006, 306.8695393053162093 ) ) ;
#31893=CARTESIAN_POINT ( 'NONE',  ( 772.4999999999993179, -512.9681489794448908, 339.9999999999999432 ) ) ;
#31896=CARTESIAN_POINT ( 'NONE',  ( 786.2694204179717872, -357.2817908451523294, 305.1769319972829067 ) ) ;
#31898=CARTESIAN_POINT ( 'NONE',  ( 782.5225473063381969, -334.2709662947829656, 375.2698199232970637 ) ) ;
#31901=DIRECTION ( 'NONE',  ( -1.000000000000000000, -0.000000000000000000, 0.000000000000000000 ) ) ;
#31902=CARTESIAN_POINT ( 'NONE',  ( 767.8955696845333705, -432.4527844766008684, 362.1676090361162323 ) ) ;
#31903=CARTESIAN_POINT ( 'NONE',  ( 757.0176451133909268, -205.0999726633346256, 349.9200121543848354 ) ) ;
#31906=CARTESIAN_POINT ( 'NONE',  ( 766.5853460496234675, -85.98741447168738716, 372.3518521366060554 ) ) ;
#31907=CARTESIAN_POINT ( 'NONE',  ( 768.0187753319979720, -392.6346026584193396, 318.0580252608186242 ) ) ;
#31908=CARTESIAN_POINT ( 'NONE',  ( 751.2241431872005251, -160.1692326535053326, 359.9636004259367610 ) ) ;
#31913=CARTESIAN_POINT ( 'NONE',  ( 791.9812246680005501, -212.6346026584198796, 361.9419747391813189 ) ) ;
#31914=CARTESIAN_POINT ( 'NONE',  ( 781.8018195045267476, -214.2709662947834772, 365.1927285166407273 ) ) ;
#31919=CARTESIAN_POINT ( 'NONE',  ( 803.6646147819161570, -425.9073299311463074, 348.8264449731210561 ) ) ;
#31922=CARTESIAN_POINT ( 'NONE',  ( 792.3570229623691148, -165.1800572038745543, 373.1304606946836770 ) ) ;
#31923=CARTESIAN_POINT ( 'NONE',  ( 801.5560724626406000, -264.5545181178798657, 326.7756240680316182 ) ) ;
#31924=ORIENTED_EDGE ( 'NONE', *, *, #29481, .F. ) ;
#31925=CARTESIAN_POINT ( 'NONE',  ( 768.8385539511368734, -191.2601417444143976, 306.4236121716840557 ) ) ;
#31931=CARTESIAN_POINT ( 'NONE',  ( 805.0264073115434940, -222.3510508353233206, 339.4763451958999099 ) ) ;
#31940=CARTESIAN_POINT ( 'NONE',  ( 768.9521613784389729, -153.8272453906075157, 373.2346286133773106 ) ) ;
#31946=MANIFOLD_SOLID_BREP ( '<Treadle Extension Return Springs>-<Move Face1>', #12899 ) ;
#31952=CARTESIAN_POINT ( 'NONE',  ( 774.6312213355099630, -23.36187538569318889, 364.6798772138717482 ) ) ;
#31954=CARTESIAN_POINT ( 'NONE',  ( 776.2046728542105711, -236.1908817542436338, 304.8212110874238761 ) ) ;
#31956=CARTESIAN_POINT ( 'NONE',  ( 814.9108240113580450, -232.2709662947834488, 337.5031285880265273 ) ) ;
#31959=CARTESIAN_POINT ( 'NONE',  ( 801.9419747391806368, -330.4527844766013231, 351.9812246680014027 ) ) ;
#31960=CARTESIAN_POINT ( 'NONE',  ( 766.9102291470427417, -90.55451811788041994, 318.6633372737382501 ) ) ;
#31961=CARTESIAN_POINT ( 'NONE',  ( 804.1105419155481968, -75.82724539060775726, 347.6308680596136469 ) ) ;
#31966=CARTESIAN_POINT ( 'NONE',  ( 790.8726784830453198, -106.7146871989600498, 362.5472867521010585 ) ) ;
#31967=CARTESIAN_POINT ( 'NONE',  ( 785.3687786644884454, -371.3618753856919739, 315.3201227861279676 ) ) ;
#31970=CARTESIAN_POINT ( 'NONE',  ( 802.1676090361156639, -110.6346026584201638, 327.8955696845344505 ) ) ;
#31971=CARTESIAN_POINT ( 'NONE',  ( 749.5768839229115201, -396.5545181178794678, 358.0661480581553064 ) ) ;
#31974=CARTESIAN_POINT ( 'NONE',  ( 749.8865473780648472, -428.5328690171409107, 322.1177392798429082 ) ) ;
#31976=CARTESIAN_POINT ( 'NONE',  ( 800.2193346964447755, -306.9982390220558273, 355.1360043628815788 ) ) ;
#31980=CARTESIAN_POINT ( 'NONE',  ( 802.1676090361156639, -422.6346026584192259, 327.8955696845344505 ) ) ;
#31981=EDGE_CURVE ( 'NONE', #13477, #29782, #43217, .T. ) ;
#31983=ORIENTED_EDGE ( 'NONE', *, *, #45264, .F. ) ;
#31989=CARTESIAN_POINT ( 'NONE',  ( 763.8424801807145741, -450.0090635724248500, 320.5453621957614700 ) ) ;
#31990=CARTESIAN_POINT ( 'NONE',  ( 764.0069404352550464, -135.0783235625962959, 359.2566176426627180 ) ) ;
#31991=FACE_OUTER_BOUND ( 'NONE', #14910, .T. ) ;
#31993=CARTESIAN_POINT ( 'NONE',  ( 744.8212110874229666, -378.8965053807772847, 336.2046728542121627 ) ) ;
#31999=CARTESIAN_POINT ( 'NONE',  ( 810.4231160770870019, -48.55451811788057626, 321.9338519418446936 ) ) ;
#32008=CARTESIAN_POINT ( 'NONE',  ( 755.3028492785439312, -375.2817908451523294, 335.9200461376539693 ) ) ;
#32009=CARTESIAN_POINT ( 'NONE',  ( 747.6481478633932056, -325.0999726633342561, 353.4146539503763620 ) ) ;
#32014=CARTESIAN_POINT ( 'NONE',  ( 766.4474001241216001, -139.0999726633348530, 307.3154664389482491 ) ) ;
#32017=CARTESIAN_POINT ( 'NONE',  ( 787.5162901302840055, -131.3618753856928834, 305.4481719005792684 ) ) ;
#32021=CARTESIAN_POINT ( 'NONE',  ( 774.6312213355099630, -215.3618753856925423, 364.6798772138717482 ) ) ;
#32024=CARTESIAN_POINT ( 'NONE',  ( 784.1219089521767955, 2.718209154846545683, 315.0488828828318333 ) ) ;
#32028=CARTESIAN_POINT ( 'NONE',  ( 811.6461892240364477, -4.714687198960358039, 324.1737431748509835 ) ) ;
#32032=CARTESIAN_POINT ( 'NONE',  ( 758.0141637701419768, -327.0783235625956991, 367.2620300519063790 ) ) ;
#32033=CARTESIAN_POINT ( 'NONE',  ( 774.6858677611749044, -129.7255117493292289, 315.5713283507209894 ) ) ;
#32037=CARTESIAN_POINT ( 'NONE',  ( 774.6858677611749044, -297.7255117493286889, 315.5713283507209894 ) ) ;
#32041=CARTESIAN_POINT ( 'NONE',  ( 749.2812353651451076, -78.45278447660211896, 323.2262854647983090 ) ) ;
#32044=ORIENTED_EDGE ( 'NONE', *, *, #6310, .T. ) ;
#32045=CARTESIAN_POINT ( 'NONE',  ( 785.3141322388236176, -21.72551174932956641, 364.4286716492789537 ) ) ;
#32047=CARTESIAN_POINT ( 'NONE',  ( 804.7487373415286811, -379.5436935675102745, 364.7487373415288516 ) ) ;
#32048=CARTESIAN_POINT ( 'NONE',  ( 788.7631598425961101, -289.4419599262321299, 305.7194118038759143 ) ) ;
#32050=CARTESIAN_POINT ( 'NONE',  ( 788.7631598425961101, -73.44195992623286884, 305.7194118038759143 ) ) ;
#32053=DIRECTION ( 'NONE',  ( 0.000000000000000000, 0.000000000000000000, 1.000000000000000000 ) ) ;
#32057=CARTESIAN_POINT ( 'NONE',  ( 777.5031285880264704, -406.8164208402375266, 374.9108240113588408 ) ) ;
#32064=CARTESIAN_POINT ( 'NONE',  ( 800.9840315886518738, -268.9181544815162397, 354.1144889064786412 ) ) ;
#32065=CARTESIAN_POINT ( 'NONE',  ( 771.2633955100217236, -167.9073299311473022, 363.4237431249939618 ) ) ;
#32069=CARTESIAN_POINT ( 'NONE',  ( 793.2243759319678702, -314.5328690171411949, 318.4439275373583200 ) ) ;
#32072=CARTESIAN_POINT ( 'NONE',  ( 771.3260364891663130, -43.64542720878966975, 306.0683387631859773 ) ) ;
#32076=CARTESIAN_POINT ( 'NONE',  ( 777.5031285880264704, -214.8164208402380666, 374.9108240113588408 ) ) ;
#32077=CARTESIAN_POINT ( 'NONE',  ( 781.8018195045266339, -70.27096629478397460, 365.1927285166406705 ) ) ;
#32080=CARTESIAN_POINT ( 'NONE',  ( 788.6739635108323228, -439.6454272087884760, 373.9316612368139090 ) ) ;
#32083=CARTESIAN_POINT ( 'NONE',  ( 770.0799878456142551, -373.9874144716864066, 362.9823548866085616 ) ) ;
#32084=CARTESIAN_POINT ( 'NONE',  ( 814.5518280994195948, -39.72551174932951312, 332.4837098697145166 ) ) ;
#32086=CARTESIAN_POINT ( 'NONE',  ( 769.1273215169530886, -70.71468719896014932, 317.4527132478988847 ) ) ;
#32090=CARTESIAN_POINT ( 'NONE',  ( 808.7758568127978833, -196.1692326535052473, 320.0363995740631822 ) ) ;
#32091=CARTESIAN_POINT ( 'NONE',  ( 774.6858677611749044, -9.725511749329603717, 315.5713283507209894 ) ) ;
#32095=CARTESIAN_POINT ( 'NONE',  ( 764.0069404352550464, -375.0783235625955285, 359.2566176426627180 ) ) ;
#32098=CARTESIAN_POINT ( 'NONE',  ( 767.8955696845333705, -216.4527844766016926, 362.1676090361162323 ) ) ;
#32100=CARTESIAN_POINT ( 'NONE',  ( 757.8323909638828582, -338.6346026584195101, 352.1044303154654358 ) ) ;
#32105=CARTESIAN_POINT ( 'NONE',  ( 804.9511171171677688, -53.80559628986930676, 335.8780910478229202 ) ) ;
#32110=CARTESIAN_POINT ( 'NONE',  ( 805.0032342141413437, -301.5436935675105588, 314.9967657858572352 ) ) ;
#32111=CARTESIAN_POINT ( 'NONE',  ( 791.1614460488616487, -11.26014174441488258, 373.5763878283158874 ) ) ;
#32117=CARTESIAN_POINT ( 'NONE',  ( 767.6429770376289525, -273.1800572038742985, 306.8695393053162093 ) ) ;
#32119=CARTESIAN_POINT ( 'NONE',  ( 773.3843516231979720, -349.4419599262320162, 364.4086373105754433 ) ) ;
#32121=CARTESIAN_POINT ( 'NONE',  ( 755.1538015810308480, -158.1908817542438612, 343.0433043558613804 ) ) ;
#32122=CARTESIAN_POINT ( 'NONE',  ( 797.8594530101008786, -37.54369356751132614, 322.1405469898980982 ) ) ;
#32127=CARTESIAN_POINT ( 'NONE',  ( 748.6759233522253680, -280.3726999360616787, 324.3348316497537098 ) ) ;
#32128=CARTESIAN_POINT ( 'NONE',  ( 787.6308680596127942, -179.2601417444143692, 364.1105419155492768 ) ) ;
#32131=CARTESIAN_POINT ( 'NONE',  ( 764.8639956371174549, 15.91085188703394238, 319.7806653035542013 ) ) ;
#32134=CARTESIAN_POINT ( 'NONE',  ( 787.5162901302840055, -11.36187538569323863, 305.4481719005792684 ) ) ;
#32135=CARTESIAN_POINT ( 'NONE',  ( 744.7301800767019131, -124.8164208402383508, 337.4774526936615757 ) ) ;
#32140=CARTESIAN_POINT ( 'NONE',  ( 764.1737431748507561, -370.3726999360613377, 371.6461892240376415 ) ) ;
#32142=CARTESIAN_POINT ( 'NONE',  ( 810.7187646348534145, -330.4527844766013231, 356.7737145352016341 ) ) ;
#32147=CARTESIAN_POINT ( 'NONE',  ( 762.3223304703356007, -439.5436935675101040, 322.3223304703362828 ) ) ;
#32148=CARTESIAN_POINT ( 'NONE',  ( 775.8780910478218402, -177.2817908451528695, 364.9511171171680530 ) ) ;
#32151=CARTESIAN_POINT ( 'NONE',  ( 746.0683387631852383, -91.44195992623282621, 331.3260364891676204 ) ) ;
#32152=CARTESIAN_POINT ( 'NONE',  ( 759.7806653035535192, -390.9982390220556567, 324.8639956371181370 ) ) ;
#32153=CARTESIAN_POINT ( 'NONE',  ( 815.1787889125755555, -150.8965053807781089, 343.7953271457877804 ) ) ;
#32158=CARTESIAN_POINT ( 'NONE',  ( 757.8323909638827445, -218.6346026584197944, 352.1044303154654358 ) ) ;
#32159=CARTESIAN_POINT ( 'NONE',  ( 803.6646147819162707, -209.9073299311471317, 348.8264449731211130 ) ) ;
#32163=CARTESIAN_POINT ( 'NONE',  ( 797.6776695296629214, -427.5436935675101040, 357.6776695296636603 ) ) ;
#32170=CARTESIAN_POINT ( 'NONE',  ( 745.0891759886404770, -148.2709662947837330, 342.4968714119734159 ) ) ;
#32171=CARTESIAN_POINT ( 'NONE',  ( 780.5236548040995785, -260.7363362996981095, 314.9735926884559944 ) ) ;
#32174=CARTESIAN_POINT ( 'NONE',  ( 746.7653713866222915, -185.2601417444143692, 351.0478386215610271 ) ) ;
#32180=CARTESIAN_POINT ( 'NONE',  ( 769.1273215169530886, -238.7146871989596661, 317.4527132478988847 ) ) ;
#32190=CARTESIAN_POINT ( 'NONE',  ( 745.5313806188320314, -183.2817908451528695, 333.7943932421247268 ) ) ;
#32199=CARTESIAN_POINT ( 'NONE',  ( 781.7834795799800531, -10.81642084023869543, 315.0636971347436202 ) ) ;
#32200=CARTESIAN_POINT ( 'NONE',  ( 750.9282345327678740, -256.9181544815163534, 319.8311093483690115 ) ) ;
#32202=CARTESIAN_POINT ( 'NONE',  ( 814.2001403089898304, -233.3618753856925423, 347.4397851343538264 ) ) ;
#32206=CARTESIAN_POINT ( 'NONE',  ( 774.6312213355099630, -311.3618753856922581, 364.6798772138717482 ) ) ;
#32208=CARTESIAN_POINT ( 'NONE',  ( 790.0220218866281812, -79.09997266333503774, 363.2186876482849129 ) ) ;
#32209=CARTESIAN_POINT ( 'NONE',  ( 804.8461984189677878, -74.19088175424410281, 336.9566956441385628 ) ) ;
#32213=CARTESIAN_POINT ( 'NONE',  ( 789.9200121543843807, -145.9874144716871740, 317.0176451133914384 ) ) ;
#32214=CARTESIAN_POINT ( 'NONE',  ( 805.1927285166397041, -352.8164208402374129, 341.8018195045277707 ) ) ;
#32218=CARTESIAN_POINT ( 'NONE',  ( 795.1360043628807261, -140.0891481129654892, 360.2193346964456282 ) ) ;
#32222=CARTESIAN_POINT ( 'NONE',  ( 747.3154664389472828, -427.9874144716862929, 326.4474001241230781 ) ) ;
#32224=CARTESIAN_POINT ( 'NONE',  ( 803.4237431249931660, -327.1800572038741279, 331.2633955100225194 ) ) ;
#32228=CARTESIAN_POINT ( 'NONE',  ( 755.3201227861273992, -435.7255117493282341, 345.3687786644892981 ) ) ;
#32234=CARTESIAN_POINT ( 'NONE',  ( 791.9812246680005501, 3.365397341579444479, 361.9419747391813189 ) ) ;
#32235=CARTESIAN_POINT ( 'NONE',  ( 808.0189434323515343, -230.0891481129652618, 319.0252816721025511 ) ) ;
#32236=CARTESIAN_POINT ( 'NONE',  ( 766.7756240680305382, -110.5328690171418629, 361.5560724626415663 ) ) ;
#32240=CARTESIAN_POINT ( 'NONE',  ( 800.1688906516307043, -394.1692326535045368, 369.0717654672308186 ) ) ;
#32245=CARTESIAN_POINT ( 'NONE',  ( 812.3518521366052028, -25.09997266333519050, 326.5853460496235243 ) ) ;
#32255=CARTESIAN_POINT ( 'NONE',  ( 776.9254006560222479, -380.1908817542431507, 314.8983024940802125 ) ) ;
#32256=CARTESIAN_POINT ( 'NONE',  ( 778.7629533639073998, -344.7363362996978253, 375.0009284576466371 ) ) ;
#32260=CARTESIAN_POINT ( 'NONE',  ( 791.0478386215596629, -141.8272453906075157, 306.7653713866226326 ) ) ;
#32262=CARTESIAN_POINT ( 'NONE',  ( 815.2698199232961542, -112.8164208402383508, 342.5225473063383106 ) ) ;
#32265=CARTESIAN_POINT ( 'NONE',  ( 799.9999999999993179, 166.4563064324884465, 360.0000000000000000 ) ) ;
#32267=CARTESIAN_POINT ( 'NONE',  ( 754.8072714833581358, -220.8164208402379529, 338.1981804954720587 ) ) ;
#32268=CARTESIAN_POINT ( 'NONE',  ( 749.5768839229115201, -444.5545181178792973, 358.0661480581553064 ) ) ;
#32273=CARTESIAN_POINT ( 'NONE',  ( 791.1614460488616487, 12.73985825558503926, 373.5763878283158874 ) ) ;
#32276=CARTESIAN_POINT ( 'NONE',  ( 762.3223304703356007, -31.54369356751135456, 322.3223304703362828 ) ) ;
#32279=CARTESIAN_POINT ( 'NONE',  ( 807.5423716828161105, -297.0783235625957559, 362.2119215644372048 ) ) ;
#32280=CARTESIAN_POINT ( 'NONE',  ( 759.9864689768902508, -170.0891481129654608, 354.9819416627836404 ) ) ;
#32283=CARTESIAN_POINT ( 'NONE',  ( 755.0636971347428243, -292.2709662947831930, 341.7834795799807353 ) ) ;
#32285=CARTESIAN_POINT ( 'NONE',  ( 813.1304606946831655, -89.90732993114752958, 352.3570229623691716 ) ) ;
#32291=CARTESIAN_POINT ( 'NONE',  ( 755.3201227861273992, -75.72551174932937101, 345.3687786644892981 ) ) ;
#32292=CARTESIAN_POINT ( 'NONE',  ( 802.9823548866075953, -337.0999726633342561, 330.0799878456151077 ) ) ;
#32294=CARTESIAN_POINT ( 'NONE',  ( 787.4397851343537695, -381.7255117493284615, 374.2001403089903988 ) ) ;
#32295=CARTESIAN_POINT ( 'NONE',  ( 759.8311093483677041, -286.1692326535048778, 310.9282345327691814 ) ) ;
#32296=CARTESIAN_POINT ( 'NONE',  ( 791.1614460488616487, -83.26014174441466764, 373.5763878283158874 ) ) ;
#32300=PLANE ( 'NONE',  #36409 ) ;
#32304=CARTESIAN_POINT ( 'NONE',  ( 751.6929314249748586, -390.9982390220557136, 318.8095938919659034 ) ) ;
#32310=CARTESIAN_POINT ( 'NONE',  ( 804.1105419155481968, -267.8272453906071746, 347.6308680596136469 ) ) ;
#32311=CARTESIAN_POINT ( 'NONE',  ( 788.8264449731200330, -141.1800572038746395, 363.6646147819171233 ) ) ;
#32315=CARTESIAN_POINT ( 'NONE',  ( 793.2243759319678702, -338.5328690171411381, 318.4439275373583200 ) ) ;
#32319=CARTESIAN_POINT ( 'NONE',  ( 797.8822607201568644, -30.55451811788062244, 370.1134526219340160 ) ) ;
#32322=CARTESIAN_POINT ( 'NONE',  ( 745.7998596910086917, -197.3618753856926560, 332.5602148656461168 ) ) ;
#32323=CARTESIAN_POINT ( 'NONE',  ( 792.1044303154645831, -108.4527844766019911, 317.8323909638837677 ) ) ;
#32326=CARTESIAN_POINT ( 'NONE',  ( 809.0717654672305343, -460.9181544815156713, 360.1688906516309885 ) ) ;
#32329=CARTESIAN_POINT ( 'NONE',  ( 759.2295555964440155, -352.1692326535046504, 353.9708237608231229 ) ) ;
#32330=CARTESIAN_POINT ( 'NONE',  ( 782.5225473063383106, -46.27096629478403855, 375.2698199232970637 ) ) ;
#32333=CARTESIAN_POINT ( 'NONE',  ( 795.9930595647434757, -51.07832356259657303, 320.7433823573372820 ) ) ;
#32336=CARTESIAN_POINT ( 'NONE',  ( 783.7566961878529810, -192.8965053807779668, 305.1792804349288417 ) ) ;
#32337=CARTESIAN_POINT ( 'NONE',  ( 795.1360043628808398, -44.08914811296585157, 360.2193346964456282 ) ) ;
#32340=CARTESIAN_POINT ( 'NONE',  ( 771.1735550268778070, -201.1800572038744690, 316.3353852180827630 ) ) ;
#32342=CARTESIAN_POINT ( 'NONE',  ( 758.0580252608178853, -342.4527844766013231, 328.0187753319985404 ) ) ;
#32347=CARTESIAN_POINT ( 'NONE',  ( 759.2295555964440155, -64.16923265350563099, 353.9708237608231229 ) ) ;
#32350=CARTESIAN_POINT ( 'NONE',  ( 804.7487373415286811, -307.5436935675104451, 364.7487373415288516 ) ) ;
#32351=CARTESIAN_POINT ( 'NONE',  ( 810.1134526219336749, 15.46713098285775878, 357.8822607201570349 ) ) ;
#32356=CARTESIAN_POINT ( 'NONE',  ( 796.9462024416508257, -300.4527844766012663, 308.9653473494370246 ) ) ;
#32358=CARTESIAN_POINT ( 'NONE',  ( 798.7617431975189675, -363.6237781080502032, 323.0428371773161871 ) ) ;
#32360=CARTESIAN_POINT ( 'NONE',  ( 766.9102291470427417, -162.5545181178802352, 318.6633372737382501 ) ) ;
#32361=CARTESIAN_POINT ( 'NONE',  ( 788.7366044899766848, -35.90732993114770011, 316.5762568750059813 ) ) ;
#32366=CARTESIAN_POINT ( 'NONE',  ( 778.7629533639073998, -272.7363362996981095, 375.0009284576466371 ) ) ;
#32367=CARTESIAN_POINT ( 'NONE',  ( 772.3691319403857278, -215.2601417444141987, 315.8894580844506663 ) ) ;
#32372=CARTESIAN_POINT ( 'NONE',  ( 788.7366044899766848, 12.09267006885214180, 316.5762568750059813 ) ) ;
#32376=CARTESIAN_POINT ( 'NONE',  ( 745.0891759886404770, -4.270966294784170003, 342.4968714119734159 ) ) ;
#32377=CARTESIAN_POINT ( 'NONE',  ( 792.2312462859673587, -107.9073299311474727, 307.2067596250082602 ) ) ;
#32378=DIRECTION ( 'NONE',  ( 1.000000000000000000, 0.000000000000000000, -0.000000000000000000 ) ) ;
#32382=CARTESIAN_POINT ( 'NONE',  ( 745.1792804349281596, -374.1908817542432075, 343.7566961878542884 ) ) ;
#32384=CARTESIAN_POINT ( 'NONE',  ( 763.0537975583475827, -336.4527844766012095, 371.0346526505627480 ) ) ;
#32389=CARTESIAN_POINT ( 'NONE',  ( 758.0580252608178853, -414.4527844766010389, 328.0187753319985404 ) ) ;
#32390=CARTESIAN_POINT ( 'NONE',  ( 758.4439275373578084, -180.5545181178801499, 353.2243759319684386 ) ) ;
#32393=CARTESIAN_POINT ( 'NONE',  ( 766.5853460496234675, -109.9874144716873019, 372.3518521366060554 ) ) ;
#32394=CARTESIAN_POINT ( 'NONE',  ( 756.3353852180820240, -413.9073299311465348, 331.1735550268787733 ) ) ;
#32396=CARTESIAN_POINT ( 'NONE',  ( 781.2497674668890113, -156.3510508353235480, 375.3608509340180603 ) ) ;
#32402=CARTESIAN_POINT ( 'NONE',  ( 759.7806653035534055, -246.9982390220560546, 324.8639956371180801 ) ) ;
#32403=CARTESIAN_POINT ( 'NONE',  ( 762.1405469898973024, -217.5436935675107293, 357.8594530101016176 ) ) ;
#32407=CARTESIAN_POINT ( 'NONE',  ( 754.8072714833581358, -436.8164208402372992, 338.1981804954720587 ) ) ;
#32409=CARTESIAN_POINT ( 'NONE',  ( 745.0891759886404770, -172.2709662947836478, 342.4968714119734159 ) ) ;
#32410=CARTESIAN_POINT ( 'NONE',  ( 773.4516893846965786, -259.6454272087890445, 315.8398074228977066 ) ) ;
#32413=CARTESIAN_POINT ( 'NONE',  ( 746.7653713866222915, -233.2601417444141987, 351.0478386215610271 ) ) ;
#32419=CARTESIAN_POINT ( 'NONE',  ( 759.2295555964440155, -256.1692326535049915, 353.9708237608231229 ) ) ;
#32427=CARTESIAN_POINT ( 'NONE',  ( 744.6391490659812007, -158.7363362996984222, 338.7502325331110455 ) ) ;
#32432=CARTESIAN_POINT ( 'NONE',  ( 777.4774526936600978, -10.27096629478414691, 304.7301800767027657 ) ) ;
#32437=CARTESIAN_POINT ( 'NONE',  ( 754.8072714833581358, -4.816420840238714085, 338.1981804954720587 ) ) ;
#32438=CARTESIAN_POINT ( 'NONE',  ( 746.4236121716829757, -279.8272453906071746, 328.8385539511384650 ) ) ;
#32440=CARTESIAN_POINT ( 'NONE',  ( 782.5225473063381969, -238.2709662947833920, 375.2698199232970637 ) ) ;
#32443=VERTEX_POINT ( 'NONE', #27211 ) ;
#32444=CARTESIAN_POINT ( 'NONE',  ( 788.7366044899766848, -323.9073299311468190, 316.5762568750059813 ) ) ;
#32445=CARTESIAN_POINT ( 'NONE',  ( 804.4086373105744769, -73.64542720878957027, 333.3843516231986541 ) ) ;
#32448=DIRECTION ( 'NONE',  ( 0.000000000000000000, 0.000000000000000000, 1.000000000000000000 ) ) ;
#32449=CARTESIAN_POINT ( 'NONE',  ( 800.7704444035546203, -148.1692326535053610, 326.0291762391768771 ) ) ;
#32450=CARTESIAN_POINT ( 'NONE',  ( 788.7366044899766848, -371.9073299311465917, 316.5762568750059813 ) ) ;
#32455=CARTESIAN_POINT ( 'NONE',  ( 815.2698199232961542, 7.183579159761247723, 342.5225473063383106 ) ) ;
#32457=CARTESIAN_POINT ( 'NONE',  ( 757.8323909638827445, -338.6346026584195101, 352.1044303154654358 ) ) ;
#32459=CARTESIAN_POINT ( 'NONE',  ( 759.9864689768902508, -434.0891481129646081, 354.9819416627836404 ) ) ;
#32465=CARTESIAN_POINT ( 'NONE',  ( 768.0187753319979720, 15.36539734157940629, 318.0580252608186242 ) ) ;
#32466=CARTESIAN_POINT ( 'NONE',  ( 805.0032342141412300, -229.5436935675106440, 314.9967657858571783 ) ) ;
#32467=CARTESIAN_POINT ( 'NONE',  ( 802.7791456095903868, -124.7146871989599930, 329.0155153010375102 ) ) ;
#32468=CARTESIAN_POINT ( 'NONE',  ( 799.9999999999993179, -462.9681489794448339, 370.0000000000000568 ) ) ;
#32470=CARTESIAN_POINT ( 'NONE',  ( 791.1614460488616487, -395.2601417444136587, 373.5763878283158874 ) ) ;
#32475=CARTESIAN_POINT ( 'NONE',  ( 745.7194118038753459, -85.64542720878952764, 348.7631598425976449 ) ) ;
#32483=CARTESIAN_POINT ( 'NONE',  ( 755.3028492785439312, -399.2817908451522726, 335.9200461376539693 ) ) ;
#32487=CARTESIAN_POINT ( 'NONE',  ( 760.0363995740630116, -154.9181544815165523, 368.7758568127991907 ) ) ;
#32489=CARTESIAN_POINT ( 'NONE',  ( 763.2262854647970016, -128.6346026584201354, 309.2812353651462445 ) ) ;
#32493=CARTESIAN_POINT ( 'NONE',  ( 785.3687786644884454, -227.3618753856925707, 315.3201227861279676 ) ) ;
#32494=CARTESIAN_POINT ( 'NONE',  ( 796.1575198192839480, -6.009063572426154742, 359.4546378042384163 ) ) ;
#32498=CARTESIAN_POINT ( 'NONE',  ( 778.7502325331095108, -48.35105083532386061, 304.6391490659818828 ) ) ;
#32502=CARTESIAN_POINT ( 'NONE',  ( 794.9819416627830151, -12.99823902205686821, 319.9864689768909898 ) ) ;
#32505=CARTESIAN_POINT ( 'NONE',  ( 803.8556311672234642, -345.6237781080501463, 365.6418435158340117 ) ) ;
#32506=CARTESIAN_POINT ( 'NONE',  ( 771.1735550268780344, -153.1800572038746111, 316.3353852180828198 ) ) ;
#32509=CARTESIAN_POINT ( 'NONE',  ( 758.0580252608178853, -342.4527844766013231, 328.0187753319985404 ) ) ;
#32515=CARTESIAN_POINT ( 'NONE',  ( 755.0636971347428243, -52.27096629478401724, 341.7834795799807353 ) ) ;
#32516=CARTESIAN_POINT ( 'NONE',  ( 790.0220218866281812, -367.0999726633342561, 363.2186876482849129 ) ) ;
#32518=CARTESIAN_POINT ( 'NONE',  ( 744.7301800767020268, -388.8164208402374129, 337.4774526936615189 ) ) ;
#32519=CARTESIAN_POINT ( 'NONE',  ( 751.2241431872005251, -280.1692326535049347, 359.9636004259367610 ) ) ;
#32520=CARTESIAN_POINT ( 'NONE',  ( 778.7502325331095108, -72.35105083532378956, 304.6391490659818828 ) ) ;
#32527=VERTEX_POINT ( 'NONE', #44072 ) ;
#32528=CARTESIAN_POINT ( 'NONE',  ( 800.9747183278959710, -420.9982390220555999, 311.9810565676471583 ) ) ;
#32535=CARTESIAN_POINT ( 'NONE',  ( 804.8461984189677878, -266.1908817542435486, 336.9566956441385628 ) ) ;
#32536=CARTESIAN_POINT ( 'NONE',  ( 757.8323909638827445, -146.6346026584200217, 352.1044303154654358 ) ) ;
#32539=CARTESIAN_POINT ( 'NONE',  ( 799.4546378042377910, -321.0783235625956991, 356.1575198192848006 ) ) ;
#32541=CARTESIAN_POINT ( 'NONE',  ( 805.6418435158337843, -29.46360902697153250, 363.8556311672236916 ) ) ;
#32543=CARTESIAN_POINT ( 'NONE',  ( 763.2262854647970016, -200.6346026584199365, 309.2812353651462445 ) ) ;
#32544=CARTESIAN_POINT ( 'NONE',  ( 757.8323909638827445, -98.63460265842024910, 352.1044303154654358 ) ) ;
#32547=CARTESIAN_POINT ( 'NONE',  ( 809.0717654672305343, -436.9181544815157281, 360.1688906516309885 ) ) ;
#32550=CARTESIAN_POINT ( 'NONE',  ( 754.8983024940795303, -402.8965053807773415, 336.9254006560228163 ) ) ;
#32554=CARTESIAN_POINT ( 'NONE',  ( 790.8726784830453198, -58.71468719896019905, 362.5472867521010585 ) ) ;
#32558=CARTESIAN_POINT ( 'NONE',  ( 744.9990715423526808, -210.3510508353233490, 341.2370466360926002 ) ) ;
#32559=CARTESIAN_POINT ( 'NONE',  ( 759.7806653035535192, -54.99823902205672965, 324.8639956371181370 ) ) ;
#32562=CARTESIAN_POINT ( 'NONE',  ( 764.8639956371174549, -248.0891481129651481, 319.7806653035542013 ) ) ;
#32564=CARTESIAN_POINT ( 'NONE',  ( 804.9363028652555840, -352.2709662947830225, 338.2165204200192079 ) ) ;
#32568=CARTESIAN_POINT ( 'NONE',  ( 782.5225473063383106, -286.2709662947833067, 375.2698199232970637 ) ) ;
#32570=CARTESIAN_POINT ( 'NONE',  ( 771.2368401574024119, -13.44195992623305713, 374.2805881961240857 ) ) ;
#32579=CARTESIAN_POINT ( 'NONE',  ( 772.5602148656447525, -273.7255117493288026, 305.7998596910095443 ) ) ;
#32581=CARTESIAN_POINT ( 'NONE',  ( 754.9735926884551418, -354.3510508353228943, 340.5236548041000333 ) ) ;
#32584=CARTESIAN_POINT ( 'NONE',  ( 772.4468031744293057, -153.8272453906075157, 363.8651313633793620 ) ) ;
#32585=CARTESIAN_POINT ( 'NONE',  ( 785.3687786644884454, -35.36187538569316047, 315.3201227861279676 ) ) ;
#32589=CARTESIAN_POINT ( 'NONE',  ( 813.5763878283155464, -267.8272453906071746, 351.1614460488615350 ) ) ;
#32590=CARTESIAN_POINT ( 'NONE',  ( 770.0799878456142551, -205.9874144716870035, 362.9823548866085616 ) ) ;
#32593=CARTESIAN_POINT ( 'NONE',  ( 755.5713283507202505, -5.361875385693257279, 334.6858677611754729 ) ) ;
#32596=CARTESIAN_POINT ( 'NONE',  ( 792.3570229623688874, -45.18005720387493085, 373.1304606946836202 ) ) ;
#32597=CARTESIAN_POINT ( 'NONE',  ( 777.4774526936600978, -106.2709662947838467, 304.7301800767027657 ) ) ;
#32601=CARTESIAN_POINT ( 'NONE',  ( 809.0717654672305343, -388.9181544815158986, 360.1688906516309885 ) ) ;
#32602=ADVANCED_FACE ( 'NONE', ( #37376 ), #16354, .F. ) ;
#32604=CARTESIAN_POINT ( 'NONE',  ( 763.2262854647970016, -320.6346026584195670, 309.2812353651462445 ) ) ;
#32607=CARTESIAN_POINT ( 'NONE',  ( 774.6312213355099630, -431.3618753856918033, 364.6798772138717482 ) ) ;
#32609=CARTESIAN_POINT ( 'NONE',  ( 758.4439275373578084, -204.5545181178800931, 353.2243759319684386 ) ) ;
#32612=CARTESIAN_POINT ( 'NONE',  ( 759.8311093483677041, -118.1692326535054463, 310.9282345327691814 ) ) ;
#32613=CARTESIAN_POINT ( 'NONE',  ( 781.8018195045267476, -430.2709662947827383, 365.1927285166407273 ) ) ;
#32619=CARTESIAN_POINT ( 'NONE',  ( 762.1405469898971887, -265.5436935675106156, 357.8594530101015607 ) ) ;
#32620=CARTESIAN_POINT ( 'NONE',  ( 804.6798772138710092, -255.7255117493287742, 334.6312213355106451 ) ) ;
#32623=CARTESIAN_POINT ( 'NONE',  ( 755.3201227861273992, -435.7255117493282341, 345.3687786644892981 ) ) ;
#32626=CARTESIAN_POINT ( 'NONE',  ( 801.1904061080338124, -188.0891481129653755, 368.3070685750236066 ) ) ;
#32628=CARTESIAN_POINT ( 'NONE',  ( 772.4468031744293057, -249.8272453906072315, 363.8651313633793620 ) ) ;
#32629=CARTESIAN_POINT ( 'NONE',  ( 761.2382568024794409, -375.6237781080501463, 356.9571628226838129 ) ) ;
#32632=CARTESIAN_POINT ( 'NONE',  ( 746.0683387631852383, -211.4419599262324709, 331.3260364891676204 ) ) ;
#32637=CARTESIAN_POINT ( 'NONE',  ( 769.1273215169530886, -262.7146871989594956, 317.4527132478988847 ) ) ;
#32644=VERTEX_POINT ( 'NONE', #12216 ) ;
#32647=CARTESIAN_POINT ( 'NONE',  ( 745.7194118038753459, -157.6454272087893287, 348.7631598425976449 ) ) ;
#32653=CARTESIAN_POINT ( 'NONE',  ( 763.2262854647970016, -8.634602658420517329, 309.2812353651462445 ) ) ;
#32658=CARTESIAN_POINT ( 'NONE',  ( 765.0180583372156207, -24.99823902205683268, 360.0135310231089534 ) ) ;
#32659=CARTESIAN_POINT ( 'NONE',  ( 745.7194118038753459, -277.6454272087889308, 348.7631598425976449 ) ) ;
#32661=CARTESIAN_POINT ( 'NONE',  ( 751.9810565676468741, -218.0891481129653187, 360.9747183278973921 ) ) ;
#32665=CARTESIAN_POINT ( 'NONE',  ( 804.9363028652555840, -328.2709662947831362, 338.2165204200192079 ) ) ;
#32667=CARTESIAN_POINT ( 'NONE',  ( 804.1105419155481968, -99.82724539060768620, 347.6308680596136469 ) ) ;
#32669=CARTESIAN_POINT ( 'NONE',  ( 767.9999999999992042, 205.0000000000000568, 319.9999999999999432 ) ) ;
#32671=CARTESIAN_POINT ( 'NONE',  ( 754.9735926884551418, -162.3510508353235196, 340.5236548041000333 ) ) ;
#32672=CARTESIAN_POINT ( 'NONE',  ( 781.8018195045266339, -358.2709662947829088, 365.1927285166406705 ) ) ;
#32675=CARTESIAN_POINT ( 'NONE',  ( 785.3141322388236176, -141.7255117493291721, 364.4286716492789537 ) ) ;
#32678=CARTESIAN_POINT ( 'NONE',  ( 767.6429770376289525, 14.81994279612486309, 306.8695393053162093 ) ) ;
#32680=CARTESIAN_POINT ( 'NONE',  ( 771.2633955100217236, -335.9073299311468190, 363.4237431249939618 ) ) ;
#32684=CARTESIAN_POINT ( 'NONE',  ( 791.9812246680005501, -452.6346026584191691, 361.9419747391813189 ) ) ;
#32690=CARTESIAN_POINT ( 'NONE',  ( 800.2193346964447755, 5.001760977943074948, 355.1360043628815788 ) ) ;
#32691=CARTESIAN_POINT ( 'NONE',  ( 810.7187646348534145, -234.4527844766016358, 356.7737145352016341 ) ) ;
#32692=CARTESIAN_POINT ( 'NONE',  ( 793.2243759319678702, -146.5328690171417350, 318.4439275373583200 ) ) ;
#32695=ORIENTED_EDGE ( 'NONE', *, *, #23250, .F. ) ;
#32700=CARTESIAN_POINT ( 'NONE',  ( 808.3070685750230950, -162.9982390220563673, 361.1904061080339261 ) ) ;
#32701=CARTESIAN_POINT ( 'NONE',  ( 781.2370466360911223, -68.73633629969867798, 304.9990715423533629 ) ) ;
#32702=DIRECTION ( 'NONE',  ( -0.000000000000000000, 1.000000000000000000, -0.000000000000000000 ) ) ;
#32709=CARTESIAN_POINT ( 'NONE',  ( 779.4763451958990572, -392.7363362996977116, 365.0264073115438919 ) ) ;
#32714=CARTESIAN_POINT ( 'NONE',  ( 749.5768839229115201, -180.5545181178801499, 358.0661480581553064 ) ) ;
#32716=CARTESIAN_POINT ( 'NONE',  ( 796.9462024416508257, -132.4527844766018916, 308.9653473494370246 ) ) ;
#32720=CARTESIAN_POINT ( 'NONE',  ( 755.0636971347428243, -220.2709662947834772, 341.7834795799807353 ) ) ;
#32721=CARTESIAN_POINT ( 'NONE',  ( 804.6971507214547046, -27.28179084515336328, 344.0799538623459739 ) ) ;
#32725=CARTESIAN_POINT ( 'NONE',  ( 778.7502325331095108, -24.35105083532392811, 304.6391490659818828 ) ) ;
#32729=CARTESIAN_POINT ( 'NONE',  ( 756.3353852180819104, -29.90732993114771787, 331.1735550268788302 ) ) ;
#32732=CARTESIAN_POINT ( 'NONE',  ( 814.8230680027162407, -341.8055962898683333, 333.7305795820267917 ) ) ;
#32733=CARTESIAN_POINT ( 'NONE',  ( 788.8264449731201466, -165.1800572038745543, 363.6646147819170665 ) ) ;
#32736=CARTESIAN_POINT ( 'NONE',  ( 803.8556311672234642, -417.6237781080499190, 365.6418435158340117 ) ) ;
#32738=CARTESIAN_POINT ( 'NONE',  ( 788.7366044899766848, -347.9073299311467053, 316.5762568750059813 ) ) ;
#32745=CARTESIAN_POINT ( 'NONE',  ( 800.2193346964447755, -66.99823902205672255, 355.1360043628815788 ) ) ;
#32746=CARTESIAN_POINT ( 'NONE',  ( 793.0897708529556667, -366.5545181178795815, 361.3366627262616362 ) ) ;
#32747=CARTESIAN_POINT ( 'NONE',  ( 777.5031285880264704, -406.8164208402375266, 374.9108240113588408 ) ) ;
#32748=CARTESIAN_POINT ( 'NONE',  ( 748.3538107759620743, -304.7146871989594388, 355.8262568251490165 ) ) ;
#32749=CARTESIAN_POINT ( 'NONE',  ( 814.8230680027162407, -101.8055962898691718, 333.7305795820267917 ) ) ;
#32756=CARTESIAN_POINT ( 'NONE',  ( 767.6429770376289525, -417.1800572038736163, 306.8695393053162093 ) ) ;
#32762=CARTESIAN_POINT ( 'NONE',  ( 772.4468031744293057, -297.8272453906070041, 363.8651313633793620 ) ) ;
#32763=CARTESIAN_POINT ( 'NONE',  ( 797.8594530101008786, -157.5436935675108998, 322.1405469898980982 ) ) ;
#32768=CARTESIAN_POINT ( 'NONE',  ( 775.9200461376533440, -335.8055962898683902, 315.3028492785443291 ) ) ;
#32770=CARTESIAN_POINT ( 'NONE',  ( 764.1737431748507561, -82.37269993606227558, 371.6461892240376415 ) ) ;
#32772=CARTESIAN_POINT ( 'NONE',  ( 759.7806653035534055, -102.9982390220565520, 324.8639956371180801 ) ) ;
#32776=CARTESIAN_POINT ( 'NONE',  ( 804.6971507214547046, -3.281790845153435221, 344.0799538623459739 ) ) ;
#32779=CARTESIAN_POINT ( 'NONE',  ( 779.4709603349208464, -384.3510508353227806, 314.7162404726379918 ) ) ;
#32785=CARTESIAN_POINT ( 'NONE',  ( 756.1443688327750579, -237.6237781080505442, 314.3581564841659315 ) ) ;
#32786=CARTESIAN_POINT ( 'NONE',  ( 768.0187753319979720, -56.63460265842036279, 318.0580252608186242 ) ) ;
#32789=CARTESIAN_POINT ( 'NONE',  ( 803.4237431249931660, -231.1800572038743553, 331.2633955100225194 ) ) ;
#32796=CARTESIAN_POINT ( 'NONE',  ( 772.4837098697145166, -287.3618753856923718, 374.5518280994205611 ) ) ;
#32797=CARTESIAN_POINT ( 'NONE',  ( 749.8865473780648472, -20.53286901714212931, 322.1177392798429082 ) ) ;
#32803=CARTESIAN_POINT ( 'NONE',  ( 796.7737145352015204, -308.6346026584195670, 370.7187646348536987 ) ) ;
#32806=CARTESIAN_POINT ( 'NONE',  ( 800.9840315886518738, -220.9181544815164102, 354.1144889064786412 ) ) ;
#32809=CARTESIAN_POINT ( 'NONE',  ( 804.1105419155481968, -195.8272453906074304, 347.6308680596136469 ) ) ;
#32810=CARTESIAN_POINT ( 'NONE',  ( 797.8594530101008786, -61.54369356751124087, 322.1405469898980982 ) ) ;
#32815=CARTESIAN_POINT ( 'NONE',  ( 781.2370466360911223, -260.7363362996981095, 304.9990715423533629 ) ) ;
#32816=CARTESIAN_POINT ( 'NONE',  ( 786.6156483768007774, -217.4419599262324141, 315.5913626894246136 ) ) ;
#32819=CARTESIAN_POINT ( 'NONE',  ( 784.1219089521767955, -453.2817908451519315, 315.0488828828318333 ) ) ;
#32823=CARTESIAN_POINT ( 'NONE',  ( 758.8095938919642549, -32.08914811296588709, 311.6929314249763365 ) ) ;
#32824=CARTESIAN_POINT ( 'NONE',  ( 745.7998596910086917, -101.3618753856929544, 332.5602148656461168 ) ) ;
#32828=AXIS2_PLACEMENT_3D ( 'NONE', #7907, #3961, #11589 ) ;
#32829=CARTESIAN_POINT ( 'NONE',  ( 748.6759233522253680, -376.3726999360614514, 324.3348316497537098 ) ) ;
#32831=CARTESIAN_POINT ( 'NONE',  ( 808.3070685750230950, -378.9982390220555999, 361.1904061080339261 ) ) ;
#32834=CARTESIAN_POINT ( 'NONE',  ( 775.9200461376533440, 0.1944037101305369775, 315.3028492785443291 ) ) ;
#32835=CARTESIAN_POINT ( 'NONE',  ( 757.0176451133909268, -181.0999726633347109, 349.9200121543848354 ) ) ;
#32838=CARTESIAN_POINT ( 'NONE',  ( 788.7631598425961101, -121.4419599262327267, 305.7194118038759143 ) ) ;
#32839=CARTESIAN_POINT ( 'NONE',  ( 762.3223304703356007, -439.5436935675101040, 322.3223304703362828 ) ) ;
#32840=VECTOR ( 'NONE', #17448, 1000.000000000000000 ) ;
#32848=CARTESIAN_POINT ( 'NONE',  ( 797.6776695296629214, -259.5436935675106156, 357.6776695296636603 ) ) ;
#32849=CARTESIAN_POINT ( 'NONE',  ( 803.4237431249931660, -255.1800572038742700, 331.2633955100225194 ) ) ;
#32852=CARTESIAN_POINT ( 'NONE',  ( 761.2382568024794409, 8.376221891948691933, 356.9571628226838129 ) ) ;
#32854=CARTESIAN_POINT ( 'NONE',  ( 804.7487373415286811, -187.5436935675108430, 364.7487373415288516 ) ) ;
#32855=CARTESIAN_POINT ( 'NONE',  ( 798.5707757039680246, -269.4636090269708006, 356.7845633553585003 ) ) ;
#32858=CARTESIAN_POINT ( 'NONE',  ( 783.7566961878529810, -216.8965053807778816, 305.1792804349288417 ) ) ;
#32867=CARTESIAN_POINT ( 'NONE',  ( 783.0433043558608688, -264.8965053807776826, 315.1538015810313027 ) ) ;
#32871=FACE_OUTER_BOUND ( 'NONE', #31420, .T. ) ;
#32875=CARTESIAN_POINT ( 'NONE',  ( 811.3240766477731540, -172.3726999360619914, 355.6651683502462902 ) ) ;
#32882=CARTESIAN_POINT ( 'NONE',  ( 796.9462024416508257, -12.45278447660232146, 308.9653473494370246 ) ) ;
#32887=CARTESIAN_POINT ( 'NONE',  ( 755.5713283507202505, -53.36187538569310362, 334.6858677611754729 ) ) ;
#32889=CARTESIAN_POINT ( 'NONE',  ( 793.5525998758768083, -295.0999726633343698, 372.6845335610516941 ) ) ;
#32891=CARTESIAN_POINT ( 'NONE',  ( 746.8695393053150156, -245.9073299311469896, 327.6429770376306010 ) ) ;
#32896=CARTESIAN_POINT ( 'NONE',  ( 767.8955696845333705, -336.4527844766012095, 362.1676090361162323 ) ) ;
#32898=CARTESIAN_POINT ( 'NONE',  ( 804.6971507214547046, -99.28179084515313946, 344.0799538623459739 ) ) ;
#32902=LINE ( 'NONE', #1248, #7097 ) ;
#32903=CARTESIAN_POINT ( 'NONE',  ( 803.8556311672234642, -129.6237781080508853, 365.6418435158340117 ) ) ;
#32904=CARTESIAN_POINT ( 'NONE',  ( 759.2295555964440155, -160.1692326535053326, 353.9708237608231229 ) ) ;
#32905=CARTESIAN_POINT ( 'NONE',  ( 762.1405469898971887, -385.5436935675102745, 357.8594530101015607 ) ) ;
#32910=CARTESIAN_POINT ( 'NONE',  ( 755.0636971347428243, -148.2709662947837330, 341.7834795799807353 ) ) ;
#32914=CARTESIAN_POINT ( 'NONE',  ( 793.4146539503750546, -433.9874144716862361, 307.6481478633938877 ) ) ;
#32916=CARTESIAN_POINT ( 'NONE',  ( 803.4237431249931660, -375.1800572038739574, 331.2633955100225194 ) ) ;
#32927=CARTESIAN_POINT ( 'NONE',  ( 754.8072714833581358, -4.816420840238714085, 338.1981804954720587 ) ) ;
#32928=CARTESIAN_POINT ( 'NONE',  ( 763.0537975583475827, -216.4527844766016926, 371.0346526505627480 ) ) ;
#32929=CARTESIAN_POINT ( 'NONE',  ( 783.0433043558608688, -144.8965053807781089, 315.1538015810313027 ) ) ;
#32936=CARTESIAN_POINT ( 'NONE',  ( 783.7953271457878373, -56.19088175424417386, 375.1787889125761239 ) ) ;
#32945=CARTESIAN_POINT ( 'NONE',  ( 790.9844846989617508, -406.3726999360612808, 317.2208543904092721 ) ) ;
#32950=CARTESIAN_POINT ( 'NONE',  ( 811.3240766477731540, -172.3726999360619914, 355.6651683502462902 ) ) ;
#32952=CARTESIAN_POINT ( 'NONE',  ( 810.7187646348534145, -138.4527844766019200, 356.7737145352016341 ) ) ;
#32958=CARTESIAN_POINT ( 'NONE',  ( 791.9812246680005501, -236.6346026584198228, 361.9419747391813189 ) ) ;
#32959=CARTESIAN_POINT ( 'NONE',  ( 755.5913626894240451, -37.64542720878968396, 346.6156483768012890 ) ) ;
#32963=CARTESIAN_POINT ( 'NONE',  ( 773.7943932421234194, -23.80559628986938847, 305.5313806188329409 ) ) ;
#32964=ORIENTED_EDGE ( 'NONE', *, *, #29445, .T. ) ;
#32967=CARTESIAN_POINT ( 'NONE',  ( 756.5762568750052424, -27.18005720387500901, 348.7366044899774238 ) ) ;
#32970=CARTESIAN_POINT ( 'NONE',  ( 778.7502325331095108, -360.3510508353228374, 304.6391490659818828 ) ) ;
#32973=CARTESIAN_POINT ( 'NONE',  ( 758.0141637701419768, -423.0783235625953580, 367.2620300519063790 ) ) ;
#32975=CARTESIAN_POINT ( 'NONE',  ( 797.6776695296629214, -355.5436935675103882, 357.6776695296636603 ) ) ;
#32985=CARTESIAN_POINT ( 'NONE',  ( 756.5762568750052424, -75.18005720387485269, 348.7366044899774238 ) ) ;
#32986=CARTESIAN_POINT ( 'NONE',  ( 763.0428371773158460, -371.4636090269705164, 358.7617431975195359 ) ) ;
#32989=CARTESIAN_POINT ( 'NONE',  ( 747.2067596250078623, -411.1800572038738437, 352.2312462859687230 ) ) ;
#32990=CARTESIAN_POINT ( 'NONE',  ( 783.7566961878529810, -336.8965053807774552, 305.1792804349288417 ) ) ;
#32991=CARTESIAN_POINT ( 'NONE',  ( 744.8212110874229666, -90.89650538077827946, 336.2046728542121627 ) ) ;
#32994=LINE ( 'NONE', #16489, #24307 ) ;
#32997=CARTESIAN_POINT ( 'NONE',  ( 758.8095938919642549, -416.0891481129645513, 311.6929314249763365 ) ) ;
#33003=CARTESIAN_POINT ( 'NONE',  ( 793.0897708529556667, -294.5545181178797520, 361.3366627262616362 ) ) ;
#33004=CARTESIAN_POINT ( 'NONE',  ( 771.1735550268778070, -153.1800572038746395, 316.3353852180827630 ) ) ;
#33007=CARTESIAN_POINT ( 'NONE',  ( 802.7791456095903868, -340.7146871989592114, 329.0155153010375102 ) ) ;
#33008=AXIS2_PLACEMENT_3D ( 'NONE', #2648, #29076, #39723 ) ;
#33009=DIRECTION ( 'NONE',  ( 0.000000000000000000, 0.000000000000000000, -1.000000000000000000 ) ) ;
#33011=CARTESIAN_POINT ( 'NONE',  ( 745.5313806188320314, -63.28179084515324604, 333.7943932421247268 ) ) ;
#33013=CARTESIAN_POINT ( 'NONE',  ( 801.1904061080336987, -212.0891481129652902, 368.3070685750235498 ) ) ;
#33014=CARTESIAN_POINT ( 'NONE',  ( 756.3353852180819104, -125.9073299311474159, 331.1735550268788302 ) ) ;
#33018=CARTESIAN_POINT ( 'NONE',  ( 757.4527132478984868, -16.37269993606248519, 329.1273215169538844 ) ) ;
#33021=CARTESIAN_POINT ( 'NONE',  ( 756.7813123517142913, -403.9874144716863498, 329.9779781133712504 ) ) ;
#33023=CARTESIAN_POINT ( 'NONE',  ( 787.6308680596127942, -83.26014174441466764, 364.1105419155492768 ) ) ;
#33028=CARTESIAN_POINT ( 'NONE',  ( 768.8385539511368734, -239.2601417444141987, 306.4236121716840557 ) ) ;
#33029=CARTESIAN_POINT ( 'NONE',  ( 755.0636971347428243, -52.27096629478401724, 341.7834795799807353 ) ) ;
#33031=CARTESIAN_POINT ( 'NONE',  ( 778.1981804954714335, -250.2709662947832783, 314.8072714833589885 ) ) ;
#33038=CARTESIAN_POINT ( 'NONE',  ( 777.4774526936600978, -274.2709662947832499, 304.7301800767028226 ) ) ;
#33040=CARTESIAN_POINT ( 'NONE',  ( 766.5853460496234675, -37.98741447168752927, 372.3518521366060554 ) ) ;
#33048=CARTESIAN_POINT ( 'NONE',  ( 748.9653473494363425, -314.6346026584194533, 356.9462024416521331 ) ) ;
#33051=CARTESIAN_POINT ( 'NONE',  ( 763.0428371773158460, -203.4636090269709996, 358.7617431975195359 ) ) ;
#33052=CARTESIAN_POINT ( 'NONE',  ( 794.9819416627830151, -60.99823902205671544, 319.9864689768909898 ) ) ;
#33056=CARTESIAN_POINT ( 'NONE',  ( 765.8855110935204493, -238.1692326535050768, 319.0159684113471599 ) ) ;
#33059=CARTESIAN_POINT ( 'NONE',  ( 814.5518280994195948, -447.7255117493280636, 332.4837098697145734 ) ) ;
#33063=CARTESIAN_POINT ( 'NONE',  ( 787.5162901302840055, -35.36187538569316047, 305.4481719005792684 ) ) ;
#33064=CARTESIAN_POINT ( 'NONE',  ( 759.0252816721024374, -120.9982390220565378, 368.0189434323527280 ) ) ;
#33066=CARTESIAN_POINT ( 'NONE',  ( 760.0363995740630116, -394.9181544815158418, 368.7758568127991907 ) ) ;
#33068=CARTESIAN_POINT ( 'NONE',  ( 808.0189434323515343, -350.0891481129648923, 319.0252816721025511 ) ) ;
#33070=CARTESIAN_POINT ( 'NONE',  ( 803.6646147819161570, -449.9073299311463643, 348.8264449731210561 ) ) ;
#33073=CARTESIAN_POINT ( 'NONE',  ( 749.8865473780648472, -140.5328690171417634, 322.1177392798429082 ) ) ;
#33074=CARTESIAN_POINT ( 'NONE',  ( 791.9812246680005501, -452.6346026584191691, 361.9419747391813189 ) ) ;
#33075=CIRCLE ( 'NONE', #2090, 10.00000000000000888 ) ;
#33076=CARTESIAN_POINT ( 'NONE',  ( 746.0683387631852383, -163.4419599262325846, 331.3260364891676204 ) ) ;
#33080=CARTESIAN_POINT ( 'NONE',  ( 754.8072714833581358, -124.8164208402383508, 338.1981804954720587 ) ) ;
#33083=CARTESIAN_POINT ( 'NONE',  ( 805.1927285166397041, -256.8164208402379245, 341.8018195045277707 ) ) ;
#33084=CARTESIAN_POINT ( 'NONE',  ( 758.0580252608178853, -270.4527844766014937, 328.0187753319985404 ) ) ;
#33086=ORIENTED_EDGE ( 'NONE', *, *, #24162, .F. ) ;
#33087=CARTESIAN_POINT ( 'NONE',  ( 766.7756240680305382, 9.467130982857780097, 361.5560724626415663 ) ) ;
#33089=CARTESIAN_POINT ( 'NONE',  ( 747.2067596250078623, -171.1800572038745543, 352.2312462859687230 ) ) ;
#33090=CARTESIAN_POINT ( 'NONE',  ( 787.5531968255692163, -309.8272453906070041, 316.1348686366205811 ) ) ;
#33091=CARTESIAN_POINT ( 'NONE',  ( 804.9511171171677688, -389.8055962898682765, 335.8780910478229202 ) ) ;
#33098=CARTESIAN_POINT ( 'NONE',  ( 758.6633372737375112, -260.5328690171413086, 326.9102291470432533 ) ) ;
#33099=CARTESIAN_POINT ( 'NONE',  ( 759.9999999999992042, -462.9681489794448339, 317.6393202250019954 ) ) ;
#33105=CARTESIAN_POINT ( 'NONE',  ( 786.2694204179717872, -165.2817908451529547, 305.1769319972829067 ) ) ;
#33116=CARTESIAN_POINT ( 'NONE',  ( 767.8955696845333705, -48.45278447660219712, 362.1676090361162323 ) ) ;
#33117=CARTESIAN_POINT ( 'NONE',  ( 809.0717654672305343, -268.9181544815162397, 360.1688906516309885 ) ) ;
#33119=CARTESIAN_POINT ( 'NONE',  ( 744.7301800767019131, -268.8164208402378108, 337.4774526936615757 ) ) ;
#33122=CARTESIAN_POINT ( 'NONE',  ( 772.4999999999993179, -512.9681489794448908, 309.9999999999998863 ) ) ;
#33123=CARTESIAN_POINT ( 'NONE',  ( 762.1405469898971887, -361.5436935675103882, 357.8594530101015607 ) ) ;
#33124=CARTESIAN_POINT ( 'NONE',  ( 783.0745993439762742, -128.1908817542439465, 365.1016975059196739 ) ) ;
#33128=CARTESIAN_POINT ( 'NONE',  ( 767.8955696845333705, -408.4527844766009252, 362.1676090361162323 ) ) ;
#33131=CARTESIAN_POINT ( 'NONE',  ( 800.0135310231082713, -158.0891481129655176, 325.0180583372163028 ) ) ;
#33133=FACE_OUTER_BOUND ( 'NONE', #40016, .T. ) ;
#33135=CARTESIAN_POINT ( 'NONE',  ( 764.8639956371174549, -344.0891481129647786, 319.7806653035542013 ) ) ;
#33141=CARTESIAN_POINT ( 'NONE',  ( 759.0252816721024374, -96.99823902205660886, 368.0189434323527280 ) ) ;
#33146=CARTESIAN_POINT ( 'NONE',  ( 788.8264449731200330, 2.819942796124898177, 363.6646147819171233 ) ) ;
#33147=CARTESIAN_POINT ( 'NONE',  ( 769.1273215169530886, -166.7146871989598367, 317.4527132478988847 ) ) ;
#33148=CARTESIAN_POINT ( 'NONE',  ( 772.4999999999993179, -512.9681489794448908, 350.0000000000000000 ) ) ;
#33155=CARTESIAN_POINT ( 'NONE',  ( 747.6481478633932056, -85.09997266333499510, 353.4146539503763620 ) ) ;
#33156=CARTESIAN_POINT ( 'NONE',  ( 759.9999999999992042, -462.9681489794448339, 309.9999999999998863 ) ) ;
#33165=CARTESIAN_POINT ( 'NONE',  ( 804.1105419155481968, -411.8272453906067199, 347.6308680596136469 ) ) ;
#33167=CARTESIAN_POINT ( 'NONE',  ( 761.4292242960306112, -233.4636090269708575, 323.2154366446414429 ) ) ;
#33171=CARTESIAN_POINT ( 'NONE',  ( 744.6391490659812007, -182.7363362996983369, 338.7502325331110455 ) ) ;
#33173=CARTESIAN_POINT ( 'NONE',  ( 767.7687537140311633, -143.9073299311473590, 372.7932403749916830 ) ) ;
#33177=CARTESIAN_POINT ( 'NONE',  ( 767.8955696845333705, -264.4527844766016074, 362.1676090361162323 ) ) ;
#33178=CARTESIAN_POINT ( 'NONE',  ( 793.9708237608222134, -22.91815448151701062, 319.2295555964448681 ) ) ;
#33184=CARTESIAN_POINT ( 'NONE',  ( 746.7653713866222915, -41.26014174441479554, 351.0478386215610271 ) ) ;
#33187=CARTESIAN_POINT ( 'NONE',  ( 804.9363028652555840, -16.27096629478413092, 338.2165204200192079 ) ) ;
#33190=CARTESIAN_POINT ( 'NONE',  ( 745.1769319972822814, -329.8055962898683902, 346.2694204179732083 ) ) ;
#33193=CARTESIAN_POINT ( 'NONE',  ( 794.9819416627830151, -324.9982390220559409, 319.9864689768909898 ) ) ;
#33198=ORIENTED_EDGE ( 'NONE', *, *, #25832, .F. ) ;
#33201=CARTESIAN_POINT ( 'NONE',  ( 788.8264449731200330, -69.18005720387488111, 363.6646147819171233 ) ) ;
#33202=CARTESIAN_POINT ( 'NONE',  ( 776.9254006560222479, -356.1908817542432075, 314.8983024940802125 ) ) ;
#33203=CARTESIAN_POINT ( 'NONE',  ( 805.0032342141413437, -421.5436935675101040, 314.9967657858572352 ) ) ;
#33205=CARTESIAN_POINT ( 'NONE',  ( 761.9338519418445230, -326.5328690171411381, 370.4231160770881957 ) ) ;
#33207=CARTESIAN_POINT ( 'NONE',  ( 745.1769319972822814, -89.80559628986918597, 346.2694204179732083 ) ) ;
#33211=CARTESIAN_POINT ( 'NONE',  ( 772.5602148656447525, -417.7255117493283478, 305.7998596910095443 ) ) ;
#33212=PLANE ( 'NONE',  #34415 ) ;
#33218=CARTESIAN_POINT ( 'NONE',  ( 755.1538015810308480, -302.1908817542433781, 343.0433043558613804 ) ) ;
#33222=CARTESIAN_POINT ( 'NONE',  ( 746.4236121716829757, -87.82724539060770041, 328.8385539511384650 ) ) ;
#33225=CARTESIAN_POINT ( 'NONE',  ( 803.4237431249931660, -111.1800572038747532, 331.2633955100225194 ) ) ;
#33228=CARTESIAN_POINT ( 'NONE',  ( 772.4468031744293057, -9.827245390607961539, 363.8651313633793620 ) ) ;
#33231=CARTESIAN_POINT ( 'NONE',  ( 766.7756240680305382, -398.5328690171409107, 361.5560724626415663 ) ) ;
#33235=CARTESIAN_POINT ( 'NONE',  ( 812.6845335610512393, -247.9874144716867761, 353.5525998758768651 ) ) ;
#33236=CARTESIAN_POINT ( 'NONE',  ( 755.3201227861273992, -51.72551174932947049, 345.3687786644892981 ) ) ;
#33239=CARTESIAN_POINT ( 'NONE',  ( 757.8323909638827445, -218.6346026584197944, 352.1044303154654358 ) ) ;
#33245=CARTESIAN_POINT ( 'NONE',  ( 812.7932403749906598, -327.1800572038741279, 327.7687537140311633 ) ) ;
#33246=CARTESIAN_POINT ( 'NONE',  ( 795.6651683502461765, -34.71468719896025590, 371.3240766477733814 ) ) ;
#33251=CARTESIAN_POINT ( 'NONE',  ( 785.3687786644884454, -227.3618753856925707, 315.3201227861279676 ) ) ;
#33254=CARTESIAN_POINT ( 'NONE',  ( 763.0537975583475827, -336.4527844766012095, 371.0346526505627480 ) ) ;
#33256=CARTESIAN_POINT ( 'NONE',  ( 803.8651313633788504, -365.2601417444137155, 332.4468031744301015 ) ) ;
#33259=CARTESIAN_POINT ( 'NONE',  ( 759.0159684113467620, -208.9181544815164102, 325.8855110935213020 ) ) ;
#33260=CARTESIAN_POINT ( 'NONE',  ( 791.9812246680005501, -68.63460265842033436, 361.9419747391813189 ) ) ;
#33264=CARTESIAN_POINT ( 'NONE',  ( 773.3843516231979720, -229.4419599262323572, 364.4086373105754433 ) ) ;
#33267=CARTESIAN_POINT ( 'NONE',  ( 813.1304606946830518, -425.9073299311463074, 352.3570229623690580 ) ) ;
#33271=CARTESIAN_POINT ( 'NONE',  ( 796.7737145352015204, -44.63460265842040542, 370.7187646348536987 ) ) ;
#33272=CARTESIAN_POINT ( 'NONE',  ( 755.2512626584698410, -127.5436935675110561, 315.2512626584710915 ) ) ;
#33276=CARTESIAN_POINT ( 'NONE',  ( 782.4968714119720516, -370.8164208402375834, 305.0891759886411023 ) ) ;
#33278=CARTESIAN_POINT ( 'NONE',  ( 766.7756240680305382, 9.467130982857780097, 361.5560724626415663 ) ) ;
#33279=CARTESIAN_POINT ( 'NONE',  ( 755.8894580844503253, -207.8272453906073451, 332.3691319403863531 ) ) ;
#33282=CARTESIAN_POINT ( 'NONE',  ( 778.7502325331095108, -144.3510508353235764, 304.6391490659818828 ) ) ;
#33283=CARTESIAN_POINT ( 'NONE',  ( 758.0580252608178853, -438.4527844766009821, 328.0187753319985404 ) ) ;
#33287=CARTESIAN_POINT ( 'NONE',  ( 785.3687786644884454, -131.3618753856928834, 315.3201227861279676 ) ) ;
#33289=CARTESIAN_POINT ( 'NONE',  ( 759.7806653035534055, -270.9982390220561115, 324.8639956371180801 ) ) ;
#33290=CARTESIAN_POINT ( 'NONE',  ( 785.3141322388236176, -261.7255117493288026, 364.4286716492789537 ) ) ;
#33293=CARTESIAN_POINT ( 'NONE',  ( 790.8726784830453198, 13.28531280103958423, 362.5472867521010585 ) ) ;
#33297=CARTESIAN_POINT ( 'NONE',  ( 796.9462024416508257, -180.4527844766017495, 308.9653473494370246 ) ) ;
#33298=CARTESIAN_POINT ( 'NONE',  ( 790.9844846989617508, -286.3726999360617356, 317.2208543904092721 ) ) ;
#33299=CARTESIAN_POINT ( 'NONE',  ( 800.7704444035546203, -388.1692326535045936, 326.0291762391768771 ) ) ;
#33306=CARTESIAN_POINT ( 'NONE',  ( 770.0799878456142551, -277.9874144716867477, 362.9823548866085616 ) ) ;
#33317=CARTESIAN_POINT ( 'NONE',  ( 804.7487373415286811, -19.54369356751139364, 364.7487373415288516 ) ) ;
#33322=CARTESIAN_POINT ( 'NONE',  ( 762.3223304703356007, -31.54369356751135456, 322.3223304703362828 ) ) ;
#33323=CARTESIAN_POINT ( 'NONE',  ( 805.6418435158337843, -269.4636090269708006, 363.8556311672236916 ) ) ;
#33324=CARTESIAN_POINT ( 'NONE',  ( 763.0537975583475827, -264.4527844766016074, 371.0346526505627480 ) ) ;
#33328=CARTESIAN_POINT ( 'NONE',  ( 804.4286716492782716, -353.3618753856922012, 345.3141322388244703 ) ) ;
#33329=CARTESIAN_POINT ( 'NONE',  ( 757.0176451133909268, -109.0999726633349241, 349.9200121543848354 ) ) ;
#33331=PLANE ( 'NONE',  #12921 ) ;
#33333=CARTESIAN_POINT ( 'NONE',  ( 814.8230680027162407, -125.8055962898690581, 333.7305795820267917 ) ) ;
#33334=CARTESIAN_POINT ( 'NONE',  ( 791.9812246680005501, -380.6346026584192828, 361.9419747391813189 ) ) ;
#33335=ORIENTED_EDGE ( 'NONE', *, *, #31752, .F. ) ;
#33337=CARTESIAN_POINT ( 'NONE',  ( 759.7806653035534055, -150.9982390220563957, 324.8639956371180801 ) ) ;
#33342=CARTESIAN_POINT ( 'NONE',  ( 791.9812246680005501, -356.6346026584193964, 361.9419747391813189 ) ) ;
#33347=CARTESIAN_POINT ( 'NONE',  ( 745.7998596910086917, -77.36187538569302546, 332.5602148656461168 ) ) ;
#33353=CARTESIAN_POINT ( 'NONE',  ( 767.7687537140311633, -263.9073299311469327, 372.7932403749916830 ) ) ;
#33354=CARTESIAN_POINT ( 'NONE',  ( 783.0433043558608688, -168.8965053807780237, 315.1538015810313027 ) ) ;
#33361=CARTESIAN_POINT ( 'NONE',  ( 805.6418435158337843, -53.46360902697146855, 363.8556311672236916 ) ) ;
#33367=CYLINDRICAL_SURFACE ( 'NONE', #29660, 30.00000000000008171 ) ;
#33370=CARTESIAN_POINT ( 'NONE',  ( 775.8780910478218402, -417.2817908451522158, 364.9511171171680530 ) ) ;
#33373=CARTESIAN_POINT ( 'NONE',  ( 799.9999999999993179, 205.0000000000000568, 360.0000000000000000 ) ) ;
#33374=LINE ( 'NONE', #1719, #29776 ) ;
#33376=CARTESIAN_POINT ( 'NONE',  ( 813.5763878283155464, -195.8272453906074304, 351.1614460488615350 ) ) ;
#33378=CARTESIAN_POINT ( 'NONE',  ( 758.8095938919642549, -152.0891481129655460, 311.6929314249763365 ) ) ;
#33381=CARTESIAN_POINT ( 'NONE',  ( 754.8072714833581358, -244.8164208402378961, 338.1981804954720587 ) ) ;
#33383=CARTESIAN_POINT ( 'NONE',  ( 796.9571628226829034, -23.46360902697155026, 321.2382568024804641 ) ) ;
#33388=CARTESIAN_POINT ( 'NONE',  ( 803.2186876482843445, -79.98741447168740137, 350.0220218866286928 ) ) ;
#33393=CARTESIAN_POINT ( 'NONE',  ( 803.4237431249931660, -63.18005720387488822, 331.2633955100225194 ) ) ;
#33396=CARTESIAN_POINT ( 'NONE',  ( 746.7653713866222915, -353.2601417444137724, 351.0478386215610271 ) ) ;
#33399=CARTESIAN_POINT ( 'NONE',  ( 767.8955696845333705, -336.4527844766012095, 362.1676090361162323 ) ) ;
#33408=CARTESIAN_POINT ( 'NONE',  ( 797.8594530101008786, -109.5436935675110988, 322.1405469898980982 ) ) ;
#33409=CARTESIAN_POINT ( 'NONE',  ( 769.0155153010367712, -370.3726999360613377, 362.7791456095907279 ) ) ;
#33410=CARTESIAN_POINT ( 'NONE',  ( 751.9810565676468741, -434.0891481129646081, 360.9747183278973921 ) ) ;
#33411=DIRECTION ( 'NONE',  ( 1.000000000000000000, 0.000000000000000000, 0.000000000000000000 ) ) ;
#33412=CARTESIAN_POINT ( 'NONE',  ( 793.4146539503750546, -313.9874144716866908, 307.6481478633938877 ) ) ;
#33413=CARTESIAN_POINT ( 'NONE',  ( 771.2368401574024119, -109.4419599262327836, 374.2805881961240857 ) ) ;
#33417=EDGE_CURVE ( 'NONE', #22578, #23899, #11343, .T. ) ;
#33418=CARTESIAN_POINT ( 'NONE',  ( 813.1304606946830518, -425.9073299311463074, 352.3570229623690580 ) ) ;
#33425=CARTESIAN_POINT ( 'NONE',  ( 804.4086373105744769, -289.6454272087889308, 333.3843516231986541 ) ) ;
#33426=CARTESIAN_POINT ( 'NONE',  ( 755.0636971347428243, -172.2709662947836478, 341.7834795799807353 ) ) ;
#33429=DIRECTION ( 'NONE',  ( 0.000000000000000000, 0.000000000000000000, -1.000000000000000000 ) ) ;
#33430=CARTESIAN_POINT ( 'NONE',  ( 815.3608509340175488, -74.73633629969866377, 341.2497674668889545 ) ) ;
#33433=CARTESIAN_POINT ( 'NONE',  ( 762.1405469898971887, -145.5436935675109851, 357.8594530101015607 ) ) ;
#33440=CARTESIAN_POINT ( 'NONE',  ( 775.8780910478218402, -9.281790845153418346, 364.9511171171680530 ) ) ;
#33442=DIRECTION ( 'NONE',  ( 0.000000000000000000, 0.000000000000000000, 1.000000000000000000 ) ) ;
#33443=CARTESIAN_POINT ( 'NONE',  ( 798.7617431975189675, -387.6237781080499758, 323.0428371773161871 ) ) ;
#33449=CARTESIAN_POINT ( 'NONE',  ( 764.3348316497523456, -238.7146871989596661, 308.6759233522265617 ) ) ;
#33450=CARTESIAN_POINT ( 'NONE',  ( 758.0580252608178853, -102.4527844766020337, 328.0187753319985404 ) ) ;
#33453=CARTESIAN_POINT ( 'NONE',  ( 774.6858677611749044, -249.7255117493288594, 315.5713283507209894 ) ) ;
#33457=ORIENTED_EDGE ( 'NONE', *, *, #23239, .T. ) ;
#33461=CARTESIAN_POINT ( 'NONE',  ( 796.9462024416508257, -324.4527844766013231, 308.9653473494370246 ) ) ;
#33462=CARTESIAN_POINT ( 'NONE',  ( 756.1443688327750579, -45.62377810805114109, 314.3581564841659315 ) ) ;
#33469=CARTESIAN_POINT ( 'NONE',  ( 795.1360043628807261, -212.0891481129652902, 360.2193346964456282 ) ) ;
#33472=CARTESIAN_POINT ( 'NONE',  ( 814.9108240113580450, -328.2709662947831362, 337.5031285880265273 ) ) ;
#33477=CARTESIAN_POINT ( 'NONE',  ( 783.0745993439762742, -176.1908817542438328, 365.1016975059196739 ) ) ;
#33478=CARTESIAN_POINT ( 'NONE',  ( 785.3687786644884454, -83.36187538569296862, 315.3201227861279676 ) ) ;
#33482=CARTESIAN_POINT ( 'NONE',  ( 790.8726784830453198, -250.7146871989595809, 362.5472867521010585 ) ) ;
#33486=CARTESIAN_POINT ( 'NONE',  ( 792.2312462859673587, -419.9073299311465348, 307.2067596250082602 ) ) ;
#33490=CARTESIAN_POINT ( 'NONE',  ( 805.0032342141412300, -61.54369356751124087, 314.9967657858571783 ) ) ;
#33491=CARTESIAN_POINT ( 'NONE',  ( 772.4837098697144029, -143.3618753856927697, 374.5518280994205611 ) ) ;
#33496=CARTESIAN_POINT ( 'NONE',  ( 812.7932403749906598, -375.1800572038739574, 327.7687537140311633 ) ) ;
#33499=CARTESIAN_POINT ( 'NONE',  ( 755.0488828828309806, 6.194403710130517382, 344.1219089521771934 ) ) ;
#33504=CARTESIAN_POINT ( 'NONE',  ( 783.7566961878529810, -144.8965053807781089, 305.1792804349288417 ) ) ;
#33505=CARTESIAN_POINT ( 'NONE',  ( 800.2193346964446619, -450.9982390220554294, 355.1360043628816925 ) ) ;
#33506=CARTESIAN_POINT ( 'NONE',  ( 783.7566961878529810, -168.8965053807780237, 305.1792804349288417 ) ) ;
#33511=CARTESIAN_POINT ( 'NONE',  ( 781.8018195045266339, -142.2709662947837330, 365.1927285166406705 ) ) ;
#33513=CARTESIAN_POINT ( 'NONE',  ( 755.0636971347428243, -268.2709662947833067, 341.7834795799807353 ) ) ;
#33516=CARTESIAN_POINT ( 'NONE',  ( 765.8855110935204493, 25.83076734649409545, 319.0159684113471599 ) ) ;
#33521=CARTESIAN_POINT ( 'NONE',  ( 810.7187646348534145, -234.4527844766016358, 356.7737145352016341 ) ) ;
#33522=CARTESIAN_POINT ( 'NONE',  ( 784.1219089521767955, -309.2817908451525568, 315.0488828828318333 ) ) ;
#33523=CARTESIAN_POINT ( 'NONE',  ( 779.4709603349208464, -408.3510508353227806, 314.7162404726379918 ) ) ;
#33531=CARTESIAN_POINT ( 'NONE',  ( 789.9200121543843807, -289.9874144716866908, 317.0176451133914384 ) ) ;
#33535=CARTESIAN_POINT ( 'NONE',  ( 791.9812246680005501, 3.365397341579444479, 361.9419747391813189 ) ) ;
#33538=VECTOR ( 'NONE', #41346, 1000.000000000000000 ) ;
#33539=CARTESIAN_POINT ( 'NONE',  ( 807.2620300519052989, -216.0090635724255037, 318.0141637701419768 ) ) ;
#33544=CARTESIAN_POINT ( 'NONE',  ( 763.2262854647970016, -32.63460265842044095, 309.2812353651462445 ) ) ;
#33548=CARTESIAN_POINT ( 'NONE',  ( 759.7806653035534055, -54.99823902205672255, 324.8639956371180801 ) ) ;
#33549=CARTESIAN_POINT ( 'NONE',  ( 748.6759233522253680, -304.3726999360615082, 324.3348316497537098 ) ) ;
#33550=CARTESIAN_POINT ( 'NONE',  ( 748.9653473494363425, -242.6346026584197659, 356.9462024416521331 ) ) ;
#33556=CARTESIAN_POINT ( 'NONE',  ( 794.9819416627830151, -348.9982390220558273, 319.9864689768909898 ) ) ;
#33557=CARTESIAN_POINT ( 'NONE',  ( 790.9844846989617508, -118.3726999360621619, 317.2208543904092721 ) ) ;
#33561=CARTESIAN_POINT ( 'NONE',  ( 762.1405469898971887, -409.5436935675101040, 357.8594530101015607 ) ) ;
#33566=CARTESIAN_POINT ( 'NONE',  ( 755.3201227861273992, -171.7255117493291152, 345.3687786644892981 ) ) ;
#33567=CARTESIAN_POINT ( 'NONE',  ( 755.5713283507202505, -173.3618753856927128, 334.6858677611754729 ) ) ;
#33571=CARTESIAN_POINT ( 'NONE',  ( 756.3353852180819104, -365.9073299311465917, 331.1735550268788302 ) ) ;
#33576=CARTESIAN_POINT ( 'NONE',  ( 745.7998596910086917, -125.3618753856928834, 332.5602148656461168 ) ) ;
#33580=ORIENTED_EDGE ( 'NONE', *, *, #31202, .T. ) ;
#33583=CARTESIAN_POINT ( 'NONE',  ( 746.8695393053150156, -245.9073299311469896, 327.6429770376306010 ) ) ;
#33584=CARTESIAN_POINT ( 'NONE',  ( 803.8651313633788504, -173.2601417444143692, 332.4468031744301015 ) ) ;
#33588=EDGE_LOOP ( 'NONE', ( #25800, #26241, #29150, #36044 ) ) ;
#33593=CARTESIAN_POINT ( 'NONE',  ( 748.6759233522253680, -88.37269993606226137, 324.3348316497537098 ) ) ;
#33602=CARTESIAN_POINT ( 'NONE',  ( 780.5236548040995785, -428.7363362996975980, 314.9735926884559944 ) ) ;
#33605=CARTESIAN_POINT ( 'NONE',  ( 796.1575198192839480, -246.0090635724253900, 359.4546378042384163 ) ) ;
#33607=LINE ( 'NONE', #12374, #9138 ) ;
#33610=CARTESIAN_POINT ( 'NONE',  ( 810.4231160770870019, -168.5545181178802352, 321.9338519418446936 ) ) ;
#33612=CARTESIAN_POINT ( 'NONE',  ( 747.2067596250078623, -147.1800572038746395, 352.2312462859687230 ) ) ;
#33615=CARTESIAN_POINT ( 'NONE',  ( 762.3223304703356007, 16.45630643248849267, 322.3223304703362828 ) ) ;
#33616=CARTESIAN_POINT ( 'NONE',  ( 778.1981804954714335, -250.2709662947832783, 314.8072714833589885 ) ) ;
#33617=CARTESIAN_POINT ( 'NONE',  ( 754.7162404726377645, -38.73633629969877035, 339.4709603349214717 ) ) ;
#33623=CARTESIAN_POINT ( 'NONE',  ( 765.8855110935204493, -94.16923265350555994, 319.0159684113471599 ) ) ;
#33627=CARTESIAN_POINT ( 'NONE',  ( 755.5713283507202505, -53.36187538569310362, 334.6858677611754729 ) ) ;
#33630=CARTESIAN_POINT ( 'NONE',  ( 744.8212110874229666, -378.8965053807772847, 336.2046728542121627 ) ) ;
#33633=CARTESIAN_POINT ( 'NONE',  ( 781.8018195045266339, -358.2709662947829088, 365.1927285166406705 ) ) ;
#33641=CARTESIAN_POINT ( 'NONE',  ( 762.1405469898971887, -97.54369356751112718, 357.8594530101015607 ) ) ;
#33642=CARTESIAN_POINT ( 'NONE',  ( 790.0220218866281812, -391.0999726633340288, 363.2186876482849129 ) ) ;
#33644=CARTESIAN_POINT ( 'NONE',  ( 758.8095938919644823, -440.0891481129645513, 311.6929314249762797 ) ) ;
#33646=CARTESIAN_POINT ( 'NONE',  ( 788.7631598425961101, -337.4419599262319593, 305.7194118038759143 ) ) ;
#33647=CARTESIAN_POINT ( 'NONE',  ( 748.3538107759620743, -112.7146871989600356, 355.8262568251490165 ) ) ;
#33651=CARTESIAN_POINT ( 'NONE',  ( 745.1792804349281596, -14.19088175424431242, 343.7566961878542884 ) ) ;
#33659=VECTOR ( 'NONE', #16377, 1000.000000000000000 ) ;
#33661=CARTESIAN_POINT ( 'NONE',  ( 773.4516893846965786, -283.6454272087889308, 315.8398074228977066 ) ) ;
#33662=CARTESIAN_POINT ( 'NONE',  ( 758.0580252608178853, -174.4527844766018063, 328.0187753319985404 ) ) ;
#33664=CARTESIAN_POINT ( 'NONE',  ( 766.4474001241216001, -283.0999726633344267, 307.3154664389482491 ) ) ;
#33667=CARTESIAN_POINT ( 'NONE',  ( 768.9521613784389729, -81.82724539060772884, 373.2346286133773106 ) ) ;
#33671=CARTESIAN_POINT ( 'NONE',  ( 788.8264449731200330, -141.1800572038746395, 363.6646147819171233 ) ) ;
#33675=CARTESIAN_POINT ( 'NONE',  ( 786.5483106153019435, -7.645427208789786100, 364.1601925771022366 ) ) ;
#33677=CARTESIAN_POINT ( 'NONE',  ( 779.9999999999992042, 126.4563064324884465, 339.9999999999999432 ) ) ;
#33678=CARTESIAN_POINT ( 'NONE',  ( 766.7756240680305382, -422.5328690171408539, 361.5560724626415663 ) ) ;
#33683=CARTESIAN_POINT ( 'NONE',  ( 812.6845335610512393, -223.9874144716869182, 353.5525998758768651 ) ) ;
#33684=CARTESIAN_POINT ( 'NONE',  ( 781.8018195045267476, -94.27096629478387513, 365.1927285166407273 ) ) ;
#33685=ORIENTED_EDGE ( 'NONE', *, *, #41968, .F. ) ;
#33689=CARTESIAN_POINT ( 'NONE',  ( 788.7366044899766848, -251.9073299311470748, 316.5762568750059813 ) ) ;
#33696=CARTESIAN_POINT ( 'NONE',  ( 751.9810565676468741, -338.0891481129649492, 360.9747183278973921 ) ) ;
#33697=CARTESIAN_POINT ( 'NONE',  ( 786.2056067578752163, -227.8055962898687596, 374.4686193811670023 ) ) ;
#33698=CARTESIAN_POINT ( 'NONE',  ( 803.8556311672234642, -33.62377810805116951, 365.6418435158340117 ) ) ;
#33703=CARTESIAN_POINT ( 'NONE',  ( 804.6798772138708955, -207.7255117493289447, 334.6312213355107019 ) ) ;
#33707=CARTESIAN_POINT ( 'NONE',  ( 796.7737145352015204, -332.6346026584195101, 370.7187646348536987 ) ) ;
#33713=CARTESIAN_POINT ( 'NONE',  ( 760.7433823573367135, -204.0090635724255606, 355.9930595647440441 ) ) ;
#33714=CARTESIAN_POINT ( 'NONE',  ( 788.8264449731200330, -69.18005720387488111, 363.6646147819171233 ) ) ;
#33718=CARTESIAN_POINT ( 'NONE',  ( 760.5453621957607311, -261.0783235625959264, 323.8424801807151425 ) ) ;
#33721=CARTESIAN_POINT ( 'NONE',  ( 777.4774526936600978, -418.2709662947827383, 304.7301800767027657 ) ) ;
#33727=CARTESIAN_POINT ( 'NONE',  ( 801.1904061080336987, -92.08914811296568814, 368.3070685750235498 ) ) ;
#33728=CARTESIAN_POINT ( 'NONE',  ( 763.2262854647970016, -128.6346026584201354, 309.2812353651462445 ) ) ;
#33732=CARTESIAN_POINT ( 'NONE',  ( 745.7998596910086917, -389.3618753856919739, 332.5602148656461168 ) ) ;
#33733=CARTESIAN_POINT ( 'NONE',  ( 808.0189434323515343, -14.08914811296595460, 319.0252816721025511 ) ) ;
#33735=CARTESIAN_POINT ( 'NONE',  ( 801.3366627262608972, 15.46713098285775878, 353.0897708529566899 ) ) ;
#33739=CARTESIAN_POINT ( 'NONE',  ( 814.8230680027162407, -125.8055962898690581, 333.7305795820267917 ) ) ;
#33745=CARTESIAN_POINT ( 'NONE',  ( 759.9864689768902508, -146.0891481129655176, 354.9819416627836404 ) ) ;
#33747=CARTESIAN_POINT ( 'NONE',  ( 788.8264449731201466, -285.1800572038741279, 363.6646147819170665 ) ) ;
#33750=CARTESIAN_POINT ( 'NONE',  ( 805.0264073115434940, 17.64894916467593688, 339.4763451958999099 ) ) ;
#33754=CARTESIAN_POINT ( 'NONE',  ( 767.6429770376291799, -225.1800572038743553, 306.8695393053162093 ) ) ;
#33755=CARTESIAN_POINT ( 'NONE',  ( 800.9840315886518738, -316.9181544815160692, 354.1144889064786412 ) ) ;
#33756=CARTESIAN_POINT ( 'NONE',  ( 775.9200461376533440, -407.8055962898681628, 315.3028492785443291 ) ) ;
#33757=VERTEX_POINT ( 'NONE', #38943 ) ;
#33766=CARTESIAN_POINT ( 'NONE',  ( 763.2154366446407039, -309.6237781080502600, 321.4292242960311228 ) ) ;
#33773=CARTESIAN_POINT ( 'NONE',  ( 810.4231160770870019, -216.5545181178800931, 321.9338519418446936 ) ) ;
#33778=CARTESIAN_POINT ( 'NONE',  ( 787.4397851343537695, -45.72551174932949181, 374.2001403089903988 ) ) ;
#33781=CARTESIAN_POINT ( 'NONE',  ( 804.6798772138708955, -39.72551174932951312, 334.6312213355107019 ) ) ;
#33783=CARTESIAN_POINT ( 'NONE',  ( 757.7880784355613741, -330.0090635724251342, 312.4576283171834916 ) ) ;
#33784=CARTESIAN_POINT ( 'NONE',  ( 754.9967657858570647, -265.5436935675106156, 365.0032342141425374 ) ) ;
#33788=CARTESIAN_POINT ( 'NONE',  ( 785.3687786644884454, -371.3618753856919739, 315.3201227861279676 ) ) ;
#33789=CARTESIAN_POINT ( 'NONE',  ( 760.7433823573367135, -108.0090635724258448, 355.9930595647440441 ) ) ;
#33791=CARTESIAN_POINT ( 'NONE',  ( 756.5762568750052424, -387.1800572038738437, 348.7366044899774238 ) ) ;
#33792=DIRECTION ( 'NONE',  ( 0.000000000000000000, -1.000000000000000000, 0.000000000000000000 ) ) ;
#33793=DIRECTION ( 'NONE',  ( -1.000000000000000000, -0.000000000000000000, 0.000000000000000000 ) ) ;
#33794=CARTESIAN_POINT ( 'NONE',  ( 792.1044303154645831, -396.4527844766010389, 317.8323909638837677 ) ) ;
#33797=CARTESIAN_POINT ( 'NONE',  ( 781.7834795799800531, -202.8164208402380950, 315.0636971347436202 ) ) ;
#33798=CARTESIAN_POINT ( 'NONE',  ( 754.8072714833583632, -148.8164208402382656, 338.1981804954721156 ) ) ;
#33802=CARTESIAN_POINT ( 'NONE',  ( 759.9864689768902508, -362.0891481129648923, 354.9819416627836404 ) ) ;
#33806=CARTESIAN_POINT ( 'NONE',  ( 810.7187646348534145, -114.4527844766020053, 356.7737145352016341 ) ) ;
#33813=CARTESIAN_POINT ( 'NONE',  ( 814.2001403089898304, -257.3618753856924286, 347.4397851343538264 ) ) ;
#33814=CARTESIAN_POINT ( 'NONE',  ( 760.5453621957607311, -189.0783235625961822, 323.8424801807151425 ) ) ;
#33824=CARTESIAN_POINT ( 'NONE',  ( 754.3581564841646241, -89.46360902697134065, 316.1443688327762516 ) ) ;
#33833=CARTESIAN_POINT ( 'NONE',  ( 761.4292242960306112, -449.4636090269702322, 323.2154366446414429 ) ) ;
#33839=CARTESIAN_POINT ( 'NONE',  ( 745.1792804349281596, -230.1908817542436338, 343.7566961878542884 ) ) ;
#33841=CARTESIAN_POINT ( 'NONE',  ( 782.4968714119720516, -154.8164208402382371, 305.0891759886411023 ) ) ;
#33844=CARTESIAN_POINT ( 'NONE',  ( 771.2633955100217236, -263.9073299311469327, 363.4237431249939618 ) ) ;
#33845=CARTESIAN_POINT ( 'NONE',  ( 784.1219089521767955, -45.28179084515329578, 315.0488828828318333 ) ) ;
#33850=CARTESIAN_POINT ( 'NONE',  ( 804.1601925771018387, -79.44195992623286884, 346.5483106153029098 ) ) ;
#33851=CARTESIAN_POINT ( 'NONE',  ( 795.1360043628807261, -308.0891481129650629, 360.2193346964456282 ) ) ;
#33852=ORIENTED_EDGE ( 'NONE', *, *, #37624, .F. ) ;
#33854=CARTESIAN_POINT ( 'NONE',  ( 774.6312213355099630, -47.36187538569312494, 364.6798772138717482 ) ) ;
#33857=CARTESIAN_POINT ( 'NONE',  ( 810.1134526219336749, -392.5328690171409107, 357.8822607201570349 ) ) ;
#33858=EDGE_LOOP ( 'NONE', ( #23525, #11982, #30170, #5743 ) ) ;
#33859=CARTESIAN_POINT ( 'NONE',  ( 792.2312462859673587, 12.09267006885214180, 307.2067596250082602 ) ) ;
#33861=CARTESIAN_POINT ( 'NONE',  ( 804.6798772138708955, -375.7255117493283478, 334.6312213355107019 ) ) ;
#33868=CARTESIAN_POINT ( 'NONE',  ( 774.6312213355099630, -95.36187538569294020, 364.6798772138717482 ) ) ;
#33869=CARTESIAN_POINT ( 'NONE',  ( 755.3028492785439312, -399.2817908451522726, 335.9200461376539693 ) ) ;
#33870=CARTESIAN_POINT ( 'NONE',  ( 777.4774526936600978, -418.2709662947828519, 304.7301800767028226 ) ) ;
#33872=CARTESIAN_POINT ( 'NONE',  ( 768.8385539511368734, -311.2601417444139429, 306.4236121716840557 ) ) ;
#33877=CARTESIAN_POINT ( 'NONE',  ( 815.2698199232961542, -448.8164208402371855, 342.5225473063383106 ) ) ;
#33883=CARTESIAN_POINT ( 'NONE',  ( 801.5560724626406000, -336.5545181178796952, 326.7756240680316182 ) ) ;
#33884=CARTESIAN_POINT ( 'NONE',  ( 788.8264449731200330, -189.1800572038744122, 363.6646147819171233 ) ) ;
#33886=CARTESIAN_POINT ( 'NONE',  ( 762.1177392798416577, -306.5545181178797520, 309.8865473780659272 ) ) ;
#33889=CARTESIAN_POINT ( 'NONE',  ( 812.3518521366052028, -121.0999726633348956, 326.5853460496235243 ) ) ;
#33892=CARTESIAN_POINT ( 'NONE',  ( 804.9363028652555840, -160.2709662947836762, 338.2165204200192079 ) ) ;
#33894=CARTESIAN_POINT ( 'NONE',  ( 786.2694204179717872, -405.2817908451522158, 305.1769319972829067 ) ) ;
#33897=CARTESIAN_POINT ( 'NONE',  ( 769.0155153010367712, -58.37269993606236085, 362.7791456095907279 ) ) ;
#33900=CARTESIAN_POINT ( 'NONE',  ( 764.0069404352550464, -423.0783235625953580, 359.2566176426627180 ) ) ;
#33902=CARTESIAN_POINT ( 'NONE',  ( 804.9511171171677688, -77.80559628986920018, 335.8780910478229202 ) ) ;
#33905=CARTESIAN_POINT ( 'NONE',  ( 810.1134526219336749, -272.5328690171413086, 357.8822607201570349 ) ) ;
#33906=CARTESIAN_POINT ( 'NONE',  ( 804.9363028652555840, -88.27096629478390355, 338.2165204200192079 ) ) ;
#33907=ORIENTED_EDGE ( 'NONE', *, *, #2999, .F. ) ;
#33909=CARTESIAN_POINT ( 'NONE',  ( 788.8264449731200330, -261.1800572038741848, 363.6646147819171233 ) ) ;
#33917=CARTESIAN_POINT ( 'NONE',  ( 814.5518280994195948, -327.7255117493285752, 332.4837098697145166 ) ) ;
#33918=CARTESIAN_POINT ( 'NONE',  ( 747.3154664389472828, -211.9874144716869750, 326.4474001241230781 ) ) ;
#33923=CARTESIAN_POINT ( 'NONE',  ( 755.3201227861273992, -219.7255117493289447, 345.3687786644892981 ) ) ;
#33926=CARTESIAN_POINT ( 'NONE',  ( 792.3570229623688874, -357.1800572038739006, 373.1304606946836202 ) ) ;
#33930=CARTESIAN_POINT ( 'NONE',  ( 799.2566176426618085, -216.0090635724255037, 324.0069404352559559 ) ) ;
#33931=CARTESIAN_POINT ( 'NONE',  ( 771.2633955100217236, -71.90732993114760063, 363.4237431249939618 ) ) ;
#33935=CARTESIAN_POINT ( 'NONE',  ( 796.7845633553578182, -273.6237781080504305, 358.5707757039688204 ) ) ;
#33938=CARTESIAN_POINT ( 'NONE',  ( 763.2262854647970016, -440.6346026584191122, 309.2812353651462445 ) ) ;
#33942=CARTESIAN_POINT ( 'NONE',  ( 796.7737145352015204, -68.63460265842033436, 370.7187646348536987 ) ) ;
#33944=CARTESIAN_POINT ( 'NONE',  ( 754.9967657858570647, -145.5436935675109851, 365.0032342141425374 ) ) ;
#33948=CARTESIAN_POINT ( 'NONE',  ( 813.5763878283155464, -411.8272453906067199, 351.1614460488615350 ) ) ;
#33950=CARTESIAN_POINT ( 'NONE',  ( 748.9653473494363425, -410.6346026584191122, 356.9462024416521331 ) ) ;
#33951=CARTESIAN_POINT ( 'NONE',  ( 747.2067596250078623, -27.18005720387500901, 352.2312462859687230 ) ) ;
#33953=CARTESIAN_POINT ( 'NONE',  ( 772.3691319403857278, -23.26014174441484883, 315.8894580844506663 ) ) ;
#33956=CARTESIAN_POINT ( 'NONE',  ( 795.6651683502461765, -154.7146871989598935, 371.3240766477733814 ) ) ;
#33960=CARTESIAN_POINT ( 'NONE',  ( 788.7366044899766848, -179.9073299311472454, 316.5762568750059813 ) ) ;
#33964=CARTESIAN_POINT ( 'NONE',  ( 805.1927285166399315, -304.8164208402376971, 341.8018195045277707 ) ) ;
#33967=CARTESIAN_POINT ( 'NONE',  ( 780.5290396650775619, -12.35105083532396897, 365.2837595273619513 ) ) ;
#33972=CARTESIAN_POINT ( 'NONE',  ( 796.7737145352015204, -236.6346026584198228, 370.7187646348536987 ) ) ;
#33973=CARTESIAN_POINT ( 'NONE',  ( 798.5707757039680246, -317.4636090269706301, 356.7845633553585003 ) ) ;
#33974=CARTESIAN_POINT ( 'NONE',  ( 775.9200461376533440, -383.8055962898682765, 315.3028492785443291 ) ) ;
#33981=CARTESIAN_POINT ( 'NONE',  ( 770.0799878456142551, -301.9874144716867477, 362.9823548866085616 ) ) ;
#33982=DIRECTION ( 'NONE',  ( -1.000000000000000000, -0.000000000000000000, 0.000000000000000000 ) ) ;
#33984=CARTESIAN_POINT ( 'NONE',  ( 778.1981804954714335, 13.72903370521577138, 314.8072714833589885 ) ) ;
#33992=CARTESIAN_POINT ( 'NONE',  ( 812.7932403749906598, -39.18005720387496638, 327.7687537140311633 ) ) ;
#33995=DIRECTION ( 'NONE',  ( 0.000000000000000000, -1.000000000000000000, 0.000000000000000000 ) ) ;
#33996=CARTESIAN_POINT ( 'NONE',  ( 766.4474001241216001, -331.0999726633342561, 307.3154664389482491 ) ) ;
#33998=CARTESIAN_POINT ( 'NONE',  ( 805.0032342141412300, -301.5436935675105588, 314.9967657858571783 ) ) ;
#34002=CARTESIAN_POINT ( 'NONE',  ( 805.1927285166397041, -376.8164208402375834, 341.8018195045277707 ) ) ;
#34003=CARTESIAN_POINT ( 'NONE',  ( 802.5472867521000353, -124.3726999360621619, 350.8726784830461156 ) ) ;
#34005=CARTESIAN_POINT ( 'NONE',  ( 749.8865473780648472, -44.53286901714205470, 322.1177392798429082 ) ) ;
#34006=CARTESIAN_POINT ( 'NONE',  ( 804.4286716492782716, -353.3618753856922012, 345.3141322388244703 ) ) ;
#34007=CARTESIAN_POINT ( 'NONE',  ( 812.7932403749906598, 8.819942796124882634, 327.7687537140311633 ) ) ;
#34010=CARTESIAN_POINT ( 'NONE',  ( 778.1981804954714335, -418.2709662947827383, 314.8072714833589885 ) ) ;
#34014=CARTESIAN_POINT ( 'NONE',  ( 781.7834795799800531, -178.8164208402381519, 315.0636971347436202 ) ) ;
#34015=CARTESIAN_POINT ( 'NONE',  ( 771.1735550268780344, -177.1800572038744974, 316.3353852180828198 ) ) ;
#34017=CARTESIAN_POINT ( 'NONE',  ( 759.9999999999992042, -462.9681489794448339, 309.9999999999998863 ) ) ;
#34018=ORIENTED_EDGE ( 'NONE', *, *, #15390, .F. ) ;
#34019=CARTESIAN_POINT ( 'NONE',  ( 794.9819416627830151, -396.9982390220556567, 319.9864689768909898 ) ) ;
#34020=ORIENTED_EDGE ( 'NONE', *, *, #39704, .T. ) ;
#34023=CARTESIAN_POINT ( 'NONE',  ( 811.0346526505617248, -134.6346026584201070, 323.0537975583478101 ) ) ;
#34029=CARTESIAN_POINT ( 'NONE',  ( 777.5031285880264704, -262.8164208402379245, 374.9108240113588408 ) ) ;
#34030=CARTESIAN_POINT ( 'NONE',  ( 803.8651313633788504, -197.2601417444143124, 332.4468031744301015 ) ) ;
#34032=LINE ( 'NONE', #20850, #10044 ) ;
#34034=ORIENTED_EDGE ( 'NONE', *, *, #29262, .T. ) ;
#34041=CARTESIAN_POINT ( 'NONE',  ( 795.8262568251477660, -118.3726999360621619, 308.3538107759623585 ) ) ;
#34046=DIRECTION ( 'NONE',  ( 0.000000000000000000, 1.000000000000000000, 0.000000000000000000 ) ) ;
#34049=CARTESIAN_POINT ( 'NONE',  ( 796.9571628226829034, -431.4636090269702322, 321.2382568024804641 ) ) ;
#34056=CARTESIAN_POINT ( 'NONE',  ( 750.9282345327678740, -208.9181544815164102, 319.8311093483690115 ) ) ;
#34058=CARTESIAN_POINT ( 'NONE',  ( 811.0346526505616112, -182.6346026584199649, 323.0537975583477532 ) ) ;
#34061=CARTESIAN_POINT ( 'NONE',  ( 754.8072714833581358, -268.8164208402378108, 338.1981804954720587 ) ) ;
#34062=CARTESIAN_POINT ( 'NONE',  ( 755.5913626894240451, -61.64542720878961291, 346.6156483768012890 ) ) ;
#34067=CARTESIAN_POINT ( 'NONE',  ( 802.7791456095903868, -76.71468719896012090, 329.0155153010375102 ) ) ;
#34070=CARTESIAN_POINT ( 'NONE',  ( 797.6776695296629214, -67.54369356751125508, 357.6776695296636603 ) ) ;
#34074=CARTESIAN_POINT ( 'NONE',  ( 815.0009284576459549, -366.3510508353228374, 338.7629533639073429 ) ) ;
#34077=CARTESIAN_POINT ( 'NONE',  ( 754.8072714833581358, -388.8164208402374129, 338.1981804954720587 ) ) ;
#34083=CARTESIAN_POINT ( 'NONE',  ( 797.6776695296629214, -91.54369356751116982, 357.6776695296636603 ) ) ;
#34084=CARTESIAN_POINT ( 'NONE',  ( 772.4468031744293057, -417.8272453906067199, 363.8651313633793620 ) ) ;
#34085=CARTESIAN_POINT ( 'NONE',  ( 747.2067596250078623, -435.1800572038737869, 352.2312462859687230 ) ) ;
#34086=CARTESIAN_POINT ( 'NONE',  ( 799.9999999999993179, -512.9681489794448908, 350.0000000000000000 ) ) ;
#34087=CARTESIAN_POINT ( 'NONE',  ( 800.1688906516307043, -346.1692326535047641, 369.0717654672308186 ) ) ;
#34092=CARTESIAN_POINT ( 'NONE',  ( 795.1271208383656131, -452.8379544210779954, 371.6178728169206238 ) ) ;
#34093=CARTESIAN_POINT ( 'NONE',  ( 791.0733055594794223, 17.05262341476191068, 312.1184307474205184 ) ) ;
#34098=CARTESIAN_POINT ( 'NONE',  ( 802.5472867521000353, -316.3726999360615082, 350.8726784830461156 ) ) ;
#34099=CARTESIAN_POINT ( 'NONE',  ( 771.2633955100217236, -191.9073299311471885, 363.4237431249939618 ) ) ;
#34101=CARTESIAN_POINT ( 'NONE',  ( 750.9282345327678740, -304.9181544815161828, 319.8311093483690115 ) ) ;
#34104=CARTESIAN_POINT ( 'NONE',  ( 771.3260364891663130, -115.6454272087894424, 306.0683387631859773 ) ) ;
#34108=CARTESIAN_POINT ( 'NONE',  ( 756.5762568750052424, -147.1800572038746395, 348.7366044899774238 ) ) ;
#34110=CARTESIAN_POINT ( 'NONE',  ( 766.4474001241216001, -427.0999726633338582, 307.3154664389482491 ) ) ;
#34113=CARTESIAN_POINT ( 'NONE',  ( 775.8780910478218402, -57.28179084515326736, 364.9511171171680530 ) ) ;
#34116=CARTESIAN_POINT ( 'NONE',  ( 759.2295555964440155, -424.1692326535044799, 353.9708237608231229 ) ) ;
#34121=CARTESIAN_POINT ( 'NONE',  ( 798.0661480581538854, -290.5328690171412518, 309.5768839229118043 ) ) ;
#34122=CARTESIAN_POINT ( 'NONE',  ( 801.9419747391806368, -90.45278447660209054, 351.9812246680014027 ) ) ;
#34125=CARTESIAN_POINT ( 'NONE',  ( 755.5713283507202505, -269.3618753856924286, 334.6858677611754729 ) ) ;
#34131=CARTESIAN_POINT ( 'NONE',  ( 801.1904061080338124, -332.0891481129649492, 368.3070685750236066 ) ) ;
#34132=CARTESIAN_POINT ( 'NONE',  ( 773.7943932421234194, -263.8055962898686175, 305.5313806188329409 ) ) ;
#34136=CARTESIAN_POINT ( 'NONE',  ( 778.2165204200184689, -214.8164208402380666, 364.9363028652563230 ) ) ;
#34138=CARTESIAN_POINT ( 'NONE',  ( 814.2001403089898304, -353.3618753856922012, 347.4397851343538264 ) ) ;
#34140=CARTESIAN_POINT ( 'NONE',  ( 772.1467562141141343, 16.45630643248850689, 315.9110025235851253 ) ) ;
#34142=CARTESIAN_POINT ( 'NONE',  ( 802.9823548866075953, -217.0999726633345972, 330.0799878456151077 ) ) ;
#34143=CARTESIAN_POINT ( 'NONE',  ( 755.0636971347428243, -100.2709662947838609, 341.7834795799807353 ) ) ;
#34146=CIRCLE ( 'NONE', #6136, 10.00000000000000888 ) ;
#34148=CARTESIAN_POINT ( 'NONE',  ( 793.2243759319678702, -242.5328690171414507, 318.4439275373583200 ) ) ;
#34151=CARTESIAN_POINT ( 'NONE',  ( 757.7880784355613741, -18.00906357242611477, 312.4576283171834916 ) ) ;
#34155=CARTESIAN_POINT ( 'NONE',  ( 754.9967657858570647, -97.54369356751112718, 365.0032342141425374 ) ) ;
#34156=CARTESIAN_POINT ( 'NONE',  ( 792.2312462859673587, -131.9073299311473875, 307.2067596250082602 ) ) ;
#34158=DIRECTION ( 'NONE',  ( -1.000000000000000000, -0.000000000000000000, -0.000000000000000000 ) ) ;
#34161=CARTESIAN_POINT ( 'NONE',  ( 754.3581564841646241, -425.4636090269703459, 316.1443688327762516 ) ) ;
#34164=CARTESIAN_POINT ( 'NONE',  ( 815.2698199232961542, -400.8164208402373561, 342.5225473063383106 ) ) ;
#34165=CARTESIAN_POINT ( 'NONE',  ( 782.4968714119720516, -10.81642084023869543, 305.0891759886411023 ) ) ;
#34167=CARTESIAN_POINT ( 'NONE',  ( 757.2208543904082489, -16.71468719896031985, 350.9844846989624330 ) ) ;
#34170=CARTESIAN_POINT ( 'NONE',  ( 815.0009284576459549, -174.3510508353234627, 338.7629533639073429 ) ) ;
#34171=CARTESIAN_POINT ( 'NONE',  ( 778.1981804954715471, 13.72903370521577315, 314.8072714833591021 ) ) ;
#34172=CARTESIAN_POINT ( 'NONE',  ( 800.1688906516307043, -178.1692326535052473, 369.0717654672308186 ) ) ;
#34176=CARTESIAN_POINT ( 'NONE',  ( 756.3353852180819104, -149.9073299311473875, 331.1735550268788302 ) ) ;
#34178=CARTESIAN_POINT ( 'NONE',  ( 800.0135310231082713, -302.0891481129650629, 325.0180583372163028 ) ) ;
#34181=ORIENTED_EDGE ( 'NONE', *, *, #29510, .T. ) ;
#34182=CARTESIAN_POINT ( 'NONE',  ( 786.6156483768007774, -25.44195992623301450, 315.5913626894246136 ) ) ;
#34187=CARTESIAN_POINT ( 'NONE',  ( 811.0346526505617248, -206.6346026584198796, 323.0537975583478101 ) ) ;
#34188=CARTESIAN_POINT ( 'NONE',  ( 755.1538015810308480, -326.1908817542433781, 343.0433043558613804 ) ) ;
#34189=CARTESIAN_POINT ( 'NONE',  ( 770.0799878456142551, -421.9874144716863498, 362.9823548866085616 ) ) ;
#34191=VERTEX_POINT ( 'NONE', #34017 ) ;
#34198=CARTESIAN_POINT ( 'NONE',  ( 760.5453621957607311, -309.0783235625957559, 323.8424801807151425 ) ) ;
#34199=CARTESIAN_POINT ( 'NONE',  ( 793.3938497862117174, -453.0432664090020580, 372.3358127763067955 ) ) ;
#34201=CARTESIAN_POINT ( 'NONE',  ( 769.9779781133707957, -115.0999726633348956, 316.7813123517150871 ) ) ;
#34203=ORIENTED_EDGE ( 'NONE', *, *, #26099, .F. ) ;
#34205=CARTESIAN_POINT ( 'NONE',  ( 804.1009440267234822, -215.4636090269709712, 314.0944755984392600 ) ) ;
#34209=CARTESIAN_POINT ( 'NONE',  ( 811.0346526505616112, -38.63460265842041252, 323.0537975583477532 ) ) ;
#34213=FACE_OUTER_BOUND ( 'NONE', #6179, .T. ) ;
#34214=CARTESIAN_POINT ( 'NONE',  ( 807.2620300519052989, -336.0090635724251911, 318.0141637701419768 ) ) ;
#34216=CARTESIAN_POINT ( 'NONE',  ( 814.2001403089898304, -281.3618753856923718, 347.4397851343538264 ) ) ;
#34221=CARTESIAN_POINT ( 'NONE',  ( 794.9819416627830151, -396.9982390220556567, 319.9864689768909898 ) ) ;
#34222=CARTESIAN_POINT ( 'NONE',  ( 804.8461984189677878, -170.1908817542438328, 336.9566956441385628 ) ) ;
#34224=CARTESIAN_POINT ( 'NONE',  ( 805.9055244015594326, -75.62377810805104161, 315.8990559732753240 ) ) ;
#34225=CARTESIAN_POINT ( 'NONE',  ( 788.7366044899766848, -371.9073299311465917, 316.5762568750059813 ) ) ;
#34227=( NAMED_UNIT ( * ) SI_UNIT ( $, .STERADIAN. ) SOLID_ANGLE_UNIT ( ) );
#34228=CARTESIAN_POINT ( 'NONE',  ( 755.5713283507202505, -437.3618753856919170, 334.6858677611754729 ) ) ;
#34233=CARTESIAN_POINT ( 'NONE',  ( 778.1981804954714335, -178.2709662947835625, 314.8072714833589885 ) ) ;
#34234=CARTESIAN_POINT ( 'NONE',  ( 802.1676090361155502, -182.6346026584199649, 327.8955696845344505 ) ) ;
#34238=CARTESIAN_POINT ( 'NONE',  ( 781.8018195045266339, -406.2709662947829088, 365.1927285166406705 ) ) ;
#34241=DIRECTION ( 'NONE',  ( 0.000000000000000000, 0.000000000000000000, 1.000000000000000000 ) ) ;
#34243=CARTESIAN_POINT ( 'NONE',  ( 745.7998596910086917, -101.3618753856929544, 332.5602148656461168 ) ) ;
#34246=ORIENTED_EDGE ( 'NONE', *, *, #59, .F. ) ;
#34253=CARTESIAN_POINT ( 'NONE',  ( 770.0799878456142551, -205.9874144716870035, 362.9823548866085616 ) ) ;
#34263=CARTESIAN_POINT ( 'NONE',  ( 764.1737431748507561, -106.3726999360621903, 371.6461892240376415 ) ) ;
#34273=CARTESIAN_POINT ( 'NONE',  ( 790.9844846989617508, -430.3726999360611671, 317.2208543904092721 ) ) ;
#34281=CARTESIAN_POINT ( 'NONE',  ( 814.8207195650702488, -218.1908817542437191, 336.2433038121456548 ) ) ;
#34283=CARTESIAN_POINT ( 'NONE',  ( 759.0252816721024374, -192.9982390220562820, 368.0189434323527280 ) ) ;
#34289=CARTESIAN_POINT ( 'NONE',  ( 764.8639956371174549, -296.0891481129650629, 319.7806653035542013 ) ) ;
#34291=CARTESIAN_POINT ( 'NONE',  ( 805.2837595273609850, -50.73633629969874193, 340.5290396650784714 ) ) ;
#34296=CARTESIAN_POINT ( 'NONE',  ( 798.7617431975189675, -75.62377810805104161, 323.0428371773161871 ) ) ;
#34297=CARTESIAN_POINT ( 'NONE',  ( 774.6312213355099630, -335.3618753856920307, 364.6798772138717482 ) ) ;
#34300=CARTESIAN_POINT ( 'NONE',  ( 788.8264449731200330, -45.18005720387493085, 363.6646147819171233 ) ) ;
#34304=CARTESIAN_POINT ( 'NONE',  ( 813.2346286133761168, -365.2601417444137155, 328.9521613784389160 ) ) ;
#34306=CARTESIAN_POINT ( 'NONE',  ( 804.4286716492782716, -281.3618753856923718, 345.3141322388244703 ) ) ;
#34308=CARTESIAN_POINT ( 'NONE',  ( 804.7487373415286811, 4.456306432488530866, 364.7487373415288516 ) ) ;
#34309=ADVANCED_FACE ( 'NONE', ( #33133, #40300 ), #12340, .T. ) ;
#34312=CARTESIAN_POINT ( 'NONE',  ( 757.8323909638827445, -386.6346026584191691, 352.1044303154654358 ) ) ;
#34316=ORIENTED_EDGE ( 'NONE', *, *, #43568, .T. ) ;
#34319=CARTESIAN_POINT ( 'NONE',  ( 785.3687786644884454, -83.36187538569296862, 315.3201227861279676 ) ) ;
#34320=CARTESIAN_POINT ( 'NONE',  ( 769.9779781133707957, -403.0999726633339719, 316.7813123517150871 ) ) ;
#34321=CARTESIAN_POINT ( 'NONE',  ( 761.2382568024794409, -87.62377810805102740, 356.9571628226838129 ) ) ;
#34322=LINE ( 'NONE', #31085, #27724 ) ;
#34324=CARTESIAN_POINT ( 'NONE',  ( 791.1614460488616487, -347.2601417444138860, 373.5763878283158874 ) ) ;
#34329=CARTESIAN_POINT ( 'NONE',  ( 764.1737431748507561, -10.37269993606250473, 371.6461892240376415 ) ) ;
#34330=VECTOR ( 'NONE', #40587, 1000.000000000000000 ) ;
#34338=CARTESIAN_POINT ( 'NONE',  ( 804.1105419155481968, -315.8272453906070609, 347.6308680596136469 ) ) ;
#34341=CARTESIAN_POINT ( 'NONE',  ( 799.9636004259356241, -310.9181544815160123, 311.2241431872006956 ) ) ;
#34345=CARTESIAN_POINT ( 'NONE',  ( 813.5763878283155464, -123.8272453906076009, 351.1614460488615350 ) ) ;
#34350=CARTESIAN_POINT ( 'NONE',  ( 791.9812246680005501, -140.6346026584201070, 361.9419747391813189 ) ) ;
#34352=CARTESIAN_POINT ( 'NONE',  ( 804.1009440267234822, -407.4636090269703459, 314.0944755984392600 ) ) ;
#34355=CARTESIAN_POINT ( 'NONE',  ( 763.0428371773158460, -59.46360902697142592, 358.7617431975195359 ) ) ;
#34358=CARTESIAN_POINT ( 'NONE',  ( 787.6308680596127942, -419.2601417444136587, 364.1105419155492768 ) ) ;
#34360=CARTESIAN_POINT ( 'NONE',  ( 757.8323909638827445, -266.6346026584197375, 352.1044303154654358 ) ) ;
#34363=CARTESIAN_POINT ( 'NONE',  ( 752.4576283171824116, -261.0783235625959264, 317.7880784355627952 ) ) ;
#34364=CARTESIAN_POINT ( 'NONE',  ( 756.3353852180820240, -101.9073299311474869, 331.1735550268787733 ) ) ;
#34368=CARTESIAN_POINT ( 'NONE',  ( 757.8323909638827445, -266.6346026584197375, 352.1044303154654358 ) ) ;
#34370=CARTESIAN_POINT ( 'NONE',  ( 792.1975848984933464, -449.0899794596732022, 370.7630750413119927 ) ) ;
#34377=CARTESIAN_POINT ( 'NONE',  ( 744.7301800767020268, -364.8164208402375266, 337.4774526936615189 ) ) ;
#34378=CARTESIAN_POINT ( 'NONE',  ( 747.3154664389472828, -259.9874144716869182, 326.4474001241230781 ) ) ;
#34382=CARTESIAN_POINT ( 'NONE',  ( 788.7366044899766848, -227.9073299311471033, 316.5762568750059813 ) ) ;
#34384=CARTESIAN_POINT ( 'NONE',  ( 772.5602148656447525, -345.7255117493285184, 305.7998596910095443 ) ) ;
#34387=CARTESIAN_POINT ( 'NONE',  ( 770.1068079863199500, 16.45630643248850333, 316.7980005127122922 ) ) ;
#34389=CARTESIAN_POINT ( 'NONE',  ( 763.8424801807145741, -234.0090635724255037, 320.5453621957614700 ) ) ;
#34390=CARTESIAN_POINT ( 'NONE',  ( 759.9864689768902508, -122.0891481129656171, 354.9819416627836404 ) ) ;
#34394=CARTESIAN_POINT ( 'NONE',  ( 761.2382568024794409, -255.6237781080504874, 356.9571628226838129 ) ) ;
#34398=CARTESIAN_POINT ( 'NONE',  ( 810.4231160770870019, -0.5545181178807169209, 321.9338519418446936 ) ) ;
#34402=CARTESIAN_POINT ( 'NONE',  ( 745.4481719005789273, -99.72551174932928575, 347.5162901302853129 ) ) ;
#34403=CARTESIAN_POINT ( 'NONE',  ( 814.2001403089898304, -185.3618753856926844, 347.4397851343538264 ) ) ;
#34408=CARTESIAN_POINT ( 'NONE',  ( 749.5768839229115201, -420.5545181178793541, 358.0661480581553064 ) ) ;
#34411=CARTESIAN_POINT ( 'NONE',  ( 754.9967657858570647, -385.5436935675102745, 365.0032342141425374 ) ) ;
#34412=CARTESIAN_POINT ( 'NONE',  ( 763.0537975583476964, -24.45278447660228949, 371.0346526505628617 ) ) ;
#34415=AXIS2_PLACEMENT_3D ( 'NONE', #1549, #12632, #15646 ) ;
#34416=CARTESIAN_POINT ( 'NONE',  ( 802.7791456095903868, -28.71468719896028077, 329.0155153010375102 ) ) ;
#34419=CARTESIAN_POINT ( 'NONE',  ( 758.0141637701419768, -183.0783235625961538, 367.2620300519063790 ) ) ;
#34420=CARTESIAN_POINT ( 'NONE',  ( 766.5853460496234675, -181.9874144716870887, 372.3518521366060554 ) ) ;
#34425=CARTESIAN_POINT ( 'NONE',  ( 771.2633955100217236, -167.9073299311473022, 363.4237431249939618 ) ) ;
#34427=CARTESIAN_POINT ( 'NONE',  ( 759.7806653035534055, -294.9982390220560546, 324.8639956371180801 ) ) ;
#34428=CARTESIAN_POINT ( 'NONE',  ( 765.0180583372156207, -288.9982390220559978, 360.0135310231089534 ) ) ;
#34431=CARTESIAN_POINT ( 'NONE',  ( 802.7791456095903868, -28.71468719896028077, 329.0155153010375102 ) ) ;
#34435=CARTESIAN_POINT ( 'NONE',  ( 759.0252816721024374, -240.9982390220561683, 368.0189434323527280 ) ) ;
#34436=CARTESIAN_POINT ( 'NONE',  ( 775.8780910478218402, -321.2817908451525000, 364.9511171171680530 ) ) ;
#34437=CARTESIAN_POINT ( 'NONE',  ( 759.2295555964440155, -424.1692326535044799, 353.9708237608231229 ) ) ;
#34445=CARTESIAN_POINT ( 'NONE',  ( 795.9930595647434757, -315.0783235625957559, 320.7433823573372820 ) ) ;
#34449=CARTESIAN_POINT ( 'NONE',  ( 766.0291762391763086, -106.9181544815167371, 360.7704444035551319 ) ) ;
#34450=CARTESIAN_POINT ( 'NONE',  ( 804.9363028652555840, 7.729033705215793582, 338.2165204200192079 ) ) ;
#34454=CARTESIAN_POINT ( 'NONE',  ( 758.4439275373578084, -228.5545181178799794, 353.2243759319684386 ) ) ;
#34455=CARTESIAN_POINT ( 'NONE',  ( 791.0478386215596629, -237.8272453906072599, 306.7653713866226326 ) ) ;
#34459=CARTESIAN_POINT ( 'NONE',  ( 800.9747183278959710, -36.99823902205679360, 311.9810565676471583 ) ) ;
#34463=VECTOR ( 'NONE', #33009, 1000.000000000000000 ) ;
#34464=CARTESIAN_POINT ( 'NONE',  ( 744.6391490659812007, -302.7363362996979959, 338.7502325331110455 ) ) ;
#34466=CARTESIAN_POINT ( 'NONE',  ( 744.7301800767019131, -292.8164208402376971, 337.4774526936615757 ) ) ;
#34471=CARTESIAN_POINT ( 'NONE',  ( 804.4286716492782716, -377.3618753856920875, 345.3141322388244703 ) ) ;
#34472=CARTESIAN_POINT ( 'NONE',  ( 802.5472867521000353, -148.3726999360620198, 350.8726784830461156 ) ) ;
#34475=CARTESIAN_POINT ( 'NONE',  ( 803.8556311672234642, -57.62377810805111267, 365.6418435158340117 ) ) ;
#34476=CARTESIAN_POINT ( 'NONE',  ( 764.8639956371174549, -368.0891481129647786, 319.7806653035542581 ) ) ;
#34480=CARTESIAN_POINT ( 'NONE',  ( 804.6798772138708955, -447.7255117493280636, 334.6312213355107019 ) ) ;
#34484=CARTESIAN_POINT ( 'NONE',  ( 756.5762568750052424, -195.1800572038744974, 348.7366044899774238 ) ) ;
#34485=CARTESIAN_POINT ( 'NONE',  ( 771.1735550268780344, -201.1800572038744690, 316.3353852180828198 ) ) ;
#34489=CARTESIAN_POINT ( 'NONE',  ( 800.0135310231082713, -398.0891481129647218, 325.0180583372163028 ) ) ;
#34492=CARTESIAN_POINT ( 'NONE',  ( 792.3570229623691148, -117.1800572038747106, 373.1304606946836770 ) ) ;
#34493=VERTEX_POINT ( 'NONE', #19252 ) ;
#34499=CARTESIAN_POINT ( 'NONE',  ( 757.2208543904082489, -184.7146871989598083, 350.9844846989624330 ) ) ;
#34501=DIRECTION ( 'NONE',  ( 0.000000000000000000, 1.000000000000000000, 0.000000000000000000 ) ) ;
#34510=CARTESIAN_POINT ( 'NONE',  ( 760.0363995740630116, -106.9181544815167371, 368.7758568127991907 ) ) ;
#34518=CARTESIAN_POINT ( 'NONE',  ( 804.8461984189677878, -434.1908817542430370, 336.9566956441385628 ) ) ;
#34519=CARTESIAN_POINT ( 'NONE',  ( 814.2805881961230625, -361.6454272087887603, 331.2368401574024119 ) ) ;
#34526=CARTESIAN_POINT ( 'NONE',  ( 811.3240766477731540, -220.3726999360618208, 355.6651683502462902 ) ) ;
#34528=CARTESIAN_POINT ( 'NONE',  ( 801.1904061080336987, -188.0891481129653187, 368.3070685750235498 ) ) ;
#34531=CARTESIAN_POINT ( 'NONE',  ( 781.7834795799800531, -274.8164208402378108, 315.0636971347436202 ) ) ;
#34532=CARTESIAN_POINT ( 'NONE',  ( 804.6971507214547046, -75.28179084515321051, 344.0799538623459739 ) ) ;
#34535=DIRECTION ( 'NONE',  ( -1.000000000000000000, -0.000000000000000000, -0.000000000000000000 ) ) ;
#34536=CARTESIAN_POINT ( 'NONE',  ( 787.6308680596127942, -107.2601417444145824, 364.1105419155492768 ) ) ;
#34537=CARTESIAN_POINT ( 'NONE',  ( 785.3141322388236176, -333.7255117493286320, 364.4286716492789537 ) ) ;
#34540=CARTESIAN_POINT ( 'NONE',  ( 792.1044303154645831, -84.45278447660206211, 317.8323909638837677 ) ) ;
#34543=CARTESIAN_POINT ( 'NONE',  ( 807.5423716828161105, -369.0783235625956422, 362.2119215644372048 ) ) ;
#34545=CARTESIAN_POINT ( 'NONE',  ( 800.0135310231082713, -278.0891481129651197, 325.0180583372163028 ) ) ;
#34549=CARTESIAN_POINT ( 'NONE',  ( 767.8955696845333705, -360.4527844766010958, 362.1676090361162323 ) ) ;
#34556=CARTESIAN_POINT ( 'NONE',  ( 801.9419747391806368, -138.4527844766019200, 351.9812246680014027 ) ) ;
#34557=CARTESIAN_POINT ( 'NONE',  ( 775.8780910478218402, -417.2817908451522158, 364.9511171171680530 ) ) ;
#34558=CARTESIAN_POINT ( 'NONE',  ( 772.3691319403857278, -95.26014174441461080, 315.8894580844506663 ) ) ;
#34561=CARTESIAN_POINT ( 'NONE',  ( 810.1134526219336749, -368.5328690171409676, 357.8822607201570349 ) ) ;
#34563=CARTESIAN_POINT ( 'NONE',  ( 764.3348316497523456, -118.7146871989600072, 308.6759233522265617 ) ) ;
#34567=CARTESIAN_POINT ( 'NONE',  ( 766.4474001241216001, 4.900027336664720679, 307.3154664389482491 ) ) ;
#34574=CARTESIAN_POINT ( 'NONE',  ( 772.4468031744293057, -345.8272453906069472, 363.8651313633793620 ) ) ;
#34575=CARTESIAN_POINT ( 'NONE',  ( 814.4686193811664907, -291.2817908451525000, 346.2056067578752732 ) ) ;
#34580=CARTESIAN_POINT ( 'NONE',  ( 788.6739635108323228, -127.6454272087894140, 373.9316612368139090 ) ) ;
#34586=CARTESIAN_POINT ( 'NONE',  ( 756.5762568750052424, -195.1800572038744974, 348.7366044899774238 ) ) ;
#34588=CARTESIAN_POINT ( 'NONE',  ( 814.2805881961230625, -409.6454272087884760, 331.2368401574024119 ) ) ;
#34591=CARTESIAN_POINT ( 'NONE',  ( 804.1105419155481968, -51.82724539060782121, 347.6308680596136469 ) ) ;
#34594=CARTESIAN_POINT ( 'NONE',  ( 803.2186876482843445, -439.9874144716862929, 350.0220218866286928 ) ) ;
#34598=CARTESIAN_POINT ( 'NONE',  ( 807.5423716828161105, -273.0783235625958696, 362.2119215644372048 ) ) ;
#34599=CARTESIAN_POINT ( 'NONE',  ( 781.7834795799800531, -130.8164208402383224, 315.0636971347436202 ) ) ;
#34602=CARTESIAN_POINT ( 'NONE',  ( 767.8955696845333705, -264.4527844766016074, 362.1676090361162323 ) ) ;
#34603=EDGE_CURVE ( 'NONE', #24990, #33757, #20160, .T. ) ;
#34609=AXIS2_PLACEMENT_3D ( 'NONE', #5995, #37425, #19637 ) ;
#34610=CARTESIAN_POINT ( 'NONE',  ( 797.8594530101008786, -37.54369356751132614, 322.1405469898980982 ) ) ;
#34613=CARTESIAN_POINT ( 'NONE',  ( 772.5602148656447525, -369.7255117493284615, 305.7998596910095443 ) ) ;
#34614=CARTESIAN_POINT ( 'NONE',  ( 773.7943932421234194, -239.8055962898687028, 305.5313806188329409 ) ) ;
#34620=CARTESIAN_POINT ( 'NONE',  ( 778.1981804954714335, -250.2709662947832783, 314.8072714833589885 ) ) ;
#34622=CARTESIAN_POINT ( 'NONE',  ( 759.0252816721024374, -360.9982390220557704, 368.0189434323527280 ) ) ;
#34627=CARTESIAN_POINT ( 'NONE',  ( 780.5236548040995785, -212.7363362996982232, 314.9735926884559944 ) ) ;
#34628=CARTESIAN_POINT ( 'NONE',  ( 803.4237431249931660, -135.1800572038746679, 331.2633955100225194 ) ) ;
#34632=CARTESIAN_POINT ( 'NONE',  ( 780.5290396650775619, -276.3510508353231785, 365.2837595273619513 ) ) ;
#34635=CARTESIAN_POINT ( 'NONE',  ( 788.6739635108323228, -7.645427208789786100, 373.9316612368139090 ) ) ;
#34637=CARTESIAN_POINT ( 'NONE',  ( 782.5225473063381969, -166.2709662947835909, 375.2698199232970637 ) ) ;
#34638=CARTESIAN_POINT ( 'NONE',  ( 804.6798772138708955, -63.72551174932939233, 334.6312213355107019 ) ) ;
#34643=CARTESIAN_POINT ( 'NONE',  ( 771.3260364891663130, -403.6454272087884760, 306.0683387631859773 ) ) ;
#34646=CARTESIAN_POINT ( 'NONE',  ( 746.8695393053150156, -413.9073299311465348, 327.6429770376306010 ) ) ;
#34647=CARTESIAN_POINT ( 'NONE',  ( 746.8695393053151292, -29.90732993114772142, 327.6429770376306578 ) ) ;
#34649=CARTESIAN_POINT ( 'NONE',  ( 790.8726784830453198, -34.71468719896025590, 362.5472867521010585 ) ) ;
#34652=CARTESIAN_POINT ( 'NONE',  ( 746.7653713866222915, -185.2601417444143692, 351.0478386215610271 ) ) ;
#34653=CARTESIAN_POINT ( 'NONE',  ( 802.1676090361155502, 9.365397341579424051, 327.8955696845344505 ) ) ;
#34658=CARTESIAN_POINT ( 'NONE',  ( 771.1735550268778070, -177.1800572038744690, 316.3353852180827630 ) ) ;
#34660=CARTESIAN_POINT ( 'NONE',  ( 791.9812246680005501, -284.6346026584196807, 361.9419747391813189 ) ) ;
#34663=CARTESIAN_POINT ( 'NONE',  ( 779.4709603349208464, -24.35105083532392811, 314.7162404726379918 ) ) ;
#34666=CARTESIAN_POINT ( 'NONE',  ( 805.0032342141413437, -253.5436935675105588, 314.9967657858572352 ) ) ;
#34667=CARTESIAN_POINT ( 'NONE',  ( 799.2566176426618085, -336.0090635724251911, 324.0069404352559559 ) ) ;
#34668=CARTESIAN_POINT ( 'NONE',  ( 768.8385539511368734, 24.73985825558500551, 306.4236121716840557 ) ) ;
#34674=CARTESIAN_POINT ( 'NONE',  ( 796.7845633553578182, -345.6237781080501463, 358.5707757039688204 ) ) ;
#34676=CARTESIAN_POINT ( 'NONE',  ( 761.4292242960306112, -137.4636090269711985, 323.2154366446414429 ) ) ;
#34677=CARTESIAN_POINT ( 'NONE',  ( 781.8018195045266339, 1.729033705215812011, 365.1927285166406705 ) ) ;
#34681=CARTESIAN_POINT ( 'NONE',  ( 804.1601925771018387, -175.4419599262325562, 346.5483106153029098 ) ) ;
#34685=CARTESIAN_POINT ( 'NONE',  ( 808.3070685750230950, -90.99823902205663728, 361.1904061080339261 ) ) ;
#34686=CARTESIAN_POINT ( 'NONE',  ( 808.6629988358042738, -452.9681489794447771, 336.2505073875255448 ) ) ;
#34689=CARTESIAN_POINT ( 'NONE',  ( 805.6418435158337843, -341.4636090269705733, 363.8556311672236916 ) ) ;
#34691=CARTESIAN_POINT ( 'NONE',  ( 748.9653473494363425, -290.6346026584195101, 356.9462024416521331 ) ) ;
#34695=CARTESIAN_POINT ( 'NONE',  ( 797.6776695296629214, -379.5436935675102745, 357.6776695296636603 ) ) ;
#34696=CARTESIAN_POINT ( 'NONE',  ( 757.0176451133909268, -157.0999726633347962, 349.9200121543848354 ) ) ;
#34699=CARTESIAN_POINT ( 'NONE',  ( 807.5423716828161105, -81.07832356259649487, 362.2119215644372048 ) ) ;
#34700=CARTESIAN_POINT ( 'NONE',  ( 767.8955696845334842, -360.4527844766011526, 362.1676090361161755 ) ) ;
#34703=CARTESIAN_POINT ( 'NONE',  ( 781.8018195045266339, -430.2709662947827383, 365.1927285166406705 ) ) ;
#34707=CARTESIAN_POINT ( 'NONE',  ( 758.0580252608178853, -198.4527844766017495, 328.0187753319985404 ) ) ;
#34708=CARTESIAN_POINT ( 'NONE',  ( 762.1405469898973024, -193.5436935675108714, 357.8594530101016176 ) ) ;
#34712=CARTESIAN_POINT ( 'NONE',  ( 795.1360043628807261, -380.0891481129646650, 360.2193346964456282 ) ) ;
#34715=CARTESIAN_POINT ( 'NONE',  ( 754.9967657858570647, -145.5436935675109851, 365.0032342141425943 ) ) ;
#34721=CARTESIAN_POINT ( 'NONE',  ( 754.9735926884551418, -210.3510508353233490, 340.5236548041000333 ) ) ;
#34730=CARTESIAN_POINT ( 'NONE',  ( 745.5313806188320314, -135.2817908451530116, 333.7943932421247268 ) ) ;
#34743=CARTESIAN_POINT ( 'NONE',  ( 791.0478386215596629, -213.8272453906073167, 306.7653713866226326 ) ) ;
#34745=CARTESIAN_POINT ( 'NONE',  ( 782.4968714119720516, -202.8164208402380950, 305.0891759886411023 ) ) ;
#34748=CARTESIAN_POINT ( 'NONE',  ( 804.9363028652555840, -280.2709662947833067, 338.2165204200192079 ) ) ;
#34749=CARTESIAN_POINT ( 'NONE',  ( 773.4516893846965786, -43.64542720878966975, 315.8398074228977066 ) ) ;
#34752=CARTESIAN_POINT ( 'NONE',  ( 779.9999999999992042, 16.45630643248849267, 339.9999999999999432 ) ) ;
#34753=CARTESIAN_POINT ( 'NONE',  ( 755.0488828828309806, -113.8055962898691149, 344.1219089521771934 ) ) ;
#34754=CARTESIAN_POINT ( 'NONE',  ( 764.8639956371174549, -320.0891481129648355, 319.7806653035542013 ) ) ;
#34757=CARTESIAN_POINT ( 'NONE',  ( 764.8639956371174549, -104.0891481129656881, 319.7806653035542013 ) ) ;
#34760=CARTESIAN_POINT ( 'NONE',  ( 781.2497674668890113, -420.3510508353225532, 375.3608509340180603 ) ) ;
#34762=CARTESIAN_POINT ( 'NONE',  ( 771.1735550268778070, -297.1800572038740711, 316.3353852180827630 ) ) ;
#34766=CARTESIAN_POINT ( 'NONE',  ( 805.1927285166397041, -424.8164208402372992, 341.8018195045277707 ) ) ;
#34772=CARTESIAN_POINT ( 'NONE',  ( 797.6776695296629214, -115.5436935675110988, 357.6776695296636603 ) ) ;
#34773=CARTESIAN_POINT ( 'NONE',  ( 757.4527132478984868, -424.3726999360612808, 329.1273215169538844 ) ) ;
#34776=CARTESIAN_POINT ( 'NONE',  ( 786.2056067578752163, -347.8055962898683333, 374.4686193811670023 ) ) ;
#34778=EDGE_CURVE ( 'NONE', #23783, #33757, #27544, .T. ) ;
#34782=CARTESIAN_POINT ( 'NONE',  ( 750.9282345327678740, -16.91815448151702839, 319.8311093483690115 ) ) ;
#34790=CARTESIAN_POINT ( 'NONE',  ( 757.0176451133909268, -349.0999726633342561, 349.9200121543848354 ) ) ;
#34791=CARTESIAN_POINT ( 'NONE',  ( 749.5768839229115201, -300.5545181178797520, 358.0661480581553064 ) ) ;
#34795=CARTESIAN_POINT ( 'NONE',  ( 745.7194118038753459, -109.6454272087894566, 348.7631598425976449 ) ) ;
#34800=CARTESIAN_POINT ( 'NONE',  ( 794.9819416627830151, -180.9982390220563389, 319.9864689768909898 ) ) ;
#34803=CARTESIAN_POINT ( 'NONE',  ( 768.9521613784389729, -441.8272453906066630, 373.2346286133773106 ) ) ;
#34809=CARTESIAN_POINT ( 'NONE',  ( 761.9338519418445230, 9.467130982857780097, 370.4231160770881957 ) ) ;
#34810=VERTEX_POINT ( 'NONE', #31479 ) ;
#34814=CARTESIAN_POINT ( 'NONE',  ( 764.3348316497523456, -286.7146871989594388, 308.6759233522265617 ) ) ;
#34815=CARTESIAN_POINT ( 'NONE',  ( 803.4237431249931660, -135.1800572038746679, 331.2633955100225194 ) ) ;
#34817=CARTESIAN_POINT ( 'NONE',  ( 785.3687786644884454, -299.3618753856922581, 315.3201227861279676 ) ) ;
#34824=CARTESIAN_POINT ( 'NONE',  ( 755.0636971347428243, -28.27096629478409540, 341.7834795799807353 ) ) ;
#34826=CARTESIAN_POINT ( 'NONE',  ( 801.1904061080338124, -356.0891481129648355, 368.3070685750236066 ) ) ;
#34827=CARTESIAN_POINT ( 'NONE',  ( 746.0683387631852383, -259.4419599262322436, 331.3260364891676204 ) ) ;
#34833=CARTESIAN_POINT ( 'NONE',  ( 804.9363028652555840, -256.2709662947834204, 338.2165204200192079 ) ) ;
#34834=CARTESIAN_POINT ( 'NONE',  ( 787.5162901302840055, -371.3618753856919739, 305.4481719005792684 ) ) ;
#34839=CARTESIAN_POINT ( 'NONE',  ( 804.8461984189677878, -218.1908817542437191, 336.9566956441385628 ) ) ;
#34840=CARTESIAN_POINT ( 'NONE',  ( 800.0135310231082713, -134.0891481129655745, 325.0180583372163028 ) ) ;
#34844=CARTESIAN_POINT ( 'NONE',  ( 794.1144889064781864, -298.1692326535049347, 360.9840315886528401 ) ) ;
#34847=CARTESIAN_POINT ( 'NONE',  ( 754.3581564841646241, 6.536390973028352924, 316.1443688327762516 ) ) ;
#34850=CARTESIAN_POINT ( 'NONE',  ( 808.0189434323515343, -182.0891481129654323, 319.0252816721025511 ) ) ;
#34851=CARTESIAN_POINT ( 'NONE',  ( 791.9812246680005501, -92.63460265842026331, 361.9419747391813189 ) ) ;
#34853=LINE ( 'NONE', #3216, #35822 ) ;
#34856=CARTESIAN_POINT ( 'NONE',  ( 757.7880784355613741, -426.0090635724247932, 312.4576283171834916 ) ) ;
#34859=CARTESIAN_POINT ( 'NONE',  ( 803.8651313633788504, -365.2601417444137155, 332.4468031744301015 ) ) ;
#34860=CARTESIAN_POINT ( 'NONE',  ( 751.6929314249750860, -54.99823902205672965, 318.8095938919659034 ) ) ;
#34865=CARTESIAN_POINT ( 'NONE',  ( 790.8726784830453198, -10.71468719896033761, 362.5472867521010585 ) ) ;
#34868=CARTESIAN_POINT ( 'NONE',  ( 773.7943932421234194, -167.8055962898689586, 305.5313806188329409 ) ) ;
#34869=CARTESIAN_POINT ( 'NONE',  ( 771.1735550268780344, -9.180057203875058747, 316.3353852180828198 ) ) ;
#34874=CARTESIAN_POINT ( 'NONE',  ( 800.0135310231082713, -182.0891481129654323, 325.0180583372163028 ) ) ;
#34876=CARTESIAN_POINT ( 'NONE',  ( 756.5762568750052424, -339.1800572038740142, 348.7366044899774238 ) ) ;
#34879=CARTESIAN_POINT ( 'NONE',  ( 805.1016975059191054, -30.89650538077846065, 343.0745993439771837 ) ) ;
#34882=CARTESIAN_POINT ( 'NONE',  ( 751.6929314249750860, -270.9982390220561115, 318.8095938919659034 ) ) ;
#34883=CARTESIAN_POINT ( 'NONE',  ( 760.7433823573367135, -348.0090635724251342, 355.9930595647440441 ) ) ;
#34884=CARTESIAN_POINT ( 'NONE',  ( 804.9511171171677688, -437.8055962898679923, 335.8780910478229202 ) ) ;
#34887=AXIS2_PLACEMENT_3D ( 'NONE', #21620, #14240, #21171 ) ;
#34889=ORIENTED_EDGE ( 'NONE', *, *, #34778, .T. ) ;
#34890=CARTESIAN_POINT ( 'NONE',  ( 746.8695393053150156, -269.9073299311468190, 327.6429770376306010 ) ) ;
#34891=CARTESIAN_POINT ( 'NONE',  ( 758.6633372737375112, -332.5328690171411381, 326.9102291470432533 ) ) ;
#34893=CARTESIAN_POINT ( 'NONE',  ( 755.1538015810308480, -110.1908817542440033, 343.0433043558613804 ) ) ;
#34894=CARTESIAN_POINT ( 'NONE',  ( 801.9419747391806368, -18.45278447660230725, 351.9812246680014027 ) ) ;
#34898=CARTESIAN_POINT ( 'NONE',  ( 745.5313806188320314, -231.2817908451527558, 333.7943932421247268 ) ) ;
#34899=CARTESIAN_POINT ( 'NONE',  ( 794.1144889064781864, -202.1692326535051905, 360.9840315886528401 ) ) ;
#34901=AXIS2_PLACEMENT_3D ( 'NONE', #44716, #13077, #28060 ) ;
#34906=CARTESIAN_POINT ( 'NONE',  ( 782.5225473063381969, 1.729033705215812011, 375.2698199232970637 ) ) ;
#34907=CARTESIAN_POINT ( 'NONE',  ( 763.0537975583475827, -72.45278447660213317, 371.0346526505627480 ) ) ;
#34908=CARTESIAN_POINT ( 'NONE',  ( 808.4681505782122031, -452.9681489794450613, 336.7690310503822388 ) ) ;
#34911=CARTESIAN_POINT ( 'NONE',  ( 760.0363995740630116, -346.9181544815160123, 368.7758568127991907 ) ) ;
#34913=CARTESIAN_POINT ( 'NONE',  ( 787.4397851343537695, -285.7255117493286889, 374.2001403089903988 ) ) ;
#34917=APPLICATION_CONTEXT ( 'automotive_design' ) ;
#34918=CARTESIAN_POINT ( 'NONE',  ( 755.3201227861273992, -411.7255117493282910, 345.3687786644892981 ) ) ;
#34920=CARTESIAN_POINT ( 'NONE',  ( 763.8424801807145741, -162.0090635724256742, 320.5453621957614700 ) ) ;
#34923=CARTESIAN_POINT ( 'NONE',  ( 800.1688906516307043, -82.16923265350558836, 369.0717654672308186 ) ) ;
#34924=CARTESIAN_POINT ( 'NONE',  ( 797.8594530101009923, -397.5436935675101040, 322.1405469898982119 ) ) ;
#34927=CARTESIAN_POINT ( 'NONE',  ( 797.6776695296629214, -427.5436935675101040, 357.6776695296636603 ) ) ;
#34931=CARTESIAN_POINT ( 'NONE',  ( 792.1044303154645831, -228.4527844766015789, 317.8323909638837677 ) ) ;
#34932=CARTESIAN_POINT ( 'NONE',  ( 764.8639956371174549, -200.0891481129653471, 319.7806653035542581 ) ) ;
#34937=CARTESIAN_POINT ( 'NONE',  ( 805.1927285166397041, -376.8164208402375834, 341.8018195045277707 ) ) ;
#34941=CARTESIAN_POINT ( 'NONE',  ( 749.2812353651451076, -150.4527844766018916, 323.2262854647983090 ) ) ;
#34944=ORIENTED_EDGE ( 'NONE', *, *, #1890, .F. ) ;
#34947=CARTESIAN_POINT ( 'NONE',  ( 795.9930595647434757, -219.0783235625960401, 320.7433823573372820 ) ) ;
#34948=DIRECTION ( 'NONE',  ( -0.000000000000000000, 1.000000000000000000, -0.000000000000000000 ) ) ;
#34957=CARTESIAN_POINT ( 'NONE',  ( 778.7629533639073998, -128.7363362996984790, 375.0009284576466371 ) ) ;
#34964=CARTESIAN_POINT ( 'NONE',  ( 786.2694204179717872, -381.2817908451523294, 305.1769319972829067 ) ) ;
#34965=LINE ( 'NONE', #20645, #29950 ) ;
#34971=CARTESIAN_POINT ( 'NONE',  ( 793.5525998758768083, -247.0999726633344835, 372.6845335610516941 ) ) ;
#34973=CARTESIAN_POINT ( 'NONE',  ( 748.9653473494363425, -194.6346026584198796, 356.9462024416521331 ) ) ;
#34976=CARTESIAN_POINT ( 'NONE',  ( 802.1676090361156639, -278.6346026584196807, 327.8955696845344505 ) ) ;
#34977=CARTESIAN_POINT ( 'NONE',  ( 773.4516893846965786, -91.64542720878951343, 315.8398074228977066 ) ) ;
#34980=CARTESIAN_POINT ( 'NONE',  ( 805.1016975059191054, -126.8965053807781516, 343.0745993439771837 ) ) ;
#34981=CARTESIAN_POINT ( 'NONE',  ( 756.5762568750052424, -315.1800572038740711, 348.7366044899774238 ) ) ;
#34986=CARTESIAN_POINT ( 'NONE',  ( 802.1676090361156639, -86.63460265842023489, 327.8955696845344505 ) ) ;
#34990=CARTESIAN_POINT ( 'NONE',  ( 748.3538107759620743, -424.7146871989589840, 355.8262568251490165 ) ) ;
#34992=CARTESIAN_POINT ( 'NONE',  ( 764.8639956371174549, -296.0891481129650629, 319.7806653035542013 ) ) ;
#34996=CARTESIAN_POINT ( 'NONE',  ( 788.7366044899766848, -395.9073299311465348, 316.5762568750059813 ) ) ;
#35002=CARTESIAN_POINT ( 'NONE',  ( 796.1575198192839480, -438.0090635724247932, 359.4546378042384163 ) ) ;
#35003=CARTESIAN_POINT ( 'NONE',  ( 803.2186876482843445, -127.9874144716872308, 350.0220218866286928 ) ) ;
#35006=CARTESIAN_POINT ( 'NONE',  ( 808.7758568127978833, -364.1692326535046504, 320.0363995740631822 ) ) ;
#35008=ORIENTED_EDGE ( 'NONE', *, *, #33417, .F. ) ;
#35012=CARTESIAN_POINT ( 'NONE',  ( 809.0717654672305343, -28.91815448151699286, 360.1688906516309885 ) ) ;
#35016=LINE ( 'NONE', #35470, #10709 ) ;
#35018=DIRECTION ( 'NONE',  ( 0.000000000000000000, 1.000000000000000000, 0.000000000000000000 ) ) ;
#35020=CARTESIAN_POINT ( 'NONE',  ( 793.9708237608222134, -382.9181544815159555, 319.2295555964448681 ) ) ;
#35021=CARTESIAN_POINT ( 'NONE',  ( 781.2370466360911223, -332.7363362996979390, 304.9990715423533629 ) ) ;
#35024=CARTESIAN_POINT ( 'NONE',  ( 799.9999999999993179, 205.0000000000000568, 360.0000000000000000 ) ) ;
#35026=CARTESIAN_POINT ( 'NONE',  ( 773.7305795820266212, -153.2817908451529831, 374.8230680027170365 ) ) ;
#35030=CARTESIAN_POINT ( 'NONE',  ( 791.9812246680005501, -188.6346026584199365, 361.9419747391813189 ) ) ;
#35032=CARTESIAN_POINT ( 'NONE',  ( 745.7194118038753459, -421.6454272087885329, 348.7631598425976449 ) ) ;
#35038=CARTESIAN_POINT ( 'NONE',  ( 811.6461892240364477, 19.28531280103956647, 324.1737431748509835 ) ) ;
#35043=CARTESIAN_POINT ( 'NONE',  ( 746.0683387631852383, -307.4419599262320730, 331.3260364891676204 ) ) ;
#35044=CARTESIAN_POINT ( 'NONE',  ( 797.6776695296629214, -115.5436935675110988, 357.6776695296636603 ) ) ;
#35047=CARTESIAN_POINT ( 'NONE',  ( 767.8955696845333705, -288.4527844766014937, 362.1676090361162323 ) ) ;
#35050=CARTESIAN_POINT ( 'NONE',  ( 793.3174859505621725, -452.3943253718131245, 372.3673656294391776 ) ) ;
#35052=EDGE_LOOP ( 'NONE', ( #10005, #20616, #35180, #8036, #39735, #29713, #22221, #34316 ) ) ;
#35057=CARTESIAN_POINT ( 'NONE',  ( 792.2312462859673587, -347.9073299311467053, 307.2067596250082602 ) ) ;
#35058=CARTESIAN_POINT ( 'NONE',  ( 793.4146539503750546, -265.9874144716867477, 307.6481478633938877 ) ) ;
#35059=CARTESIAN_POINT ( 'NONE',  ( 812.6845335610512393, -79.98741447168740137, 353.5525998758768651 ) ) ;
#35065=CARTESIAN_POINT ( 'NONE',  ( 785.3141322388236176, -237.7255117493289163, 364.4286716492789537 ) ) ;
#35073=CARTESIAN_POINT ( 'NONE',  ( 783.0745993439762742, -248.1908817542435202, 365.1016975059196739 ) ) ;
#35074=CARTESIAN_POINT ( 'NONE',  ( 762.1405469898971887, -121.5436935675110419, 357.8594530101015607 ) ) ;
#35078=CARTESIAN_POINT ( 'NONE',  ( 780.5290396650775619, -300.3510508353230080, 365.2837595273619513 ) ) ;
#35080=CARTESIAN_POINT ( 'NONE',  ( 745.7194118038753459, -13.64542720878976390, 348.7631598425976449 ) ) ;
#35082=CARTESIAN_POINT ( 'NONE',  ( 754.9967657858570647, -169.5436935675108430, 365.0032342141425374 ) ) ;
#35083=CARTESIAN_POINT ( 'NONE',  ( 797.6776695296629214, -67.54369356751125508, 357.6776695296636603 ) ) ;
#35087=CARTESIAN_POINT ( 'NONE',  ( 776.9254006560222479, 3.809118245755632959, 314.8983024940802125 ) ) ;
#35090=CARTESIAN_POINT ( 'NONE',  ( 780.5290396650775619, -372.3510508353228374, 365.2837595273619513 ) ) ;
#35091=CARTESIAN_POINT ( 'NONE',  ( 772.5602148656447525, -33.72551174932952733, 305.7998596910095443 ) ) ;
#35093=CARTESIAN_POINT ( 'NONE',  ( 755.0488828828309806, -65.80559628986925702, 344.1219089521771934 ) ) ;
#35097=CARTESIAN_POINT ( 'NONE',  ( 795.6651683502461765, -202.7146871989597514, 371.3240766477733814 ) ) ;
#35098=CARTESIAN_POINT ( 'NONE',  ( 757.8323909638828582, -2.634602658420536425, 352.1044303154654358 ) ) ;
#35101=CARTESIAN_POINT ( 'NONE',  ( 755.0636971347428243, -196.2709662947835909, 341.7834795799807353 ) ) ;
#35105=CARTESIAN_POINT ( 'NONE',  ( 788.7366044899766848, -323.9073299311468190, 316.5762568750059813 ) ) ;
#35108=CARTESIAN_POINT ( 'NONE',  ( 793.2243759319678702, -50.53286901714203339, 318.4439275373583200 ) ) ;
#35111=CARTESIAN_POINT ( 'NONE',  ( 777.4774526936600978, -250.2709662947833351, 304.7301800767028226 ) ) ;
#35113=CARTESIAN_POINT ( 'NONE',  ( 794.1144889064781864, -442.1692326535044231, 360.9840315886528401 ) ) ;
#35117=ORIENTED_EDGE ( 'NONE', *, *, #2078, .F. ) ;
#35119=CARTESIAN_POINT ( 'NONE',  ( 814.2001403089898304, -305.3618753856922581, 347.4397851343538264 ) ) ;
#35120=CARTESIAN_POINT ( 'NONE',  ( 759.2295555964440155, -328.1692326535048210, 353.9708237608231229 ) ) ;
#35123=CARTESIAN_POINT ( 'NONE',  ( 790.9844846989617508, -166.3726999360620198, 317.2208543904092721 ) ) ;
#35124=CARTESIAN_POINT ( 'NONE',  ( 778.2165204200184689, -22.81642084023865280, 364.9363028652563230 ) ) ;
#35127=CARTESIAN_POINT ( 'NONE',  ( 799.9999999999993179, -512.9681489794448908, 309.9999999999998863 ) ) ;
#35128=CARTESIAN_POINT ( 'NONE',  ( 811.3240766477731540, -244.3726999360617924, 355.6651683502462902 ) ) ;
#35129=CARTESIAN_POINT ( 'NONE',  ( 761.2382568024794409, -183.6237781080507148, 356.9571628226838129 ) ) ;
#35134=CARTESIAN_POINT ( 'NONE',  ( 810.7187646348534145, -18.45278447660230725, 356.7737145352016341 ) ) ;
#35135=CARTESIAN_POINT ( 'NONE',  ( 805.0032342141412300, -85.54369356751118403, 314.9967657858571783 ) ) ;
#35140=CARTESIAN_POINT ( 'NONE',  ( 812.3518521366052028, -361.0999726633341425, 326.5853460496235243 ) ) ;
#35143=CARTESIAN_POINT ( 'NONE',  ( 758.8095938919642549, -320.0891481129648355, 311.6929314249763365 ) ) ;
#35147=CARTESIAN_POINT ( 'NONE',  ( 762.3223304703356007, -391.5436935675101608, 322.3223304703362828 ) ) ;
#35148=CARTESIAN_POINT ( 'NONE',  ( 766.9102291470427417, -138.5545181178802636, 318.6633372737382501 ) ) ;
#35151=CARTESIAN_POINT ( 'NONE',  ( 744.8212110874229666, -90.89650538077827946, 336.2046728542121627 ) ) ;
#35152=CARTESIAN_POINT ( 'NONE',  ( 797.6776695296629214, -403.5436935675101608, 357.6776695296636603 ) ) ;
#35153=CARTESIAN_POINT ( 'NONE',  ( 814.2001403089898304, 6.638124614306706306, 347.4397851343538264 ) ) ;
#35161=CARTESIAN_POINT ( 'NONE',  ( 788.7366044899766848, -227.9073299311471033, 316.5762568750059813 ) ) ;
#35162=CARTESIAN_POINT ( 'NONE',  ( 788.8264449731201466, -213.1800572038743837, 363.6646147819170665 ) ) ;
#35163=VECTOR ( 'NONE', #33982, 1000.000000000000000 ) ;
#35169=CARTESIAN_POINT ( 'NONE',  ( 785.3687786644884454, -443.3618753856917465, 315.3201227861279676 ) ) ;
#35176=CARTESIAN_POINT ( 'NONE',  ( 792.2312462859673587, -155.9073299311473306, 307.2067596250082602 ) ) ;
#35180=ORIENTED_EDGE ( 'NONE', *, *, #38840, .F. ) ;
#35183=CARTESIAN_POINT ( 'NONE',  ( 754.8983024940795303, -234.8965053807777963, 336.9254006560228163 ) ) ;
#35189=FACE_BOUND ( 'NONE', #17458, .T. ) ;
#35192=CARTESIAN_POINT ( 'NONE',  ( 815.3608509340175488, -122.7363362996985074, 341.2497674668889545 ) ) ;
#35199=CARTESIAN_POINT ( 'NONE',  ( 760.0363995740630116, -394.9181544815158418, 368.7758568127991907 ) ) ;
#35206=CARTESIAN_POINT ( 'NONE',  ( 745.7194118038753459, -253.6454272087889876, 348.7631598425976449 ) ) ;
#35208=CARTESIAN_POINT ( 'NONE',  ( 782.4968714119720516, -226.8164208402380098, 305.0891759886411023 ) ) ;
#35212=CARTESIAN_POINT ( 'NONE',  ( 801.9419747391806368, -306.4527844766013800, 351.9812246680014027 ) ) ;
#35213=CARTESIAN_POINT ( 'NONE',  ( 804.8461984189677878, -98.19088175424404596, 336.9566956441385628 ) ) ;
#35217=CARTESIAN_POINT ( 'NONE',  ( 802.7791456095903868, -124.7146871989599930, 329.0155153010375102 ) ) ;
#35218=CARTESIAN_POINT ( 'NONE',  ( 764.8639956371174549, -368.0891481129647786, 319.7806653035542013 ) ) ;
#35221=CARTESIAN_POINT ( 'NONE',  ( 756.5762568750052424, -99.18005720387478164, 348.7366044899774238 ) ) ;
#35224=CARTESIAN_POINT ( 'NONE',  ( 751.2241431872005251, -424.1692326535044799, 359.9636004259367610 ) ) ;
#35226=CARTESIAN_POINT ( 'NONE',  ( 758.0580252608178853, -318.4527844766014368, 328.0187753319985404 ) ) ;
#35229=CARTESIAN_POINT ( 'NONE',  ( 801.9419747391806368, -402.4527844766010389, 351.9812246680014027 ) ) ;
#35235=CARTESIAN_POINT ( 'NONE',  ( 771.1735550268778070, -129.1800572038746111, 316.3353852180827630 ) ) ;
#35236=CARTESIAN_POINT ( 'NONE',  ( 790.9844846989617508, -430.3726999360611671, 317.2208543904092721 ) ) ;
#35237=CARTESIAN_POINT ( 'NONE',  ( 773.3843516231979720, -133.4419599262326699, 364.4086373105754433 ) ) ;
#35239=CARTESIAN_POINT ( 'NONE',  ( 799.9999999999993179, -512.9681489794448908, 339.9999999999999432 ) ) ;
#35240=CARTESIAN_POINT ( 'NONE',  ( 783.7566961878529810, -384.8965053807772847, 305.1792804349288417 ) ) ;
#35245=CARTESIAN_POINT ( 'NONE',  ( 748.6759233522253680, -40.37269993606240348, 324.3348316497537098 ) ) ;
#35246=DIRECTION ( 'NONE',  ( -0.000000000000000000, 1.000000000000000000, -0.000000000000000000 ) ) ;
#35253=CARTESIAN_POINT ( 'NONE',  ( 766.9102291470427417, -354.5545181178796383, 318.6633372737382501 ) ) ;
#35254=CARTESIAN_POINT ( 'NONE',  ( 809.0717654672305343, -340.9181544815160123, 360.1688906516309885 ) ) ;
#35258=CARTESIAN_POINT ( 'NONE',  ( 809.0717654672305343, -148.9181544815166092, 360.1688906516309885 ) ) ;
#35260=CARTESIAN_POINT ( 'NONE',  ( 804.7487373415286811, -67.54369356751125508, 364.7487373415288516 ) ) ;
#35264=CARTESIAN_POINT ( 'NONE',  ( 762.3223304703356007, -199.5436935675108430, 322.3223304703362828 ) ) ;
#35265=CARTESIAN_POINT ( 'NONE',  ( 804.1009440267234822, -455.4636090269701754, 314.0944755984392600 ) ) ;
#35271=CARTESIAN_POINT ( 'NONE',  ( 805.9055244015594326, 20.37622189194865285, 315.8990559732753240 ) ) ;
#35275=CARTESIAN_POINT ( 'NONE',  ( 744.9990715423526808, -306.3510508353230648, 341.2370466360926002 ) ) ;
#35276=CARTESIAN_POINT ( 'NONE',  ( 759.7806653035535192, -126.9982390220565094, 324.8639956371181370 ) ) ;
#35278=CARTESIAN_POINT ( 'NONE',  ( 804.9363028652555840, -304.2709662947832499, 338.2165204200192079 ) ) ;
#35280=ADVANCED_FACE ( 'NONE', ( #2098, #23338 ), #1198, .F. ) ;
#35281=CARTESIAN_POINT ( 'NONE',  ( 758.8095938919644823, -80.08914811296574499, 311.6929314249762797 ) ) ;
#35286=CARTESIAN_POINT ( 'NONE',  ( 778.1981804954714335, -10.27096629478414691, 314.8072714833589885 ) ) ;
#35288=CARTESIAN_POINT ( 'NONE',  ( 767.7687537140311633, -359.9073299311467053, 372.7932403749916830 ) ) ;
#35289=CARTESIAN_POINT ( 'NONE',  ( 771.2368401574024119, -277.4419599262322436, 374.2805881961240857 ) ) ;
#35290=CARTESIAN_POINT ( 'NONE',  ( 771.2368401574024119, -61.44195992623291147, 374.2805881961240857 ) ) ;
#35295=CARTESIAN_POINT ( 'NONE',  ( 785.3141322388236176, -261.7255117493288026, 364.4286716492789537 ) ) ;
#35297=CARTESIAN_POINT ( 'NONE',  ( 808.0189434323515343, -398.0891481129647218, 319.0252816721025511 ) ) ;
#35303=CARTESIAN_POINT ( 'NONE',  ( 769.0155153010367712, -274.3726999360617356, 362.7791456095907279 ) ) ;
#35304=CARTESIAN_POINT ( 'NONE',  ( 774.6858677611749044, -105.7255117493293000, 315.5713283507209894 ) ) ;
#35308=CARTESIAN_POINT ( 'NONE',  ( 769.1273215169530886, -286.7146871989594388, 317.4527132478988847 ) ) ;
#35310=CARTESIAN_POINT ( 'NONE',  ( 791.0478386215596629, -45.82724539060783542, 306.7653713866226326 ) ) ;
#35312=CARTESIAN_POINT ( 'NONE',  ( 792.2312462859673587, -179.9073299311472454, 307.2067596250082602 ) ) ;
#35313=CARTESIAN_POINT ( 'NONE',  ( 785.3687786644884454, -83.36187538569296862, 315.3201227861279676 ) ) ;
#35315=CARTESIAN_POINT ( 'NONE',  ( 813.5763878283155464, -459.8272453906066062, 351.1614460488615350 ) ) ;
#35318=CARTESIAN_POINT ( 'NONE',  ( 796.7845633553578182, -369.6237781080500895, 358.5707757039688204 ) ) ;
#35319=CARTESIAN_POINT ( 'NONE',  ( 751.9810565676468741, -50.08914811296584446, 360.9747183278973921 ) ) ;
#35321=CARTESIAN_POINT ( 'NONE',  ( 779.4709603349208464, -48.35105083532386061, 314.7162404726379918 ) ) ;
#35324=CARTESIAN_POINT ( 'NONE',  ( 793.4146539503750546, -217.9874144716870035, 307.6481478633938877 ) ) ;
#35325=CARTESIAN_POINT ( 'NONE',  ( 758.0580252608178853, -30.45278447660226817, 328.0187753319985404 ) ) ;
#35329=CARTESIAN_POINT ( 'NONE',  ( 803.4237431249931660, -207.1800572038744406, 331.2633955100225194 ) ) ;
#35332=CARTESIAN_POINT ( 'NONE',  ( 768.0187753319979720, -320.6346026584195670, 318.0580252608186242 ) ) ;
#35335=CARTESIAN_POINT ( 'NONE',  ( 779.4709603349208464, -48.35105083532386061, 314.7162404726379918 ) ) ;
#35337=( BOUNDED_CURVE ( )  B_SPLINE_CURVE ( 3, ( #15816, #40543, #40331, #19502 ),
 .UNSPECIFIED., .F., .T. ) 
 B_SPLINE_CURVE_WITH_KNOTS ( ( 4, 4 ),
 ( 4.691336726374857768, 4.712707788662813257 ),
 .UNSPECIFIED. ) 
 CURVE ( )  GEOMETRIC_REPRESENTATION_ITEM ( )  RATIONAL_B_SPLINE_CURVE ( ( 1.000000000000000000, 0.9999619401702002364, 0.9999619401702002364, 1.000000000000000000 ) ) 
 REPRESENTATION_ITEM ( '' )  );
#35338=CARTESIAN_POINT ( 'NONE',  ( 787.4397851343537695, -261.7255117493288026, 374.2001403089903988 ) ) ;
#35339=CARTESIAN_POINT ( 'NONE',  ( 815.1787889125755555, 17.10349461922139369, 343.7953271457877804 ) ) ;
#35344=CARTESIAN_POINT ( 'NONE',  ( 800.9747183278959710, -276.9982390220559978, 311.9810565676471583 ) ) ;
#35346=CARTESIAN_POINT ( 'NONE',  ( 773.3843516231979720, -325.4419599262320162, 364.4086373105754433 ) ) ;
#35348=CARTESIAN_POINT ( 'NONE',  ( 757.4527132478984868, -160.3726999360620482, 329.1273215169538844 ) ) ;
#35349=CARTESIAN_POINT ( 'NONE',  ( 797.8594530101008786, -13.54369356751140785, 322.1405469898980982 ) ) ;
#35354=CARTESIAN_POINT ( 'NONE',  ( 778.7629533639073998, -224.7363362996982232, 375.0009284576466371 ) ) ;
#35356=CARTESIAN_POINT ( 'NONE',  ( 805.0264073115434940, -174.3510508353234627, 339.4763451958999099 ) ) ;
#35358=CARTESIAN_POINT ( 'NONE',  ( 796.9571628226829034, -455.4636090269701754, 321.2382568024804641 ) ) ;
#35360=CARTESIAN_POINT ( 'NONE',  ( 751.9810565676468741, -2.089148112965993231, 360.9747183278973921 ) ) ;
#35361=CARTESIAN_POINT ( 'NONE',  ( 745.4481719005789273, -75.72551174932937101, 347.5162901302853129 ) ) ;
#35365=CARTESIAN_POINT ( 'NONE',  ( 805.6418435158337843, -365.4636090269705164, 363.8556311672236916 ) ) ;
#35367=CARTESIAN_POINT ( 'NONE',  ( 772.5602148656447525, -321.7255117493286320, 305.7998596910095443 ) ) ;
#35372=CARTESIAN_POINT ( 'NONE',  ( 804.4286716492782716, -425.3618753856919170, 345.3141322388244703 ) ) ;
#35373=CARTESIAN_POINT ( 'NONE',  ( 766.0291762391763086, -202.9181544815164386, 360.7704444035551319 ) ) ;
#35376=CARTESIAN_POINT ( 'NONE',  ( 776.2433038121456548, -84.89650538077830788, 374.8207195650711014 ) ) ;
#35377=CARTESIAN_POINT ( 'NONE',  ( 754.8072714833583632, -388.8164208402374129, 338.1981804954721156 ) ) ;
#35378=CARTESIAN_POINT ( 'NONE',  ( 795.1360043628807261, -452.0891481129646650, 360.2193346964456282 ) ) ;
#35381=ADVANCED_FACE ( 'NONE', ( #16188 ), #5116, .T. ) ;
#35384=CARTESIAN_POINT ( 'NONE',  ( 805.1927285166397041, -232.8164208402379245, 341.8018195045277707 ) ) ;
#35385=CARTESIAN_POINT ( 'NONE',  ( 801.9419747391806368, -234.4527844766016358, 351.9812246680014027 ) ) ;
#35389=CARTESIAN_POINT ( 'NONE',  ( 755.5713283507202505, -413.3618753856920307, 334.6858677611754729 ) ) ;
#35393=CARTESIAN_POINT ( 'NONE',  ( 801.1904061080338124, -164.0891481129654892, 368.3070685750236066 ) ) ;
#35394=CARTESIAN_POINT ( 'NONE',  ( 757.4527132478984868, -280.3726999360616787, 329.1273215169538844 ) ) ;
#35402=CARTESIAN_POINT ( 'NONE',  ( 786.6156483768007774, -241.4419599262322720, 315.5913626894246136 ) ) ;
#35408=DIRECTION ( 'NONE',  ( 0.000000000000000000, 0.000000000000000000, 1.000000000000000000 ) ) ;
#35412=CARTESIAN_POINT ( 'NONE',  ( 786.2694204179717872, -141.2817908451530400, 305.1769319972829067 ) ) ;
#35421=CARTESIAN_POINT ( 'NONE',  ( 772.4999999999993179, -462.9681489794448339, 370.0000000000000568 ) ) ;
#35422=CARTESIAN_POINT ( 'NONE',  ( 795.1360043628807261, -20.08914811296592973, 360.2193346964456282 ) ) ;
#35424=CARTESIAN_POINT ( 'NONE',  ( 812.3518521366052028, -265.0999726633344267, 326.5853460496235243 ) ) ;
#35426=CARTESIAN_POINT ( 'NONE',  ( 814.5518280994195948, -207.7255117493289447, 332.4837098697145734 ) ) ;
#35430=CARTESIAN_POINT ( 'NONE',  ( 771.1735550268778070, -321.1800572038740142, 316.3353852180827630 ) ) ;
#35431=CARTESIAN_POINT ( 'NONE',  ( 786.5483106153019435, -79.64542720878957027, 364.1601925771022366 ) ) ;
#35432=CARTESIAN_POINT ( 'NONE',  ( 763.8424801807145741, -42.00906357242603661, 320.5453621957614700 ) ) ;
#35435=DIRECTION ( 'NONE',  ( -0.000000000000000000, 1.000000000000000000, -0.000000000000000000 ) ) ;
#35436=CARTESIAN_POINT ( 'NONE',  ( 775.9200461376533440, -119.8055962898690865, 315.3028492785443291 ) ) ;
#35437=CARTESIAN_POINT ( 'NONE',  ( 781.7834795799800531, -346.8164208402376971, 315.0636971347436202 ) ) ;
#35442=CARTESIAN_POINT ( 'NONE',  ( 754.8072714833581358, -100.8164208402383792, 338.1981804954720587 ) ) ;
#35445=CARTESIAN_POINT ( 'NONE',  ( 745.1769319972822814, -425.8055962898680491, 346.2694204179732083 ) ) ;
#35447=CARTESIAN_POINT ( 'NONE',  ( 754.8072714833581358, -316.8164208402377540, 338.1981804954720587 ) ) ;
#35451=CARTESIAN_POINT ( 'NONE',  ( 797.8594530101008786, -421.5436935675101040, 322.1405469898980982 ) ) ;
#35457=CARTESIAN_POINT ( 'NONE',  ( 805.1927285166397041, -136.8164208402382371, 341.8018195045277707 ) ) ;
#35458=CARTESIAN_POINT ( 'NONE',  ( 787.6308680596127942, -131.2601417444144829, 364.1105419155492768 ) ) ;
#35461=CARTESIAN_POINT ( 'NONE',  ( 773.7943932421234194, -407.8055962898681628, 305.5313806188329409 ) ) ;
#35466=CARTESIAN_POINT ( 'NONE',  ( 757.7880784355613741, -42.00906357242603661, 312.4576283171834916 ) ) ;
#35470=CARTESIAN_POINT ( 'NONE',  ( 799.9999999999993179, -512.9681489794448908, 309.9999999999998863 ) ) ;
#35474=CARTESIAN_POINT ( 'NONE',  ( 802.9823548866075953, -361.0999726633341425, 330.0799878456151077 ) ) ;
#35475=CARTESIAN_POINT ( 'NONE',  ( 749.5768839229115201, -348.5545181178796383, 358.0661480581553064 ) ) ;
#35480=CARTESIAN_POINT ( 'NONE',  ( 762.1177392798416577, -162.5545181178802352, 309.8865473780659272 ) ) ;
#35482=CARTESIAN_POINT ( 'NONE',  ( 751.9810565676468741, -122.0891481129656171, 360.9747183278973921 ) ) ;
#35487=CARTESIAN_POINT ( 'NONE',  ( 771.1735550268778070, -177.1800572038744690, 316.3353852180827630 ) ) ;
#35488=CARTESIAN_POINT ( 'NONE',  ( 809.0717654672305343, -460.9181544815156713, 360.1688906516309885 ) ) ;
#35492=CARTESIAN_POINT ( 'NONE',  ( 812.6845335610512393, -7.987414471687621642, 353.5525998758768651 ) ) ;
#35497=CARTESIAN_POINT ( 'NONE',  ( 793.4146539503750546, -313.9874144716866908, 307.6481478633938877 ) ) ;
#35498=CARTESIAN_POINT ( 'NONE',  ( 797.8594530101009923, -133.5436935675110419, 322.1405469898982119 ) ) ;
#35499=EDGE_LOOP ( 'NONE', ( #41941, #44184 ) ) ;
#35500=CARTESIAN_POINT ( 'NONE',  ( 764.8639956371174549, -296.0891481129650629, 319.7806653035542013 ) ) ;
#35502=CARTESIAN_POINT ( 'NONE',  ( 767.7687537140311633, -71.90732993114760063, 372.7932403749916830 ) ) ;
#35507=CARTESIAN_POINT ( 'NONE',  ( 781.7834795799800531, -34.81642084023861372, 315.0636971347436202 ) ) ;
#35509=CARTESIAN_POINT ( 'NONE',  ( 747.2067596250078623, -387.1800572038738437, 352.2312462859687230 ) ) ;
#35510=CARTESIAN_POINT ( 'NONE',  ( 810.1134526219336749, -272.5328690171413086, 357.8822607201570349 ) ) ;
#35511=CARTESIAN_POINT ( 'NONE',  ( 744.9990715423526808, -66.35105083532378956, 341.2370466360926002 ) ) ;
#35517=CARTESIAN_POINT ( 'NONE',  ( 792.3570229623688874, -405.1800572038737300, 373.1304606946836202 ) ) ;
#35521=FACE_OUTER_BOUND ( 'NONE', #6586, .T. ) ;
#35523=CARTESIAN_POINT ( 'NONE',  ( 757.0176451133909268, -253.0999726633345119, 349.9200121543848354 ) ) ;
#35524=CARTESIAN_POINT ( 'NONE',  ( 768.0187753319979720, -152.6346026584200786, 318.0580252608186242 ) ) ;
#35529=CARTESIAN_POINT ( 'NONE',  ( 760.5453621957607311, -309.0783235625957559, 323.8424801807151425 ) ) ;
#35531=CARTESIAN_POINT ( 'NONE',  ( 747.6481478633932056, -37.09997266333514432, 353.4146539503763620 ) ) ;
#35532=VECTOR ( 'NONE', #6632, 1000.000000000000000 ) ;
#35534=CARTESIAN_POINT ( 'NONE',  ( 792.3570229623688874, -213.1800572038743553, 373.1304606946836202 ) ) ;
#35535=CARTESIAN_POINT ( 'NONE',  ( 804.4286716492782716, -89.36187538569299704, 345.3141322388244703 ) ) ;
#35536=DIRECTION ( 'NONE',  ( -1.000000000000000000, -0.000000000000000000, 0.000000000000000000 ) ) ;
#35538=CARTESIAN_POINT ( 'NONE',  ( 757.7880784355613741, -450.0090635724248500, 312.4576283171834916 ) ) ;
#35541=CARTESIAN_POINT ( 'NONE',  ( 755.0488828828309806, -353.8055962898683333, 344.1219089521771934 ) ) ;
#35542=CARTESIAN_POINT ( 'NONE',  ( 772.5602148656447525, -57.72551174932945628, 305.7998596910095443 ) ) ;
#35544=CARTESIAN_POINT ( 'NONE',  ( 756.7813123517142913, -67.98741447168742980, 329.9779781133712504 ) ) ;
#35546=CARTESIAN_POINT ( 'NONE',  ( 778.7502325331095108, -192.3510508353233774, 304.6391490659818828 ) ) ;
#35547=CARTESIAN_POINT ( 'NONE',  ( 768.0187753319979720, -32.63460265842044095, 318.0580252608186242 ) ) ;
#35550=CARTESIAN_POINT ( 'NONE',  ( 800.2193346964447755, -210.9982390220561967, 355.1360043628815788 ) ) ;
#35552=CARTESIAN_POINT ( 'NONE',  ( 774.6858677611749044, -321.7255117493286320, 315.5713283507209894 ) ) ;
#35557=CARTESIAN_POINT ( 'NONE',  ( 755.0488828828309806, -65.80559628986925702, 344.1219089521771934 ) ) ;
#35559=CARTESIAN_POINT ( 'NONE',  ( 745.4481719005789273, -291.7255117493286320, 347.5162901302853697 ) ) ;
#35560=CARTESIAN_POINT ( 'NONE',  ( 814.8230680027162407, -5.805596289869448867, 333.7305795820267917 ) ) ;
#35565=CARTESIAN_POINT ( 'NONE',  ( 814.9108240113580450, -280.2709662947833067, 337.5031285880265273 ) ) ;
#35567=CARTESIAN_POINT ( 'NONE',  ( 772.3691319403857278, -335.2601417444137724, 315.8894580844506663 ) ) ;
#35569=CARTESIAN_POINT ( 'NONE',  ( 805.2837595273609850, -170.7363362996983938, 340.5290396650784714 ) ) ;
#35570=CARTESIAN_POINT ( 'NONE',  ( 755.3201227861273992, -3.725511749329622813, 345.3687786644892981 ) ) ;
#35575=CARTESIAN_POINT ( 'NONE',  ( 791.0478386215596629, -285.8272453906071178, 306.7653713866226326 ) ) ;
#35576=CARTESIAN_POINT ( 'NONE',  ( 804.1601925771018387, -199.4419599262324709, 346.5483106153029098 ) ) ;
#35578=CARTESIAN_POINT ( 'NONE',  ( 767.8955696845333705, -0.4527844766023628176, 362.1676090361162323 ) ) ;
#35581=CARTESIAN_POINT ( 'NONE',  ( 777.5031285880264704, -22.81642084023865280, 374.9108240113588408 ) ) ;
#35582=CARTESIAN_POINT ( 'NONE',  ( 812.7932403749906598, -87.18005720387481006, 327.7687537140311633 ) ) ;
#35588=CARTESIAN_POINT ( 'NONE',  ( 752.7379699480933368, -372.0090635724250205, 361.9858362298580232 ) ) ;
#35590=CARTESIAN_POINT ( 'NONE',  ( 805.0032342141412300, -325.5436935675105019, 314.9967657858571783 ) ) ;
#35594=CARTESIAN_POINT ( 'NONE',  ( 755.0636971347428243, -436.2709662947827951, 341.7834795799807353 ) ) ;
#35595=CARTESIAN_POINT ( 'NONE',  ( 772.4468031744293057, -201.8272453906073451, 363.8651313633793620 ) ) ;
#35598=CARTESIAN_POINT ( 'NONE',  ( 786.2056067578752163, -83.80559628986920018, 374.4686193811670023 ) ) ;
#35599=CARTESIAN_POINT ( 'NONE',  ( 758.0580252608178853, -414.4527844766010389, 328.0187753319985404 ) ) ;
#35606=EDGE_CURVE ( 'NONE', #37078, #22109, #36038, .T. ) ;
#35607=CARTESIAN_POINT ( 'NONE',  ( 762.1405469898971887, -217.5436935675107293, 357.8594530101015607 ) ) ;
#35608=CARTESIAN_POINT ( 'NONE',  ( 767.8955696845334842, -240.4527844766015789, 362.1676090361161755 ) ) ;
#35613=CARTESIAN_POINT ( 'NONE',  ( 774.6858677611749044, -417.7255117493283478, 315.5713283507209894 ) ) ;
#35618=CARTESIAN_POINT ( 'NONE',  ( 782.4968714119720516, -154.8164208402382371, 305.0891759886411023 ) ) ;
#35619=CARTESIAN_POINT ( 'NONE',  ( 758.4439275373578084, -276.5545181178798657, 353.2243759319684386 ) ) ;
#35626=CARTESIAN_POINT ( 'NONE',  ( 764.0069404352550464, -231.0783235625960401, 359.2566176426627180 ) ) ;
#35636=CARTESIAN_POINT ( 'NONE',  ( 793.5525998758768083, -127.0999726633348672, 372.6845335610516941 ) ) ;
#35642=CARTESIAN_POINT ( 'NONE',  ( 771.3260364891663130, -379.6454272087886466, 306.0683387631859773 ) ) ;
#35648=CARTESIAN_POINT ( 'NONE',  ( 802.1676090361156639, -14.63460265842049424, 327.8955696845344505 ) ) ;
#35650=CARTESIAN_POINT ( 'NONE',  ( 799.9636004259356241, -238.9181544815163534, 311.2241431872006956 ) ) ;
#35652=CARTESIAN_POINT ( 'NONE',  ( 804.7487373415286811, -235.5436935675107293, 364.7487373415288516 ) ) ;
#35654=CARTESIAN_POINT ( 'NONE',  ( 799.9999999999993179, -512.9681489794448908, 339.9999999999999432 ) ) ;
#35655=CARTESIAN_POINT ( 'NONE',  ( 804.6798772138708955, -327.7255117493285184, 334.6312213355107019 ) ) ;
#35656=CARTESIAN_POINT ( 'NONE',  ( 786.5483106153019435, -103.6454272087894850, 364.1601925771022366 ) ) ;
#35657=CARTESIAN_POINT ( 'NONE',  ( 783.0745993439762742, -80.19088175424411702, 365.1016975059196739 ) ) ;
#35662=CARTESIAN_POINT ( 'NONE',  ( 756.1348686366196716, -161.2601417444143976, 347.5531968255698416 ) ) ;
#35663=CARTESIAN_POINT ( 'NONE',  ( 797.8594530101008786, -349.5436935675102745, 322.1405469898980982 ) ) ;
#35666=CARTESIAN_POINT ( 'NONE',  ( 778.2165204200184689, -118.8164208402383508, 364.9363028652563230 ) ) ;
#35669=CARTESIAN_POINT ( 'NONE',  ( 756.1443688327750579, -429.6237781080499190, 314.3581564841659315 ) ) ;
#35671=CARTESIAN_POINT ( 'NONE',  ( 755.0636971347428243, -316.2709662947832499, 341.7834795799807353 ) ) ;
#35675=CARTESIAN_POINT ( 'NONE',  ( 778.2165204200184689, -430.8164208402374129, 364.9363028652563230 ) ) ;
#35684=CARTESIAN_POINT ( 'NONE',  ( 784.1219089521767955, -453.2817908451519315, 315.0488828828318333 ) ) ;
#35685=CARTESIAN_POINT ( 'NONE',  ( 764.0069404352550464, -111.0783235625964096, 359.2566176426627180 ) ) ;
#35688=CARTESIAN_POINT ( 'NONE',  ( 810.1134526219336749, -392.5328690171409107, 357.8822607201570349 ) ) ;
#35694=CARTESIAN_POINT ( 'NONE',  ( 814.8207195650702488, -26.19088175424427334, 336.2433038121456548 ) ) ;
#35705=CARTESIAN_POINT ( 'NONE',  ( 773.4516893846965786, -379.6454272087886466, 315.8398074228977066 ) ) ;
#35706=CARTESIAN_POINT ( 'NONE',  ( 748.6759233522253680, -328.3726999360615650, 324.3348316497537098 ) ) ;
#35710=CARTESIAN_POINT ( 'NONE',  ( 750.9282345327678740, -136.9181544815166376, 319.8311093483690115 ) ) ;
#35712=CARTESIAN_POINT ( 'NONE',  ( 792.2312462859673587, -107.9073299311474727, 307.2067596250082602 ) ) ;
#35716=CARTESIAN_POINT ( 'NONE',  ( 795.1360043628807261, -212.0891481129652902, 360.2193346964456282 ) ) ;
#35719=CARTESIAN_POINT ( 'NONE',  ( 761.4292242960306112, 6.536390973028352924, 323.2154366446414429 ) ) ;
#35724=EDGE_CURVE ( 'NONE', #11197, #36800, #36563, .T. ) ;
#35725=CARTESIAN_POINT ( 'NONE',  ( 746.7653713866222915, 6.739858255585061464, 351.0478386215610271 ) ) ;
#35727=CARTESIAN_POINT ( 'NONE',  ( 764.8639956371174549, -8.089148112965974136, 319.7806653035542013 ) ) ;
#35730=CARTESIAN_POINT ( 'NONE',  ( 756.1443688327750579, -309.6237781080502600, 314.3581564841659315 ) ) ;
#35731=CARTESIAN_POINT ( 'NONE',  ( 755.3201227861273992, -147.7255117493291721, 345.3687786644892981 ) ) ;
#35734=CARTESIAN_POINT ( 'NONE',  ( 788.8264449731200330, -309.1800572038740711, 363.6646147819171233 ) ) ;
#35737=CARTESIAN_POINT ( 'NONE',  ( 782.4968714119720516, -82.81642084023846451, 305.0891759886411023 ) ) ;
#35743=CARTESIAN_POINT ( 'NONE',  ( 803.6646147819161570, -65.90732993114758642, 348.8264449731210561 ) ) ;
#35744=CARTESIAN_POINT ( 'NONE',  ( 760.7433823573367135, -324.0090635724251911, 355.9930595647440441 ) ) ;
#35746=CARTESIAN_POINT ( 'NONE',  ( 745.4481719005789273, -387.7255117493284047, 347.5162901302853697 ) ) ;
#35747=CARTESIAN_POINT ( 'NONE',  ( 800.1688906516307043, -298.1692326535049347, 369.0717654672308186 ) ) ;
#35750=CARTESIAN_POINT ( 'NONE',  ( 786.2056067578752163, -59.80559628986927834, 374.4686193811670023 ) ) ;
#35757=CARTESIAN_POINT ( 'NONE',  ( 759.0252816721024374, -384.9982390220556567, 368.0189434323527280 ) ) ;
#35763=CARTESIAN_POINT ( 'NONE',  ( 786.5483106153019435, -247.6454272087890160, 364.1601925771022366 ) ) ;
#35764=CARTESIAN_POINT ( 'NONE',  ( 755.5713283507202505, -149.3618753856928265, 334.6858677611754729 ) ) ;
#35766=VERTEX_POINT ( 'NONE', #14329 ) ;
#35769=CARTESIAN_POINT ( 'NONE',  ( 804.1601925771018387, -343.4419599262320162, 346.5483106153029098 ) ) ;
#35771=CARTESIAN_POINT ( 'NONE',  ( 786.2694204179717872, -45.28179084515329578, 305.1769319972829067 ) ) ;
#35774=AXIS2_PLACEMENT_3D ( 'NONE', #2019, #7657, #25428 ) ;
#35775=CARTESIAN_POINT ( 'NONE',  ( 767.6429770376289525, -201.1800572038744690, 306.8695393053162093 ) ) ;
#35776=CARTESIAN_POINT ( 'NONE',  ( 795.1360043628807261, -116.0891481129656029, 360.2193346964456282 ) ) ;
#35779=CARTESIAN_POINT ( 'NONE',  ( 766.4474001241216001, -451.0999726633339151, 307.3154664389482491 ) ) ;
#35782=CARTESIAN_POINT ( 'NONE',  ( 779.4709603349208464, -360.3510508353228374, 314.7162404726379918 ) ) ;
#35783=CARTESIAN_POINT ( 'NONE',  ( 814.5518280994195948, -63.72551174932941365, 332.4837098697145166 ) ) ;
#35785=CARTESIAN_POINT ( 'NONE',  ( 784.0799538623451781, -59.80559628986927834, 364.6971507214555572 ) ) ;
#35789=CARTESIAN_POINT ( 'NONE',  ( 747.3154664389472828, -211.9874144716869750, 326.4474001241230781 ) ) ;
#35790=CARTESIAN_POINT ( 'NONE',  ( 800.2193346964446619, -42.99823902205676518, 355.1360043628816925 ) ) ;
#35794=CARTESIAN_POINT ( 'NONE',  ( 800.0135310231082713, -206.0891481129653471, 325.0180583372163028 ) ) ;
#35796=CARTESIAN_POINT ( 'NONE',  ( 755.3201227861273992, -339.7255117493285184, 345.3687786644892981 ) ) ;
#35797=AXIS2_PLACEMENT_3D ( 'NONE', #15713, #26095, #5531 ) ;
#35801=CARTESIAN_POINT ( 'NONE',  ( 790.8726784830453198, -58.71468719896019905, 362.5472867521010585 ) ) ;
#35805=CARTESIAN_POINT ( 'NONE',  ( 787.5162901302840055, -275.3618753856924286, 305.4481719005793252 ) ) ;
#35806=CARTESIAN_POINT ( 'NONE',  ( 778.7502325331095108, -0.3510508353240099355, 304.6391490659818828 ) ) ;
#35811=CARTESIAN_POINT ( 'NONE',  ( 744.7301800767019131, -292.8164208402376971, 337.4774526936615757 ) ) ;
#35814=CARTESIAN_POINT ( 'NONE',  ( 769.0155153010367712, -154.3726999360620198, 362.7791456095907279 ) ) ;
#35815=CARTESIAN_POINT ( 'NONE',  ( 803.6646147819161570, -41.90732993114767169, 348.8264449731210561 ) ) ;
#35820=CARTESIAN_POINT ( 'NONE',  ( 793.5525998758768083, -271.0999726633344267, 372.6845335610516941 ) ) ;
#35821=CARTESIAN_POINT ( 'NONE',  ( 769.1273215169530886, -214.7146871989597230, 317.4527132478988847 ) ) ;
#35822=VECTOR ( 'NONE', #12936, 1000.000000000000114 ) ;
#35825=CARTESIAN_POINT ( 'NONE',  ( 790.7339360641449275, -462.9631818684622999, 362.6136660859752965 ) ) ;
#35828=VECTOR ( 'NONE', #9851, 1000.000000000000000 ) ;
#35829=CARTESIAN_POINT ( 'NONE',  ( 746.8695393053150156, -29.90732993114771787, 327.6429770376306010 ) ) ;
#35830=CARTESIAN_POINT ( 'NONE',  ( 777.5031285880264704, -94.81642084023843609, 374.9108240113588408 ) ) ;
#35833=LINE ( 'NONE', #29372, #37959 ) ;
#35835=CARTESIAN_POINT ( 'NONE',  ( 795.8262568251477660, -406.3726999360612808, 308.3538107759623585 ) ) ;
#35837=CARTESIAN_POINT ( 'NONE',  ( 751.6929314249748586, -342.9982390220557136, 318.8095938919659034 ) ) ;
#35842=CARTESIAN_POINT ( 'NONE',  ( 765.0180583372156207, -432.9982390220555999, 360.0135310231089534 ) ) ;
#35843=CARTESIAN_POINT ( 'NONE',  ( 755.5913626894240451, -181.6454272087892434, 346.6156483768012890 ) ) ;
#35846=CARTESIAN_POINT ( 'NONE',  ( 776.2433038121456548, -108.8965053807782084, 374.8207195650711014 ) ) ;
#35847=CARTESIAN_POINT ( 'NONE',  ( 774.6312213355098493, -407.3618753856920307, 364.6798772138717482 ) ) ;
#35853=CARTESIAN_POINT ( 'NONE',  ( 755.0636971347428243, -220.2709662947834772, 341.7834795799807353 ) ) ;
#35854=CARTESIAN_POINT ( 'NONE',  ( 792.1044303154646968, -228.4527844766016074, 317.8323909638837677 ) ) ;
#35858=CARTESIAN_POINT ( 'NONE',  ( 756.5762568750052424, -435.1800572038737869, 348.7366044899774238 ) ) ;
#35862=CARTESIAN_POINT ( 'NONE',  ( 782.5225473063383106, -190.2709662947835625, 375.2698199232970637 ) ) ;
#35863=CARTESIAN_POINT ( 'NONE',  ( 757.4527132478984868, -256.3726999360617924, 329.1273215169538844 ) ) ;
#35866=CARTESIAN_POINT ( 'NONE',  ( 776.2433038121456548, -228.8965053807778816, 374.8207195650711014 ) ) ;
#35872=CARTESIAN_POINT ( 'NONE',  ( 763.2154366446407039, -237.6237781080505442, 321.4292242960311228 ) ) ;
#35881=CARTESIAN_POINT ( 'NONE',  ( 814.2805881961230625, -169.6454272087892718, 331.2368401574024119 ) ) ;
#35886=CARTESIAN_POINT ( 'NONE',  ( 811.0346526505616112, -14.63460265842049424, 323.0537975583477532 ) ) ;
#35890=CARTESIAN_POINT ( 'NONE',  ( 767.8955696845333705, -0.4527844766023628176, 362.1676090361162323 ) ) ;
#35891=CARTESIAN_POINT ( 'NONE',  ( 750.9282345327678740, -232.9181544815163249, 319.8311093483690115 ) ) ;
#35893=CARTESIAN_POINT ( 'NONE',  ( 796.9462024416508257, -228.4527844766015789, 308.9653473494370246 ) ) ;
#35898=CARTESIAN_POINT ( 'NONE',  ( 797.6776695296629214, -307.5436935675104451, 357.6776695296636603 ) ) ;
#35900=CARTESIAN_POINT ( 'NONE',  ( 802.9823548866075953, -73.09997266333502353, 330.0799878456151077 ) ) ;
#35904=CARTESIAN_POINT ( 'NONE',  ( 804.1601925771018387, -151.4419599262326415, 346.5483106153029098 ) ) ;
#35905=CARTESIAN_POINT ( 'NONE',  ( 778.1981804954714335, -370.2709662947831362, 314.8072714833589885 ) ) ;
#35911=CARTESIAN_POINT ( 'NONE',  ( 800.9747183278959710, 11.00176097794305541, 311.9810565676471583 ) ) ;
#35914=CARTESIAN_POINT ( 'NONE',  ( 756.5762568750052424, -339.1800572038740142, 348.7366044899774238 ) ) ;
#35916=CARTESIAN_POINT ( 'NONE',  ( 790.8050863131179540, -452.8379544210779954, 362.5841948692291226 ) ) ;
#35924=CARTESIAN_POINT ( 'NONE',  ( 774.6858677611749044, 14.27448825067031812, 315.5713283507209894 ) ) ;
#35925=CARTESIAN_POINT ( 'NONE',  ( 760.5453621957607311, -141.0783235625962959, 323.8424801807151425 ) ) ;
#35929=CARTESIAN_POINT ( 'NONE',  ( 786.2056067578752163, -395.8055962898682765, 374.4686193811670023 ) ) ;
#35934=CARTESIAN_POINT ( 'NONE',  ( 797.8822607201568644, -78.55451811788046257, 370.1134526219340160 ) ) ;
#35939=CARTESIAN_POINT ( 'NONE',  ( 791.7608162188021197, 205.0000000000000568, 319.9999999999999432 ) ) ;
#35944=CARTESIAN_POINT ( 'NONE',  ( 798.5707757039680246, -389.4636090269704027, 356.7845633553585003 ) ) ;
#35946=CARTESIAN_POINT ( 'NONE',  ( 757.7880784355613741, -354.0090635724250774, 312.4576283171834916 ) ) ;
#35950=CARTESIAN_POINT ( 'NONE',  ( 793.5525998758768083, -151.0999726633347677, 372.6845335610516941 ) ) ;
#35952=CARTESIAN_POINT ( 'NONE',  ( 814.5518280994195948, -111.7255117493293000, 332.4837098697145734 ) ) ;
#35956=CARTESIAN_POINT ( 'NONE',  ( 765.0180583372156207, -216.9982390220562252, 360.0135310231089534 ) ) ;
#35957=CARTESIAN_POINT ( 'NONE',  ( 745.5313806188320314, -447.2817908451521021, 333.7943932421247268 ) ) ;
#35960=CARTESIAN_POINT ( 'NONE',  ( 799.9999999999993179, -462.9681489794448339, 317.6393202250019954 ) ) ;
#35961=CARTESIAN_POINT ( 'NONE',  ( 761.9338519418445230, -14.53286901714214707, 370.4231160770881957 ) ) ;
#35966=CARTESIAN_POINT ( 'NONE',  ( 759.7806653035534055, -30.99823902205680071, 324.8639956371180801 ) ) ;
#35968=CARTESIAN_POINT ( 'NONE',  ( 744.9990715423526808, -354.3510508353228943, 341.2370466360926002 ) ) ;
#35969=CARTESIAN_POINT ( 'NONE',  ( 774.6312213355098493, -143.3618753856927697, 364.6798772138717482 ) ) ;
#35974=CARTESIAN_POINT ( 'NONE',  ( 800.2193346964447755, -330.9982390220558273, 355.1360043628815788 ) ) ;
#35979=ORIENTED_EDGE ( 'NONE', *, *, #2646, .T. ) ;
#35981=CARTESIAN_POINT ( 'NONE',  ( 778.2165204200184689, -46.81642084023858530, 364.9363028652563230 ) ) ;
#35982=CARTESIAN_POINT ( 'NONE',  ( 804.6971507214547046, -387.2817908451522726, 344.0799538623459739 ) ) ;
#35984=CARTESIAN_POINT ( 'NONE',  ( 800.9747183278959710, -396.9982390220556567, 311.9810565676471583 ) ) ;
#35985=CARTESIAN_POINT ( 'NONE',  ( 815.1787889125755555, -294.8965053807775689, 343.7953271457877804 ) ) ;
#35986=CARTESIAN_POINT ( 'NONE',  ( 810.1134526219336749, -56.53286901714201917, 357.8822607201570349 ) ) ;
#35991=EDGE_CURVE ( 'NONE', #24420, #19781, #33075, .T. ) ;
#35994=CARTESIAN_POINT ( 'NONE',  ( 763.2262854647970016, -440.6346026584191122, 309.2812353651462445 ) ) ;
#36001=CARTESIAN_POINT ( 'NONE',  ( 799.2566176426618085, -264.0090635724253616, 324.0069404352559559 ) ) ;
#36002=CARTESIAN_POINT ( 'NONE',  ( 757.8323909638827445, -170.6346026584199649, 352.1044303154654358 ) ) ;
#36006=CARTESIAN_POINT ( 'NONE',  ( 795.9930595647434757, -315.0783235625957559, 320.7433823573372820 ) ) ;
#36009=CARTESIAN_POINT ( 'NONE',  ( 762.1177392798416577, -42.55451811788057626, 309.8865473780659272 ) ) ;
#36011=CARTESIAN_POINT ( 'NONE',  ( 755.0636971347428243, -124.2709662947837899, 341.7834795799807353 ) ) ;
#36015=CARTESIAN_POINT ( 'NONE',  ( 796.2681130854250569, -462.7578698805381237, 371.0719813302654870 ) ) ;
#36018=CARTESIAN_POINT ( 'NONE',  ( 800.7704444035546203, -388.1692326535045936, 326.0291762391768771 ) ) ;
#36023=CARTESIAN_POINT ( 'NONE',  ( 754.8983024940795303, -66.89650538077835051, 336.9254006560228163 ) ) ;
#36026=CARTESIAN_POINT ( 'NONE',  ( 751.2241431872005251, -208.1692326535051905, 359.9636004259367610 ) ) ;
#36027=CARTESIAN_POINT ( 'NONE',  ( 804.4286716492782716, -41.36187538569314626, 345.3141322388244703 ) ) ;
#36031=CARTESIAN_POINT ( 'NONE',  ( 759.9864689768902508, -218.0891481129653187, 354.9819416627836404 ) ) ;
#36034=CARTESIAN_POINT ( 'NONE',  ( 781.7834795799800531, -346.8164208402376971, 315.0636971347436202 ) ) ;
#36038=CIRCLE ( 'NONE', #15369, 10.00000000000000888 ) ;
#36039=CARTESIAN_POINT ( 'NONE',  ( 814.2001403089898304, -281.3618753856923718, 347.4397851343538264 ) ) ;
#36040=CARTESIAN_POINT ( 'NONE',  ( 788.7631598425961101, -1.441959926233096656, 305.7194118038759143 ) ) ;
#36044=ORIENTED_EDGE ( 'NONE', *, *, #16217, .F. ) ;
#36047=CARTESIAN_POINT ( 'NONE',  ( 815.2698199232961542, -280.8164208402378677, 342.5225473063383106 ) ) ;
#36049=CARTESIAN_POINT ( 'NONE',  ( 757.4527132478984868, -208.3726999360619061, 329.1273215169538844 ) ) ;
#36051=CARTESIAN_POINT ( 'NONE',  ( 780.5236548040995785, -164.7363362996983938, 314.9735926884559944 ) ) ;
#36052=CARTESIAN_POINT ( 'NONE',  ( 781.7834795799800531, -34.81642084023861372, 315.0636971347436202 ) ) ;
#36053=ORIENTED_EDGE ( 'NONE', *, *, #26099, .T. ) ;
#36056=CARTESIAN_POINT ( 'NONE',  ( 811.3240766477731540, -268.3726999360616787, 355.6651683502462902 ) ) ;
#36057=CARTESIAN_POINT ( 'NONE',  ( 756.7813123517142913, -211.9874144716869750, 329.9779781133712504 ) ) ;
#36060=CARTESIAN_POINT ( 'NONE',  ( 793.0897708529556667, -462.5545181178792973, 361.3366627262616362 ) ) ;
#36062=CARTESIAN_POINT ( 'NONE',  ( 811.0346526505616112, -62.63460265842031305, 323.0537975583477532 ) ) ;
#36063=CARTESIAN_POINT ( 'NONE',  ( 804.7487373415286811, -115.5436935675110988, 364.7487373415288516 ) ) ;
#36067=CARTESIAN_POINT ( 'NONE',  ( 771.3260364891663130, -379.6454272087886466, 306.0683387631859773 ) ) ;
#36070=CARTESIAN_POINT ( 'NONE',  ( 767.7687537140311633, -311.9073299311468759, 372.7932403749916830 ) ) ;
#36073=CARTESIAN_POINT ( 'NONE',  ( 771.1735550268778070, -417.1800572038736163, 316.3353852180827630 ) ) ;
#36074=CARTESIAN_POINT ( 'NONE',  ( 804.8461984189677878, -194.1908817542437475, 336.9566956441385628 ) ) ;
#36077=CARTESIAN_POINT ( 'NONE',  ( 749.8865473780648472, -116.5328690171418202, 322.1177392798429082 ) ) ;
#36078=CARTESIAN_POINT ( 'NONE',  ( 755.5713283507202505, -437.3618753856919170, 334.6858677611754729 ) ) ;
#36085=CARTESIAN_POINT ( 'NONE',  ( 771.1735550268778070, -249.1800572038742416, 316.3353852180827630 ) ) ;
#36086=CARTESIAN_POINT ( 'NONE',  ( 774.6858677611749044, -225.7255117493289163, 315.5713283507209894 ) ) ;
#36089=CARTESIAN_POINT ( 'NONE',  ( 771.2633955100217236, -431.9073299311464211, 363.4237431249939618 ) ) ;
#36092=CARTESIAN_POINT ( 'NONE',  ( 745.7998596910086917, -197.3618753856926560, 332.5602148656461168 ) ) ;
#36093=CARTESIAN_POINT ( 'NONE',  ( 755.5913626894240451, -253.6454272087889876, 346.6156483768012890 ) ) ;
#36096=CARTESIAN_POINT ( 'NONE',  ( 805.9055244015594326, -219.6237781080506295, 315.8990559732753240 ) ) ;
#36098=ORIENTED_EDGE ( 'NONE', *, *, #3514, .F. ) ;
#36102=CARTESIAN_POINT ( 'NONE',  ( 805.0264073115434940, -270.3510508353231216, 339.4763451958999099 ) ) ;
#36109=CARTESIAN_POINT ( 'NONE',  ( 746.4236121716829757, -183.8272453906074020, 328.8385539511384650 ) ) ;
#36113=CARTESIAN_POINT ( 'NONE',  ( 747.2067596250078623, -27.18005720387500901, 352.2312462859687230 ) ) ;
#36118=CARTESIAN_POINT ( 'NONE',  ( 774.6312213355099630, 0.6381246143067236254, 364.6798772138717482 ) ) ;
#36119=CARTESIAN_POINT ( 'NONE',  ( 773.7305795820266212, -273.2817908451526137, 374.8230680027170365 ) ) ;
#36121=CARTESIAN_POINT ( 'NONE',  ( 772.4837098697144029, -239.3618753856924570, 374.5518280994205611 ) ) ;
#36125=CARTESIAN_POINT ( 'NONE',  ( 765.0180583372156207, -312.9982390220559409, 360.0135310231089534 ) ) ;
#36128=CARTESIAN_POINT ( 'NONE',  ( 805.2837595273609850, -98.73633629969859271, 340.5290396650784714 ) ) ;
#36133=CARTESIAN_POINT ( 'NONE',  ( 770.0799878456142551, -157.9874144716871456, 362.9823548866085616 ) ) ;
#36134=CARTESIAN_POINT ( 'NONE',  ( 805.1927285166397041, -376.8164208402375834, 341.8018195045277707 ) ) ;
#36137=CARTESIAN_POINT ( 'NONE',  ( 759.7806653035534055, -174.9982390220563673, 324.8639956371180801 ) ) ;
#36140=CARTESIAN_POINT ( 'NONE',  ( 796.9462024416508257, 11.54721552339760038, 308.9653473494370246 ) ) ;
#36142=CARTESIAN_POINT ( 'NONE',  ( 795.1360043628807261, -332.0891481129649492, 360.2193346964456282 ) ) ;
#36144=CARTESIAN_POINT ( 'NONE',  ( 789.5670355615794733, -453.0432664090020012, 363.0970091259334822 ) ) ;
#36150=CARTESIAN_POINT ( 'NONE',  ( 804.6971507214547046, -459.2817908451519884, 344.0799538623459739 ) ) ;
#36151=CARTESIAN_POINT ( 'NONE',  ( 751.6929314249748586, -222.9982390220561399, 318.8095938919659034 ) ) ;
#36152=CARTESIAN_POINT ( 'NONE',  ( 772.3691319403857278, -143.2601417444144829, 315.8894580844506663 ) ) ;
#36155=CARTESIAN_POINT ( 'NONE',  ( 746.7653713866222915, -401.2601417444137155, 351.0478386215610271 ) ) ;
#36160=CARTESIAN_POINT ( 'NONE',  ( 811.3240766477731540, -52.37269993606237506, 355.6651683502462902 ) ) ;
#36161=CARTESIAN_POINT ( 'NONE',  ( 779.9999999999992042, -452.9681489794448339, 339.9999999999999432 ) ) ;
#36164=( BOUNDED_CURVE ( )  B_SPLINE_CURVE ( 2, ( #20325, #5791, #13188, #19880, #5553, #34171, #16407, #30487, #41137, #44592, #44124, #27038, #23089, #34653, #2787, #30043, #12952, #30962, #2544, #13411, #9019, #44829, #16648, #27270, #19647, #9709, #23772, #45056, #27482, #24007, #20557, #15960, #41822, #13871, #25153, #35098, #13634, #39263, #28396, #6926, #17565, #17321, #461, #42043, #10389, #6697, #14566, #34869, #32091, #7619, #227, #24464, #20776, #42496, #10167, #4, #28641, #24698, #14095, #31637, #3474, #28169, #27946, #31180, #42261, #24243, #21695, #7395, #17100, #21007, #21469, #10621, #42719, #45275, #17790, #3232, #38816, #3012, #39045, #38572, #14320, #38352, #31855, #7171, #10864, #21245, #35325, #27717, #3703, #24931, #35547, #3923, #18018, #11083, #15677, #29094, #8533, #903, #7863, #11991, #15470, #8758, #21941, #5058, #39741, #36242, #36027, #22597, #4390, #35790, #4167, #32337, #4602, #29548, #43834, #26297, #43624, #39507, #19150, #43179, #28862, #43408, #18481, #11774, #18696, #33236, #33029, #1577, #15006, #11548, #11311, #32559, #1366, #18263, #32786, #4831, #25631, #29757, #36700, #29336, #8091, #12218, #18934, #22153, #25844, #26057, #1136, #8300, #15247, #39956, #22364, #40168, #36469, #40409, #691, #14789, #42943, #25388, #30679, #16128, #26520, #40841, #5954, #5272, #44535, #2034, #13356, #30436, #12895, #27430, #30213, #37378, #16828, #44304, #23275, #40620, #26979, #5736, #41079, #5494, #9435, #19823, #12440, #12659, #36918, #37601, #1794, #27213, #19589, #23500, #20044, #22824, #33906, #8971, #2259, #37135, #34122, #44777, #2735, #2488, #9201, #16356, #45001, #33684, #30907, #26739, #19365, #6183, #16597, #13135, #41307, #41528, #20273, #9658, #29988, #23721, #37833, #34364, #33450, #15901, #44074, #6647, #7116, #24194, #27660, #31805, #3418, #24638, #6430, #38995, #406, #21196, #17266, #13581, #3654, #17044, #6867, #7345, #31591, #20947, #38515, #3176, #35044, #38301, #38071, #17513, #31123, #28587, #14265, #23952, #13820, #28333, #27899, #21422, #20511, #38759, #10118, #45694, #14509, #174, #41767, #31355, #45219, #35276, #14047, #17742, #2957, #20721, #32033, #41995, #34599, #9880, #42436, #10338, #24411, #35498, #45460, #10805, #34815, #28117, #24880, #42211, #3872, #10561, #17964, #39687, #43124, #25574, #9080, #11494, #42892, #11036, #1917, #35969, #26625, #19712, #5616, #4337, #2150, #18426, #23146, #35731, #7805, #33798, #29039, #7569, #16242, #22930, #855, #8035, #37253, #32506, #16024, #21880, #14738, #19471, #37023, #5378, #42673, #28812, #12550, #22101, #36191, #25102, #4553, #11258, #39217, #30103, #14955, #40723, #21645, #4109, #18644, #32733, #1079, #25334, #15192, #29277, #43354, #39448, #11721, #26412, #32280, #40513, #18204, #8863, #636, #44189, #33567, #6303, #45114, #30321, #27325, #2370, #41418, #34015, #41645, #6533, #10224, #13471, #16709, #9767, #6759, #16468, #24302, #34234, #26848, #13700, #2844, #27541, #20613, #38408, #27780, #16937, #37491, #24070, #20158, #19939, #2608, #10000, #12767, #27103, #38188, #44651, #30551, #34708, #23834, #3066, #40957, #41880, #20832, #17156, #37718, #13013, #31242, #5851, #37949, #34932, #20387, #34485, #13247, #9319, #41194, #9548, #31016, #44412, #6068, #45338, #3298, #23390, #23611, #30794, #44886, #3758, #7680, #32159, #17627, #7455, #21078, #24765, #13929, #35162, #28004, #31914, #42781, #25453, #7927, #11143, #3541, #32403, #10683, #10449, #17392, #38882, #7237, #39572, #17848, #6995, #21308, #31477, #524, #38635, #31693, #14630, #36086, #286, #28702, #28223, #753, #35854, #10926, #61, #21760, #18323, #4231, #14153, #28464, #21997, #42318, #43006, #35385, #14386, #14851, #18079, #45581, #21529, #42564, #25213, #24994, #39324, #39105, #35608, #3982, #28928, #11370, #42098, #24525, #1635, #18759, #22210, #26358, #11827, #18991, #44133, #5115, #40672, #40239, #22424, #40462, #8814, #36303, #15734, #15305, #39799, #22662, #4660, #43460, #29603, #32849, #32620, #15523, #25897, #22883, #1862, #19203, #43681, #963, #40008, #36533, #36974, #33290, #1197, #8596, #8147, #8358, #15068, #4890, #29388, #29823, #12052, #43905, #1421, #33513, #29155, #43238, #26124, #33084, #5327, #15968, #36759, #12282, #30050, #19421, #12498, #26574, #9026, #23095, #4452, #18540, #11609, #25687, #37663, #37440, #9944, #9269, #10174, #5562, #41587, #19654, #41144, #24016, #9496, #34660, #33747, #6245, #5800, #30741, #27726, #27489, #23337, #34428, #26795, #20335, #44835, #2795, #30268, #2315, #13642, #23559, #2097, #41828, #16887, #6012, #20104, #31188, #30494, #38135, #16414, #19886, #13419, #30968, #6486, #13198, #3020, #34178, #2550, #16657, #45282, #41369, #33964, #16187, #37196, #44598, #44360, #12716, #40900, #12960, #27046, #9715, #23781, #37894, #45065, #31642, #14101, #698, #24704, #13876, #10, #38359, #39052, #3239, #28647, #21015, #232, #7401, #24251, #21252, #42048, #35332, #27952, #35552, #14571, #25159, #11089, #35105, #3709, #14794, #10396, #4175, #28174, #20782, #7624, #42504, #21475, #469, #18270, #21700, #10870, #31418, #18023, #42267, #10627, #38826, #17796, #7178, #3481, #3928, #38579, #24471, #42725, #31861, #32100, #34876, #35796, #28868, #39268, #14327, #6932, #32342, #45524, #28404, #17571, #24936, #42948, #6705, #17329, #36034, #39513, #11316, #4396, #7870, #25393, #18487, #15012, #908, #21948, #32564, #29100, #34006, #2360, #30311, #5845, #30786, #23825, #9072, #6058, #26839, #20149, #12760, #20379, #31008, #34700, #37936, #41185, #2600, #6294, #37484, #27317, #16459, #23381, #44644, #9760, #17148, #13239, #19931, #34476, #9539, #16928, #30542, #40948, #27093, #23603, #34225, #37709, #13005, #2836, #16701, #9311, #45106, #44877, #13463, #3059, #27532, #45329, #41410, #41632, #9991, #24060, #38178, #6526, #20605, #44405, #31233, #13691, #27770, #23138, #37244, #5607, #19701, #16232, #33791, #2143, #10918, #35377, #38399, #3529, #28216, #32152, #24987, #42089, #31907, #45570, #17615, #6749, #31684, #31465, #39097, #3752, #7447, #34924, #6984, #20823, #3288, #17840, #21069, #18070, #7672, #42310, #10440, #39316, #35152, #51, #13922, #21750, #27994, #515, #279, #35847, #38873, #10674, #24758, #14623, #24515, #14844, #10216, #17383, #7228, #21522, #4222, #32394, #35599, #38624, #11134, #14145, #21299, #41872, #28695, #18315, #25206, #14376, #28457, #42556, #3976, #42774, #745, #24293, #29382, #25679, #26115, #43230, #954, #5108, #22418, #43674, #25443, #12274, #19415, #40229, #36296, #32613, #22652, #15060, #8588, #39792, #18531, #1413, #29146, #22204, #8350, #11601, #11364, #40002, #36078, #1853, #33283, #42998, #32839, #1628, #1190, #26349, #39564, #12045, #8140, #18984, #4654, #18751, #7919, #15298, #43454, #36750, #36521, #19196, #21989, #11821, #5320, #25889, #4445, #33505, #15727, #4882, #33074, #15516, #40453 ),
 .UNSPECIFIED., .F., .T. ) 
 B_SPLINE_CURVE_WITH_KNOTS ( ( 3, 2, 2, 2, 2, 2, 2, 2, 2, 2, 2, 2, 2, 2, 2, 2, 2, 2, 2, 2, 2, 2, 2, 2, 2, 2, 2, 2, 2, 2, 2, 2, 2, 2, 2, 2, 2, 2, 2, 2, 2, 2, 2, 2, 2, 2, 2, 2, 2, 2, 2, 2, 2, 2, 2, 2, 2, 2, 2, 2, 2, 2, 2, 2, 2, 2, 2, 2, 2, 2, 2, 2, 2, 2, 2, 2, 2, 2, 2, 2, 2, 2, 2, 2, 2, 2, 2, 2, 2, 2, 2, 2, 2, 2, 2, 2, 2, 2, 2, 2, 2, 2, 2, 2, 2, 2, 2, 2, 2, 2, 2, 2, 2, 2, 2, 2, 2, 2, 2, 2, 2, 2, 2, 2, 2, 2, 2, 2, 2, 2, 2, 2, 2, 2, 2, 2, 2, 2, 2, 2, 2, 2, 2, 2, 2, 2, 2, 2, 2, 2, 2, 2, 2, 2, 2, 2, 2, 2, 2, 2, 2, 2, 2, 2, 2, 2, 2, 2, 2, 2, 2, 2, 2, 2, 2, 2, 2, 2, 2, 2, 2, 2, 2, 2, 2, 2, 2, 2, 2, 2, 2, 2, 2, 2, 2, 2, 2, 2, 2, 2, 2, 2, 2, 2, 2, 2, 2, 2, 2, 2, 2, 2, 2, 2, 2, 2, 2, 2, 2, 2, 2, 2, 2, 2, 2, 2, 2, 2, 2, 2, 2, 2, 2, 2, 2, 2, 2, 2, 2, 2, 2, 2, 2, 2, 2, 2, 2, 2, 2, 2, 2, 2, 2, 2, 2, 2, 2, 2, 2, 2, 2, 2, 2, 2, 2, 2, 2, 2, 2, 2, 2, 2, 2, 2, 2, 2, 2, 2, 2, 2, 2, 2, 2, 2, 2, 2, 2, 2, 2, 2, 2, 2, 2, 2, 2, 2, 2, 2, 2, 2, 2, 2, 2, 2, 2, 2, 2, 2, 2, 2, 2, 2, 2, 2, 2, 2, 2, 2, 2, 2, 2, 2, 2, 2, 2, 2, 2, 2, 2, 2, 2, 2, 2, 2, 2, 2, 2, 2, 2, 2, 2, 2, 2, 2, 2, 2, 2, 2, 2, 2, 2, 2, 2, 2, 2, 2, 2, 2, 2, 2, 2, 2, 2, 2, 2, 2, 2, 2, 2, 2, 2, 2, 2, 2, 2, 2, 2, 2, 2, 2, 2, 2, 2, 2, 2, 2, 2, 2, 2, 2, 2, 2, 2, 2, 2, 2, 2, 2, 2, 2, 2, 2, 2, 2, 2, 2, 2, 2, 2, 2, 2, 2, 2, 2, 2, 2, 2, 2, 2, 2, 2, 2, 2, 2, 2, 2, 2, 2, 2, 2, 2, 3 ),
 ( 0.000000000000000000, 0.002272727272727272617, 0.004545454545454545234, 0.006818181818181817851, 0.009090909090909090468, 0.01136363636363636395, 0.01363636363636363570, 0.01590909090909090745, 0.01818181818181818094, 0.02045454545454545442, 0.02272727272727272790, 0.02500000000000000139, 0.02727272727272727140, 0.02954545454545454489, 0.03181818181818181490, 0.03409090909090908839, 0.03636363636363636187, 0.03863636363636363535, 0.04090909090909090884, 0.04318181818181818232, 0.04545454545454545581, 0.04772727272727272929, 0.05000000000000000278, 0.05227272727272727626, 0.05454545454545454281, 0.05681818181818181629, 0.05909090909090908977, 0.06136363636363636326, 0.06363636363636362980, 0.06590909090909090329, 0.06818181818181817677, 0.07045454545454545026, 0.07272727272727272374, 0.07499999999999999722, 0.07727272727272727071, 0.07954545454545454419, 0.08181818181818181768, 0.08409090909090909116, 0.08636363636363636465, 0.08863636363636363813, 0.09090909090909091161, 0.09318181818181818510, 0.09545454545454545858, 0.09772727272727273207, 0.1000000000000000056, 0.1022727272727272790, 0.1045454545454545525, 0.1068181818181818121, 0.1090909090909090856, 0.1113636363636363591, 0.1136363636363636326, 0.1159090909090909061, 0.1181818181818181795, 0.1204545454545454530, 0.1227272727272727265, 0.1250000000000000000, 0.1272727272727272596, 0.1295454545454545470, 0.1318181818181818066, 0.1340909090909090939, 0.1363636363636363535, 0.1386363636363636409, 0.1409090909090909005, 0.1431818181818181879, 0.1454545454545454475, 0.1477272727272727348, 0.1499999999999999944, 0.1522727272727272818, 0.1545454545454545414, 0.1568181818181818288, 0.1590909090909090884, 0.1613636363636363757, 0.1636363636363636354, 0.1659090909090909227, 0.1681818181818181823, 0.1704545454545454419, 0.1727272727272727293, 0.1749999999999999889, 0.1772727272727272763, 0.1795454545454545359, 0.1818181818181818232, 0.1840909090909090828, 0.1863636363636363702, 0.1886363636363636298, 0.1909090909090909172, 0.1931818181818181768, 0.1954545454545454641, 0.1977272727272727237, 0.2000000000000000111, 0.2022727272727272707, 0.2045454545454545581, 0.2068181818181818177, 0.2090909090909091050, 0.2113636363636363646, 0.2136363636363636243, 0.2159090909090909116, 0.2181818181818181712, 0.2204545454545454586, 0.2227272727272727182, 0.2250000000000000056, 0.2272727272727272652, 0.2295454545454545525, 0.2318181818181818121, 0.2340909090909090995, 0.2363636363636363591, 0.2386363636363636465, 0.2409090909090909061, 0.2431818181818181934, 0.2454545454545454530, 0.2477272727272727404, 0.2500000000000000000, 0.2522727272727272596, 0.2545454545454545192, 0.2568181818181818343, 0.2590909090909090939, 0.2613636363636363535, 0.2636363636363636131, 0.2659090909090909283, 0.2681818181818181879, 0.2704545454545454475, 0.2727272727272727071, 0.2750000000000000222, 0.2772727272727272818, 0.2795454545454545414, 0.2818181818181818010, 0.2840909090909091161, 0.2863636363636363757, 0.2886363636363636354, 0.2909090909090908950, 0.2931818181818181546, 0.2954545454545454697, 0.2977272727272727293, 0.2999999999999999889, 0.3022727272727272485, 0.3045454545454545636, 0.3068181818181818232, 0.3090909090909090828, 0.3113636363636363424, 0.3136363636363636576, 0.3159090909090909172, 0.3181818181818181768, 0.3204545454545454364, 0.3227272727272727515, 0.3250000000000000111, 0.3272727272727272707, 0.3295454545454545303, 0.3318181818181818454, 0.3340909090909090495, 0.3363636363636363646, 0.3386363636363636243, 0.3409090909090908839, 0.3431818181818181990, 0.3454545454545454586, 0.3477272727272727182, 0.3499999999999999778, 0.3522727272727272929, 0.3545454545454545525, 0.3568181818181818121, 0.3590909090909090717, 0.3613636363636363869, 0.3636363636363636465, 0.3659090909090909061, 0.3681818181818181657, 0.3704545454545454808, 0.3727272727272727404, 0.3750000000000000000, 0.3772727272727272596, 0.3795454545454545192, 0.3818181818181818343, 0.3840909090909090939, 0.3863636363636363535, 0.3886363636363636131, 0.3909090909090909283, 0.3931818181818181879, 0.3954545454545454475, 0.3977272727272727071, 0.4000000000000000222, 0.4022727272727272818, 0.4045454545454545414, 0.4068181818181818010, 0.4090909090909091161, 0.4113636363636363757, 0.4136363636363636354, 0.4159090909090908950, 0.4181818181818182101, 0.4204545454545454697, 0.4227272727272727293, 0.4249999999999999889, 0.4272727272727272485, 0.4295454545454545636, 0.4318181818181818232, 0.4340909090909090828, 0.4363636363636363424, 0.4386363636363636576, 0.4409090909090909172, 0.4431818181818181768, 0.4454545454545454364, 0.4477272727272727515, 0.4500000000000000111, 0.4522727272727272707, 0.4545454545454545303, 0.4568181818181818454, 0.4590909090909091050, 0.4613636363636363646, 0.4636363636363636243, 0.4659090909090908839, 0.4681818181818181990, 0.4704545454545454586, 0.4727272727272727182, 0.4749999999999999778, 0.4772727272727272929, 0.4795454545454545525, 0.4818181818181818121, 0.4840909090909090717, 0.4863636363636363869, 0.4886363636363636465, 0.4909090909090909061, 0.4931818181818181657, 0.4954545454545454808, 0.4977272727272727959, 0.5000000000000000000, 0.5022727272727273151, 0.5045454545454545192, 0.5068181818181818343, 0.5090909090909090384, 0.5113636363636363535, 0.5136363636363636687, 0.5159090909090908728, 0.5181818181818181879, 0.5204545454545455030, 0.5227272727272727071, 0.5250000000000000222, 0.5272727272727272263, 0.5295454545454545414, 0.5318181818181818565, 0.5340909090909090606, 0.5363636363636363757, 0.5386363636363636909, 0.5409090909090908950, 0.5431818181818182101, 0.5454545454545454142, 0.5477272727272727293, 0.5500000000000000444, 0.5522727272727272485, 0.5545454545454545636, 0.5568181818181817677, 0.5590909090909090828, 0.5613636363636363980, 0.5636363636363636020, 0.5659090909090909172, 0.5681818181818182323, 0.5704545454545454364, 0.5727272727272727515, 0.5749999999999999556, 0.5772727272727272707, 0.5795454545454545858, 0.5818181818181817899, 0.5840909090909089940, 0.5863636363636363091, 0.5886363636363636243, 0.5909090909090909394, 0.5931818181818181435, 0.5954545454545454586, 0.5977272727272727737, 0.5999999999999999778, 0.6022727272727272929, 0.6045454545454544970, 0.6068181818181818121, 0.6090909090909091272, 0.6113636363636363313, 0.6136363636363636465, 0.6159090909090909616, 0.6181818181818181657, 0.6204545454545454808, 0.6227272727272726849, 0.6250000000000000000, 0.6272727272727273151, 0.6295454545454545192, 0.6318181818181818343, 0.6340909090909090384, 0.6363636363636363535, 0.6386363636363636687, 0.6409090909090908728, 0.6431818181818181879, 0.6454545454545455030, 0.6477272727272727071, 0.6500000000000000222, 0.6522727272727272263, 0.6545454545454545414, 0.6568181818181818565, 0.6590909090909090606, 0.6613636363636363757, 0.6636363636363636909, 0.6659090909090908950, 0.6681818181818180991, 0.6704545454545454142, 0.6727272727272727293, 0.6750000000000000444, 0.6772727272727272485, 0.6795454545454545636, 0.6818181818181817677, 0.6840909090909090828, 0.6863636363636363980, 0.6886363636363636020, 0.6909090909090909172, 0.6931818181818182323, 0.6954545454545454364, 0.6977272727272727515, 0.6999999999999999556, 0.7022727272727272707, 0.7045454545454545858, 0.7068181818181817899, 0.7090909090909091050, 0.7113636363636363091, 0.7136363636363636243, 0.7159090909090909394, 0.7181818181818181435, 0.7204545454545454586, 0.7227272727272727737, 0.7249999999999999778, 0.7272727272727272929, 0.7295454545454544970, 0.7318181818181818121, 0.7340909090909091272, 0.7363636363636363313, 0.7386363636363636465, 0.7409090909090909616, 0.7431818181818181657, 0.7454545454545454808, 0.7477272727272726849, 0.7500000000000000000, 0.7522727272727273151, 0.7545454545454545192, 0.7568181818181818343, 0.7590909090909090384, 0.7613636363636363535, 0.7636363636363636687, 0.7659090909090908728, 0.7681818181818181879, 0.7704545454545455030, 0.7727272727272727071, 0.7750000000000000222, 0.7772727272727272263, 0.7795454545454545414, 0.7818181818181818565, 0.7840909090909090606, 0.7863636363636363757, 0.7886363636363636909, 0.7909090909090908950, 0.7931818181818182101, 0.7954545454545454142, 0.7977272727272727293, 0.8000000000000000444, 0.8022727272727272485, 0.8045454545454545636, 0.8068181818181817677, 0.8090909090909090828, 0.8113636363636363980, 0.8136363636363636020, 0.8159090909090909172, 0.8181818181818182323, 0.8204545454545454364, 0.8227272727272727515, 0.8249999999999999556, 0.8272727272727272707, 0.8295454545454545858, 0.8318181818181817899, 0.8340909090909091050, 0.8363636363636364202, 0.8386363636363636243, 0.8409090909090909394, 0.8431818181818181435, 0.8454545454545454586, 0.8477272727272727737, 0.8499999999999999778, 0.8522727272727272929, 0.8545454545454544970, 0.8568181818181818121, 0.8590909090909091272, 0.8613636363636363313, 0.8636363636363636465, 0.8659090909090909616, 0.8681818181818181657, 0.8704545454545454808, 0.8727272727272726849, 0.8750000000000000000, 0.8772727272727273151, 0.8795454545454545192, 0.8818181818181818343, 0.8840909090909090384, 0.8863636363636363535, 0.8886363636363636687, 0.8909090909090908728, 0.8931818181818181879, 0.8954545454545455030, 0.8977272727272727071, 0.9000000000000000222, 0.9022727272727272263, 0.9045454545454545414, 0.9068181818181818565, 0.9090909090909090606, 0.9113636363636363757, 0.9136363636363636909, 0.9159090909090908950, 0.9181818181818182101, 0.9204545454545453032, 0.9227272727272727293, 0.9250000000000000444, 0.9272727272727272485, 0.9295454545454545636, 0.9318181818181817677, 0.9340909090909090828, 0.9363636363636363980, 0.9386363636363636020, 0.9409090909090909172, 0.9431818181818182323, 0.9454545454545454364, 0.9477272727272727515, 0.9499999999999999556, 0.9522727272727272707, 0.9545454545454545858, 0.9568181818181817899, 0.9590909090909091050, 0.9613636363636363091, 0.9636363636363636243, 0.9659090909090909394, 0.9681818181818181435, 0.9704545454545454586, 0.9727272727272727737, 0.9749999999999999778, 0.9772727272727272929, 0.9779695260516495514 ),
 .UNSPECIFIED. ) 
 CURVE ( )  GEOMETRIC_REPRESENTATION_ITEM ( )  RATIONAL_B_SPLINE_CURVE ( ( 1.000000000000000000, 0.9898214418809326842, 1.000000000000000000, 0.9898214418809326842, 1.000000000000000000, 0.9898214418809326842, 1.000000000000000000, 0.9898214418809326842, 1.000000000000000000, 0.9898214418809326842, 1.000000000000000000, 0.9898214418809326842, 1.000000000000000000, 0.9898214418809326842, 1.000000000000000000, 0.9898214418809326842, 1.000000000000000000, 0.9898214418809326842, 1.000000000000000000, 0.9898214418809326842, 1.000000000000000000, 0.9898214418809326842, 1.000000000000000000, 0.9898214418809326842, 1.000000000000000000, 0.9898214418809326842, 1.000000000000000000, 0.9898214418809326842, 1.000000000000000000, 0.9898214418809326842, 1.000000000000000000, 0.9898214418809326842, 1.000000000000000000, 0.9898214418809326842, 1.000000000000000000, 0.9898214418809326842, 1.000000000000000000, 0.9898214418809326842, 1.000000000000000000, 0.9898214418809326842, 1.000000000000000000, 0.9898214418809326842, 1.000000000000000000, 0.9898214418809326842, 1.000000000000000000, 0.9898214418809326842, 1.000000000000000000, 0.9898214418809326842, 1.000000000000000000, 0.9898214418809326842, 1.000000000000000000, 0.9898214418809326842, 1.000000000000000000, 0.9898214418809326842, 1.000000000000000000, 0.9898214418809326842, 1.000000000000000000, 0.9898214418809326842, 1.000000000000000000, 0.9898214418809326842, 1.000000000000000000, 0.9898214418809326842, 1.000000000000000000, 0.9898214418809326842, 1.000000000000000000, 0.9898214418809326842, 1.000000000000000000, 0.9898214418809326842, 1.000000000000000000, 0.9898214418809326842, 1.000000000000000000, 0.9898214418809326842, 1.000000000000000000, 0.9898214418809326842, 1.000000000000000000, 0.9898214418809326842, 1.000000000000000000, 0.9898214418809326842, 1.000000000000000000, 0.9898214418809326842, 1.000000000000000000, 0.9898214418809326842, 1.000000000000000000, 0.9898214418809326842, 1.000000000000000000, 0.9898214418809326842, 1.000000000000000000, 0.9898214418809326842, 1.000000000000000000, 0.9898214418809326842, 1.000000000000000000, 0.9898214418809326842, 1.000000000000000000, 0.9898214418809326842, 1.000000000000000000, 0.9898214418809326842, 1.000000000000000000, 0.9898214418809326842, 1.000000000000000000, 0.9898214418809326842, 1.000000000000000000, 0.9898214418809326842, 1.000000000000000000, 0.9898214418809326842, 1.000000000000000000, 0.9898214418809326842, 1.000000000000000000, 0.9898214418809326842, 1.000000000000000000, 0.9898214418809326842, 1.000000000000000000, 0.9898214418809326842, 1.000000000000000000, 0.9898214418809326842, 1.000000000000000000, 0.9898214418809326842, 1.000000000000000000, 0.9898214418809326842, 1.000000000000000000, 0.9898214418809326842, 1.000000000000000000, 0.9898214418809326842, 1.000000000000000000, 0.9898214418809326842, 1.000000000000000000, 0.9898214418809326842, 1.000000000000000000, 0.9898214418809326842, 1.000000000000000000, 0.9898214418809326842, 1.000000000000000000, 0.9898214418809326842, 1.000000000000000000, 0.9898214418809326842, 1.000000000000000000, 0.9898214418809326842, 1.000000000000000000, 0.9898214418809326842, 1.000000000000000000, 0.9898214418809326842, 1.000000000000000000, 0.9898214418809326842, 1.000000000000000000, 0.9898214418809326842, 1.000000000000000000, 0.9898214418809326842, 1.000000000000000000, 0.9898214418809326842, 1.000000000000000000, 0.9898214418809326842, 1.000000000000000000, 0.9898214418809326842, 1.000000000000000000, 0.9898214418809326842, 1.000000000000000000, 0.9898214418809326842, 1.000000000000000000, 0.9898214418809326842, 1.000000000000000000, 0.9898214418809326842, 1.000000000000000000, 0.9898214418809326842, 1.000000000000000000, 0.9898214418809326842, 1.000000000000000000, 0.9898214418809326842, 1.000000000000000000, 0.9898214418809326842, 1.000000000000000000, 0.9898214418809326842, 1.000000000000000000, 0.9898214418809326842, 1.000000000000000000, 0.9898214418809326842, 1.000000000000000000, 0.9898214418809326842, 1.000000000000000000, 0.9898214418809326842, 1.000000000000000000, 0.9898214418809326842, 1.000000000000000000, 0.9898214418809326842, 1.000000000000000000, 0.9898214418809326842, 1.000000000000000000, 0.9898214418809326842, 1.000000000000000000, 0.9898214418809326842, 1.000000000000000000, 0.9898214418809326842, 1.000000000000000000, 0.9898214418809326842, 1.000000000000000000, 0.9898214418809326842, 1.000000000000000000, 0.9898214418809326842, 1.000000000000000000, 0.9898214418809326842, 1.000000000000000000, 0.9898214418809326842, 1.000000000000000000, 0.9898214418809326842, 1.000000000000000000, 0.9898214418809326842, 1.000000000000000000, 0.9898214418809326842, 1.000000000000000000, 0.9898214418809326842, 1.000000000000000000, 0.9898214418809326842, 1.000000000000000000, 0.9898214418809326842, 1.000000000000000000, 0.9898214418809326842, 1.000000000000000000, 0.9898214418809326842, 1.000000000000000000, 0.9898214418809326842, 1.000000000000000000, 0.9898214418809326842, 1.000000000000000000, 0.9898214418809326842, 1.000000000000000000, 0.9898214418809326842, 1.000000000000000000, 0.9898214418809326842, 1.000000000000000000, 0.9898214418809326842, 1.000000000000000000, 0.9898214418809326842, 1.000000000000000000, 0.9898214418809326842, 1.000000000000000000, 0.9898214418809326842, 1.000000000000000000, 0.9898214418809326842, 1.000000000000000000, 0.9898214418809326842, 1.000000000000000000, 0.9898214418809326842, 1.000000000000000000, 0.9898214418809326842, 1.000000000000000000, 0.9898214418809326842, 1.000000000000000000, 0.9898214418809326842, 1.000000000000000000, 0.9898214418809326842, 1.000000000000000000, 0.9898214418809326842, 1.000000000000000000, 0.9898214418809326842, 1.000000000000000000, 0.9898214418809326842, 1.000000000000000000, 0.9898214418809326842, 1.000000000000000000, 0.9898214418809326842, 1.000000000000000000, 0.9898214418809326842, 1.000000000000000000, 0.9898214418809326842, 1.000000000000000000, 0.9898214418809326842, 1.000000000000000000, 0.9898214418809326842, 1.000000000000000000, 0.9898214418809326842, 1.000000000000000000, 0.9898214418809326842, 1.000000000000000000, 0.9898214418809326842, 1.000000000000000000, 0.9898214418809326842, 1.000000000000000000, 0.9898214418809326842, 1.000000000000000000, 0.9898214418809326842, 1.000000000000000000, 0.9898214418809326842, 1.000000000000000000, 0.9898214418809326842, 1.000000000000000000, 0.9898214418809326842, 1.000000000000000000, 0.9898214418809326842, 1.000000000000000000, 0.9898214418809326842, 1.000000000000000000, 0.9898214418809326842, 1.000000000000000000, 0.9898214418809326842, 1.000000000000000000, 0.9898214418809326842, 1.000000000000000000, 0.9898214418809326842, 1.000000000000000000, 0.9898214418809326842, 1.000000000000000000, 0.9898214418809326842, 1.000000000000000000, 0.9898214418809326842, 1.000000000000000000, 0.9898214418809326842, 1.000000000000000000, 0.9898214418809326842, 1.000000000000000000, 0.9898214418809326842, 1.000000000000000000, 0.9898214418809326842, 1.000000000000000000, 0.9898214418809326842, 1.000000000000000000, 0.9898214418809326842, 1.000000000000000000, 0.9898214418809326842, 1.000000000000000000, 0.9898214418809326842, 1.000000000000000000, 0.9898214418809326842, 1.000000000000000000, 0.9898214418809326842, 1.000000000000000000, 0.9898214418809326842, 1.000000000000000000, 0.9898214418809326842, 1.000000000000000000, 0.9898214418809326842, 1.000000000000000000, 0.9898214418809326842, 1.000000000000000000, 0.9898214418809326842, 1.000000000000000000, 0.9898214418809326842, 1.000000000000000000, 0.9898214418809326842, 1.000000000000000000, 0.9898214418809326842, 1.000000000000000000, 0.9898214418809326842, 1.000000000000000000, 0.9898214418809326842, 1.000000000000000000, 0.9898214418809326842, 1.000000000000000000, 0.9898214418809326842, 1.000000000000000000, 0.9898214418809326842, 1.000000000000000000, 0.9898214418809326842, 1.000000000000000000, 0.9898214418809326842, 1.000000000000000000, 0.9898214418809326842, 1.000000000000000000, 0.9898214418809326842, 1.000000000000000000, 0.9898214418809326842, 1.000000000000000000, 0.9898214418809326842, 1.000000000000000000, 0.9898214418809326842, 1.000000000000000000, 0.9898214418809326842, 1.000000000000000000, 0.9898214418809326842, 1.000000000000000000, 0.9898214418809326842, 1.000000000000000000, 0.9898214418809326842, 1.000000000000000000, 0.9898214418809326842, 1.000000000000000000, 0.9898214418809326842, 1.000000000000000000, 0.9898214418809326842, 1.000000000000000000, 0.9898214418809326842, 1.000000000000000000, 0.9898214418809326842, 1.000000000000000000, 0.9898214418809326842, 1.000000000000000000, 0.9898214418809326842, 1.000000000000000000, 0.9898214418809326842, 1.000000000000000000, 0.9898214418809326842, 1.000000000000000000, 0.9898214418809326842, 1.000000000000000000, 0.9898214418809326842, 1.000000000000000000, 0.9898214418809326842, 1.000000000000000000, 0.9898214418809326842, 1.000000000000000000, 0.9898214418809326842, 1.000000000000000000, 0.9898214418809326842, 1.000000000000000000, 0.9898214418809326842, 1.000000000000000000, 0.9898214418809326842, 1.000000000000000000, 0.9898214418809326842, 1.000000000000000000, 0.9898214418809326842, 1.000000000000000000, 0.9898214418809326842, 1.000000000000000000, 0.9898214418809326842, 1.000000000000000000, 0.9898214418809326842, 1.000000000000000000, 0.9898214418809326842, 1.000000000000000000, 0.9898214418809326842, 1.000000000000000000, 0.9898214418809326842, 1.000000000000000000, 0.9898214418809326842, 1.000000000000000000, 0.9898214418809326842, 1.000000000000000000, 0.9898214418809326842, 1.000000000000000000, 0.9898214418809326842, 1.000000000000000000, 0.9898214418809326842, 1.000000000000000000, 0.9898214418809326842, 1.000000000000000000, 0.9898214418809326842, 1.000000000000000000, 0.9898214418809326842, 1.000000000000000000, 0.9898214418809326842, 1.000000000000000000, 0.9898214418809326842, 1.000000000000000000, 0.9898214418809326842, 1.000000000000000000, 0.9898214418809326842, 1.000000000000000000, 0.9898214418809326842, 1.000000000000000000, 0.9898214418809326842, 1.000000000000000000, 0.9898214418809326842, 1.000000000000000000, 0.9898214418809326842, 1.000000000000000000, 0.9898214418809326842, 1.000000000000000000, 0.9898214418809326842, 1.000000000000000000, 0.9898214418809326842, 1.000000000000000000, 0.9898214418809326842, 1.000000000000000000, 0.9898214418809326842, 1.000000000000000000, 0.9898214418809326842, 1.000000000000000000, 0.9898214418809326842, 1.000000000000000000, 0.9898214418809326842, 1.000000000000000000, 0.9898214418809326842, 1.000000000000000000, 0.9898214418809326842, 1.000000000000000000, 0.9898214418809326842, 1.000000000000000000, 0.9898214418809326842, 1.000000000000000000, 0.9898214418809326842, 1.000000000000000000, 0.9898214418809326842, 1.000000000000000000, 0.9898214418809326842, 1.000000000000000000, 0.9898214418809326842, 1.000000000000000000, 0.9898214418809326842, 1.000000000000000000, 0.9898214418809326842, 1.000000000000000000, 0.9898214418809326842, 1.000000000000000000, 0.9898214418809326842, 1.000000000000000000, 0.9898214418809326842, 1.000000000000000000, 0.9898214418809326842, 1.000000000000000000, 0.9898214418809326842, 1.000000000000000000, 0.9898214418809326842, 1.000000000000000000, 0.9898214418809326842, 1.000000000000000000, 0.9898214418809326842, 1.000000000000000000, 0.9898214418809326842, 1.000000000000000000, 0.9898214418809326842, 1.000000000000000000, 0.9898214418809326842, 1.000000000000000000, 0.9898214418809326842, 1.000000000000000000, 0.9898214418809326842, 1.000000000000000000, 0.9898214418809326842, 1.000000000000000000, 0.9898214418809326842, 1.000000000000000000, 0.9898214418809326842, 1.000000000000000000, 0.9898214418809326842, 1.000000000000000000, 0.9898214418809326842, 1.000000000000000000, 0.9898214418809326842, 1.000000000000000000, 0.9898214418809326842, 1.000000000000000000, 0.9898214418809326842, 1.000000000000000000, 0.9898214418809326842, 1.000000000000000000, 0.9898214418809326842, 1.000000000000000000, 0.9898214418809326842, 1.000000000000000000, 0.9898214418809326842, 1.000000000000000000, 0.9898214418809326842, 1.000000000000000000, 0.9898214418809326842, 1.000000000000000000, 0.9898214418809326842, 1.000000000000000000, 0.9898214418809326842, 1.000000000000000000, 0.9898214418809326842, 1.000000000000000000, 0.9898214418809326842, 1.000000000000000000, 0.9898214418809326842, 1.000000000000000000, 0.9898214418809326842, 1.000000000000000000, 0.9898214418809326842, 1.000000000000000000, 0.9898214418809326842, 1.000000000000000000, 0.9898214418809326842, 1.000000000000000000, 0.9898214418809326842, 1.000000000000000000, 0.9898214418809326842, 1.000000000000000000, 0.9898214418809326842, 1.000000000000000000, 0.9898214418809326842, 1.000000000000000000, 0.9898214418809326842, 1.000000000000000000, 0.9898214418809326842, 1.000000000000000000, 0.9898214418809326842, 1.000000000000000000, 0.9898214418809326842, 1.000000000000000000, 0.9898214418809326842, 1.000000000000000000, 0.9898214418809326842, 1.000000000000000000, 0.9898214418809326842, 1.000000000000000000, 0.9898214418809326842, 1.000000000000000000, 0.9898214418809326842, 1.000000000000000000, 0.9898214418809326842, 1.000000000000000000, 0.9898214418809326842, 1.000000000000000000, 0.9898214418809326842, 1.000000000000000000, 0.9898214418809326842, 1.000000000000000000, 0.9898214418809326842, 1.000000000000000000, 0.9898214418809326842, 1.000000000000000000, 0.9898214418809326842, 1.000000000000000000, 0.9898214418809326842, 1.000000000000000000, 0.9898214418809326842, 1.000000000000000000, 0.9898214418809326842, 1.000000000000000000, 0.9898214418809326842, 1.000000000000000000, 0.9898214418809326842, 1.000000000000000000, 0.9898214418809326842, 1.000000000000000000, 0.9898214418809326842, 1.000000000000000000, 0.9898214418809326842, 1.000000000000000000, 0.9898214418809326842, 1.000000000000000000, 0.9898214418809326842, 1.000000000000000000, 0.9898214418809326842, 1.000000000000000000, 0.9898214418809326842, 1.000000000000000000, 0.9898214418809326842, 1.000000000000000000, 0.9898214418809326842, 1.000000000000000000, 0.9898214418809326842, 1.000000000000000000, 0.9898214418809326842, 1.000000000000000000, 0.9898214418809326842, 1.000000000000000000, 0.9898214418809326842, 1.000000000000000000, 0.9898214418809326842, 1.000000000000000000, 0.9898214418809326842, 1.000000000000000000, 0.9898214418809326842, 1.000000000000000000, 0.9898214418809326842, 1.000000000000000000, 0.9898214418809326842, 1.000000000000000000, 0.9898214418809326842, 1.000000000000000000, 0.9898214418809326842, 1.000000000000000000, 0.9898214418809326842, 1.000000000000000000, 0.9898214418809326842, 1.000000000000000000, 0.9898214418809326842, 1.000000000000000000, 0.9898214418809326842, 1.000000000000000000, 0.9898214418809326842, 1.000000000000000000, 0.9898214418809326842, 1.000000000000000000, 0.9898214418809326842, 1.000000000000000000, 0.9898214418809326842, 1.000000000000000000, 0.9898214418809326842, 1.000000000000000000, 0.9898214418809326842, 1.000000000000000000, 0.9898214418809326842, 1.000000000000000000, 0.9898214418809326842, 1.000000000000000000, 0.9898214418809326842, 1.000000000000000000, 0.9898214418809326842, 1.000000000000000000, 0.9898214418809326842, 1.000000000000000000, 0.9898214418809326842, 1.000000000000000000, 0.9898214418809326842, 1.000000000000000000, 0.9898214418809326842, 1.000000000000000000, 0.9898214418809326842, 1.000000000000000000, 0.9898214418809326842, 1.000000000000000000, 0.9898214418809326842, 1.000000000000000000, 0.9898214418809326842, 1.000000000000000000, 0.9898214418809326842, 1.000000000000000000, 0.9898214418809326842, 1.000000000000000000, 0.9898214418809326842, 1.000000000000000000, 0.9898214418809326842, 1.000000000000000000, 0.9898214418809326842, 1.000000000000000000, 0.9898214418809326842, 1.000000000000000000, 0.9898214418809326842, 1.000000000000000000, 0.9898214418809326842, 1.000000000000000000, 0.9898214418809326842, 1.000000000000000000, 0.9898214418809326842, 1.000000000000000000, 0.9898214418809326842, 1.000000000000000000, 0.9898214418809326842, 1.000000000000000000, 0.9898214418809326842, 1.000000000000000000, 0.9898214418809326842, 1.000000000000000000, 0.9898214418809326842, 1.000000000000000000, 0.9898214418809326842, 1.000000000000000000, 0.9898214418809326842, 1.000000000000000000, 0.9898214418809326842, 1.000000000000000000, 0.9898214418809326842, 1.000000000000000000, 0.9898214418809326842, 1.000000000000000000, 0.9898214418809326842, 1.000000000000000000, 0.9898214418809326842, 1.000000000000000000, 0.9898214418809326842, 1.000000000000000000, 0.9898214418809326842, 1.000000000000000000, 0.9898214418809326842, 1.000000000000000000, 0.9898214418809326842, 1.000000000000000000, 0.9898214418809326842, 1.000000000000000000, 0.9898214418809326842, 1.000000000000000000, 0.9898214418809326842, 1.000000000000000000, 0.9898214418809326842, 1.000000000000000000, 0.9898214418809326842, 1.000000000000000000, 0.9898214418809326842, 1.000000000000000000, 0.9898214418809326842, 1.000000000000000000, 0.9898214418809326842, 1.000000000000000000, 0.9898214418809326842, 1.000000000000000000, 0.9898214418809326842, 1.000000000000000000, 0.9898214418809326842, 1.000000000000000000, 0.9898214418809326842, 1.000000000000000000, 0.9898214418809326842, 1.000000000000000000, 0.9898214418809326842, 1.000000000000000000, 0.9898214418809326842, 1.000000000000000000, 0.9898214418809326842, 1.000000000000000000, 0.9898214418809326842, 1.000000000000000000, 0.9898214418809326842, 1.000000000000000000, 0.9898214418809326842, 1.000000000000000000, 0.9898214418809326842, 1.000000000000000000, 0.9898214418809326842, 1.000000000000000000, 0.9898214418809326842, 1.000000000000000000, 0.9898214418809326842, 1.000000000000000000, 0.9898214418809326842, 1.000000000000000000, 0.9898214418809326842, 1.000000000000000000, 0.9898214418809326842, 1.000000000000000000, 0.9898214418809326842, 1.000000000000000000, 0.9898214418809326842, 1.000000000000000000, 0.9898214418809326842, 1.000000000000000000, 0.9898214418809326842, 1.000000000000000000, 0.9898214418809326842, 1.000000000000000000, 0.9898214418809326842, 1.000000000000000000, 0.9898214418809326842, 1.000000000000000000, 0.9898214418809326842, 1.000000000000000000, 0.9898214418809326842, 1.000000000000000000, 0.9898214418809326842, 1.000000000000000000, 0.9898214418809326842, 1.000000000000000000, 0.9898214418809326842, 1.000000000000000000, 0.9898214418809326842, 1.000000000000000000, 0.9898214418809326842, 1.000000000000000000, 0.9898214418809326842, 1.000000000000000000, 0.9898214418809326842, 1.000000000000000000, 0.9898214418809326842, 1.000000000000000000, 0.9898214418809326842, 1.000000000000000000, 0.9898214418809326842, 1.000000000000000000, 0.9898214418809326842, 1.000000000000000000, 0.9898214418809326842, 1.000000000000000000, 0.9898214418809326842, 1.000000000000000000, 0.9898214418809326842, 1.000000000000000000, 0.9898214418809326842, 1.000000000000000000, 0.9898214418809326842, 1.000000000000000000, 0.9898214418809326842, 1.000000000000000000, 0.9898214418809326842, 1.000000000000000000, 0.9898214418809326842, 1.000000000000000000, 0.9898214418809326842, 1.000000000000000000, 0.9898214418809326842, 1.000000000000000000, 0.9898214418809326842, 1.000000000000000000, 0.9968793409778355930, 0.9956722167842187998 ) ) 
 REPRESENTATION_ITEM ( '' )  );
#36169=CARTESIAN_POINT ( 'NONE',  ( 804.4086373105744769, -409.6454272087884760, 333.3843516231986541 ) ) ;
#36170=CARTESIAN_POINT ( 'NONE',  ( 781.2370466360911223, -356.7363362996978253, 304.9990715423533629 ) ) ;
#36172=CARTESIAN_POINT ( 'NONE',  ( 791.4716058693660443, -452.9681489794448339, 367.7200696026887954 ) ) ;
#36174=CARTESIAN_POINT ( 'NONE',  ( 747.6481478633932056, -181.0999726633347109, 353.4146539503763620 ) ) ;
#36176=CARTESIAN_POINT ( 'NONE',  ( 745.0891759886404770, -124.2709662947837899, 342.4968714119734159 ) ) ;
#36180=CARTESIAN_POINT ( 'NONE',  ( 788.8264449731200330, -213.1800572038743553, 363.6646147819171233 ) ) ;
#36181=CARTESIAN_POINT ( 'NONE',  ( 786.2694204179717872, -453.2817908451519315, 305.1769319972829067 ) ) ;
#36185=CARTESIAN_POINT ( 'NONE',  ( 805.9055244015594326, -27.62377810805120149, 315.8990559732753240 ) ) ;
#36188=CARTESIAN_POINT ( 'NONE',  ( 767.8955696845333705, -24.45278447660229304, 362.1676090361162323 ) ) ;
#36190=CARTESIAN_POINT ( 'NONE',  ( 788.7631598425961101, -337.4419599262319593, 305.7194118038759143 ) ) ;
#36191=CARTESIAN_POINT ( 'NONE',  ( 803.4237431249931660, -159.1800572038746111, 331.2633955100225194 ) ) ;
#36194=CARTESIAN_POINT ( 'NONE',  ( 781.8018195045266339, -334.2709662947829656, 365.1927285166406705 ) ) ;
#36201=CARTESIAN_POINT ( 'NONE',  ( 764.8639956371174549, -56.08914811296580893, 319.7806653035542013 ) ) ;
#36202=CARTESIAN_POINT ( 'NONE',  ( 766.9102291470427417, -378.5545181178795247, 318.6633372737382501 ) ) ;
#36203=CARTESIAN_POINT ( 'NONE',  ( 782.5225473063383106, -406.2709662947828519, 375.2698199232970637 ) ) ;
#36204=CARTESIAN_POINT ( 'NONE',  ( 791.1614460488616487, -275.2601417444140566, 373.5763878283158874 ) ) ;
#36210=ORIENTED_EDGE ( 'NONE', *, *, #18266, .F. ) ;
#36211=CARTESIAN_POINT ( 'NONE',  ( 777.4774526936600978, -442.2709662947826814, 304.7301800767027657 ) ) ;
#36218=CARTESIAN_POINT ( 'NONE',  ( 796.9571628226829034, -287.4636090269708575, 321.2382568024804641 ) ) ;
#36219=CARTESIAN_POINT ( 'NONE',  ( 797.6776695296629214, -139.5436935675110135, 357.6776695296636603 ) ) ;
#36222=CARTESIAN_POINT ( 'NONE',  ( 796.7845633553578182, -321.6237781080502600, 358.5707757039688204 ) ) ;
#36224=CARTESIAN_POINT ( 'NONE',  ( 799.9636004259356241, -46.91815448151694312, 311.2241431872006956 ) ) ;
#36227=CARTESIAN_POINT ( 'NONE',  ( 800.9747183278959710, -204.9982390220562820, 311.9810565676471583 ) ) ;
#36228=CARTESIAN_POINT ( 'NONE',  ( 778.1981804954714335, -130.2709662947837899, 314.8072714833589885 ) ) ;
#36229=LINE ( 'NONE', #14551, #15869 ) ;
#36231=CARTESIAN_POINT ( 'NONE',  ( 786.5483106153019435, -31.64542720878970883, 364.1601925771022366 ) ) ;
#36234=CARTESIAN_POINT ( 'NONE',  ( 754.9735926884551418, -402.3510508353228374, 340.5236548041000333 ) ) ;
#36241=CARTESIAN_POINT ( 'NONE',  ( 810.1134526219336749, -224.5328690171415076, 357.8822607201570349 ) ) ;
#36242=CARTESIAN_POINT ( 'NONE',  ( 805.1927285166399315, -40.81642084023859951, 341.8018195045277707 ) ) ;
#36245=CARTESIAN_POINT ( 'NONE',  ( 797.8594530101008786, -229.5436935675106440, 322.1405469898980982 ) ) ;
#36252=CARTESIAN_POINT ( 'NONE',  ( 755.2512626584698410, -295.5436935675105588, 315.2512626584710915 ) ) ;
#36253=CARTESIAN_POINT ( 'NONE',  ( 800.1688906516307043, -10.16923265350579442, 369.0717654672308186 ) ) ;
#36261=CARTESIAN_POINT ( 'NONE',  ( 810.7187646348534145, -330.4527844766013231, 356.7737145352016341 ) ) ;
#36264=CARTESIAN_POINT ( 'NONE',  ( 804.6971507214547046, -219.2817908451527558, 344.0799538623459739 ) ) ;
#36266=CARTESIAN_POINT ( 'NONE',  ( 805.1016975059191054, -366.8965053807773984, 343.0745993439771837 ) ) ;
#36269=CARTESIAN_POINT ( 'NONE',  ( 804.8461984189677878, -194.1908817542437475, 336.9566956441385628 ) ) ;
#36270=CARTESIAN_POINT ( 'NONE',  ( 802.1676090361156639, -62.63460265842031305, 327.8955696845344505 ) ) ;
#36274=CARTESIAN_POINT ( 'NONE',  ( 745.7194118038753459, -253.6454272087889876, 348.7631598425976449 ) ) ;
#36275=CARTESIAN_POINT ( 'NONE',  ( 798.7617431975189675, -219.6237781080506295, 323.0428371773161871 ) ) ;
#36278=CARTESIAN_POINT ( 'NONE',  ( 774.6858677611749044, 14.27448825067031812, 315.5713283507209894 ) ) ;
#36282=CARTESIAN_POINT ( 'NONE',  ( 749.2812353651451076, -54.45278447660219001, 323.2262854647983090 ) ) ;
#36283=CARTESIAN_POINT ( 'NONE',  ( 763.0537975583475827, -120.4527844766019484, 371.0346526505627480 ) ) ;
#36286=CARTESIAN_POINT ( 'NONE',  ( 804.1009440267234822, -383.4636090269704596, 314.0944755984392600 ) ) ;
#36288=CARTESIAN_POINT ( 'NONE',  ( 814.5518280994195948, -375.7255117493283478, 332.4837098697145734 ) ) ;
#36290=CARTESIAN_POINT ( 'NONE',  ( 803.4237431249931660, -423.1800572038737300, 331.2633955100225194 ) ) ;
#36292=CARTESIAN_POINT ( 'NONE',  ( 779.4763451958990572, -176.7363362996983369, 365.0264073115438919 ) ) ;
#36295=CARTESIAN_POINT ( 'NONE',  ( 766.5853460496234675, -133.9874144716872024, 372.3518521366060554 ) ) ;
#36296=CARTESIAN_POINT ( 'NONE',  ( 785.3141322388236176, -429.7255117493282910, 364.4286716492789537 ) ) ;
#36302=CARTESIAN_POINT ( 'NONE',  ( 756.3353852180819104, -245.9073299311469896, 331.1735550268788302 ) ) ;
#36303=CARTESIAN_POINT ( 'NONE',  ( 781.7834795799800531, -250.8164208402379245, 315.0636971347436202 ) ) ;
#36306=CARTESIAN_POINT ( 'NONE',  ( 805.1927285166397041, -448.8164208402371855, 341.8018195045277707 ) ) ;
#36308=CARTESIAN_POINT ( 'NONE',  ( 777.5031285880264704, -190.8164208402381234, 374.9108240113588408 ) ) ;
#36309=CARTESIAN_POINT ( 'NONE',  ( 763.0428371773158460, -275.4636090269708575, 358.7617431975195359 ) ) ;
#36313=CARTESIAN_POINT ( 'NONE',  ( 758.0141637701419768, -207.0783235625960685, 367.2620300519063790 ) ) ;
#36319=CARTESIAN_POINT ( 'NONE',  ( 760.5453621957607311, -261.0783235625959264, 323.8424801807151425 ) ) ;
#36325=ORIENTED_EDGE ( 'NONE', *, *, #18811, .F. ) ;
#36328=CARTESIAN_POINT ( 'NONE',  ( 776.2046728542105711, -164.1908817542438612, 304.8212110874238761 ) ) ;
#36338=CARTESIAN_POINT ( 'NONE',  ( 757.8323909638827445, -2.634602658420536869, 352.1044303154654358 ) ) ;
#36339=CARTESIAN_POINT ( 'NONE',  ( 791.0478386215596629, -285.8272453906071178, 306.7653713866226326 ) ) ;
#36341=CARTESIAN_POINT ( 'NONE',  ( 767.7687537140311633, -263.9073299311469327, 372.7932403749916830 ) ) ;
#36345=CARTESIAN_POINT ( 'NONE',  ( 755.0636971347428243, -340.2709662947831362, 341.7834795799807353 ) ) ;
#36347=CARTESIAN_POINT ( 'NONE',  ( 761.4292242960306112, -89.46360902697134065, 323.2154366446414429 ) ) ;
#36351=CARTESIAN_POINT ( 'NONE',  ( 807.5423716828161105, -129.0783235625963243, 362.2119215644372048 ) ) ;
#36352=CARTESIAN_POINT ( 'NONE',  ( 783.0433043558608688, -168.8965053807780237, 315.1538015810313027 ) ) ;
#36353=CARTESIAN_POINT ( 'NONE',  ( 778.2165204200184689, -382.8164208402374697, 364.9363028652563230 ) ) ;
#36356=CARTESIAN_POINT ( 'NONE',  ( 804.6798772138708955, -159.7255117493291436, 334.6312213355107019 ) ) ;
#36359=CARTESIAN_POINT ( 'NONE',  ( 783.7566961878529810, -432.8965053807771142, 305.1792804349288417 ) ) ;
#36361=CARTESIAN_POINT ( 'NONE',  ( 767.8955696845333705, -360.4527844766010958, 362.1676090361162323 ) ) ;
#36364=CARTESIAN_POINT ( 'NONE',  ( 800.2193346964447755, -426.9982390220554862, 355.1360043628815788 ) ) ;
#36370=CARTESIAN_POINT ( 'NONE',  ( 805.2837595273609850, -458.7363362996973706, 340.5290396650784714 ) ) ;
#36371=CARTESIAN_POINT ( 'NONE',  ( 747.2067596250078623, -219.1800572038744122, 352.2312462859687230 ) ) ;
#36372=CARTESIAN_POINT ( 'NONE',  ( 804.9511171171677688, -149.8055962898689870, 335.8780910478229202 ) ) ;
#36380=CARTESIAN_POINT ( 'NONE',  ( 745.5313806188320314, -63.28179084515324604, 333.7943932421247268 ) ) ;
#36388=CARTESIAN_POINT ( 'NONE',  ( 796.9571628226829034, -407.4636090269703459, 321.2382568024804641 ) ) ;
#36390=CARTESIAN_POINT ( 'NONE',  ( 757.4527132478984868, -232.3726999360617924, 329.1273215169538844 ) ) ;
#36394=CARTESIAN_POINT ( 'NONE',  ( 795.8262568251477660, -190.3726999360619629, 308.3538107759623585 ) ) ;
#36396=CARTESIAN_POINT ( 'NONE',  ( 801.1904061080336987, -116.0891481129656029, 368.3070685750235498 ) ) ;
#36399=DIRECTION ( 'NONE',  ( -1.000000000000000000, -0.000000000000000000, -0.000000000000000000 ) ) ;
#36400=CARTESIAN_POINT ( 'NONE',  ( 759.7806653035534055, -222.9982390220561399, 324.8639956371180801 ) ) ;
#36401=CARTESIAN_POINT ( 'NONE',  ( 766.0291762391763086, -34.91815448151697154, 360.7704444035551319 ) ) ;
#36405=CARTESIAN_POINT ( 'NONE',  ( 801.9858362298568863, -27.07832356259665474, 312.7379699480935642 ) ) ;
#36409=AXIS2_PLACEMENT_3D ( 'NONE', #17983, #38776, #32053 ) ;
#36410=CARTESIAN_POINT ( 'NONE',  ( 781.7834795799800531, -34.81642084023861372, 315.0636971347436202 ) ) ;
#36413=CARTESIAN_POINT ( 'NONE',  ( 749.8865473780648472, -356.5328690171410813, 322.1177392798429082 ) ) ;
#36416=CARTESIAN_POINT ( 'NONE',  ( 748.3538107759620743, -424.7146871989589840, 355.8262568251490165 ) ) ;
#36417=CARTESIAN_POINT ( 'NONE',  ( 762.1405469898971887, -337.5436935675102177, 357.8594530101015607 ) ) ;
#36424=CARTESIAN_POINT ( 'NONE',  ( 785.3141322388236176, -45.72551174932949181, 364.4286716492789537 ) ) ;
#36425=CARTESIAN_POINT ( 'NONE',  ( 769.9779781133707957, -355.0999726633341993, 316.7813123517150871 ) ) ;
#36427=CARTESIAN_POINT ( 'NONE',  ( 810.7187646348534145, -402.4527844766010389, 356.7737145352016341 ) ) ;
#36428=CARTESIAN_POINT ( 'NONE',  ( 759.8311093483677041, -334.1692326535047073, 310.9282345327691814 ) ) ;
#36435=CARTESIAN_POINT ( 'NONE',  ( 744.7301800767019131, -412.8164208402372992, 337.4774526936615757 ) ) ;
#36441=CARTESIAN_POINT ( 'NONE',  ( 802.5472867521000353, -292.3726999360616219, 350.8726784830461156 ) ) ;
#36442=CARTESIAN_POINT ( 'NONE',  ( 800.2193346964447755, -138.9982390220563957, 355.1360043628815788 ) ) ;
#36447=CARTESIAN_POINT ( 'NONE',  ( 800.7704444035546203, -340.1692326535047641, 326.0291762391768771 ) ) ;
#36450=CARTESIAN_POINT ( 'NONE',  ( 754.3581564841646241, -65.46360902697142592, 316.1443688327762516 ) ) ;
#36453=CARTESIAN_POINT ( 'NONE',  ( 808.3070685750230950, -210.9982390220561967, 361.1904061080339261 ) ) ;
#36454=CARTESIAN_POINT ( 'NONE',  ( 755.3201227861273992, -123.7255117493292147, 345.3687786644892981 ) ) ;
#36459=CARTESIAN_POINT ( 'NONE',  ( 757.0176451133909268, -13.09997266333522248, 349.9200121543848354 ) ) ;
#36462=CARTESIAN_POINT ( 'NONE',  ( 784.0799538623451781, -395.8055962898682765, 364.6971507214555572 ) ) ;
#36468=CARTESIAN_POINT ( 'NONE',  ( 758.0141637701419768, -231.0783235625960401, 367.2620300519063790 ) ) ;
#36469=CARTESIAN_POINT ( 'NONE',  ( 801.9419747391806368, -66.45278447660216159, 351.9812246680014027 ) ) ;
#36471=CARTESIAN_POINT ( 'NONE',  ( 756.3353852180819104, -245.9073299311469896, 331.1735550268788302 ) ) ;
#36479=CARTESIAN_POINT ( 'NONE',  ( 815.2698199232962679, -304.8164208402376971, 342.5225473063383674 ) ) ;
#36480=CARTESIAN_POINT ( 'NONE',  ( 744.9990715423526808, -18.35105083532395298, 341.2370466360926002 ) ) ;
#36486=CARTESIAN_POINT ( 'NONE',  ( 801.1904061080336987, -308.0891481129650629, 368.3070685750235498 ) ) ;
#36489=CARTESIAN_POINT ( 'NONE',  ( 801.5560724626406000, -216.5545181178800931, 326.7756240680316182 ) ) ;
#36492=CARTESIAN_POINT ( 'NONE',  ( 804.4086373105744769, -193.6454272087891582, 333.3843516231986541 ) ) ;
#36493=CARTESIAN_POINT ( 'NONE',  ( 756.5762568750052424, -51.18005720387493085, 348.7366044899774238 ) ) ;
#36497=CARTESIAN_POINT ( 'NONE',  ( 776.9566956441375396, -228.8965053807778816, 364.8461984189686405 ) ) ;
#36500=CARTESIAN_POINT ( 'NONE',  ( 751.9810565676468741, -434.0891481129646081, 360.9747183278973921 ) ) ;
#36505=CARTESIAN_POINT ( 'NONE',  ( 813.1304606946830518, -65.90732993114758642, 352.3570229623690580 ) ) ;
#36507=CARTESIAN_POINT ( 'NONE',  ( 763.2262854647970016, -104.6346026584202207, 309.2812353651462445 ) ) ;
#36509=AXIS2_PLACEMENT_3D ( 'NONE', #9920, #34158, #20761 ) ;
#36512=CARTESIAN_POINT ( 'NONE',  ( 807.2620300519052989, -384.0090635724249637, 318.0141637701419768 ) ) ;
#36514=CARTESIAN_POINT ( 'NONE',  ( 796.7737145352015204, -356.6346026584193964, 370.7187646348536987 ) ) ;
#36516=CARTESIAN_POINT ( 'NONE',  ( 796.7845633553578182, 14.37622189194867417, 358.5707757039688204 ) ) ;
#36520=CARTESIAN_POINT ( 'NONE',  ( 752.4576283171824116, -141.0783235625962959, 317.7880784355627952 ) ) ;
#36521=CARTESIAN_POINT ( 'NONE',  ( 803.4237431249931660, -447.1800572038736732, 331.2633955100225194 ) ) ;
#36523=CARTESIAN_POINT ( 'NONE',  ( 744.8212110874229666, -162.8965053807780521, 336.2046728542121627 ) ) ;
#36527=CARTESIAN_POINT ( 'NONE',  ( 804.9363028652555840, -112.2709662947838325, 338.2165204200192079 ) ) ;
#36532=CARTESIAN_POINT ( 'NONE',  ( 803.6646147819161570, -257.9073299311469896, 348.8264449731210561 ) ) ;
#36533=CARTESIAN_POINT ( 'NONE',  ( 791.9812246680005501, -260.6346026584197375, 361.9419747391813189 ) ) ;
#36536=CARTESIAN_POINT ( 'NONE',  ( 805.1016975059191054, 17.10349461922139369, 343.0745993439771837 ) ) ;
#36539=CARTESIAN_POINT ( 'NONE',  ( 758.8095938919644823, -176.0891481129654039, 311.6929314249762797 ) ) ;
#36540=CARTESIAN_POINT ( 'NONE',  ( 760.7433823573367135, -300.0090635724252479, 355.9930595647440441 ) ) ;
#36541=CARTESIAN_POINT ( 'NONE',  ( 793.2243759319678702, -386.5328690171409676, 318.4439275373583200 ) ) ;
#36544=CARTESIAN_POINT ( 'NONE',  ( 781.2497674668890113, -204.3510508353233774, 375.3608509340180603 ) ) ;
#36551=CARTESIAN_POINT ( 'NONE',  ( 803.2186876482843445, -271.9874144716868045, 350.0220218866286928 ) ) ;
#36559=CARTESIAN_POINT ( 'NONE',  ( 804.1009440267234822, -167.4636090269711133, 314.0944755984392600 ) ) ;
#36563=( BOUNDED_CURVE ( )  B_SPLINE_CURVE ( 3, ( #3930, #471, #14102, #38828 ),
 .UNSPECIFIED., .F., .T. ) 
 B_SPLINE_CURVE_WITH_KNOTS ( ( 4, 4 ),
 ( 4.712388980384714543, 4.733441231200429478 ),
 .UNSPECIFIED. ) 
 CURVE ( )  GEOMETRIC_REPRESENTATION_ITEM ( )  RATIONAL_B_SPLINE_CURVE ( ( 1.000000000000000000, 0.9999630672356449868, 0.9999630672356449868, 1.000000000000000000 ) ) 
 REPRESENTATION_ITEM ( '' )  );
#36567=CARTESIAN_POINT ( 'NONE',  ( 814.9108240113580450, -16.27096629478413092, 337.5031285880265273 ) ) ;
#36572=CARTESIAN_POINT ( 'NONE',  ( 795.1360043628807261, -44.08914811296584446, 360.2193346964456282 ) ) ;
#36573=CARTESIAN_POINT ( 'NONE',  ( 755.8990559732751535, -299.4636090269707438, 365.9055244015606831 ) ) ;
#36575=CARTESIAN_POINT ( 'NONE',  ( 810.7187646348534145, -258.4527844766016074, 356.7737145352016341 ) ) ;
#36577=CARTESIAN_POINT ( 'NONE',  ( 779.9999999999992042, 126.4563064324884465, 339.9999999999999432 ) ) ;
#36579=CARTESIAN_POINT ( 'NONE',  ( 781.8018195045266339, -358.2709662947829088, 365.1927285166406705 ) ) ;
#36580=CARTESIAN_POINT ( 'NONE',  ( 755.3028492785439312, -87.28179084515316788, 335.9200461376539693 ) ) ;
#36586=CARTESIAN_POINT ( 'NONE',  ( 797.6776695296629214, -379.5436935675102745, 357.6776695296636603 ) ) ;
#36591=CARTESIAN_POINT ( 'NONE',  ( 771.2633955100217236, -143.9073299311473590, 363.4237431249939618 ) ) ;
#36595=CARTESIAN_POINT ( 'NONE',  ( 814.8230680027162407, -437.8055962898679923, 333.7305795820267917 ) ) ;
#36597=CARTESIAN_POINT ( 'NONE',  ( 788.7366044899766848, -347.9073299311467053, 316.5762568750059813 ) ) ;
#36601=CARTESIAN_POINT ( 'NONE',  ( 791.7608162188021197, 205.0000000000000568, 360.0000000000000000 ) ) ;
#36604=CARTESIAN_POINT ( 'NONE',  ( 767.7687537140311633, -95.90732993114751537, 372.7932403749916830 ) ) ;
#36609=CARTESIAN_POINT ( 'NONE',  ( 771.2633955100217236, 0.09267006885218045942, 363.4237431249939618 ) ) ;
#36610=CARTESIAN_POINT ( 'NONE',  ( 800.9747183278959710, -228.9982390220561683, 311.9810565676471583 ) ) ;
#36611=CARTESIAN_POINT ( 'NONE',  ( 776.9566956441375396, -156.8965053807780805, 364.8461984189686405 ) ) ;
#36618=CARTESIAN_POINT ( 'NONE',  ( 768.9521613784389729, -81.82724539060772884, 373.2346286133773106 ) ) ;
#36629=CARTESIAN_POINT ( 'NONE',  ( 804.4086373105744769, -385.6454272087888171, 333.3843516231986541 ) ) ;
#36631=CARTESIAN_POINT ( 'NONE',  ( 769.9779781133707957, -235.0999726633344835, 316.7813123517150871 ) ) ;
#36634=CARTESIAN_POINT ( 'NONE',  ( 809.0717654672305343, -172.9181544815165239, 360.1688906516309885 ) ) ;
#36636=CARTESIAN_POINT ( 'NONE',  ( 796.7737145352015204, -164.6346026584200217, 370.7187646348536987 ) ) ;
#36641=CARTESIAN_POINT ( 'NONE',  ( 792.1044303154645831, -204.4527844766016926, 317.8323909638837677 ) ) ;
#36642=CARTESIAN_POINT ( 'NONE',  ( 754.7162404726377645, -14.73633629969885384, 339.4709603349214717 ) ) ;
#36646=CARTESIAN_POINT ( 'NONE',  ( 744.8212110874229666, -42.89650538077842157, 336.2046728542121627 ) ) ;
#36649=CARTESIAN_POINT ( 'NONE',  ( 802.1676090361156639, -38.63460265842041252, 327.8955696845344505 ) ) ;
#36651=CARTESIAN_POINT ( 'NONE',  ( 810.1134526219336749, -344.5328690171410813, 357.8822607201570349 ) ) ;
#36654=CARTESIAN_POINT ( 'NONE',  ( 755.0636971347428243, -340.2709662947831362, 341.7834795799807353 ) ) ;
#36662=CARTESIAN_POINT ( 'NONE',  ( 800.0135310231082713, -62.08914811296580183, 325.0180583372163028 ) ) ;
#36663=CARTESIAN_POINT ( 'NONE',  ( 796.1575198192839480, -366.0090635724250774, 359.4546378042384163 ) ) ;
#36665=CARTESIAN_POINT ( 'NONE',  ( 772.5602148656447525, -417.7255117493283478, 305.7998596910095443 ) ) ;
#36667=CARTESIAN_POINT ( 'NONE',  ( 759.8311093483677041, -310.1692326535048778, 310.9282345327691814 ) ) ;
#36668=CARTESIAN_POINT ( 'NONE',  ( 805.9055244015594326, -99.62377810805098477, 315.8990559732753240 ) ) ;
#36672=CARTESIAN_POINT ( 'NONE',  ( 751.9810565676468741, -410.0891481129647218, 360.9747183278973921 ) ) ;
#36673=CARTESIAN_POINT ( 'NONE',  ( 772.4999999999993179, -462.9681489794447202, 270.0000000000000568 ) ) ;
#36678=CARTESIAN_POINT ( 'NONE',  ( 773.4516893846965786, -307.6454272087888171, 315.8398074228977066 ) ) ;
#36679=CARTESIAN_POINT ( 'NONE',  ( 785.3687786644884454, -179.3618753856927128, 315.3201227861279676 ) ) ;
#36683=CARTESIAN_POINT ( 'NONE',  ( 745.1792804349281596, -86.19088175424408860, 343.7566961878542884 ) ) ;
#36686=CARTESIAN_POINT ( 'NONE',  ( 755.5713283507202505, -125.3618753856928834, 334.6858677611754729 ) ) ;
#36691=CARTESIAN_POINT ( 'NONE',  ( 804.4086373105744769, -25.64542720878973014, 333.3843516231986541 ) ) ;
#36694=CARTESIAN_POINT ( 'NONE',  ( 765.8855110935204493, -406.1692326535045368, 319.0159684113471599 ) ) ;
#36699=CARTESIAN_POINT ( 'NONE',  ( 808.7758568127978833, -244.1692326535050768, 320.0363995740631822 ) ) ;
#36700=CARTESIAN_POINT ( 'NONE',  ( 781.7834795799800531, -58.81642084023854267, 315.0636971347436202 ) ) ;
#36703=CARTESIAN_POINT ( 'NONE',  ( 788.8264449731200330, -237.1800572038742985, 363.6646147819171233 ) ) ;
#36710=CARTESIAN_POINT ( 'NONE',  ( 763.0537975583476964, -312.4527844766013800, 371.0346526505628617 ) ) ;
#36711=CARTESIAN_POINT ( 'NONE',  ( 811.6461892240364477, -28.71468719896028077, 324.1737431748509835 ) ) ;
#36716=CARTESIAN_POINT ( 'NONE',  ( 774.6858677611749044, -225.7255117493289163, 315.5713283507209894 ) ) ;
#36720=CARTESIAN_POINT ( 'NONE',  ( 787.4397851343537695, -309.7255117493287457, 374.2001403089903988 ) ) ;
#36722=CARTESIAN_POINT ( 'NONE',  ( 779.4709603349208464, -360.3510508353228374, 314.7162404726379918 ) ) ;
#36725=CARTESIAN_POINT ( 'NONE',  ( 754.7162404726377645, -206.7363362996982801, 339.4709603349214717 ) ) ;
#36726=CARTESIAN_POINT ( 'NONE',  ( 800.0135310231082713, -62.08914811296580183, 325.0180583372163028 ) ) ;
#36730=CARTESIAN_POINT ( 'NONE',  ( 802.7791456095903868, -220.7146871989596661, 329.0155153010375102 ) ) ;
#36733=CARTESIAN_POINT ( 'NONE',  ( 751.6929314249748586, -414.9982390220555430, 318.8095938919659034 ) ) ;
#36737=CARTESIAN_POINT ( 'NONE',  ( 767.6429770376289525, -33.18005720387498769, 306.8695393053162093 ) ) ;
#36738=CARTESIAN_POINT ( 'NONE',  ( 745.0891759886404770, -124.2709662947837899, 342.4968714119734159 ) ) ;
#36741=CARTESIAN_POINT ( 'NONE',  ( 745.1792804349281596, -398.1908817542431507, 343.7566961878542884 ) ) ;
#36743=CARTESIAN_POINT ( 'NONE',  ( 746.8695393053150156, -365.9073299311465917, 327.6429770376306010 ) ) ;
#36746=CARTESIAN_POINT ( 'NONE',  ( 776.9566956441375396, 11.10349461922141145, 364.8461984189686405 ) ) ;
#36749=CARTESIAN_POINT ( 'NONE',  ( 798.0661480581538854, -146.5328690171417350, 309.5768839229118043 ) ) ;
#36750=CARTESIAN_POINT ( 'NONE',  ( 802.1676090361155502, -446.6346026584191122, 327.8955696845344505 ) ) ;
#36752=CARTESIAN_POINT ( 'NONE',  ( 768.8385539511368734, -167.2601417444143976, 306.4236121716840557 ) ) ;
#36756=CARTESIAN_POINT ( 'NONE',  ( 795.1360043628807261, -116.0891481129656029, 360.2193346964456282 ) ) ;
#36758=CARTESIAN_POINT ( 'NONE',  ( 758.0580252608178853, -246.4527844766016074, 328.0187753319985404 ) ) ;
#36759=CARTESIAN_POINT ( 'NONE',  ( 764.8639956371174549, -272.0891481129651197, 319.7806653035542581 ) ) ;
#36762=CARTESIAN_POINT ( 'NONE',  ( 754.9735926884551418, 5.648949164675971524, 340.5236548041000333 ) ) ;
#36766=CARTESIAN_POINT ( 'NONE',  ( 767.7687537140311633, -191.9073299311471885, 372.7932403749916830 ) ) ;
#36767=CARTESIAN_POINT ( 'NONE',  ( 766.0291762391763086, -298.9181544815161828, 360.7704444035551319 ) ) ;
#36768=CARTESIAN_POINT ( 'NONE',  ( 789.9200121543843807, -385.9874144716864066, 317.0176451133914384 ) ) ;
#36776=CARTESIAN_POINT ( 'NONE',  ( 794.1144889064781864, -274.1692326535049915, 360.9840315886528401 ) ) ;
#36778=DIRECTION ( 'NONE',  ( -1.000000000000000000, -0.000000000000000000, -0.000000000000000000 ) ) ;
#36783=CARTESIAN_POINT ( 'NONE',  ( 757.7880784355613741, -210.0090635724255321, 312.4576283171834916 ) ) ;
#36794=CARTESIAN_POINT ( 'NONE',  ( 791.9812246680005501, -44.63460265842040542, 361.9419747391813189 ) ) ;
#36795=CARTESIAN_POINT ( 'NONE',  ( 745.7194118038753459, -301.6454272087889308, 348.7631598425976449 ) ) ;
#36796=CARTESIAN_POINT ( 'NONE',  ( 745.4481719005789273, -243.7255117493287742, 347.5162901302853129 ) ) ;
#36798=EDGE_CURVE ( 'NONE', #5612, #56, #19092, .T. ) ;
#36799=DIRECTION ( 'NONE',  ( 0.000000000000000000, 0.000000000000000000, -1.000000000000000000 ) ) ;
#36800=VERTEX_POINT ( 'NONE', #6049 ) ;
#36801=CARTESIAN_POINT ( 'NONE',  ( 778.2165204200184689, -358.8164208402375834, 364.9363028652563230 ) ) ;
#36802=CARTESIAN_POINT ( 'NONE',  ( 779.4763451958990572, -104.7363362996985785, 365.0264073115438919 ) ) ;
#36805=DIRECTION ( 'NONE',  ( 0.000000000000000000, 0.000000000000000000, 1.000000000000000000 ) ) ;
#36806=CARTESIAN_POINT ( 'NONE',  ( 794.9819416627830151, -396.9982390220556567, 319.9864689768909898 ) ) ;
#36810=CARTESIAN_POINT ( 'NONE',  ( 762.1405469898971887, -169.5436935675108430, 357.8594530101015607 ) ) ;
#36813=ADVANCED_FACE ( 'NONE', ( #8233, #19088 ), #20138, .F. ) ;
#36815=CARTESIAN_POINT ( 'NONE',  ( 754.8072714833581358, -364.8164208402374697, 338.1981804954720587 ) ) ;
#36820=CARTESIAN_POINT ( 'NONE',  ( 800.9747183278959710, -84.99823902205663728, 311.9810565676471583 ) ) ;
#36827=CARTESIAN_POINT ( 'NONE',  ( 744.7301800767019131, -244.8164208402378961, 337.4774526936615757 ) ) ;
#36828=CARTESIAN_POINT ( 'NONE',  ( 775.9200461376533440, -167.8055962898689586, 315.3028492785443291 ) ) ;
#36835=CARTESIAN_POINT ( 'NONE',  ( 745.7194118038753459, -61.64542720878961291, 348.7631598425976449 ) ) ;
#36846=CARTESIAN_POINT ( 'NONE',  ( 779.4763451958990572, -416.7363362996975980, 365.0264073115438919 ) ) ;
#36852=CARTESIAN_POINT ( 'NONE',  ( 815.3608509340175488, -194.7363362996982517, 341.2497674668889545 ) ) ;
#36854=CARTESIAN_POINT ( 'NONE',  ( 801.1904061080336987, -140.0891481129654892, 368.3070685750235498 ) ) ;
#36858=CARTESIAN_POINT ( 'NONE',  ( 764.8639956371174549, -272.0891481129651197, 319.7806653035542013 ) ) ;
#36859=CARTESIAN_POINT ( 'NONE',  ( 775.8780910478218402, -33.28179084515333130, 364.9511171171680530 ) ) ;
#36864=CARTESIAN_POINT ( 'NONE',  ( 789.9200121543843807, -97.98741447168734453, 317.0176451133914384 ) ) ;
#36866=CARTESIAN_POINT ( 'NONE',  ( 754.8072714833581358, -268.8164208402378108, 338.1981804954720587 ) ) ;
#36868=CARTESIAN_POINT ( 'NONE',  ( 755.3201227861273992, -51.72551174932946338, 345.3687786644892981 ) ) ;
#36871=CARTESIAN_POINT ( 'NONE',  ( 773.7943932421234194, -335.8055962898683902, 305.5313806188329409 ) ) ;
#36873=CARTESIAN_POINT ( 'NONE',  ( 813.2346286133761168, -437.2601417444135450, 328.9521613784389160 ) ) ;
#36876=CARTESIAN_POINT ( 'NONE',  ( 781.7834795799800531, -346.8164208402376971, 315.0636971347436202 ) ) ;
#36883=CARTESIAN_POINT ( 'NONE',  ( 762.3223304703356007, -103.5436935675111272, 322.3223304703362828 ) ) ;
#36884=CARTESIAN_POINT ( 'NONE',  ( 804.1105419155481968, -363.8272453906068336, 347.6308680596136469 ) ) ;
#36885=CARTESIAN_POINT ( 'NONE',  ( 782.5225473063383106, -430.2709662947827383, 375.2698199232970637 ) ) ;
#36887=CARTESIAN_POINT ( 'NONE',  ( 744.9990715423526808, -306.3510508353230648, 341.2370466360926002 ) ) ;
#36888=CARTESIAN_POINT ( 'NONE',  ( 786.2056067578752163, -107.8055962898691433, 374.4686193811670023 ) ) ;
#36891=CARTESIAN_POINT ( 'NONE',  ( 745.0891759886404770, -436.2709662947827951, 342.4968714119734159 ) ) ;
#36897=CARTESIAN_POINT ( 'NONE',  ( 802.9823548866075953, -313.0999726633342561, 330.0799878456151077 ) ) ;
#36898=CARTESIAN_POINT ( 'NONE',  ( 803.6646147819161570, -185.9073299311472454, 348.8264449731210561 ) ) ;
#36901=CYLINDRICAL_SURFACE ( 'NONE', #1703, 30.00000000000002842 ) ;
#36902=CARTESIAN_POINT ( 'NONE',  ( 764.1737431748507561, -58.37269993606236085, 371.6461892240376415 ) ) ;
#36905=CARTESIAN_POINT ( 'NONE',  ( 800.2193346964447755, -138.9982390220563957, 355.1360043628815788 ) ) ;
#36908=CARTESIAN_POINT ( 'NONE',  ( 754.7162404726377645, -14.73633629969885384, 339.4709603349214717 ) ) ;
#36910=DIRECTION ( 'NONE',  ( -1.000000000000000000, -0.000000000000000000, -0.000000000000000000 ) ) ;
#36911=CARTESIAN_POINT ( 'NONE',  ( 793.2243759319678702, -410.5328690171408539, 318.4439275373583200 ) ) ;
#36913=CARTESIAN_POINT ( 'NONE',  ( 793.2243759319678702, -74.53286901714196233, 318.4439275373583200 ) ) ;
#36917=CARTESIAN_POINT ( 'NONE',  ( 793.4146539503750546, -241.9874144716869182, 307.6481478633938877 ) ) ;
#36918=CARTESIAN_POINT ( 'NONE',  ( 788.7366044899766848, -83.90732993114754379, 316.5762568750059813 ) ) ;
#36922=CARTESIAN_POINT ( 'NONE',  ( 785.3141322388236176, -237.7255117493289163, 364.4286716492789537 ) ) ;
#36930=CARTESIAN_POINT ( 'NONE',  ( 745.0891759886404770, -340.2709662947831362, 342.4968714119734159 ) ) ;
#36931=CARTESIAN_POINT ( 'NONE',  ( 747.3154664389472828, -43.98741447168752217, 326.4474001241230781 ) ) ;
#36936=CARTESIAN_POINT ( 'NONE',  ( 771.1735550268778070, -201.1800572038744690, 316.3353852180827630 ) ) ;
#36939=CARTESIAN_POINT ( 'NONE',  ( 811.0346526505616112, -326.6346026584193396, 323.0537975583477532 ) ) ;
#36940=CARTESIAN_POINT ( 'NONE',  ( 779.9999999999992042, 126.4563064324884465, 339.9999999999999432 ) ) ;
#36943=CARTESIAN_POINT ( 'NONE',  ( 758.4439275373578084, -180.5545181178801499, 353.2243759319684386 ) ) ;
#36944=CARTESIAN_POINT ( 'NONE',  ( 755.3201227861273992, -75.72551174932937101, 345.3687786644892981 ) ) ;
#36948=CARTESIAN_POINT ( 'NONE',  ( 754.8983024940795303, -258.8965053807777963, 336.9254006560228163 ) ) ;
#36951=CARTESIAN_POINT ( 'NONE',  ( 804.7487373415286811, -427.5436935675101040, 364.7487373415288516 ) ) ;
#36955=CARTESIAN_POINT ( 'NONE',  ( 814.9108240113580450, -64.27096629478397460, 337.5031285880265273 ) ) ;
#36956=CARTESIAN_POINT ( 'NONE',  ( 749.2812353651451076, -126.4527844766019626, 323.2262854647983090 ) ) ;
#36960=CARTESIAN_POINT ( 'NONE',  ( 758.8095938919642549, -368.0891481129647786, 311.6929314249763365 ) ) ;
#36962=CARTESIAN_POINT ( 'NONE',  ( 755.8398074228967971, 4.558040073766884248, 333.4516893846970333 ) ) ;
#36965=CARTESIAN_POINT ( 'NONE',  ( 800.1688906516307043, -130.1692326535054463, 369.0717654672308186 ) ) ;
#36967=CARTESIAN_POINT ( 'NONE',  ( 759.8311093483677041, -166.1692326535053041, 310.9282345327691814 ) ) ;
#36971=CARTESIAN_POINT ( 'NONE',  ( 785.3141322388236176, -141.7255117493291721, 364.4286716492789537 ) ) ;
#36973=CARTESIAN_POINT ( 'NONE',  ( 792.1044303154645831, -276.4527844766013800, 317.8323909638837677 ) ) ;
#36974=CARTESIAN_POINT ( 'NONE',  ( 788.8264449731201466, -261.1800572038742416, 363.6646147819170665 ) ) ;
#36977=CARTESIAN_POINT ( 'NONE',  ( 760.5453621957607311, 2.921676437403253779, 323.8424801807151425 ) ) ;
#36981=CARTESIAN_POINT ( 'NONE',  ( 745.7998596910086917, -221.3618753856925707, 332.5602148656461168 ) ) ;
#36982=CARTESIAN_POINT ( 'NONE',  ( 804.8461984189677878, -290.1908817542434349, 336.9566956441385628 ) ) ;
#36983=CARTESIAN_POINT ( 'NONE',  ( 759.2295555964440155, -400.1692326535045936, 353.9708237608231229 ) ) ;
#36990=CARTESIAN_POINT ( 'NONE',  ( 783.0433043558608688, -288.8965053807775121, 315.1538015810313027 ) ) ;
#36993=CARTESIAN_POINT ( 'NONE',  ( 795.1360043628807261, 3.910851887033985896, 360.2193346964456282 ) ) ;
#36996=CARTESIAN_POINT ( 'NONE',  ( 745.1792804349281596, -206.1908817542437191, 343.7566961878542884 ) ) ;
#37002=CARTESIAN_POINT ( 'NONE',  ( 792.2312462859673587, -59.90732993114762905, 307.2067596250082602 ) ) ;
#37005=CARTESIAN_POINT ( 'NONE',  ( 755.3201227861273992, -51.72551174932946338, 345.3687786644892981 ) ) ;
#37006=CARTESIAN_POINT ( 'NONE',  ( 755.8990559732751535, -275.4636090269708575, 365.9055244015606831 ) ) ;
#37008=CARTESIAN_POINT ( 'NONE',  ( 758.8095938919642549, -248.0891481129651481, 311.6929314249763365 ) ) ;
#37013=CARTESIAN_POINT ( 'NONE',  ( 781.7834795799800531, -370.8164208402375834, 315.0636971347436202 ) ) ;
#37014=CARTESIAN_POINT ( 'NONE',  ( 800.9840315886518738, -124.9181544815167086, 354.1144889064786412 ) ) ;
#37018=CARTESIAN_POINT ( 'NONE',  ( 795.6651683502461765, -130.7146871989599504, 371.3240766477733814 ) ) ;
#37019=CARTESIAN_POINT ( 'NONE',  ( 759.9864689768902508, -386.0891481129647786, 354.9819416627836404 ) ) ;
#37022=CARTESIAN_POINT ( 'NONE',  ( 755.5713283507202505, -149.3618753856928265, 334.6858677611754729 ) ) ;
#37023=CARTESIAN_POINT ( 'NONE',  ( 788.7366044899766848, -155.9073299311473306, 316.5762568750059813 ) ) ;
#37028=CARTESIAN_POINT ( 'NONE',  ( 800.0135310231082713, -350.0891481129648923, 325.0180583372163028 ) ) ;
#37033=CARTESIAN_POINT ( 'NONE',  ( 782.5225473063383106, -118.2709662947838041, 375.2698199232970637 ) ) ;
#37039=CARTESIAN_POINT ( 'NONE',  ( 759.0252816721024374, -264.9982390220561115, 368.0189434323527280 ) ) ;
#37040=CARTESIAN_POINT ( 'NONE',  ( 805.1016975059191054, -174.8965053807779952, 343.0745993439771837 ) ) ;
#37044=ORIENTED_EDGE ( 'NONE', *, *, #31546, .T. ) ;
#37048=CARTESIAN_POINT ( 'NONE',  ( 795.8262568251477660, -94.37269993606224716, 308.3538107759623585 ) ) ;
#37057=CARTESIAN_POINT ( 'NONE',  ( 755.3028492785439312, -447.2817908451521021, 335.9200461376539693 ) ) ;
#37060=CARTESIAN_POINT ( 'NONE',  ( 802.5472867521000353, -244.3726999360617924, 350.8726784830461156 ) ) ;
#37064=CARTESIAN_POINT ( 'NONE',  ( 786.2694204179717872, -165.2817908451529547, 305.1769319972829067 ) ) ;
#37067=CARTESIAN_POINT ( 'NONE',  ( 767.6429770376289525, -153.1800572038746395, 306.8695393053162093 ) ) ;
#37070=CARTESIAN_POINT ( 'NONE',  ( 774.6858677611749044, -249.7255117493288594, 315.5713283507209894 ) ) ;
#37072=CARTESIAN_POINT ( 'NONE',  ( 786.5483106153019435, -7.645427208789786100, 364.1601925771022366 ) ) ;
#37077=CARTESIAN_POINT ( 'NONE',  ( 756.7813123517142913, -91.98741447168737295, 329.9779781133712504 ) ) ;
#37078=VERTEX_POINT ( 'NONE', #15608 ) ;
#37080=CARTESIAN_POINT ( 'NONE',  ( 771.1735550268778070, -57.18005720387489532, 316.3353852180827630 ) ) ;
#37082=CARTESIAN_POINT ( 'NONE',  ( 808.7758568127978833, -388.1692326535045936, 320.0363995740631822 ) ) ;
#37086=CARTESIAN_POINT ( 'NONE',  ( 804.4286716492782716, -377.3618753856920875, 345.3141322388244703 ) ) ;
#37095=CARTESIAN_POINT ( 'NONE',  ( 800.0135310231082713, -86.08914811296573077, 325.0180583372163028 ) ) ;
#37096=CARTESIAN_POINT ( 'NONE',  ( 790.0220218866281812, -415.0999726633340288, 363.2186876482849129 ) ) ;
#37097=CARTESIAN_POINT ( 'NONE',  ( 748.9653473494365699, -434.6346026584190554, 356.9462024416520762 ) ) ;
#37099=CARTESIAN_POINT ( 'NONE',  ( 773.7943932421234194, -335.8055962898683902, 305.5313806188329409 ) ) ;
#37100=ADVANCED_FACE ( 'NONE', ( #12148 ), #505, .T. ) ;
#37104=CARTESIAN_POINT ( 'NONE',  ( 809.0717654672305343, -4.918154481517067467, 360.1688906516309885 ) ) ;
#37109=CARTESIAN_POINT ( 'NONE',  ( 789.5584187865343893, -452.9681489794450613, 363.1011989789364520 ) ) ;
#37111=CARTESIAN_POINT ( 'NONE',  ( 790.0220218866281812, -295.0999726633343698, 363.2186876482849129 ) ) ;
#37115=PLANE ( 'NONE',  #31228 ) ;
#37116=CARTESIAN_POINT ( 'NONE',  ( 760.0363995740630116, -58.91815448151690759, 368.7758568127991907 ) ) ;
#37119=PLANE ( 'NONE',  #35774 ) ;
#37120=CARTESIAN_POINT ( 'NONE',  ( 797.8594530101008786, -133.5436935675110135, 322.1405469898980982 ) ) ;
#37126=CARTESIAN_POINT ( 'NONE',  ( 763.0428371773158460, -11.46360902697159290, 358.7617431975195359 ) ) ;
#37129=CARTESIAN_POINT ( 'NONE',  ( 790.8726784830453198, -418.7146871989590409, 362.5472867521010585 ) ) ;
#37133=DIRECTION ( 'NONE',  ( -1.000000000000000000, -0.000000000000000000, 0.000000000000000000 ) ) ;
#37134=CARTESIAN_POINT ( 'NONE',  ( 752.4576283171824116, -237.0783235625960117, 317.7880784355627952 ) ) ;
#37135=CARTESIAN_POINT ( 'NONE',  ( 803.6646147819162707, -89.90732993114752958, 348.8264449731211130 ) ) ;
#37140=CARTESIAN_POINT ( 'NONE',  ( 803.4237431249931660, -255.1800572038742700, 331.2633955100225194 ) ) ;
#37148=CARTESIAN_POINT ( 'NONE',  ( 813.1304606946831655, -329.9073299311467622, 352.3570229623691716 ) ) ;
#37149=CARTESIAN_POINT ( 'NONE',  ( 768.8385539511368734, -47.26014174441477422, 306.4236121716840557 ) ) ;
#37156=CARTESIAN_POINT ( 'NONE',  ( 755.3201227861273992, -195.7255117493289731, 345.3687786644892981 ) ) ;
#37159=CARTESIAN_POINT ( 'NONE',  ( 812.7932403749906598, -327.1800572038741279, 327.7687537140311633 ) ) ;
#37163=CARTESIAN_POINT ( 'NONE',  ( 757.0176451133909268, -181.0999726633347109, 349.9200121543848354 ) ) ;
#37164=CARTESIAN_POINT ( 'NONE',  ( 801.9419747391806368, -66.45278447660216159, 351.9812246680014027 ) ) ;
#37168=CARTESIAN_POINT ( 'NONE',  ( 795.9930595647434757, -243.0783235625959833, 320.7433823573372820 ) ) ;
#37172=CARTESIAN_POINT ( 'NONE',  ( 767.7687537140311633, -431.9073299311464211, 372.7932403749916830 ) ) ;
#37176=CARTESIAN_POINT ( 'NONE',  ( 782.4968714119720516, -82.81642084023846451, 305.0891759886411023 ) ) ;
#37177=CARTESIAN_POINT ( 'NONE',  ( 801.1904061080336987, -140.0891481129654892, 368.3070685750235498 ) ) ;
#37181=CARTESIAN_POINT ( 'NONE',  ( 754.9967657858570647, -361.5436935675103882, 365.0032342141425374 ) ) ;
#37184=CARTESIAN_POINT ( 'NONE',  ( 789.5670355615794733, -453.0432664090020012, 363.0970091259334822 ) ) ;
#37188=CARTESIAN_POINT ( 'NONE',  ( 807.5423716828161105, -129.0783235625963243, 362.2119215644372048 ) ) ;
#37193=CARTESIAN_POINT ( 'NONE',  ( 797.6776695296629214, -139.5436935675110135, 357.6776695296636603 ) ) ;
#37195=CARTESIAN_POINT ( 'NONE',  ( 791.9812246680005501, -284.6346026584196807, 361.9419747391813189 ) ) ;
#37196=CARTESIAN_POINT ( 'NONE',  ( 803.6646147819162707, -305.9073299311468190, 348.8264449731211130 ) ) ;
#37199=CARTESIAN_POINT ( 'NONE',  ( 780.5290396650775619, 11.64894916467595642, 365.2837595273619513 ) ) ;
#37205=CARTESIAN_POINT ( 'NONE',  ( 744.7301800767020268, -220.8164208402380098, 337.4774526936615189 ) ) ;
#37206=CARTESIAN_POINT ( 'NONE',  ( 776.9254006560222479, -284.1908817542434917, 314.8983024940802125 ) ) ;
#37207=CARTESIAN_POINT ( 'NONE',  ( 779.4709603349208464, -384.3510508353227806, 314.7162404726379918 ) ) ;
#37215=CARTESIAN_POINT ( 'NONE',  ( 772.3691319403857278, -287.2601417444140566, 315.8894580844506663 ) ) ;
#37217=CARTESIAN_POINT ( 'NONE',  ( 779.9999999999992042, -452.9681489794448339, 339.9999999999999432 ) ) ;
#37223=CARTESIAN_POINT ( 'NONE',  ( 768.9521613784389729, -201.8272453906073451, 373.2346286133773106 ) ) ;
#37228=CARTESIAN_POINT ( 'NONE',  ( 810.7187646348534145, -42.45278447660223264, 356.7737145352016341 ) ) ;
#37232=CARTESIAN_POINT ( 'NONE',  ( 788.7366044899766848, -59.90732993114762905, 316.5762568750059813 ) ) ;
#37233=CIRCLE ( 'NONE', #44603, 10.00000000000000888 ) ;
#37234=CARTESIAN_POINT ( 'NONE',  ( 745.1792804349281596, -326.1908817542433781, 343.7566961878542884 ) ) ;
#37235=CARTESIAN_POINT ( 'NONE',  ( 745.0891759886404770, -244.2709662947834204, 342.4968714119734159 ) ) ;
#37241=CARTESIAN_POINT ( 'NONE',  ( 762.3223304703356007, -343.5436935675103314, 322.3223304703362828 ) ) ;
#37242=CARTESIAN_POINT ( 'NONE',  ( 757.4527132478984868, -136.3726999360621051, 329.1273215169538844 ) ) ;
#37244=CARTESIAN_POINT ( 'NONE',  ( 765.0180583372156207, -384.9982390220556567, 360.0135310231089534 ) ) ;
#37247=CARTESIAN_POINT ( 'NONE',  ( 754.8072714833581358, -412.8164208402372992, 338.1981804954720587 ) ) ;
#37252=CARTESIAN_POINT ( 'NONE',  ( 797.6776695296629214, -187.5436935675108430, 357.6776695296636603 ) ) ;
#37253=CARTESIAN_POINT ( 'NONE',  ( 768.0187753319979720, -152.6346026584200786, 318.0580252608186242 ) ) ;
#37259=CARTESIAN_POINT ( 'NONE',  ( 778.1981804954714335, -370.2709662947831362, 314.8072714833589885 ) ) ;
#37260=VECTOR ( 'NONE', #5537, 1000.000000000000000 ) ;
#37264=CARTESIAN_POINT ( 'NONE',  ( 814.9108240113580450, -112.2709662947838325, 337.5031285880265273 ) ) ;
#37271=CARTESIAN_POINT ( 'NONE',  ( 748.9653473494363425, -266.6346026584197375, 356.9462024416521331 ) ) ;
#37272=CARTESIAN_POINT ( 'NONE',  ( 754.8983024940795303, -210.8965053807778816, 336.9254006560228163 ) ) ;
#37283=CARTESIAN_POINT ( 'NONE',  ( 771.3260364891663130, -115.6454272087894424, 306.0683387631859773 ) ) ;
#37292=CARTESIAN_POINT ( 'NONE',  ( 780.5236548040995785, -452.7363362996975411, 314.9735926884559944 ) ) ;
#37300=CARTESIAN_POINT ( 'NONE',  ( 802.2119215644370342, -222.0090635724254184, 367.5423716828165084 ) ) ;
#37302=CARTESIAN_POINT ( 'NONE',  ( 772.4837098697144029, -143.3618753856927697, 374.5518280994205611 ) ) ;
#37305=CARTESIAN_POINT ( 'NONE',  ( 771.1735550268778070, -249.1800572038742416, 316.3353852180827630 ) ) ;
#37306=CARTESIAN_POINT ( 'NONE',  ( 804.1105419155481968, -27.82724539060790292, 347.6308680596136469 ) ) ;
#37311=CARTESIAN_POINT ( 'NONE',  ( 804.9511171171677688, -77.80559628986920018, 335.8780910478229202 ) ) ;
#37312=CARTESIAN_POINT ( 'NONE',  ( 801.9419747391806368, -306.4527844766013800, 351.9812246680014027 ) ) ;
#37314=CARTESIAN_POINT ( 'NONE',  ( 755.5713283507202505, -269.3618753856924286, 334.6858677611754729 ) ) ;
#37319=CARTESIAN_POINT ( 'NONE',  ( 764.8639956371174549, -56.08914811296580893, 319.7806653035542013 ) ) ;
#37322=CARTESIAN_POINT ( 'NONE',  ( 800.1688906516307043, -394.1692326535045368, 369.0717654672308186 ) ) ;
#37324=CARTESIAN_POINT ( 'NONE',  ( 813.9316612368132837, -439.4419599262316751, 348.6739635108323228 ) ) ;
#37326=CARTESIAN_POINT ( 'NONE',  ( 778.2165204200184689, -358.8164208402375834, 364.9363028652563230 ) ) ;
#37329=ORIENTED_EDGE ( 'NONE', *, *, #202, .T. ) ;
#37334=CARTESIAN_POINT ( 'NONE',  ( 778.2165204200184689, -94.81642084023843609, 364.9363028652563230 ) ) ;
#37335=CARTESIAN_POINT ( 'NONE',  ( 779.4763451958990572, -392.7363362996977116, 365.0264073115438919 ) ) ;
#37337=CARTESIAN_POINT ( 'NONE',  ( 777.5031285880264704, -430.8164208402374129, 374.9108240113588408 ) ) ;
#37339=CARTESIAN_POINT ( 'NONE',  ( 813.9316612368132837, -319.4419599262320730, 348.6739635108323228 ) ) ;
#37340=CARTESIAN_POINT ( 'NONE',  ( 744.9990715423526808, -114.3510508353236617, 341.2370466360926002 ) ) ;
#37344=CARTESIAN_POINT ( 'NONE',  ( 801.1904061080336987, -452.0891481129646650, 368.3070685750235498 ) ) ;
#37351=CARTESIAN_POINT ( 'NONE',  ( 760.7433823573367135, -324.0090635724251911, 355.9930595647440441 ) ) ;
#37352=CARTESIAN_POINT ( 'NONE',  ( 797.6776695296629214, -187.5436935675108430, 357.6776695296636603 ) ) ;
#37354=CARTESIAN_POINT ( 'NONE',  ( 745.5313806188320314, -303.2817908451525000, 333.7943932421247268 ) ) ;
#37356=FACE_OUTER_BOUND ( 'NONE', #28369, .T. ) ;
#37357=CARTESIAN_POINT ( 'NONE',  ( 809.0717654672305343, -124.9181544815167086, 360.1688906516309885 ) ) ;
#37361=CARTESIAN_POINT ( 'NONE',  ( 788.8264449731200330, -165.1800572038745258, 363.6646147819171233 ) ) ;
#37363=CARTESIAN_POINT ( 'NONE',  ( 766.4474001241216001, -403.0999726633339719, 307.3154664389482491 ) ) ;
#37366=CARTESIAN_POINT ( 'NONE',  ( 755.1538015810308480, -62.19088175424416676, 343.0433043558613804 ) ) ;
#37369=CARTESIAN_POINT ( 'NONE',  ( 799.4546378042377910, -417.0783235625954148, 356.1575198192848006 ) ) ;
#37371=CARTESIAN_POINT ( 'NONE',  ( 789.9200121543843807, -73.98741447168741558, 317.0176451133914384 ) ) ;
#37376=FACE_OUTER_BOUND ( 'NONE', #6456, .T. ) ;
#37377=CARTESIAN_POINT ( 'NONE',  ( 815.0009284576459549, -270.3510508353231216, 338.7629533639073429 ) ) ;
#37378=CARTESIAN_POINT ( 'NONE',  ( 754.8072714833583632, -76.81642084023847872, 338.1981804954721156 ) ) ;
#37381=CARTESIAN_POINT ( 'NONE',  ( 803.4237431249931660, -279.1800572038741848, 331.2633955100225194 ) ) ;
#37391=CARTESIAN_POINT ( 'NONE',  ( 772.5602148656447525, -321.7255117493286320, 305.7998596910095443 ) ) ;
#37392=CARTESIAN_POINT ( 'NONE',  ( 758.0141637701419768, -231.0783235625960401, 367.2620300519063790 ) ) ;
#37398=CARTESIAN_POINT ( 'NONE',  ( 767.8955696845333705, -216.4527844766016926, 362.1676090361162323 ) ) ;
#37401=CARTESIAN_POINT ( 'NONE',  ( 767.6429770376289525, -369.1800572038739574, 306.8695393053162093 ) ) ;
#37403=CARTESIAN_POINT ( 'NONE',  ( 795.2260422076361692, 16.45630643248849978, 314.2591110605560516 ) ) ;
#37404=CARTESIAN_POINT ( 'NONE',  ( 779.9999999999992042, 126.4563064324884465, 339.9999999999999432 ) ) ;
#37405=CARTESIAN_POINT ( 'NONE',  ( 802.5472867521000353, -220.3726999360618208, 350.8726784830461156 ) ) ;
#37406=CARTESIAN_POINT ( 'NONE',  ( 804.6798772138708955, -87.72551174932937101, 334.6312213355107019 ) ) ;
#37409=CARTESIAN_POINT ( 'NONE',  ( 805.0264073115434940, -270.3510508353231216, 339.4763451958999099 ) ) ;
#37414=CARTESIAN_POINT ( 'NONE',  ( 758.8095938919642549, -440.0891481129644944, 311.6929314249763365 ) ) ;
#37419=CARTESIAN_POINT ( 'NONE',  ( 792.2312462859673587, -83.90732993114754379, 307.2067596250082602 ) ) ;
#37420=CARTESIAN_POINT ( 'NONE',  ( 745.0891759886404770, -148.2709662947837330, 342.4968714119734159 ) ) ;
#37422=CARTESIAN_POINT ( 'NONE',  ( 779.9999999999992042, 16.45630643248849267, 309.9999999999998863 ) ) ;
#37424=CARTESIAN_POINT ( 'NONE',  ( 752.7379699480933368, -420.0090635724249069, 361.9858362298580232 ) ) ;
#37425=DIRECTION ( 'NONE',  ( -0.000000000000000000, 1.000000000000000000, -0.000000000000000000 ) ) ;
#37426=CARTESIAN_POINT ( 'NONE',  ( 801.1904061080336987, -404.0891481129646081, 368.3070685750235498 ) ) ;
#37427=CARTESIAN_POINT ( 'NONE',  ( 812.7932403749906598, -15.18005720387504631, 327.7687537140311633 ) ) ;
#37430=CARTESIAN_POINT ( 'NONE',  ( 759.2295555964440155, 7.830767346494148740, 353.9708237608231229 ) ) ;
#37433=CARTESIAN_POINT ( 'NONE',  ( 810.1134526219336749, -176.5328690171416213, 357.8822607201570349 ) ) ;
#37437=CARTESIAN_POINT ( 'NONE',  ( 759.7806653035534055, -174.9982390220563673, 324.8639956371180801 ) ) ;
#37439=CARTESIAN_POINT ( 'NONE',  ( 762.1405469898971887, -289.5436935675103882, 357.8594530101015607 ) ) ;
#37440=CARTESIAN_POINT ( 'NONE',  ( 803.4237431249931660, -279.1800572038741848, 331.2633955100225194 ) ) ;
#37443=CARTESIAN_POINT ( 'NONE',  ( 754.9735926884551418, -18.35105083532395298, 340.5236548041000333 ) ) ;
#37448=CARTESIAN_POINT ( 'NONE',  ( 800.9747183278959710, -228.9982390220561683, 311.9810565676471583 ) ) ;
#37449=CARTESIAN_POINT ( 'NONE',  ( 783.0745993439762742, -296.1908817542434917, 365.1016975059196739 ) ) ;
#37450=CARTESIAN_POINT ( 'NONE',  ( 803.8651313633788504, -413.2601417444136018, 332.4468031744301015 ) ) ;
#37455=VERTEX_POINT ( 'NONE', #11124 ) ;
#37457=CARTESIAN_POINT ( 'NONE',  ( 769.1273215169530886, -286.7146871989594388, 317.4527132478988847 ) ) ;
#37458=CARTESIAN_POINT ( 'NONE',  ( 758.7867965644026071, 16.45630643248849267, 318.7867965644036303 ) ) ;
#37463=CARTESIAN_POINT ( 'NONE',  ( 783.7953271457878373, -200.1908817542436907, 375.1787889125761239 ) ) ;
#37468=CARTESIAN_POINT ( 'NONE',  ( 763.2262854647970016, -56.63460265842036279, 309.2812353651462445 ) ) ;
#37472=CARTESIAN_POINT ( 'NONE',  ( 800.2193346964447755, -66.99823902205672255, 355.1360043628815788 ) ) ;
#37474=CARTESIAN_POINT ( 'NONE',  ( 768.9521613784389729, -321.8272453906070609, 373.2346286133773106 ) ) ;
#37476=CARTESIAN_POINT ( 'NONE',  ( 796.9462024416508257, -300.4527844766012663, 308.9653473494370246 ) ) ;
#37480=CARTESIAN_POINT ( 'NONE',  ( 785.3141322388236176, -357.7255117493285184, 364.4286716492789537 ) ) ;
#37481=CARTESIAN_POINT ( 'NONE',  ( 780.5236548040995785, -116.7363362996985217, 314.9735926884559944 ) ) ;
#37483=CARTESIAN_POINT ( 'NONE',  ( 781.2497674668890113, -36.35105083532390324, 375.3608509340180603 ) ) ;
#37484=CARTESIAN_POINT ( 'NONE',  ( 756.5762568750052424, -363.1800572038739006, 348.7366044899774238 ) ) ;
#37487=CARTESIAN_POINT ( 'NONE',  ( 755.0636971347428243, -436.2709662947827951, 341.7834795799807353 ) ) ;
#37488=ORIENTED_EDGE ( 'NONE', *, *, #30882, .F. ) ;
#37490=CARTESIAN_POINT ( 'NONE',  ( 802.1676090361156639, -182.6346026584199649, 327.8955696845344505 ) ) ;
#37491=CARTESIAN_POINT ( 'NONE',  ( 797.6776695296629214, -187.5436935675108430, 357.6776695296636603 ) ) ;
#37495=CARTESIAN_POINT ( 'NONE',  ( 764.8639956371174549, -392.0891481129648355, 319.7806653035542013 ) ) ;
#37499=CARTESIAN_POINT ( 'NONE',  ( 800.9747183278959710, -132.9982390220564810, 311.9810565676471583 ) ) ;
#37506=CARTESIAN_POINT ( 'NONE',  ( 745.0891759886404770, -244.2709662947834204, 342.4968714119734159 ) ) ;
#37507=CARTESIAN_POINT ( 'NONE',  ( 766.7756240680305382, -182.5328690171416497, 361.5560724626415663 ) ) ;
#37511=ORIENTED_EDGE ( 'NONE', *, *, #2688, .T. ) ;
#37517=CARTESIAN_POINT ( 'NONE',  ( 757.7880784355613741, -114.0090635724258163, 312.4576283171834916 ) ) ;
#37525=CARTESIAN_POINT ( 'NONE',  ( 769.0155153010367712, -418.3726999360612808, 362.7791456095907279 ) ) ;
#37532=CARTESIAN_POINT ( 'NONE',  ( 788.6739635108323228, -223.6454272087891013, 373.9316612368139090 ) ) ;
#37534=CARTESIAN_POINT ( 'NONE',  ( 754.9967657858570647, -169.5436935675108430, 365.0032342141425374 ) ) ;
#37537=CARTESIAN_POINT ( 'NONE',  ( 757.8323909638827445, -266.6346026584197375, 352.1044303154654358 ) ) ;
#37538=CARTESIAN_POINT ( 'NONE',  ( 786.5483106153019435, -55.64542720878963422, 364.1601925771022366 ) ) ;
#37543=CARTESIAN_POINT ( 'NONE',  ( 794.1144889064781864, -82.16923265350558836, 360.9840315886528401 ) ) ;
#37546=CARTESIAN_POINT ( 'NONE',  ( 762.1405469898971887, -73.54369356751118403, 357.8594530101015607 ) ) ;
#37549=CARTESIAN_POINT ( 'NONE',  ( 752.4576283171824116, -381.0783235625954717, 317.7880784355627952 ) ) ;
#37552=CARTESIAN_POINT ( 'NONE',  ( 755.0636971347428243, -388.2709662947829656, 341.7834795799807353 ) ) ;
#37555=EDGE_LOOP ( 'NONE', ( #35117, #27737, #41506, #9174 ) ) ;
#37559=CARTESIAN_POINT ( 'NONE',  ( 758.0580252608178853, -102.4527844766020337, 328.0187753319985404 ) ) ;
#37560=CARTESIAN_POINT ( 'NONE',  ( 769.0155153010367712, -394.3726999360613377, 362.7791456095907279 ) ) ;
#37561=CARTESIAN_POINT ( 'NONE',  ( 789.9200121543843807, -97.98741447168734453, 317.0176451133914384 ) ) ;
#37562=CARTESIAN_POINT ( 'NONE',  ( 811.0346526505617248, -446.6346026584191122, 323.0537975583478101 ) ) ;
#37563=FACE_OUTER_BOUND ( 'NONE', #37897, .T. ) ;
#37564=CARTESIAN_POINT ( 'NONE',  ( 744.8212110874229666, -354.8965053807774552, 336.2046728542121627 ) ) ;
#37569=CARTESIAN_POINT ( 'NONE',  ( 787.5162901302840055, -443.3618753856917465, 305.4481719005792684 ) ) ;
#37576=CARTESIAN_POINT ( 'NONE',  ( 786.5483106153019435, -319.6454272087888739, 364.1601925771022366 ) ) ;
#37577=CARTESIAN_POINT ( 'NONE',  ( 781.8018195045266339, -190.2709662947835909, 365.1927285166406705 ) ) ;
#37579=CARTESIAN_POINT ( 'NONE',  ( 812.3518521366052028, -289.0999726633343698, 326.5853460496235243 ) ) ;
#37583=CARTESIAN_POINT ( 'NONE',  ( 811.3240766477731540, -100.3726999360622187, 355.6651683502462902 ) ) ;
#37586=CARTESIAN_POINT ( 'NONE',  ( 785.3141322388236176, -165.7255117493291152, 364.4286716492789537 ) ) ;
#37588=CARTESIAN_POINT ( 'NONE',  ( 750.9282345327678740, -424.9181544815158986, 319.8311093483690115 ) ) ;
#37591=CARTESIAN_POINT ( 'NONE',  ( 772.4468031744293057, -33.82724539060788516, 363.8651313633793620 ) ) ;
#37594=CARTESIAN_POINT ( 'NONE',  ( 764.3348316497523456, 25.28531280103955226, 308.6759233522265617 ) ) ;
#37596=CARTESIAN_POINT ( 'NONE',  ( 794.1144889064781864, -82.16923265350558836, 360.9840315886528401 ) ) ;
#37600=CARTESIAN_POINT ( 'NONE',  ( 749.8865473780648472, -284.5328690171412518, 322.1177392798429082 ) ) ;
#37601=CARTESIAN_POINT ( 'NONE',  ( 792.1044303154646968, -84.45278447660207632, 317.8323909638837677 ) ) ;
#37604=CARTESIAN_POINT ( 'NONE',  ( 785.3141322388236176, -261.7255117493288026, 364.4286716492789537 ) ) ;
#37607=ORIENTED_EDGE ( 'NONE', *, *, #11433, .T. ) ;
#37610=CARTESIAN_POINT ( 'NONE',  ( 814.2001403089898304, -329.3618753856922581, 347.4397851343538264 ) ) ;
#37611=CARTESIAN_POINT ( 'NONE',  ( 798.0661480581538854, -266.5328690171413655, 309.5768839229118043 ) ) ;
#37616=CARTESIAN_POINT ( 'NONE',  ( 804.9363028652555840, -208.2709662947835341, 338.2165204200192079 ) ) ;
#37619=CARTESIAN_POINT ( 'NONE',  ( 754.9967657858570647, -361.5436935675103882, 365.0032342141425374 ) ) ;
#37622=CARTESIAN_POINT ( 'NONE',  ( 772.8365271371600329, 16.45630643248849267, 315.6518837687410723 ) ) ;
#37624=EDGE_CURVE ( 'NONE', #20178, #18957, #25670, .T. ) ;
#37625=CARTESIAN_POINT ( 'NONE',  ( 766.9102291470427417, -234.5545181178799794, 318.6633372737382501 ) ) ;
#37626=CARTESIAN_POINT ( 'NONE',  ( 791.9812246680005501, -92.63460265842026331, 361.9419747391813189 ) ) ;
#37630=CARTESIAN_POINT ( 'NONE',  ( 804.9511171171677688, -245.8055962898686460, 335.8780910478229202 ) ) ;
#37633=CARTESIAN_POINT ( 'NONE',  ( 804.1009440267234822, 0.5363909730283709099, 314.0944755984392600 ) ) ;
#37637=CARTESIAN_POINT ( 'NONE',  ( 792.3570229623688874, -69.18005720387488111, 373.1304606946836202 ) ) ;
#37638=CARTESIAN_POINT ( 'NONE',  ( 749.2812353651451076, -150.4527844766018916, 323.2262854647983090 ) ) ;
#37643=CARTESIAN_POINT ( 'NONE',  ( 791.0478386215596629, -405.8272453906067199, 306.7653713866226326 ) ) ;
#37647=CARTESIAN_POINT ( 'NONE',  ( 759.0252816721024374, -384.9982390220556567, 368.0189434323527280 ) ) ;
#37648=CARTESIAN_POINT ( 'NONE',  ( 777.5031285880264704, 1.183579159761269040, 374.9108240113588408 ) ) ;
#37650=CARTESIAN_POINT ( 'NONE',  ( 786.6156483768007774, -1.441959926233096656, 315.5913626894246136 ) ) ;
#37654=CARTESIAN_POINT ( 'NONE',  ( 771.2368401574024119, -157.4419599262326130, 374.2805881961240857 ) ) ;
#37655=FACE_BOUND ( 'NONE', #11650, .T. ) ;
#37659=CARTESIAN_POINT ( 'NONE',  ( 797.8594530101008786, -157.5436935675108998, 322.1405469898980982 ) ) ;
#37662=CARTESIAN_POINT ( 'NONE',  ( 754.8072714833581358, -292.8164208402376971, 338.1981804954720587 ) ) ;
#37663=CARTESIAN_POINT ( 'NONE',  ( 802.1676090361155502, -278.6346026584196807, 327.8955696845344505 ) ) ;
#37665=ORIENTED_EDGE ( 'NONE', *, *, #19631, .F. ) ;
#37666=CARTESIAN_POINT ( 'NONE',  ( 790.8726784830453198, -10.71468719896033761, 362.5472867521010585 ) ) ;
#37671=CARTESIAN_POINT ( 'NONE',  ( 815.2698199232962679, -232.8164208402379529, 342.5225473063383674 ) ) ;
#37673=CARTESIAN_POINT ( 'NONE',  ( 800.9840315886518738, -340.9181544815160123, 354.1144889064786412 ) ) ;
#37674=CARTESIAN_POINT ( 'NONE',  ( 803.2186876482843445, -439.9874144716862929, 350.0220218866286928 ) ) ;
#37681=CARTESIAN_POINT ( 'NONE',  ( 783.0433043558608688, -312.8965053807775689, 315.1538015810313027 ) ) ;
#37686=CARTESIAN_POINT ( 'NONE',  ( 760.7433823573367135, -108.0090635724258448, 355.9930595647440441 ) ) ;
#37687=CARTESIAN_POINT ( 'NONE',  ( 803.4237431249931660, 8.819942796124882634, 331.2633955100225194 ) ) ;
#37690=CARTESIAN_POINT ( 'NONE',  ( 781.2370466360911223, -212.7363362996982232, 304.9990715423533629 ) ) ;
#37694=CARTESIAN_POINT ( 'NONE',  ( 801.1904061080336987, -44.08914811296584446, 368.3070685750235498 ) ) ;
#37698=CARTESIAN_POINT ( 'NONE',  ( 750.9282345327678740, -304.9181544815161828, 319.8311093483690115 ) ) ;
#37701=CARTESIAN_POINT ( 'NONE',  ( 759.0252816721024374, -288.9982390220559978, 368.0189434323527280 ) ) ;
#37705=CARTESIAN_POINT ( 'NONE',  ( 781.7834795799800531, -394.8164208402374697, 315.0636971347436202 ) ) ;
#37706=CARTESIAN_POINT ( 'NONE',  ( 804.6971507214547046, -123.2817908451530542, 344.0799538623459739 ) ) ;
#37708=CARTESIAN_POINT ( 'NONE',  ( 756.1443688327750579, -69.62377810805107003, 314.3581564841659315 ) ) ;
#37709=CARTESIAN_POINT ( 'NONE',  ( 792.1044303154646968, -372.4527844766012095, 317.8323909638837677 ) ) ;
#37712=CARTESIAN_POINT ( 'NONE',  ( 756.1443688327750579, -141.6237781080508569, 314.3581564841659315 ) ) ;
#37713=CARTESIAN_POINT ( 'NONE',  ( 755.5713283507202505, -413.3618753856920307, 334.6858677611754729 ) ) ;
#37717=CARTESIAN_POINT ( 'NONE',  ( 755.5713283507202505, -197.3618753856926560, 334.6858677611754729 ) ) ;
#37718=CARTESIAN_POINT ( 'NONE',  ( 755.5713283507202505, -197.3618753856926560, 334.6858677611754729 ) ) ;
#37722=CARTESIAN_POINT ( 'NONE',  ( 805.1927285166397041, -400.8164208402373561, 341.8018195045277707 ) ) ;
#37726=CARTESIAN_POINT ( 'NONE',  ( 813.1304606946831655, -113.9073299311474585, 352.3570229623691716 ) ) ;
#37733=CARTESIAN_POINT ( 'NONE',  ( 787.4397851343537695, -237.7255117493289163, 374.2001403089903988 ) ) ;
#37734=CARTESIAN_POINT ( 'NONE',  ( 779.4709603349208464, -192.3510508353233774, 314.7162404726379918 ) ) ;
#37737=FACE_OUTER_BOUND ( 'NONE', #15025, .T. ) ;
#37745=CARTESIAN_POINT ( 'NONE',  ( 747.6481478633932056, -109.0999726633349241, 353.4146539503763620 ) ) ;
#37754=CARTESIAN_POINT ( 'NONE',  ( 755.1538015810308480, -446.1908817542429802, 343.0433043558613804 ) ) ;
#37755=CARTESIAN_POINT ( 'NONE',  ( 814.4686193811664907, -363.2817908451523294, 346.2056067578752732 ) ) ;
#37762=CARTESIAN_POINT ( 'NONE',  ( 778.7629533639073998, -200.7363362996982801, 375.0009284576466371 ) ) ;
#37764=CARTESIAN_POINT ( 'NONE',  ( 745.4481719005789273, -171.7255117493291152, 347.5162901302853129 ) ) ;
#37767=CARTESIAN_POINT ( 'NONE',  ( 756.3353852180819104, -269.9073299311468190, 331.1735550268788302 ) ) ;
#37768=CARTESIAN_POINT ( 'NONE',  ( 784.1219089521767955, -69.28179084515321051, 315.0488828828318333 ) ) ;
#37773=CARTESIAN_POINT ( 'NONE',  ( 805.0264073115434940, -78.35105083532376113, 339.4763451958999099 ) ) ;
#37774=CARTESIAN_POINT ( 'NONE',  ( 794.9819416627830151, -324.9982390220559409, 319.9864689768909898 ) ) ;
#37777=CARTESIAN_POINT ( 'NONE',  ( 754.8072714833581358, -76.81642084023845030, 338.1981804954720587 ) ) ;
#37781=CARTESIAN_POINT ( 'NONE',  ( 801.9858362298568863, -387.0783235625955285, 312.7379699480935642 ) ) ;
#37783=CARTESIAN_POINT ( 'NONE',  ( 794.9819416627830151, -300.9982390220559409, 319.9864689768909898 ) ) ;
#37784=CARTESIAN_POINT ( 'NONE',  ( 796.7737145352015204, 3.365397341579444479, 370.7187646348536987 ) ) ;
#37786=CARTESIAN_POINT ( 'NONE',  ( 759.7806653035534055, -390.9982390220557136, 324.8639956371180801 ) ) ;
#37792=CARTESIAN_POINT ( 'NONE',  ( 771.1735550268778070, -105.1800572038747248, 316.3353852180827630 ) ) ;
#37793=CARTESIAN_POINT ( 'NONE',  ( 804.6971507214547046, -411.2817908451521589, 344.0799538623459739 ) ) ;
#37794=CARTESIAN_POINT ( 'NONE',  ( 801.3366627262608972, -104.5328690171418913, 353.0897708529566899 ) ) ;
#37795=CARTESIAN_POINT ( 'NONE',  ( 814.2001403089898304, -449.3618753856918602, 347.4397851343538264 ) ) ;
#37797=CARTESIAN_POINT ( 'NONE',  ( 778.7502325331095108, -360.3510508353228374, 304.6391490659818828 ) ) ;
#37798=CARTESIAN_POINT ( 'NONE',  ( 746.0683387631852383, -115.4419599262327409, 331.3260364891676204 ) ) ;
#37803=CARTESIAN_POINT ( 'NONE',  ( 778.7629533639073998, -8.736336299698871599, 375.0009284576466371 ) ) ;
#37810=CARTESIAN_POINT ( 'NONE',  ( 790.0220218866281812, -319.0999726633342561, 363.2186876482849129 ) ) ;
#37812=CARTESIAN_POINT ( 'NONE',  ( 791.0478386215596629, -309.8272453906070041, 306.7653713866226326 ) ) ;
#37815=CARTESIAN_POINT ( 'NONE',  ( 757.7880784355613741, -114.0090635724258163, 312.4576283171834916 ) ) ;
#37819=CARTESIAN_POINT ( 'NONE',  ( 802.1676090361156639, -134.6346026584201070, 327.8955696845344505 ) ) ;
#37821=CARTESIAN_POINT ( 'NONE',  ( 805.6418435158337843, -437.4636090269703459, 363.8556311672236916 ) ) ;
#37824=CARTESIAN_POINT ( 'NONE',  ( 755.8894580844503253, -39.82724539060786384, 332.3691319403863531 ) ) ;
#37827=CARTESIAN_POINT ( 'NONE',  ( 793.4146539503750546, 22.01258552831228599, 307.6481478633938877 ) ) ;
#37832=CARTESIAN_POINT ( 'NONE',  ( 746.0683387631852383, -283.4419599262321867, 331.3260364891676204 ) ) ;
#37833=CARTESIAN_POINT ( 'NONE',  ( 755.5713283507202505, -101.3618753856929544, 334.6858677611754729 ) ) ;
#37837=CARTESIAN_POINT ( 'NONE',  ( 805.1927285166397041, -280.8164208402378677, 341.8018195045277707 ) ) ;
#37844=CARTESIAN_POINT ( 'NONE',  ( 792.3570229623691148, -357.1800572038739574, 373.1304606946836770 ) ) ;
#37845=CARTESIAN_POINT ( 'NONE',  ( 752.4576283171824116, -237.0783235625960117, 317.7880784355627952 ) ) ;
#37849=CARTESIAN_POINT ( 'NONE',  ( 794.9819416627830151, -228.9982390220561683, 319.9864689768909898 ) ) ;
#37851=CARTESIAN_POINT ( 'NONE',  ( 782.5225473063381969, -358.2709662947829088, 375.2698199232970637 ) ) ;
#37856=CARTESIAN_POINT ( 'NONE',  ( 804.8461984189677878, -242.1908817542435770, 336.9566956441385628 ) ) ;
#37857=CARTESIAN_POINT ( 'NONE',  ( 771.1735550268778070, -81.18005720387481006, 316.3353852180827630 ) ) ;
#37864=CARTESIAN_POINT ( 'NONE',  ( 783.0433043558608688, -240.8965053807777963, 315.1538015810313027 ) ) ;
#37867=CARTESIAN_POINT ( 'NONE',  ( 760.0363995740630116, -10.91815448151704793, 368.7758568127991907 ) ) ;
#37870=CARTESIAN_POINT ( 'NONE',  ( 755.2512626584698410, -79.54369356751119824, 315.2512626584710915 ) ) ;
#37871=CARTESIAN_POINT ( 'NONE',  ( 751.6929314249748586, -126.9982390220565094, 318.8095938919659034 ) ) ;
#37875=CARTESIAN_POINT ( 'NONE',  ( 783.7953271457878373, -416.1908817542430938, 375.1787889125761239 ) ) ;
#37878=CARTESIAN_POINT ( 'NONE',  ( 796.7737145352015204, -404.6346026584193396, 370.7187646348536987 ) ) ;
#37879=CARTESIAN_POINT ( 'NONE',  ( 792.3570229623691148, -21.18005720387502322, 373.1304606946836770 ) ) ;
#37881=CARTESIAN_POINT ( 'NONE',  ( 793.2243759319678702, -26.53286901714210799, 318.4439275373583200 ) ) ;
#37884=CARTESIAN_POINT ( 'NONE',  ( 766.5853460496234675, -181.9874144716870887, 372.3518521366060554 ) ) ;
#37886=CARTESIAN_POINT ( 'NONE',  ( 776.2433038121456548, -180.8965053807779952, 374.8207195650711014 ) ) ;
#37890=CARTESIAN_POINT ( 'NONE',  ( 788.8264449731200330, -165.1800572038745258, 363.6646147819171233 ) ) ;
#37893=CARTESIAN_POINT ( 'NONE',  ( 755.3201227861273992, -291.7255117493285752, 345.3687786644892981 ) ) ;
#37894=CARTESIAN_POINT ( 'NONE',  ( 778.2165204200184689, -310.8164208402377540, 364.9363028652563230 ) ) ;
#37897=EDGE_LOOP ( 'NONE', ( #1779, #27802, #33335, #35979, #26423, #41601, #19902, #37511 ) ) ;
#37898=CARTESIAN_POINT ( 'NONE',  ( 804.9511171171677688, -5.805596289869448867, 335.8780910478229202 ) ) ;
#37900=CARTESIAN_POINT ( 'NONE',  ( 755.2512626584698410, -223.5436935675107577, 315.2512626584710915 ) ) ;
#37901=CARTESIAN_POINT ( 'NONE',  ( 804.8461984189677878, -338.1908817542433212, 336.9566956441385628 ) ) ;
#37902=CARTESIAN_POINT ( 'NONE',  ( 796.7845633553578182, -417.6237781080499190, 358.5707757039688204 ) ) ;
#37906=ORIENTED_EDGE ( 'NONE', *, *, #43568, .F. ) ;
#37909=CARTESIAN_POINT ( 'NONE',  ( 779.4709603349208464, -312.3510508353230080, 314.7162404726379918 ) ) ;
#37911=CARTESIAN_POINT ( 'NONE',  ( 799.9999999999993179, -462.9681489794448339, 370.0000000000000568 ) ) ;
#37912=CARTESIAN_POINT ( 'NONE',  ( 796.1575198192839480, -126.0090635724257737, 359.4546378042384163 ) ) ;
#37914=ORIENTED_EDGE ( 'NONE', *, *, #28125, .F. ) ;
#37916=CARTESIAN_POINT ( 'NONE',  ( 762.1177392798416577, -234.5545181178799794, 309.8865473780659272 ) ) ;
#37920=CARTESIAN_POINT ( 'NONE',  ( 815.2698199232961542, -40.81642084023859951, 342.5225473063383106 ) ) ;
#37921=CARTESIAN_POINT ( 'NONE',  ( 805.7454966640377734, -452.9681489794450044, 346.1170114844039745 ) ) ;
#37925=CARTESIAN_POINT ( 'NONE',  ( 776.2046728542105711, -332.1908817542433781, 304.8212110874238761 ) ) ;
#37927=CARTESIAN_POINT ( 'NONE',  ( 801.1904061080336987, -308.0891481129650629, 368.3070685750235498 ) ) ;
#37932=CARTESIAN_POINT ( 'NONE',  ( 774.6312213355099630, -407.3618753856920307, 364.6798772138717482 ) ) ;
#37933=CARTESIAN_POINT ( 'NONE',  ( 760.7433823573367135, -156.0090635724256742, 355.9930595647440441 ) ) ;
#37935=CARTESIAN_POINT ( 'NONE',  ( 805.9055244015594326, -51.62377810805111267, 315.8990559732753240 ) ) ;
#37936=CARTESIAN_POINT ( 'NONE',  ( 765.0180583372156207, -360.9982390220557704, 360.0135310231089534 ) ) ;
#37940=CARTESIAN_POINT ( 'NONE',  ( 744.9990715423526808, -138.3510508353236048, 341.2370466360926002 ) ) ;
#37941=CARTESIAN_POINT ( 'NONE',  ( 768.0187753319979720, -440.6346026584191122, 318.0580252608186242 ) ) ;
#37944=EDGE_CURVE ( 'NONE', #10891, #45297, #1404, .T. ) ;
#37948=CARTESIAN_POINT ( 'NONE',  ( 802.1676090361156639, -206.6346026584198512, 327.8955696845344505 ) ) ;
#37949=CARTESIAN_POINT ( 'NONE',  ( 762.3223304703356007, -199.5436935675108430, 322.3223304703362828 ) ) ;
#37953=CARTESIAN_POINT ( 'NONE',  ( 774.6312213355099630, -383.3618753856921444, 364.6798772138717482 ) ) ;
#37956=CARTESIAN_POINT ( 'NONE',  ( 755.2512626584698410, -127.5436935675110561, 315.2512626584710915 ) ) ;
#37959=VECTOR ( 'NONE', #4210, 1000.000000000000000 ) ;
#37966=CARTESIAN_POINT ( 'NONE',  ( 794.1144889064781864, -202.1692326535051905, 360.9840315886528401 ) ) ;
#37967=CARTESIAN_POINT ( 'NONE',  ( 794.9285562942586694, -457.5945560043289788, 366.0218793896430043 ) ) ;
#37977=CARTESIAN_POINT ( 'NONE',  ( 793.5525998758768083, -103.0999726633349525, 372.6845335610516941 ) ) ;
#37979=CARTESIAN_POINT ( 'NONE',  ( 787.4999999999992042, -512.9681489794448908, 350.0000000000000000 ) ) ;
#37986=CARTESIAN_POINT ( 'NONE',  ( 793.0897708529556667, -438.5545181178793541, 361.3366627262616362 ) ) ;
#37989=CARTESIAN_POINT ( 'NONE',  ( 797.8822607201568644, -366.5545181178795815, 370.1134526219340160 ) ) ;
#37990=CARTESIAN_POINT ( 'NONE',  ( 799.9999999999993179, -512.9681489794448908, 339.9999999999999432 ) ) ;
#37994=CARTESIAN_POINT ( 'NONE',  ( 785.3687786644884454, 12.63812461430668321, 315.3201227861279676 ) ) ;
#37997=CARTESIAN_POINT ( 'NONE',  ( 747.6481478633932056, -205.0999726633346256, 353.4146539503763620 ) ) ;
#37999=CARTESIAN_POINT ( 'NONE',  ( 772.5602148656447525, -201.7255117493290015, 305.7998596910095443 ) ) ;
#38004=CARTESIAN_POINT ( 'NONE',  ( 788.7366044899766848, -299.9073299311468759, 316.5762568750059813 ) ) ;
#38005=CARTESIAN_POINT ( 'NONE',  ( 802.5472867521000353, -52.37269993606237506, 350.8726784830461156 ) ) ;
#38009=CARTESIAN_POINT ( 'NONE',  ( 759.9999999999992042, -512.9681489794448908, 339.9999999999999432 ) ) ;
#38010=CARTESIAN_POINT ( 'NONE',  ( 769.1273215169530886, -118.7146871989600072, 317.4527132478988847 ) ) ;
#38011=CARTESIAN_POINT ( 'NONE',  ( 792.1044303154645831, -324.4527844766013231, 317.8323909638837677 ) ) ;
#38015=CARTESIAN_POINT ( 'NONE',  ( 778.1981804954714335, -106.2709662947838467, 314.8072714833589885 ) ) ;
#38018=CARTESIAN_POINT ( 'NONE',  ( 771.2368401574024119, -373.4419599262319593, 374.2805881961240857 ) ) ;
#38020=CARTESIAN_POINT ( 'NONE',  ( 785.3687786644884454, -299.3618753856922581, 315.3201227861279676 ) ) ;
#38024=CARTESIAN_POINT ( 'NONE',  ( 759.7806653035534055, -366.9982390220556567, 324.8639956371180801 ) ) ;
#38031=CARTESIAN_POINT ( 'NONE',  ( 804.4286716492782716, -113.3618753856929260, 345.3141322388244703 ) ) ;
#38032=CARTESIAN_POINT ( 'NONE',  ( 804.1105419155481968, -411.8272453906067199, 347.6308680596136469 ) ) ;
#38035=CARTESIAN_POINT ( 'NONE',  ( 744.9990715423526808, -354.3510508353228943, 341.2370466360926002 ) ) ;
#38036=CARTESIAN_POINT ( 'NONE',  ( 745.1769319972822814, -113.8055962898691149, 346.2694204179732083 ) ) ;
#38041=CARTESIAN_POINT ( 'NONE',  ( 747.6481478633932056, -13.09997266333522248, 353.4146539503763620 ) ) ;
#38042=DIRECTION ( 'NONE',  ( 0.000000000000000000, 0.000000000000000000, 1.000000000000000000 ) ) ;
#38047=CARTESIAN_POINT ( 'NONE',  ( 775.8780910478218402, -345.2817908451523863, 364.9511171171680530 ) ) ;
#38049=CARTESIAN_POINT ( 'NONE',  ( 811.3240766477731540, -292.3726999360616219, 355.6651683502462902 ) ) ;
#38052=CARTESIAN_POINT ( 'NONE',  ( 810.4231160770870019, -120.5545181178803205, 321.9338519418446936 ) ) ;
#38058=CARTESIAN_POINT ( 'NONE',  ( 759.9864689768902508, -194.0891481129654039, 354.9819416627836404 ) ) ;
#38059=VERTEX_POINT ( 'NONE', #12943 ) ;
#38060=CARTESIAN_POINT ( 'NONE',  ( 757.7880784355613741, -426.0090635724247932, 312.4576283171834916 ) ) ;
#38063=CARTESIAN_POINT ( 'NONE',  ( 776.9254006560222479, -44.19088175424421649, 314.8983024940802125 ) ) ;
#38066=CARTESIAN_POINT ( 'NONE',  ( 805.0264073115434940, -438.3510508353226669, 339.4763451958999099 ) ) ;
#38070=CARTESIAN_POINT ( 'NONE',  ( 768.8385539511368734, -263.2601417444141134, 306.4236121716840557 ) ) ;
#38071=CARTESIAN_POINT ( 'NONE',  ( 791.9812246680005501, -116.6346026584201780, 361.9419747391813189 ) ) ;
#38073=AXIS2_PLACEMENT_3D ( 'NONE', #6088, #34948, #41434 ) ;
#38075=CARTESIAN_POINT ( 'NONE',  ( 800.2193346964447755, -282.9982390220558841, 355.1360043628815788 ) ) ;
#38086=CARTESIAN_POINT ( 'NONE',  ( 815.2698199232962679, -352.8164208402375266, 342.5225473063383674 ) ) ;
#38087=CARTESIAN_POINT ( 'NONE',  ( 761.9338519418445230, -254.5328690171413655, 370.4231160770881957 ) ) ;
#38092=CARTESIAN_POINT ( 'NONE',  ( 797.6776695296629214, -235.5436935675107293, 357.6776695296636603 ) ) ;
#38093=ORIENTED_EDGE ( 'NONE', *, *, #5775, .F. ) ;
#38094=CARTESIAN_POINT ( 'NONE',  ( 746.8695393053150156, -341.9073299311465917, 327.6429770376306010 ) ) ;
#38097=CARTESIAN_POINT ( 'NONE',  ( 770.7832876896738981, 16.45630643248850333, 316.4833103687052471 ) ) ;
#38098=CARTESIAN_POINT ( 'NONE',  ( 799.9999999999993179, -512.9681489794448908, 309.9999999999998863 ) ) ;
#38099=CARTESIAN_POINT ( 'NONE',  ( 802.5472867521000353, -244.3726999360617924, 350.8726784830461156 ) ) ;
#38100=CARTESIAN_POINT ( 'NONE',  ( 781.7834795799800531, -130.8164208402383224, 315.0636971347436202 ) ) ;
#38103=CARTESIAN_POINT ( 'NONE',  ( 754.9735926884551418, -282.3510508353230080, 340.5236548041000333 ) ) ;
#38104=AXIS2_PLACEMENT_3D ( 'NONE', #28239, #7945, #7255 ) ;
#38107=CARTESIAN_POINT ( 'NONE',  ( 799.9636004259356241, 1.081845518482914104, 311.2241431872006956 ) ) ;
#38110=CARTESIAN_POINT ( 'NONE',  ( 801.1904061080336987, -68.08914811296575920, 368.3070685750235498 ) ) ;
#38111=CARTESIAN_POINT ( 'NONE',  ( 759.0252816721024374, -168.9982390220563673, 368.0189434323527280 ) ) ;
#38117=CARTESIAN_POINT ( 'NONE',  ( 746.4236121716829757, -399.8272453906067767, 328.8385539511384650 ) ) ;
#38120=CARTESIAN_POINT ( 'NONE',  ( 792.2312462859673587, -395.9073299311465348, 307.2067596250082602 ) ) ;
#38121=CARTESIAN_POINT ( 'NONE',  ( 772.4837098697145166, -23.36187538569319244, 374.5518280994205611 ) ) ;
#38124=CARTESIAN_POINT ( 'NONE',  ( 763.2154366446407039, -21.62377810805121570, 321.4292242960311228 ) ) ;
#38128=CARTESIAN_POINT ( 'NONE',  ( 800.1688906516307043, -178.1692326535052473, 369.0717654672308186 ) ) ;
#38130=ORIENTED_EDGE ( 'NONE', *, *, #7470, .T. ) ;
#38133=CARTESIAN_POINT ( 'NONE',  ( 768.0187753319979720, -176.6346026584199933, 318.0580252608186242 ) ) ;
#38135=CARTESIAN_POINT ( 'NONE',  ( 774.6858677611749044, -297.7255117493286889, 315.5713283507209894 ) ) ;
#38138=CARTESIAN_POINT ( 'NONE',  ( 787.6308680596127942, -11.26014174441488258, 364.1105419155492768 ) ) ;
#38141=CARTESIAN_POINT ( 'NONE',  ( 751.9810565676468741, -266.0891481129651197, 360.9747183278973921 ) ) ;
#38142=CARTESIAN_POINT ( 'NONE',  ( 754.7162404726377645, -326.7363362996979390, 339.4709603349214717 ) ) ;
#38143=CARTESIAN_POINT ( 'NONE',  ( 787.6308680596127942, -419.2601417444136587, 364.1105419155492768 ) ) ;
#38149=CARTESIAN_POINT ( 'NONE',  ( 763.2154366446407039, -333.6237781080502600, 321.4292242960311228 ) ) ;
#38152=CARTESIAN_POINT ( 'NONE',  ( 757.0176451133909268, -109.0999726633349241, 349.9200121543848354 ) ) ;
#38153=CARTESIAN_POINT ( 'NONE',  ( 771.2633955100217236, -23.90732993114773919, 363.4237431249939618 ) ) ;
#38154=ORIENTED_EDGE ( 'NONE', *, *, #24465, .T. ) ;
#38158=CARTESIAN_POINT ( 'NONE',  ( 768.9521613784389729, -225.8272453906072599, 373.2346286133773106 ) ) ;
#38159=CARTESIAN_POINT ( 'NONE',  ( 802.7791456095903868, -196.7146871989598083, 329.0155153010375102 ) ) ;
#38167=CARTESIAN_POINT ( 'NONE',  ( 746.4236121716829757, -351.8272453906068336, 328.8385539511384650 ) ) ;
#38169=CARTESIAN_POINT ( 'NONE',  ( 763.0537975583475827, -288.4527844766014937, 371.0346526505627480 ) ) ;
#38173=CARTESIAN_POINT ( 'NONE',  ( 788.7366044899766848, -395.9073299311465348, 316.5762568750059813 ) ) ;
#38174=CARTESIAN_POINT ( 'NONE',  ( 805.2837595273609850, -146.7363362996984506, 340.5290396650784714 ) ) ;
#38177=CARTESIAN_POINT ( 'NONE',  ( 744.8212110874229666, -66.89650538077835051, 336.2046728542121627 ) ) ;
#38178=CARTESIAN_POINT ( 'NONE',  ( 791.9812246680005501, -380.6346026584192828, 361.9419747391813189 ) ) ;
#38182=CARTESIAN_POINT ( 'NONE',  ( 767.8955696845333705, -432.4527844766008684, 362.1676090361162323 ) ) ;
#38187=CARTESIAN_POINT ( 'NONE',  ( 804.4286716492782716, -185.3618753856926844, 345.3141322388244703 ) ) ;
#38188=CARTESIAN_POINT ( 'NONE',  ( 771.2633955100217236, -191.9073299311471885, 363.4237431249939618 ) ) ;
#38192=CARTESIAN_POINT ( 'NONE',  ( 795.1360043628807261, -404.0891481129646081, 360.2193346964456282 ) ) ;
#38195=CARTESIAN_POINT ( 'NONE',  ( 813.1304606946831655, -137.9073299311473875, 352.3570229623691716 ) ) ;
#38201=CARTESIAN_POINT ( 'NONE',  ( 755.0488828828309806, -209.8055962898687881, 344.1219089521771934 ) ) ;
#38210=CARTESIAN_POINT ( 'NONE',  ( 747.6481478633932056, -133.0999726633348246, 353.4146539503763620 ) ) ;
#38219=CARTESIAN_POINT ( 'NONE',  ( 814.2805881961230625, -385.6454272087888171, 331.2368401574024119 ) ) ;
#38220=DIRECTION ( 'NONE',  ( -1.000000000000000000, 0.000000000000000000, -0.000000000000000000 ) ) ;
#38226=CARTESIAN_POINT ( 'NONE',  ( 786.2694204179717872, -213.2817908451527842, 305.1769319972829067 ) ) ;
#38228=CARTESIAN_POINT ( 'NONE',  ( 800.9747183278959710, -180.9982390220563389, 311.9810565676471583 ) ) ;
#38231=CARTESIAN_POINT ( 'NONE',  ( 803.6646147819161570, -281.9073299311468759, 348.8264449731210561 ) ) ;
#38232=CARTESIAN_POINT ( 'NONE',  ( 754.7162404726377645, -62.73633629969871350, 339.4709603349214717 ) ) ;
#38238=CARTESIAN_POINT ( 'NONE',  ( 795.9930595647434757, -123.0783235625963385, 320.7433823573372820 ) ) ;
#38239=CARTESIAN_POINT ( 'NONE',  ( 804.4286716492782716, -329.3618753856922581, 345.3141322388244703 ) ) ;
#38243=CARTESIAN_POINT ( 'NONE',  ( 803.6646147819161570, -89.90732993114750116, 348.8264449731210561 ) ) ;
#38246=CARTESIAN_POINT ( 'NONE',  ( 754.0944755984390895, -423.6237781080499190, 364.1009440267246760 ) ) ;
#38248=CARTESIAN_POINT ( 'NONE',  ( 762.1405469898971887, -289.5436935675103882, 357.8594530101015607 ) ) ;
#38252=CARTESIAN_POINT ( 'NONE',  ( 788.7366044899766848, -419.9073299311465348, 316.5762568750059813 ) ) ;
#38259=CARTESIAN_POINT ( 'NONE',  ( 800.0135310231082713, -134.0891481129655745, 325.0180583372163028 ) ) ;
#38260=CARTESIAN_POINT ( 'NONE',  ( 790.9844846989617508, -454.3726999360611103, 317.2208543904092721 ) ) ;
#38261=CARTESIAN_POINT ( 'NONE',  ( 799.4546378042377910, -105.0783235625964096, 356.1575198192848006 ) ) ;
#38264=CARTESIAN_POINT ( 'NONE',  ( 771.2368401574024119, -373.4419599262319593, 374.2805881961240857 ) ) ;
#38270=CARTESIAN_POINT ( 'NONE',  ( 754.3581564841646241, -41.46360902697149697, 316.1443688327762516 ) ) ;
#38279=CARTESIAN_POINT ( 'NONE',  ( 773.4516893846965786, -331.6454272087888171, 315.8398074228977066 ) ) ;
#38280=CARTESIAN_POINT ( 'NONE',  ( 797.8822607201568644, -318.5545181178796952, 370.1134526219340160 ) ) ;
#38283=CARTESIAN_POINT ( 'NONE',  ( 786.2694204179717872, -117.2817908451530684, 305.1769319972829067 ) ) ;
#38285=CARTESIAN_POINT ( 'NONE',  ( 799.9999999999993179, 205.0000000000000568, 319.9999999999999432 ) ) ;
#38287=CARTESIAN_POINT ( 'NONE',  ( 804.4286716492782716, -185.3618753856926844, 345.3141322388244703 ) ) ;
#38289=CARTESIAN_POINT ( 'NONE',  ( 811.3240766477731540, -436.3726999360612240, 355.6651683502462902 ) ) ;
#38292=CARTESIAN_POINT ( 'NONE',  ( 759.0159684113467620, -64.91815448151686496, 325.8855110935213020 ) ) ;
#38296=CARTESIAN_POINT ( 'NONE',  ( 759.8311093483677041, 1.830767346494167391, 310.9282345327691814 ) ) ;
#38300=CARTESIAN_POINT ( 'NONE',  ( 814.8230680027162407, -269.8055962898686175, 333.7305795820267917 ) ) ;
#38301=CARTESIAN_POINT ( 'NONE',  ( 795.1360043628808398, -116.0891481129656313, 360.2193346964456282 ) ) ;
#38303=CARTESIAN_POINT ( 'NONE',  ( 762.3223304703356007, -295.5436935675105588, 322.3223304703362828 ) ) ;
#38305=CARTESIAN_POINT ( 'NONE',  ( 791.4252870525732533, -448.2207382684695176, 369.1877814561917717 ) ) ;
#38310=CARTESIAN_POINT ( 'NONE',  ( 802.1676090361156639, -14.63460265842049424, 327.8955696845344505 ) ) ;
#38312=CARTESIAN_POINT ( 'NONE',  ( 754.9967657858570647, -361.5436935675103882, 365.0032342141425943 ) ) ;
#38313=CARTESIAN_POINT ( 'NONE',  ( 752.4576283171824116, -261.0783235625959264, 317.7880784355627952 ) ) ;
#38319=CARTESIAN_POINT ( 'NONE',  ( 755.5713283507202505, -245.3618753856925139, 334.6858677611754729 ) ) ;
#38321=CARTESIAN_POINT ( 'NONE',  ( 777.4774526936600978, -370.2709662947831362, 304.7301800767027657 ) ) ;
#38325=FACE_OUTER_BOUND ( 'NONE', #22895, .T. ) ;
#38326=CARTESIAN_POINT ( 'NONE',  ( 805.2837595273609850, -218.7363362996982232, 340.5290396650784714 ) ) ;
#38327=CARTESIAN_POINT ( 'NONE',  ( 771.1735550268778070, -129.1800572038746111, 316.3353852180827630 ) ) ;
#38331=CARTESIAN_POINT ( 'NONE',  ( 798.7617431975189675, -291.6237781080503169, 323.0428371773161871 ) ) ;
#38334=CARTESIAN_POINT ( 'NONE',  ( 771.3260364891663130, 4.354572791210176597, 306.0683387631859773 ) ) ;
#38336=CARTESIAN_POINT ( 'NONE',  ( 801.1904061080336987, -164.0891481129655176, 368.3070685750235498 ) ) ;
#38337=CARTESIAN_POINT ( 'NONE',  ( 800.2193346964447755, -90.99823902205663728, 355.1360043628815788 ) ) ;
#38342=CARTESIAN_POINT ( 'NONE',  ( 814.2805881961230625, -433.6454272087884760, 331.2368401574024119 ) ) ;
#38345=CARTESIAN_POINT ( 'NONE',  ( 746.8695393053150156, -389.9073299311465348, 327.6429770376306010 ) ) ;
#38346=CARTESIAN_POINT ( 'NONE',  ( 767.7687537140311633, -47.90732993114767169, 372.7932403749916830 ) ) ;
#38348=CARTESIAN_POINT ( 'NONE',  ( 755.8398074228967971, -19.44195992623303937, 333.4516893846970333 ) ) ;
#38351=CARTESIAN_POINT ( 'NONE',  ( 748.3538107759620743, -184.7146871989598083, 355.8262568251490165 ) ) ;
#38352=CARTESIAN_POINT ( 'NONE',  ( 755.3201227861273992, -27.72551174932954510, 345.3687786644892981 ) ) ;
#38353=CARTESIAN_POINT ( 'NONE',  ( 761.9338519418445230, -182.5328690171416497, 370.4231160770881957 ) ) ;
#38357=CARTESIAN_POINT ( 'NONE',  ( 762.1405469898971887, -169.5436935675108430, 357.8594530101015607 ) ) ;
#38359=CARTESIAN_POINT ( 'NONE',  ( 756.5762568750052424, -315.1800572038740711, 348.7366044899774238 ) ) ;
#38362=CARTESIAN_POINT ( 'NONE',  ( 769.1273215169530886, -22.71468719896029853, 317.4527132478988847 ) ) ;
#38364=CARTESIAN_POINT ( 'NONE',  ( 746.8695393053151292, -269.9073299311469327, 327.6429770376306578 ) ) ;
#38365=CARTESIAN_POINT ( 'NONE',  ( 775.8780910478218402, -345.2817908451523863, 364.9511171171680530 ) ) ;
#38366=CARTESIAN_POINT ( 'NONE',  ( 800.7704444035546203, -436.1692326535044231, 326.0291762391768771 ) ) ;
#38371=CARTESIAN_POINT ( 'NONE',  ( 799.4546378042377910, -321.0783235625956991, 356.1575198192848006 ) ) ;
#38373=CARTESIAN_POINT ( 'NONE',  ( 772.4468031744293057, -105.8272453906076578, 363.8651313633793620 ) ) ;
#38374=CARTESIAN_POINT ( 'NONE',  ( 802.1676090361156639, -14.63460265842049424, 327.8955696845344505 ) ) ;
#38378=CARTESIAN_POINT ( 'NONE',  ( 775.8780910478218402, -225.2817908451527273, 364.9511171171680530 ) ) ;
#38379=CARTESIAN_POINT ( 'NONE',  ( 754.3581564841646241, -233.4636090269708575, 316.1443688327762516 ) ) ;
#38380=CARTESIAN_POINT ( 'NONE',  ( 805.1016975059191054, -174.8965053807779952, 343.0745993439771837 ) ) ;
#38384=CARTESIAN_POINT ( 'NONE',  ( 754.9967657858570647, -1.543693567511449150, 365.0032342141425374 ) ) ;
#38385=CARTESIAN_POINT ( 'NONE',  ( 808.0106897970731552, -452.9681489794447771, 338.3625385368115985 ) ) ;
#38388=CARTESIAN_POINT ( 'NONE',  ( 797.8822607201568644, -366.5545181178795815, 370.1134526219340160 ) ) ;
#38390=CARTESIAN_POINT ( 'NONE',  ( 782.4968714119720516, -298.8164208402377540, 305.0891759886411023 ) ) ;
#38394=CARTESIAN_POINT ( 'NONE',  ( 781.8018195045266339, -406.2709662947829088, 365.1927285166406705 ) ) ;
#38395=CARTESIAN_POINT ( 'NONE',  ( 784.1219089521767955, -165.2817908451529547, 315.0488828828318333 ) ) ;
#38398=CARTESIAN_POINT ( 'NONE',  ( 747.3154664389472828, -67.98741447168742980, 326.4474001241230781 ) ) ;
#38399=CARTESIAN_POINT ( 'NONE',  ( 755.5713283507202505, -389.3618753856919739, 334.6858677611754729 ) ) ;
#38400=CARTESIAN_POINT ( 'NONE',  ( 792.2312462859673587, 12.09267006885214180, 307.2067596250082602 ) ) ;
#38402=CARTESIAN_POINT ( 'NONE',  ( 748.3538107759620743, -136.7146871989600072, 355.8262568251490165 ) ) ;
#38403=CARTESIAN_POINT ( 'NONE',  ( 788.7366044899766848, -419.9073299311465348, 316.5762568750059813 ) ) ;
#38407=CARTESIAN_POINT ( 'NONE',  ( 778.2165204200184689, -238.8164208402379813, 364.9363028652563230 ) ) ;
#38408=CARTESIAN_POINT ( 'NONE',  ( 803.6646147819162707, -185.9073299311472169, 348.8264449731211130 ) ) ;
#38413=CARTESIAN_POINT ( 'NONE',  ( 758.0580252608178853, -390.4527844766011526, 328.0187753319985404 ) ) ;
#38414=ORIENTED_EDGE ( 'NONE', *, *, #3233, .T. ) ;
#38416=CARTESIAN_POINT ( 'NONE',  ( 800.9747183278959710, -156.9982390220564241, 311.9810565676471583 ) ) ;
#38419=VERTEX_POINT ( 'NONE', #13861 ) ;
#38422=CARTESIAN_POINT ( 'NONE',  ( 799.4546378042377910, -225.0783235625959833, 356.1575198192848006 ) ) ;
#38431=CARTESIAN_POINT ( 'NONE',  ( 764.1737431748507561, -130.3726999360621619, 371.6461892240376415 ) ) ;
#38438=CARTESIAN_POINT ( 'NONE',  ( 778.7629533639073998, -392.7363362996977116, 375.0009284576466371 ) ) ;
#38445=CARTESIAN_POINT ( 'NONE',  ( 781.2370466360911223, -236.7363362996981380, 304.9990715423533629 ) ) ;
#38447=CARTESIAN_POINT ( 'NONE',  ( 815.2698199232961542, -184.8164208402380950, 342.5225473063383106 ) ) ;
#38449=DIRECTION ( 'NONE',  ( 0.000000000000000000, 0.000000000000000000, 1.000000000000000000 ) ) ;
#38450=CARTESIAN_POINT ( 'NONE',  ( 785.3687786644884454, -299.3618753856922581, 315.3201227861279676 ) ) ;
#38451=CARTESIAN_POINT ( 'NONE',  ( 796.9571628226829034, -71.46360902697141171, 321.2382568024804641 ) ) ;
#38455=CARTESIAN_POINT ( 'NONE',  ( 756.1348686366196716, -137.2601417444144829, 347.5531968255698416 ) ) ;
#38456=CARTESIAN_POINT ( 'NONE',  ( 759.9864689768902508, -314.0891481129650629, 354.9819416627836404 ) ) ;
#38459=CARTESIAN_POINT ( 'NONE',  ( 785.3141322388236176, -93.72551174932934259, 364.4286716492789537 ) ) ;
#38462=CARTESIAN_POINT ( 'NONE',  ( 795.6651683502461765, -418.7146871989590409, 371.3240766477733814 ) ) ;
#38464=CARTESIAN_POINT ( 'NONE',  ( 803.6646147819161570, -281.9073299311468759, 348.8264449731210561 ) ) ;
#38467=CARTESIAN_POINT ( 'NONE',  ( 774.6312213355099630, -407.3618753856920307, 364.6798772138717482 ) ) ;
#38474=CARTESIAN_POINT ( 'NONE',  ( 785.3141322388236176, -117.7255117493292715, 364.4286716492789537 ) ) ;
#38475=CARTESIAN_POINT ( 'NONE',  ( 793.9708237608222134, -430.9181544815157849, 319.2295555964448681 ) ) ;
#38476=CARTESIAN_POINT ( 'NONE',  ( 795.9930595647434757, -123.0783235625963385, 320.7433823573372820 ) ) ;
#38477=DIRECTION ( 'NONE',  ( -1.000000000000000000, -0.000000000000000000, 0.000000000000000000 ) ) ;
#38479=CARTESIAN_POINT ( 'NONE',  ( 803.8556311672234642, -369.6237781080500895, 365.6418435158340117 ) ) ;
#38484=CARTESIAN_POINT ( 'NONE',  ( 750.9282345327678740, -40.91815448151695023, 319.8311093483690115 ) ) ;
#38492=CARTESIAN_POINT ( 'NONE',  ( 766.9102291470427417, -378.5545181178795247, 318.6633372737382501 ) ) ;
#38493=CARTESIAN_POINT ( 'NONE',  ( 766.4474001241216001, -355.0999726633341993, 307.3154664389482491 ) ) ;
#38496=CARTESIAN_POINT ( 'NONE',  ( 748.6759233522253680, -136.3726999360621051, 324.3348316497537098 ) ) ;
#38500=CARTESIAN_POINT ( 'NONE',  ( 785.3687786644884454, -179.3618753856927128, 315.3201227861279676 ) ) ;
#38503=CARTESIAN_POINT ( 'NONE',  ( 815.3608509340175488, -410.7363362996976548, 341.2497674668889545 ) ) ;
#38509=CARTESIAN_POINT ( 'NONE',  ( 815.0009284576459549, -6.351050835323991173, 338.7629533639073429 ) ) ;
#38514=CARTESIAN_POINT ( 'NONE',  ( 812.6845335610512393, -295.9874144716866908, 353.5525998758768651 ) ) ;
#38515=CARTESIAN_POINT ( 'NONE',  ( 801.9419747391806368, -114.4527844766020053, 351.9812246680014027 ) ) ;
#38518=CARTESIAN_POINT ( 'NONE',  ( 756.3353852180819104, -293.9073299311468759, 331.1735550268788302 ) ) ;
#38522=CARTESIAN_POINT ( 'NONE',  ( 792.6574999928877787, -450.0087184351455107, 371.5677366416246059 ) ) ;
#38526=CARTESIAN_POINT ( 'NONE',  ( 805.1927285166397041, -40.81642084023859951, 341.8018195045277707 ) ) ;
#38528=CARTESIAN_POINT ( 'NONE',  ( 810.7187646348534145, -354.4527844766012095, 356.7737145352016341 ) ) ;
#38529=CARTESIAN_POINT ( 'NONE',  ( 744.9990715423526808, -258.3510508353231785, 341.2370466360926002 ) ) ;
#38530=CARTESIAN_POINT ( 'NONE',  ( 813.2346286133761168, -77.26014174441466764, 328.9521613784389160 ) ) ;
#38537=CARTESIAN_POINT ( 'NONE',  ( 781.8018195045266339, -238.2709662947833920, 365.1927285166406705 ) ) ;
#38538=CARTESIAN_POINT ( 'NONE',  ( 787.5162901302840055, -395.3618753856918602, 305.4481719005792684 ) ) ;
#38544=CARTESIAN_POINT ( 'NONE',  ( 758.4439275373578084, -252.5545181178799226, 353.2243759319684386 ) ) ;
#38545=CARTESIAN_POINT ( 'NONE',  ( 797.6776695296629214, -115.5436935675110988, 357.6776695296636603 ) ) ;
#38549=CARTESIAN_POINT ( 'NONE',  ( 804.1601925771018387, -295.4419599262320730, 346.5483106153029098 ) ) ;
#38551=CARTESIAN_POINT ( 'NONE',  ( 745.5313806188320314, -15.28179084515340058, 333.7943932421247268 ) ) ;
#38553=CARTESIAN_POINT ( 'NONE',  ( 804.7487373415286811, -163.5436935675109567, 364.7487373415288516 ) ) ;
#38554=CARTESIAN_POINT ( 'NONE',  ( 762.3223304703356007, -79.54369356751119824, 322.3223304703362828 ) ) ;
#38557=EDGE_CURVE ( 'NONE', #16040, #13477, #32994, .T. ) ;
#38560=CARTESIAN_POINT ( 'NONE',  ( 766.9102291470427417, 5.445481882119263872, 318.6633372737382501 ) ) ;
#38563=CARTESIAN_POINT ( 'NONE',  ( 764.0069404352550464, -375.0783235625955285, 359.2566176426627180 ) ) ;
#38564=CARTESIAN_POINT ( 'NONE',  ( 749.2812353651451076, -54.45278447660219001, 323.2262854647983090 ) ) ;
#38568=CARTESIAN_POINT ( 'NONE',  ( 760.5453621957607311, -21.07832356259667250, 323.8424801807151425 ) ) ;
#38571=CARTESIAN_POINT ( 'NONE',  ( 766.5853460496234675, -205.9874144716870035, 372.3518521366060554 ) ) ;
#38572=CARTESIAN_POINT ( 'NONE',  ( 757.8323909638828582, -26.63460265842046226, 352.1044303154654358 ) ) ;
#38576=CARTESIAN_POINT ( 'NONE',  ( 797.6776695296629214, -187.5436935675108430, 357.6776695296636603 ) ) ;
#38579=CARTESIAN_POINT ( 'NONE',  ( 767.8955696845334842, -336.4527844766012663, 362.1676090361161755 ) ) ;
#38582=CARTESIAN_POINT ( 'NONE',  ( 758.6633372737375112, -44.53286901714205470, 326.9102291470432533 ) ) ;
#38584=CARTESIAN_POINT ( 'NONE',  ( 792.2312462859673587, -251.9073299311470748, 307.2067596250082602 ) ) ;
#38585=CARTESIAN_POINT ( 'NONE',  ( 755.5913626894240451, -325.6454272087888739, 346.6156483768012890 ) ) ;
#38586=CARTESIAN_POINT ( 'NONE',  ( 802.7791456095903868, -436.7146871989589272, 329.0155153010375102 ) ) ;
#38592=CARTESIAN_POINT ( 'NONE',  ( 787.5162901302840055, -299.3618753856922581, 305.4481719005792684 ) ) ;
#38593=CARTESIAN_POINT ( 'NONE',  ( 754.8983024940795303, -330.8965053807774552, 336.9254006560228163 ) ) ;
#38595=CARTESIAN_POINT ( 'NONE',  ( 793.9708237608222134, -118.9181544815167229, 319.2295555964448681 ) ) ;
#38596=CARTESIAN_POINT ( 'NONE',  ( 762.1405469898971887, -1.543693567511449150, 357.8594530101015607 ) ) ;
#38600=CARTESIAN_POINT ( 'NONE',  ( 772.4468031744293057, -225.8272453906072599, 363.8651313633793620 ) ) ;
#38601=CARTESIAN_POINT ( 'NONE',  ( 802.2119215644370342, -246.0090635724253900, 367.5423716828165084 ) ) ;
#38602=CARTESIAN_POINT ( 'NONE',  ( 780.5290396650775619, -180.3510508353234343, 365.2837595273619513 ) ) ;
#38607=CARTESIAN_POINT ( 'NONE',  ( 744.7301800767019131, -28.81642084023863148, 337.4774526936615757 ) ) ;
#38608=CARTESIAN_POINT ( 'NONE',  ( 792.3570229623688874, -69.18005720387488111, 373.1304606946836202 ) ) ;
#38612=CARTESIAN_POINT ( 'NONE',  ( 749.5768839229115201, -348.5545181178796383, 358.0661480581553064 ) ) ;
#38614=CARTESIAN_POINT ( 'NONE',  ( 772.4837098697144029, -311.3618753856922581, 374.5518280994205611 ) ) ;
#38618=CARTESIAN_POINT ( 'NONE',  ( 791.9812246680005501, -380.6346026584192828, 361.9419747391813189 ) ) ;
#38620=CARTESIAN_POINT ( 'NONE',  ( 776.9254006560222479, -164.1908817542438612, 314.8983024940802125 ) ) ;
#38623=CARTESIAN_POINT ( 'NONE',  ( 786.2056067578752163, -59.80559628986927834, 374.4686193811670023 ) ) ;
#38624=CARTESIAN_POINT ( 'NONE',  ( 759.7806653035535192, -414.9982390220555430, 324.8639956371181370 ) ) ;
#38626=CARTESIAN_POINT ( 'NONE',  ( 811.0346526505617248, 9.365397341579424051, 323.0537975583478101 ) ) ;
#38628=CARTESIAN_POINT ( 'NONE',  ( 791.1614460488616487, -155.2601417444144261, 373.5763878283158874 ) ) ;
#38634=CARTESIAN_POINT ( 'NONE',  ( 781.8018195045266339, -238.2709662947833920, 365.1927285166406705 ) ) ;
#38635=CARTESIAN_POINT ( 'NONE',  ( 764.8639956371174549, -224.0891481129652902, 319.7806653035542581 ) ) ;
#38638=CARTESIAN_POINT ( 'NONE',  ( 807.5423716828161105, -441.0783235625953580, 362.2119215644372048 ) ) ;
#38641=CARTESIAN_POINT ( 'NONE',  ( 778.1981804954714335, -442.2709662947826814, 314.8072714833589885 ) ) ;
#38646=CARTESIAN_POINT ( 'NONE',  ( 808.0189434323515343, -158.0891481129655176, 319.0252816721025511 ) ) ;
#38652=CARTESIAN_POINT ( 'NONE',  ( 796.7845633553578182, -225.6237781080506011, 358.5707757039688204 ) ) ;
#38663=CARTESIAN_POINT ( 'NONE',  ( 768.9521613784389729, -129.8272453906075725, 373.2346286133773106 ) ) ;
#38670=CARTESIAN_POINT ( 'NONE',  ( 773.7305795820266212, -393.2817908451522726, 374.8230680027170365 ) ) ;
#38678=CARTESIAN_POINT ( 'NONE',  ( 814.4686193811664907, -243.2817908451526705, 346.2056067578752732 ) ) ;
#38680=CARTESIAN_POINT ( 'NONE',  ( 749.2812353651451076, -198.4527844766017495, 323.2262854647983090 ) ) ;
#38682=DIRECTION ( 'NONE',  ( 0.000000000000000000, 0.000000000000000000, -1.000000000000000000 ) ) ;
#38684=CARTESIAN_POINT ( 'NONE',  ( 804.4286716492782716, -305.3618753856922581, 345.3141322388244703 ) ) ;
#38686=CARTESIAN_POINT ( 'NONE',  ( 780.5236548040995785, -92.73633629969860692, 314.9735926884559944 ) ) ;
#38690=CARTESIAN_POINT ( 'NONE',  ( 793.2243759319678702, -122.5328690171417918, 318.4439275373583200 ) ) ;
#38691=CARTESIAN_POINT ( 'NONE',  ( 804.9363028652555840, -328.2709662947831362, 338.2165204200192079 ) ) ;
#38692=ORIENTED_EDGE ( 'NONE', *, *, #15287, .F. ) ;
#38695=CARTESIAN_POINT ( 'NONE',  ( 781.8018195045266339, -94.27096629478386092, 365.1927285166406705 ) ) ;
#38698=CARTESIAN_POINT ( 'NONE',  ( 745.1769319972822814, -401.8055962898681059, 346.2694204179732083 ) ) ;
#38700=CARTESIAN_POINT ( 'NONE',  ( 791.9812246680005501, -284.6346026584196807, 361.9419747391813189 ) ) ;
#38704=CARTESIAN_POINT ( 'NONE',  ( 762.3223304703356007, -391.5436935675101608, 322.3223304703362828 ) ) ;
#38710=CARTESIAN_POINT ( 'NONE',  ( 756.5762568750052424, -123.1800572038747106, 348.7366044899774238 ) ) ;
#38711=CARTESIAN_POINT ( 'NONE',  ( 754.7162404726377645, -446.7363362996975980, 339.4709603349214717 ) ) ;
#38712=CARTESIAN_POINT ( 'NONE',  ( 784.0799538623451781, -131.8055962898690439, 364.6971507214555572 ) ) ;
#38715=CARTESIAN_POINT ( 'NONE',  ( 813.9316612368132837, -391.4419599262317888, 348.6739635108323228 ) ) ;
#38721=CARTESIAN_POINT ( 'NONE',  ( 814.2805881961230625, -49.64542720878965554, 331.2368401574024119 ) ) ;
#38729=CARTESIAN_POINT ( 'NONE',  ( 796.1575198192839480, -366.0090635724250774, 359.4546378042384163 ) ) ;
#38731=CARTESIAN_POINT ( 'NONE',  ( 745.1792804349281596, -326.1908817542433781, 343.7566961878542884 ) ) ;
#38738=CARTESIAN_POINT ( 'NONE',  ( 815.3608509340175488, -146.7363362996984506, 341.2497674668889545 ) ) ;
#38744=CARTESIAN_POINT ( 'NONE',  ( 800.0135310231082713, -182.0891481129654323, 325.0180583372163028 ) ) ;
#38745=DIRECTION ( 'NONE',  ( 0.000000000000000000, 1.000000000000000000, 0.000000000000000000 ) ) ;
#38747=CARTESIAN_POINT ( 'NONE',  ( 745.7194118038753459, -445.6454272087883055, 348.7631598425976449 ) ) ;
#38753=CARTESIAN_POINT ( 'NONE',  ( 786.2056067578752163, -11.80559628986942577, 374.4686193811670023 ) ) ;
#38755=VECTOR ( 'NONE', #3505, 1000.000000000000000 ) ;
#38758=CARTESIAN_POINT ( 'NONE',  ( 786.2056067578752163, -299.8055962898685038, 374.4686193811670023 ) ) ;
#38759=CARTESIAN_POINT ( 'NONE',  ( 757.8323909638828582, -122.6346026584201496, 352.1044303154654358 ) ) ;
#38761=CARTESIAN_POINT ( 'NONE',  ( 767.8955696845333705, -312.4527844766012663, 362.1676090361162323 ) ) ;
#38763=CARTESIAN_POINT ( 'NONE',  ( 793.3938497862117174, -453.0432664090020580, 372.3358127763067955 ) ) ;
#38769=CARTESIAN_POINT ( 'NONE',  ( 785.3687786644884454, -11.36187538569323863, 315.3201227861279676 ) ) ;
#38771=CARTESIAN_POINT ( 'NONE',  ( 772.4837098697145166, -359.3618753856921444, 374.5518280994205611 ) ) ;
#38772=CARTESIAN_POINT ( 'NONE',  ( 756.1443688327750579, -285.6237781080502600, 314.3581564841659315 ) ) ;
#38773=CARTESIAN_POINT ( 'NONE',  ( 754.0944755984390895, -63.62377810805107714, 364.1009440267246760 ) ) ;
#38776=DIRECTION ( 'NONE',  ( 0.000000000000000000, -1.000000000000000000, 0.000000000000000000 ) ) ;
#38778=CARTESIAN_POINT ( 'NONE',  ( 800.2193346964447755, -258.9982390220561115, 355.1360043628815788 ) ) ;
#38779=CARTESIAN_POINT ( 'NONE',  ( 772.5602148656447525, -393.7255117493283478, 305.7998596910095443 ) ) ;
#38784=DIRECTION ( 'NONE',  ( -0.000000000000000000, 1.000000000000000000, -0.000000000000000000 ) ) ;
#38786=AXIS2_PLACEMENT_3D ( 'NONE', #26866, #40975, #22277 ) ;
#38788=CARTESIAN_POINT ( 'NONE',  ( 757.4527132478984868, -256.3726999360617924, 329.1273215169538844 ) ) ;
#38790=CARTESIAN_POINT ( 'NONE',  ( 802.1676090361156639, -110.6346026584201638, 327.8955696845344505 ) ) ;
#38794=CARTESIAN_POINT ( 'NONE',  ( 787.6308680596127942, -275.2601417444140566, 364.1105419155492768 ) ) ;
#38796=CARTESIAN_POINT ( 'NONE',  ( 793.5525998758768083, -31.09997266333516919, 372.6845335610516941 ) ) ;
#38799=CARTESIAN_POINT ( 'NONE',  ( 810.7187646348534145, -162.4527844766018632, 356.7737145352016341 ) ) ;
#38800=CARTESIAN_POINT ( 'NONE',  ( 767.8955696845333705, -96.45278447660203369, 362.1676090361162323 ) ) ;
#38805=CARTESIAN_POINT ( 'NONE',  ( 810.4231160770870019, -456.5545181178792404, 321.9338519418446936 ) ) ;
#38808=CARTESIAN_POINT ( 'NONE',  ( 798.7617431975189675, -363.6237781080502032, 323.0428371773161871 ) ) ;
#38809=CARTESIAN_POINT ( 'NONE',  ( 801.1904061080338124, -44.08914811296585157, 368.3070685750236066 ) ) ;
#38812=CARTESIAN_POINT ( 'NONE',  ( 769.1273215169530886, -46.71468719896022748, 317.4527132478988847 ) ) ;
#38815=CARTESIAN_POINT ( 'NONE',  ( 778.7502325331095108, -216.3510508353233490, 304.6391490659818828 ) ) ;
#38816=CARTESIAN_POINT ( 'NONE',  ( 765.0180583372156207, -24.99823902205683268, 360.0135310231089534 ) ) ;
#38822=CARTESIAN_POINT ( 'NONE',  ( 767.8955696845333705, -192.4527844766016926, 362.1676090361162323 ) ) ;
#38826=CARTESIAN_POINT ( 'NONE',  ( 785.3141322388236176, -333.7255117493286320, 364.4286716492789537 ) ) ;
#38827=ADVANCED_FACE ( 'NONE', ( #37737 ), #20851, .F. ) ;
#38828=CARTESIAN_POINT ( 'NONE',  ( 759.2380499001254748, 21.41625977839825978, 318.3449445151863415 ) ) ;
#38829=VERTEX_POINT ( 'NONE', #31031 ) ;
#38830=CARTESIAN_POINT ( 'NONE',  ( 754.8983024940795303, -42.89650538077842157, 336.9254006560228163 ) ) ;
#38832=CARTESIAN_POINT ( 'NONE',  ( 751.9810565676468741, -242.0891481129652618, 360.9747183278973921 ) ) ;
#38833=CARTESIAN_POINT ( 'NONE',  ( 805.9055244015594326, -3.623778108051270319, 315.8990559732753240 ) ) ;
#38839=CARTESIAN_POINT ( 'NONE',  ( 772.5602148656447525, -297.7255117493286889, 305.7998596910095443 ) ) ;
#38840=EDGE_CURVE ( 'NONE', #9771, #38829, #17678, .T. ) ;
#38842=CARTESIAN_POINT ( 'NONE',  ( 787.6308680596127942, -323.2601417444138860, 364.1105419155492768 ) ) ;
#38845=CARTESIAN_POINT ( 'NONE',  ( 766.0291762391763086, -154.9181544815165523, 360.7704444035551319 ) ) ;
#38846=CARTESIAN_POINT ( 'NONE',  ( 756.3353852180819104, -5.907329931147798696, 331.1735550268788302 ) ) ;
#38850=CARTESIAN_POINT ( 'NONE',  ( 790.0220218866281812, -223.0999726633346256, 363.2186876482849129 ) ) ;
#38851=CARTESIAN_POINT ( 'NONE',  ( 749.5768839229115201, -252.5545181178799226, 358.0661480581553064 ) ) ;
#38852=CARTESIAN_POINT ( 'NONE',  ( 790.8726784830453198, -178.7146871989598083, 362.5472867521010585 ) ) ;
#38854=CARTESIAN_POINT ( 'NONE',  ( 803.6646147819161570, 6.092670068852159559, 348.8264449731210561 ) ) ;
#38858=CARTESIAN_POINT ( 'NONE',  ( 808.0189434323515343, -14.08914811296595460, 319.0252816721025511 ) ) ;
#38859=CARTESIAN_POINT ( 'NONE',  ( 810.7187646348534145, -66.45278447660216159, 356.7737145352016341 ) ) ;
#38863=CARTESIAN_POINT ( 'NONE',  ( 752.7379699480933368, -348.0090635724251342, 361.9858362298580232 ) ) ;
#38864=CARTESIAN_POINT ( 'NONE',  ( 759.0252816721024374, -336.9982390220558273, 368.0189434323527280 ) ) ;
#38868=CARTESIAN_POINT ( 'NONE',  ( 762.3223304703356007, -415.5436935675102177, 322.3223304703362828 ) ) ;
#38869=CARTESIAN_POINT ( 'NONE',  ( 804.1105419155481968, -195.8272453906074304, 347.6308680596136469 ) ) ;
#38872=CARTESIAN_POINT ( 'NONE',  ( 744.9990715423526808, -114.3510508353236617, 341.2370466360926002 ) ) ;
#38873=CARTESIAN_POINT ( 'NONE',  ( 771.2633955100217236, -407.9073299311465348, 363.4237431249939618 ) ) ;
#38875=CARTESIAN_POINT ( 'NONE',  ( 800.1688906516307043, -154.1692326535053894, 369.0717654672308186 ) ) ;
#38876=CARTESIAN_POINT ( 'NONE',  ( 805.1927285166397041, -448.8164208402371855, 341.8018195045277707 ) ) ;
#38881=CARTESIAN_POINT ( 'NONE',  ( 767.8955696845333705, -216.4527844766016926, 362.1676090361162323 ) ) ;
#38882=CARTESIAN_POINT ( 'NONE',  ( 755.3201227861273992, -219.7255117493289447, 345.3687786644892981 ) ) ;
#38884=CARTESIAN_POINT ( 'NONE',  ( 754.9967657858570647, -1.543693567511449150, 365.0032342141425374 ) ) ;
#38887=CARTESIAN_POINT ( 'NONE',  ( 768.0187753319979720, -416.6346026584192259, 318.0580252608186242 ) ) ;
#38892=CARTESIAN_POINT ( 'NONE',  ( 810.7187646348534145, -162.4527844766018632, 356.7737145352016341 ) ) ;
#38893=CARTESIAN_POINT ( 'NONE',  ( 758.6633372737375112, -380.5328690171409676, 326.9102291470432533 ) ) ;
#38895=CARTESIAN_POINT ( 'NONE',  ( 759.8311093483677041, -190.1692326535052189, 310.9282345327691814 ) ) ;
#38901=CARTESIAN_POINT ( 'NONE',  ( 761.2382568024794409, -231.6237781080504874, 356.9571628226838129 ) ) ;
#38908=ORIENTED_EDGE ( 'NONE', *, *, #6310, .F. ) ;
#38910=CARTESIAN_POINT ( 'NONE',  ( 815.3608509340175488, -146.7363362996984506, 341.2497674668889545 ) ) ;
#38918=CARTESIAN_POINT ( 'NONE',  ( 744.6391490659812007, -374.7363362996978253, 338.7502325331110455 ) ) ;
#38922=DIRECTION ( 'NONE',  ( 0.000000000000000000, 0.000000000000000000, 1.000000000000000000 ) ) ;
#38923=CARTESIAN_POINT ( 'NONE',  ( 803.6646147819161570, -17.90732993114776406, 348.8264449731210561 ) ) ;
#38926=CARTESIAN_POINT ( 'NONE',  ( 749.5768839229115201, -252.5545181178799226, 358.0661480581553064 ) ) ;
#38928=CARTESIAN_POINT ( 'NONE',  ( 748.9653473494363425, -218.6346026584197944, 356.9462024416521331 ) ) ;
#38931=CARTESIAN_POINT ( 'NONE',  ( 785.3141322388236176, -333.7255117493286320, 364.4286716492789537 ) ) ;
#38932=CARTESIAN_POINT ( 'NONE',  ( 796.1575198192839480, -102.0090635724258448, 359.4546378042384163 ) ) ;
#38936=CARTESIAN_POINT ( 'NONE',  ( 754.8983024940795303, -138.8965053807781374, 336.9254006560228163 ) ) ;
#38937=CARTESIAN_POINT ( 'NONE',  ( 771.2633955100217236, -359.9073299311467053, 363.4237431249939618 ) ) ;
#38940=CARTESIAN_POINT ( 'NONE',  ( 791.9812246680005501, -140.6346026584201070, 361.9419747391813189 ) ) ;
#38941=CARTESIAN_POINT ( 'NONE',  ( 797.8594530101008786, -109.5436935675110988, 322.1405469898980982 ) ) ;
#38943=CARTESIAN_POINT ( 'NONE',  ( 767.9999999999992042, 178.9475563372491251, 360.0000000000000000 ) ) ;
#38944=CARTESIAN_POINT ( 'NONE',  ( 746.7653713866222915, -425.2601417444136018, 351.0478386215610271 ) ) ;
#38946=CARTESIAN_POINT ( 'NONE',  ( 801.9419747391806368, -306.4527844766013800, 351.9812246680014027 ) ) ;
#38950=CARTESIAN_POINT ( 'NONE',  ( 762.3223304703356007, -415.5436935675102177, 322.3223304703362828 ) ) ;
#38956=CARTESIAN_POINT ( 'NONE',  ( 803.6646147819161570, -113.9073299311474301, 348.8264449731210561 ) ) ;
#38957=CARTESIAN_POINT ( 'NONE',  ( 766.9102291470427417, -426.5545181178794678, 318.6633372737382501 ) ) ;
#38958=CARTESIAN_POINT ( 'NONE',  ( 803.8651313633788504, -125.2601417444145255, 332.4468031744301015 ) ) ;
#38961=CARTESIAN_POINT ( 'NONE',  ( 773.7943932421234194, -383.8055962898682765, 305.5313806188329409 ) ) ;
#38962=ORIENTED_EDGE ( 'NONE', *, *, #44198, .T. ) ;
#38966=CARTESIAN_POINT ( 'NONE',  ( 744.6391490659812007, -38.73633629969877035, 338.7502325331110455 ) ) ;
#38974=CARTESIAN_POINT ( 'NONE',  ( 755.1538015810308480, -350.1908817542433212, 343.0433043558613804 ) ) ;
#38975=CARTESIAN_POINT ( 'NONE',  ( 807.2620300519052989, -336.0090635724251911, 318.0141637701419768 ) ) ;
#38979=CARTESIAN_POINT ( 'NONE',  ( 754.3581564841646241, -161.4636090269711133, 316.1443688327762516 ) ) ;
#38981=CARTESIAN_POINT ( 'NONE',  ( 782.5225473063381969, -118.2709662947837899, 375.2698199232970637 ) ) ;
#38985=CARTESIAN_POINT ( 'NONE',  ( 759.7806653035534055, -174.9982390220563673, 324.8639956371180801 ) ) ;
#38986=CARTESIAN_POINT ( 'NONE',  ( 804.4086373105744769, -1.645427208789804308, 333.3843516231986541 ) ) ;
#38990=CARTESIAN_POINT ( 'NONE',  ( 801.9858362298568863, 20.92167643740319605, 312.7379699480935642 ) ) ;
#38994=CARTESIAN_POINT ( 'NONE',  ( 749.8865473780648472, -308.5328690171412518, 322.1177392798429082 ) ) ;
#38995=CARTESIAN_POINT ( 'NONE',  ( 792.1044303154646968, -108.4527844766020053, 317.8323909638837677 ) ) ;
#38997=CARTESIAN_POINT ( 'NONE',  ( 756.3353852180819104, -317.9073299311468190, 331.1735550268788302 ) ) ;
#38999=CARTESIAN_POINT ( 'NONE',  ( 772.4837098697145166, -95.36187538569296862, 374.5518280994205611 ) ) ;
#39004=CARTESIAN_POINT ( 'NONE',  ( 774.6858677611749044, -9.725511749329603717, 315.5713283507209894 ) ) ;
#39006=CARTESIAN_POINT ( 'NONE',  ( 745.4481719005789273, -411.7255117493282910, 347.5162901302853697 ) ) ;
#39007=CARTESIAN_POINT ( 'NONE',  ( 781.2497674668890113, -300.3510508353230080, 375.3608509340180603 ) ) ;
#39008=CARTESIAN_POINT ( 'NONE',  ( 766.5853460496234675, -85.98741447168738716, 372.3518521366060554 ) ) ;
#39015=CARTESIAN_POINT ( 'NONE',  ( 814.2001403089898304, -401.3618753856920307, 347.4397851343538264 ) ) ;
#39021=CARTESIAN_POINT ( 'NONE',  ( 787.5531968255692163, -261.8272453906071746, 316.1348686366205811 ) ) ;
#39022=CARTESIAN_POINT ( 'NONE',  ( 797.6776695296629214, -163.5436935675109567, 357.6776695296636603 ) ) ;
#39026=CARTESIAN_POINT ( 'NONE',  ( 756.7813123517142913, -307.9874144716866340, 329.9779781133712504 ) ) ;
#39028=CARTESIAN_POINT ( 'NONE',  ( 810.4231160770870019, -24.55451811788064020, 321.9338519418446936 ) ) ;
#39031=CARTESIAN_POINT ( 'NONE',  ( 751.6929314249748586, -198.9982390220562252, 318.8095938919659034 ) ) ;
#39032=CARTESIAN_POINT ( 'NONE',  ( 805.1927285166397041, -88.81642084023842187, 341.8018195045277707 ) ) ;
#39035=CARTESIAN_POINT ( 'NONE',  ( 764.1737431748507561, -442.3726999360611103, 371.6461892240376415 ) ) ;
#39038=CARTESIAN_POINT ( 'NONE',  ( 773.3843516231979720, -349.4419599262320162, 364.4086373105754433 ) ) ;
#39039=CARTESIAN_POINT ( 'NONE',  ( 763.2262854647970016, -32.63460265842044095, 309.2812353651462445 ) ) ;
#39041=CARTESIAN_POINT ( 'NONE',  ( 766.7756240680305382, -62.53286901714199786, 361.5560724626415663 ) ) ;
#39044=CARTESIAN_POINT ( 'NONE',  ( 752.4576283171824116, -213.0783235625960401, 317.7880784355627952 ) ) ;
#39045=CARTESIAN_POINT ( 'NONE',  ( 759.9864689768902508, -26.08914811296592262, 354.9819416627836404 ) ) ;
#39049=CARTESIAN_POINT ( 'NONE',  ( 778.2165204200184689, -214.8164208402380666, 364.9363028652563230 ) ) ;
#39052=CARTESIAN_POINT ( 'NONE',  ( 755.3201227861273992, -315.7255117493286320, 345.3687786644892981 ) ) ;
#39056=CARTESIAN_POINT ( 'NONE',  ( 764.0069404352550464, -63.07832356259653750, 359.2566176426627180 ) ) ;
#39059=CARTESIAN_POINT ( 'NONE',  ( 754.9967657858570647, -241.5436935675106440, 365.0032342141425943 ) ) ;
#39060=CARTESIAN_POINT ( 'NONE',  ( 746.0683387631852383, 4.558040073766884248, 331.3260364891676204 ) ) ;
#39066=CARTESIAN_POINT ( 'NONE',  ( 814.2001403089898304, -281.3618753856923718, 347.4397851343538264 ) ) ;
#39067=CARTESIAN_POINT ( 'NONE',  ( 793.5337260303429048, -457.7979077669877483, 366.8220830107578649 ) ) ;
#39068=CARTESIAN_POINT ( 'NONE',  ( 780.5290396650775619, -348.3510508353228943, 365.2837595273619513 ) ) ;
#39070=CARTESIAN_POINT ( 'NONE',  ( 802.9823548866075953, -169.0999726633347393, 330.0799878456151077 ) ) ;
#39071=CARTESIAN_POINT ( 'NONE',  ( 755.3201227861273992, -27.72551174932954510, 345.3687786644892981 ) ) ;
#39075=CARTESIAN_POINT ( 'NONE',  ( 802.2119215644370342, -270.0090635724253048, 367.5423716828165084 ) ) ;
#39076=CARTESIAN_POINT ( 'NONE',  ( 790.8726784830453198, -202.7146871989597514, 362.5472867521010585 ) ) ;
#39079=CARTESIAN_POINT ( 'NONE',  ( 774.6312213355099630, 0.6381246143067236254, 364.6798772138717482 ) ) ;
#39082=CARTESIAN_POINT ( 'NONE',  ( 804.7487373415286811, -19.54369356751139364, 364.7487373415288516 ) ) ;
#39083=CARTESIAN_POINT ( 'NONE',  ( 787.4999999999992042, -462.9681489794447202, 270.0000000000000568 ) ) ;
#39085=DIRECTION ( 'NONE',  ( 0.000000000000000000, 1.000000000000000000, 0.000000000000000000 ) ) ;
#39086=CARTESIAN_POINT ( 'NONE',  ( 760.0363995740630116, -370.9181544815159555, 368.7758568127991907 ) ) ;
#39088=CARTESIAN_POINT ( 'NONE',  ( 745.7998596910086917, -341.3618753856922012, 332.5602148656461168 ) ) ;
#39092=CARTESIAN_POINT ( 'NONE',  ( 757.8323909638827445, -434.6346026584190554, 352.1044303154654358 ) ) ;
#39093=CARTESIAN_POINT ( 'NONE',  ( 757.4527132478984868, -184.3726999360619629, 329.1273215169538844 ) ) ;
#39096=CARTESIAN_POINT ( 'NONE',  ( 808.7758568127978833, -100.1692326535055315, 320.0363995740631822 ) ) ;
#39097=CARTESIAN_POINT ( 'NONE',  ( 788.7366044899766848, -395.9073299311465348, 316.5762568750059813 ) ) ;
#39104=CARTESIAN_POINT ( 'NONE',  ( 785.3687786644884454, -227.3618753856925707, 315.3201227861279676 ) ) ;
#39105=CARTESIAN_POINT ( 'NONE',  ( 771.2633955100217236, -239.9073299311470748, 363.4237431249939618 ) ) ;
#39110=CARTESIAN_POINT ( 'NONE',  ( 762.3223304703356007, -415.5436935675102177, 322.3223304703362828 ) ) ;
#39114=CARTESIAN_POINT ( 'NONE',  ( 772.4837098697145166, -167.3618753856927412, 374.5518280994205611 ) ) ;
#39115=CARTESIAN_POINT ( 'NONE',  ( 763.8424801807145741, -258.0090635724253616, 320.5453621957614700 ) ) ;
#39116=CARTESIAN_POINT ( 'NONE',  ( 754.8983024940795303, -378.8965053807772847, 336.9254006560228163 ) ) ;
#39123=CARTESIAN_POINT ( 'NONE',  ( 789.9200121543843807, -217.9874144716870035, 317.0176451133914384 ) ) ;
#39133=CARTESIAN_POINT ( 'NONE',  ( 813.5763878283155464, -147.8272453906075157, 351.1614460488615350 ) ) ;
#39143=CARTESIAN_POINT ( 'NONE',  ( 805.1927285166397041, -16.81642084023866701, 341.8018195045277707 ) ) ;
#39144=CARTESIAN_POINT ( 'NONE',  ( 745.5313806188320314, -255.2817908451526705, 333.7943932421247268 ) ) ;
#39146=CARTESIAN_POINT ( 'NONE',  ( 815.2698199232961542, -232.8164208402379245, 342.5225473063383106 ) ) ;
#39149=CARTESIAN_POINT ( 'NONE',  ( 767.8955696845333705, -312.4527844766012663, 362.1676090361162323 ) ) ;
#39150=CARTESIAN_POINT ( 'NONE',  ( 802.5472867521000353, -100.3726999360622187, 350.8726784830461156 ) ) ;
#39151=CARTESIAN_POINT ( 'NONE',  ( 802.5472867521000353, -100.3726999360622187, 350.8726784830461156 ) ) ;
#39156=CARTESIAN_POINT ( 'NONE',  ( 803.2186876482843445, -151.9874144716871740, 350.0220218866286928 ) ) ;
#39157=CARTESIAN_POINT ( 'NONE',  ( 762.3223304703356007, -367.5436935675102745, 322.3223304703362828 ) ) ;
#39162=CARTESIAN_POINT ( 'NONE',  ( 788.7366044899766848, -131.9073299311473875, 316.5762568750059813 ) ) ;
#39165=CARTESIAN_POINT ( 'NONE',  ( 793.4146539503750546, -409.9874144716863498, 307.6481478633938877 ) ) ;
#39167=CARTESIAN_POINT ( 'NONE',  ( 791.9812246680005501, -308.6346026584195670, 361.9419747391813189 ) ) ;
#39171=CARTESIAN_POINT ( 'NONE',  ( 755.0636971347428243, -412.2709662947829088, 341.7834795799807353 ) ) ;
#39178=CARTESIAN_POINT ( 'NONE',  ( 804.4086373105744769, -433.6454272087884760, 333.3843516231986541 ) ) ;
#39179=CARTESIAN_POINT ( 'NONE',  ( 758.6633372737375112, -140.5328690171417634, 326.9102291470432533 ) ) ;
#39182=CARTESIAN_POINT ( 'NONE',  ( 798.0661480581538854, -386.5328690171409676, 309.5768839229118043 ) ) ;
#39187=CARTESIAN_POINT ( 'NONE',  ( 762.1177392798416577, -18.55451811788065797, 309.8865473780659272 ) ) ;
#39195=CARTESIAN_POINT ( 'NONE',  ( 755.1538015810308480, -374.1908817542432075, 343.0433043558613804 ) ) ;
#39196=CARTESIAN_POINT ( 'NONE',  ( 768.9521613784389729, -345.8272453906069472, 373.2346286133773106 ) ) ;
#39200=CARTESIAN_POINT ( 'NONE',  ( 755.8990559732751535, -155.4636090269711417, 365.9055244015606831 ) ) ;
#39202=CARTESIAN_POINT ( 'NONE',  ( 796.9462024416508257, -108.4527844766019911, 308.9653473494370246 ) ) ;
#39206=CARTESIAN_POINT ( 'NONE',  ( 767.8955696845333705, -216.4527844766016926, 362.1676090361162323 ) ) ;
#39207=CARTESIAN_POINT ( 'NONE',  ( 773.4516893846965786, 4.354572791210176597, 315.8398074228977066 ) ) ;
#39211=CARTESIAN_POINT ( 'NONE',  ( 813.9316612368132837, -7.441959926233078448, 348.6739635108323228 ) ) ;
#39216=CARTESIAN_POINT ( 'NONE',  ( 746.7653713866222915, -305.2601417444139429, 351.0478386215610271 ) ) ;
#39217=CARTESIAN_POINT ( 'NONE',  ( 804.4286716492782716, -161.3618753856927697, 345.3141322388244703 ) ) ;
#39219=CARTESIAN_POINT ( 'NONE',  ( 771.1735550268778070, -321.1800572038740142, 316.3353852180827630 ) ) ;
#39221=CARTESIAN_POINT ( 'NONE',  ( 751.9810565676468741, -74.08914811296577341, 360.9747183278973921 ) ) ;
#39226=CARTESIAN_POINT ( 'NONE',  ( 762.3223304703356007, -31.54369356751135456, 322.3223304703362828 ) ) ;
#39228=CARTESIAN_POINT ( 'NONE',  ( 763.0537975583476964, -384.4527844766011526, 371.0346526505628617 ) ) ;
#39229=CARTESIAN_POINT ( 'NONE',  ( 811.6461892240364477, -292.7146871989594956, 324.1737431748509835 ) ) ;
#39230=CARTESIAN_POINT ( 'NONE',  ( 776.2433038121456548, -60.89650538077837894, 374.8207195650711014 ) ) ;
#39236=CARTESIAN_POINT ( 'NONE',  ( 801.1904061080336987, -380.0891481129646650, 368.3070685750235498 ) ) ;
#39240=DIRECTION ( 'NONE',  ( 0.000000000000000000, 0.000000000000000000, 1.000000000000000000 ) ) ;
#39242=CARTESIAN_POINT ( 'NONE',  ( 775.8780910478218402, -249.2817908451526421, 364.9511171171680530 ) ) ;
#39243=CARTESIAN_POINT ( 'NONE',  ( 765.0180583372156207, -168.9982390220563673, 360.0135310231089534 ) ) ;
#39248=CARTESIAN_POINT ( 'NONE',  ( 795.9930595647434757, -339.0783235625956422, 320.7433823573372820 ) ) ;
#39249=CARTESIAN_POINT ( 'NONE',  ( 759.9999999999992042, -512.9681489794448908, 329.9999999999999432 ) ) ;
#39250=CARTESIAN_POINT ( 'NONE',  ( 811.3240766477731540, -28.37269993606244967, 355.6651683502462902 ) ) ;
#39252=CARTESIAN_POINT ( 'NONE',  ( 804.9363028652555840, -112.2709662947838325, 338.2165204200192079 ) ) ;
#39255=CARTESIAN_POINT ( 'NONE',  ( 781.2370466360911223, -452.7363362996975411, 304.9990715423533629 ) ) ;
#39257=CARTESIAN_POINT ( 'NONE',  ( 780.5290396650775619, -348.3510508353228943, 365.2837595273619513 ) ) ;
#39258=CARTESIAN_POINT ( 'NONE',  ( 811.0346526505617248, -62.63460265842032726, 323.0537975583478101 ) ) ;
#39260=CARTESIAN_POINT ( 'NONE',  ( 755.8398074228967971, -43.44195992623296831, 333.4516893846970333 ) ) ;
#39262=CARTESIAN_POINT ( 'NONE',  ( 788.7631598425961101, -217.4419599262324141, 305.7194118038759143 ) ) ;
#39263=CARTESIAN_POINT ( 'NONE',  ( 755.3201227861273992, -3.725511749329622813, 345.3687786644892981 ) ) ;
#39266=CARTESIAN_POINT ( 'NONE',  ( 791.9812246680005501, -188.6346026584199365, 361.9419747391813189 ) ) ;
#39268=CARTESIAN_POINT ( 'NONE',  ( 754.8072714833583632, -340.8164208402376403, 338.1981804954721156 ) ) ;
#39272=ORIENTED_EDGE ( 'NONE', *, *, #28615, .T. ) ;
#39273=CARTESIAN_POINT ( 'NONE',  ( 766.7756240680305382, -62.53286901714199786, 361.5560724626415663 ) ) ;
#39275=CARTESIAN_POINT ( 'NONE',  ( 749.2812353651451076, -294.4527844766013800, 323.2262854647983090 ) ) ;
#39276=CARTESIAN_POINT ( 'NONE',  ( 761.9338519418445230, 9.467130982857780097, 370.4231160770881957 ) ) ;
#39283=CARTESIAN_POINT ( 'NONE',  ( 758.8095938919642549, -296.0891481129650629, 311.6929314249763365 ) ) ;
#39285=CARTESIAN_POINT ( 'NONE',  ( 756.1348686366196716, -353.2601417444137724, 347.5531968255698416 ) ) ;
#39287=CARTESIAN_POINT ( 'NONE',  ( 798.5707757039680246, -173.4636090269710849, 356.7845633553585003 ) ) ;
#39288=CARTESIAN_POINT ( 'NONE',  ( 755.3201227861273992, -51.72551174932946338, 345.3687786644892981 ) ) ;
#39293=CARTESIAN_POINT ( 'NONE',  ( 797.8822607201568644, -270.5545181178798657, 370.1134526219340160 ) ) ;
#39294=CARTESIAN_POINT ( 'NONE',  ( 795.9930595647434757, -219.0783235625960401, 320.7433823573372820 ) ) ;
#39296=CARTESIAN_POINT ( 'NONE',  ( 771.1735550268778070, 14.81994279612486309, 316.3353852180827630 ) ) ;
#39299=CARTESIAN_POINT ( 'NONE',  ( 745.7998596910086917, -29.36187538569318178, 332.5602148656461168 ) ) ;
#39300=CARTESIAN_POINT ( 'NONE',  ( 767.7687537140311633, -95.90732993114751537, 372.7932403749916830 ) ) ;
#39305=CARTESIAN_POINT ( 'NONE',  ( 805.6418435158337843, -389.4636090269704027, 363.8556311672236916 ) ) ;
#39307=CARTESIAN_POINT ( 'NONE',  ( 749.2812353651451076, -318.4527844766014368, 323.2262854647983090 ) ) ;
#39312=CARTESIAN_POINT ( 'NONE',  ( 758.0580252608178853, -438.4527844766009821, 328.0187753319985404 ) ) ;
#39315=CARTESIAN_POINT ( 'NONE',  ( 791.1614460488616487, -107.2601417444145824, 373.5763878283158874 ) ) ;
#39316=CARTESIAN_POINT ( 'NONE',  ( 800.2193346964446619, -402.9982390220555999, 355.1360043628816925 ) ) ;
#39317=CARTESIAN_POINT ( 'NONE',  ( 795.6651683502461765, -154.7146871989598935, 371.3240766477733814 ) ) ;
#39323=CARTESIAN_POINT ( 'NONE',  ( 771.1735550268778070, -225.1800572038743269, 316.3353852180827630 ) ) ;
#39324=CARTESIAN_POINT ( 'NONE',  ( 774.6312213355098493, -239.3618753856924855, 364.6798772138717482 ) ) ;
#39329=CARTESIAN_POINT ( 'NONE',  ( 771.1735550268778070, -417.1800572038736163, 316.3353852180827630 ) ) ;
#39333=CARTESIAN_POINT ( 'NONE',  ( 815.2698199232962679, -184.8164208402381234, 342.5225473063383674 ) ) ;
#39334=CARTESIAN_POINT ( 'NONE',  ( 779.4763451958990572, -272.7363362996981095, 365.0264073115438919 ) ) ;
#39338=CARTESIAN_POINT ( 'NONE',  ( 815.1787889125755555, -198.8965053807779384, 343.7953271457877804 ) ) ;
#39343=CARTESIAN_POINT ( 'NONE',  ( 773.3843516231979720, -229.4419599262323572, 364.4086373105754433 ) ) ;
#39352=CARTESIAN_POINT ( 'NONE',  ( 766.4474001241216001, -187.0999726633346825, 307.3154664389482491 ) ) ;
#39357=CARTESIAN_POINT ( 'NONE',  ( 763.0537975583475827, -24.45278447660229304, 371.0346526505627480 ) ) ;
#39362=CARTESIAN_POINT ( 'NONE',  ( 797.6776695296629214, 4.456306432488530866, 357.6776695296636603 ) ) ;
#39364=CARTESIAN_POINT ( 'NONE',  ( 811.3240766477731540, -244.3726999360617924, 355.6651683502462902 ) ) ;
#39366=CARTESIAN_POINT ( 'NONE',  ( 796.7737145352015204, -212.6346026584198796, 370.7187646348536987 ) ) ;
#39370=CARTESIAN_POINT ( 'NONE',  ( 797.8594530101008786, -325.5436935675105019, 322.1405469898980982 ) ) ;
#39371=CARTESIAN_POINT ( 'NONE',  ( 769.0155153010367712, -82.37269993606227558, 362.7791456095907279 ) ) ;
#39372=CARTESIAN_POINT ( 'NONE',  ( 766.0291762391763086, -82.91815448151682233, 360.7704444035551319 ) ) ;
#39377=CARTESIAN_POINT ( 'NONE',  ( 754.8983024940795303, -162.8965053807780521, 336.9254006560228163 ) ) ;
#39378=CARTESIAN_POINT ( 'NONE',  ( 755.0636971347428243, -364.2709662947830793, 341.7834795799807353 ) ) ;
#39383=CARTESIAN_POINT ( 'NONE',  ( 788.8264449731200330, -141.1800572038746395, 363.6646147819171233 ) ) ;
#39386=CARTESIAN_POINT ( 'NONE',  ( 808.7758568127978833, -436.1692326535044231, 320.0363995740631822 ) ) ;
#39389=CARTESIAN_POINT ( 'NONE',  ( 778.2165204200184689, -334.8164208402376403, 364.9363028652563230 ) ) ;
#39392=CARTESIAN_POINT ( 'NONE',  ( 797.8594530101008786, -445.5436935675098766, 322.1405469898980982 ) ) ;
#39400=CARTESIAN_POINT ( 'NONE',  ( 793.0897708529556667, -462.5545181178792973, 361.3366627262616362 ) ) ;
#39401=CARTESIAN_POINT ( 'NONE',  ( 754.9967657858570647, -217.5436935675107293, 365.0032342141425374 ) ) ;
#39402=CARTESIAN_POINT ( 'NONE',  ( 786.6156483768007774, -121.4419599262327267, 315.5913626894246136 ) ) ;
#39405=CARTESIAN_POINT ( 'NONE',  ( 758.0141637701419768, -375.0783235625955285, 367.2620300519063790 ) ) ;
#39410=CARTESIAN_POINT ( 'NONE',  ( 795.8262568251477660, -70.37269993606230400, 308.3538107759623585 ) ) ;
#39419=DIRECTION ( 'NONE',  ( -1.000000000000000000, -0.000000000000000000, 0.000000000000000000 ) ) ;
#39420=CARTESIAN_POINT ( 'NONE',  ( 766.0291762391763086, -370.9181544815159555, 360.7704444035551319 ) ) ;
#39422=CARTESIAN_POINT ( 'NONE',  ( 750.9282345327678740, -352.9181544815159555, 319.8311093483690115 ) ) ;
#39426=CARTESIAN_POINT ( 'NONE',  ( 745.1792804349281596, -134.1908817542439181, 343.7566961878542884 ) ) ;
#39428=CARTESIAN_POINT ( 'NONE',  ( 749.2812353651451076, -102.4527844766020337, 323.2262854647983090 ) ) ;
#39434=CARTESIAN_POINT ( 'NONE',  ( 794.9819416627830151, -204.9982390220562820, 319.9864689768909898 ) ) ;
#39437=CARTESIAN_POINT ( 'NONE',  ( 799.9636004259356241, -454.9181544815156713, 311.2241431872006956 ) ) ;
#39441=CARTESIAN_POINT ( 'NONE',  ( 759.8311093483677041, -22.16923265350575889, 310.9282345327691814 ) ) ;
#39445=CARTESIAN_POINT ( 'NONE',  ( 804.4286716492782716, -41.36187538569314626, 345.3141322388244703 ) ) ;
#39447=CARTESIAN_POINT ( 'NONE',  ( 771.2368401574024119, -301.4419599262320730, 374.2805881961240857 ) ) ;
#39448=CARTESIAN_POINT ( 'NONE',  ( 767.8955696845334842, -168.4527844766018347, 362.1676090361161755 ) ) ;
#39451=CARTESIAN_POINT ( 'NONE',  ( 778.1981804954714335, -322.2709662947830225, 314.8072714833589885 ) ) ;
#39454=CARTESIAN_POINT ( 'NONE',  ( 782.5225473063383106, -94.27096629478387513, 375.2698199232970637 ) ) ;
#39459=CARTESIAN_POINT ( 'NONE',  ( 801.9419747391806368, -42.45278447660223264, 351.9812246680014027 ) ) ;
#39460=CARTESIAN_POINT ( 'NONE',  ( 802.9823548866075953, -361.0999726633341425, 330.0799878456151077 ) ) ;
#39462=CARTESIAN_POINT ( 'NONE',  ( 796.9462024416508257, -396.4527844766010958, 308.9653473494370246 ) ) ;
#39463=CARTESIAN_POINT ( 'NONE',  ( 766.5853460496234675, -61.98741447168745822, 372.3518521366060554 ) ) ;
#39471=CARTESIAN_POINT ( 'NONE',  ( 745.7998596910086917, -389.3618753856919739, 332.5602148656461168 ) ) ;
#39473=CARTESIAN_POINT ( 'NONE',  ( 799.9999999999993179, -462.9681489794448339, 309.9999999999998863 ) ) ;
#39479=CARTESIAN_POINT ( 'NONE',  ( 755.3028492785439312, -279.2817908451526137, 335.9200461376539693 ) ) ;
#39480=CARTESIAN_POINT ( 'NONE',  ( 759.9864689768902508, -170.0891481129654608, 354.9819416627836404 ) ) ;
#39483=CARTESIAN_POINT ( 'NONE',  ( 766.7756240680305382, -326.5328690171411381, 361.5560724626415663 ) ) ;
#39486=CARTESIAN_POINT ( 'NONE',  ( 804.1009440267234822, -47.46360902697148987, 314.0944755984392600 ) ) ;
#39488=EDGE_CURVE ( 'NONE', #26042, #7675, #28945, .T. ) ;
#39491=CARTESIAN_POINT ( 'NONE',  ( 754.9967657858570647, -193.5436935675108714, 365.0032342141425374 ) ) ;
#39492=CARTESIAN_POINT ( 'NONE',  ( 800.0135310231082713, -110.0891481129656597, 325.0180583372163028 ) ) ;
#39495=CARTESIAN_POINT ( 'NONE',  ( 802.2119215644370342, -462.0090635724247932, 367.5423716828165084 ) ) ;
#39498=CARTESIAN_POINT ( 'NONE',  ( 754.9735926884551418, -354.3510508353228943, 340.5236548041000333 ) ) ;
#39502=CARTESIAN_POINT ( 'NONE',  ( 756.7813123517142913, -43.98741447168752217, 329.9779781133712504 ) ) ;
#39506=CARTESIAN_POINT ( 'NONE',  ( 748.3538107759620743, -208.7146871989596946, 355.8262568251490165 ) ) ;
#39507=CARTESIAN_POINT ( 'NONE',  ( 774.6312213355098493, -47.36187538569312494, 364.6798772138717482 ) ) ;
#39508=CIRCLE ( 'NONE', #25469, 30.00000000000002842 ) ;
#39511=CARTESIAN_POINT ( 'NONE',  ( 774.6858677611749044, -201.7255117493290015, 315.5713283507209894 ) ) ;
#39513=CARTESIAN_POINT ( 'NONE',  ( 785.3687786644885591, -347.3618753856922012, 315.3201227861280813 ) ) ;
#39518=CARTESIAN_POINT ( 'NONE',  ( 766.7756240680305382, -38.53286901714206891, 361.5560724626415663 ) ) ;
#39522=CARTESIAN_POINT ( 'NONE',  ( 747.2067596250078623, -291.1800572038741848, 352.2312462859687230 ) ) ;
#39523=CARTESIAN_POINT ( 'NONE',  ( 813.9316612368132837, 16.55804007376685050, 348.6739635108323228 ) ) ;
#39529=CARTESIAN_POINT ( 'NONE',  ( 796.9462024416508257, -276.4527844766013800, 308.9653473494370246 ) ) ;
#39530=CARTESIAN_POINT ( 'NONE',  ( 779.9999999999992042, -452.9681489794448339, 350.0000000000000000 ) ) ;
#39531=CARTESIAN_POINT ( 'NONE',  ( 755.0488828828309806, -353.8055962898683333, 344.1219089521771934 ) ) ;
#39533=CARTESIAN_POINT ( 'NONE',  ( 796.9571628226829034, -143.4636090269711701, 321.2382568024804641 ) ) ;
#39534=CARTESIAN_POINT ( 'NONE',  ( 791.9812246680005501, -44.63460265842040542, 361.9419747391813189 ) ) ;
#39535=ORIENTED_EDGE ( 'NONE', *, *, #7772, .F. ) ;
#39539=CARTESIAN_POINT ( 'NONE',  ( 809.0717654672305343, -268.9181544815162397, 360.1688906516309885 ) ) ;
#39540=CARTESIAN_POINT ( 'NONE',  ( 755.8398074228967971, -235.4419599262323857, 333.4516893846970333 ) ) ;
#39544=CARTESIAN_POINT ( 'NONE',  ( 757.8323909638827445, -2.634602658420536869, 352.1044303154654358 ) ) ;
#39548=CARTESIAN_POINT ( 'NONE',  ( 763.2262854647970016, -32.63460265842044095, 309.2812353651462445 ) ) ;
#39549=CARTESIAN_POINT ( 'NONE',  ( 782.5225473063381969, -94.27096629478386092, 375.2698199232970637 ) ) ;
#39554=CARTESIAN_POINT ( 'NONE',  ( 776.2046728542105711, -380.1908817542431507, 304.8212110874238761 ) ) ;
#39556=CARTESIAN_POINT ( 'NONE',  ( 787.5162901302840055, -323.3618753856923149, 305.4481719005792684 ) ) ;
#39559=CARTESIAN_POINT ( 'NONE',  ( 805.1927285166397041, -424.8164208402372992, 341.8018195045277707 ) ) ;
#39560=CARTESIAN_POINT ( 'NONE',  ( 802.5472867521000353, -196.3726999360619061, 350.8726784830461156 ) ) ;
#39563=CARTESIAN_POINT ( 'NONE',  ( 752.4576283171824116, -93.07832356259645223, 317.7880784355627952 ) ) ;
#39564=CARTESIAN_POINT ( 'NONE',  ( 774.6858677611749044, -441.7255117493282910, 315.5713283507209894 ) ) ;
#39565=CARTESIAN_POINT ( 'NONE',  ( 815.0009284576459549, -150.3510508353235480, 338.7629533639073429 ) ) ;
#39571=CARTESIAN_POINT ( 'NONE',  ( 762.3223304703356007, -271.5436935675106156, 322.3223304703362828 ) ) ;
#39572=CARTESIAN_POINT ( 'NONE',  ( 754.8072714833583632, -220.8164208402380098, 338.1981804954721156 ) ) ;
#39575=CARTESIAN_POINT ( 'NONE',  ( 778.2165204200184689, -430.8164208402374129, 364.9363028652563230 ) ) ;
#39578=CARTESIAN_POINT ( 'NONE',  ( 746.8695393053151292, -173.9073299311472454, 327.6429770376306578 ) ) ;
#39579=CARTESIAN_POINT ( 'NONE',  ( 754.7162404726377645, -254.7363362996981095, 339.4709603349214717 ) ) ;
#39582=CARTESIAN_POINT ( 'NONE',  ( 756.1443688327750579, -213.6237781080506011, 314.3581564841659315 ) ) ;
#39588=CARTESIAN_POINT ( 'NONE',  ( 787.6308680596127942, -251.2601417444141134, 364.1105419155492768 ) ) ;
#39596=CARTESIAN_POINT ( 'NONE',  ( 807.2620300519052989, -168.0090635724256458, 318.0141637701419768 ) ) ;
#39605=CARTESIAN_POINT ( 'NONE',  ( 778.2165204200184689, -22.81642084023865280, 364.9363028652563230 ) ) ;
#39606=CARTESIAN_POINT ( 'NONE',  ( 804.1009440267234822, -287.4636090269708575, 314.0944755984392600 ) ) ;
#39608=CARTESIAN_POINT ( 'NONE',  ( 777.4774526936600978, -226.2709662947834204, 304.7301800767027657 ) ) ;
#39613=CARTESIAN_POINT ( 'NONE',  ( 755.3201227861273992, -315.7255117493286320, 345.3687786644892981 ) ) ;
#39615=CARTESIAN_POINT ( 'NONE',  ( 801.5560724626406000, -96.55451811788039151, 326.7756240680316182 ) ) ;
#39620=CARTESIAN_POINT ( 'NONE',  ( 775.9200461376533440, -143.8055962898690154, 315.3028492785443291 ) ) ;
#39621=CARTESIAN_POINT ( 'NONE',  ( 795.1360043628807261, -356.0891481129647218, 360.2193346964456282 ) ) ;
#39625=CARTESIAN_POINT ( 'NONE',  ( 755.3201227861273992, -147.7255117493291152, 345.3687786644892981 ) ) ;
#39628=CARTESIAN_POINT ( 'NONE',  ( 815.0009284576459549, -438.3510508353226669, 338.7629533639073429 ) ) ;
#39630=CARTESIAN_POINT ( 'NONE',  ( 778.1981804954714335, -322.2709662947830225, 314.8072714833589885 ) ) ;
#39632=CARTESIAN_POINT ( 'NONE',  ( 801.9419747391806368, -426.4527844766010389, 351.9812246680014027 ) ) ;
#39640=CARTESIAN_POINT ( 'NONE',  ( 804.4286716492782716, 6.638124614306706306, 345.3141322388244703 ) ) ;
#39641=CARTESIAN_POINT ( 'NONE',  ( 813.1304606946830518, -233.9073299311470180, 352.3570229623690580 ) ) ;
#39642=CARTESIAN_POINT ( 'NONE',  ( 800.7704444035546203, -172.1692326535052757, 326.0291762391768771 ) ) ;
#39645=CARTESIAN_POINT ( 'NONE',  ( 759.8311093483677041, -382.1692326535045936, 310.9282345327691814 ) ) ;
#39651=CARTESIAN_POINT ( 'NONE',  ( 815.3608509340175488, -74.73633629969866377, 341.2497674668889545 ) ) ;
#39661=CARTESIAN_POINT ( 'NONE',  ( 766.9102291470427417, -402.5545181178795247, 318.6633372737382501 ) ) ;
#39663=ADVANCED_FACE ( 'NONE', ( #1215 ), #43477, .T. ) ;
#39666=CARTESIAN_POINT ( 'NONE',  ( 799.9636004259356241, -166.9181544815165523, 311.2241431872006956 ) ) ;
#39667=EDGE_CURVE ( 'NONE', #36800, #3123, #1961, .T. ) ;
#39669=CARTESIAN_POINT ( 'NONE',  ( 748.9653473494363425, -122.6346026584201354, 356.9462024416521331 ) ) ;
#39674=CARTESIAN_POINT ( 'NONE',  ( 757.8323909638827445, -218.6346026584197944, 352.1044303154654358 ) ) ;
#39675=CARTESIAN_POINT ( 'NONE',  ( 791.0478386215596629, -453.8272453906066630, 306.7653713866226326 ) ) ;
#39679=CARTESIAN_POINT ( 'NONE',  ( 813.9316612368132837, -31.44195992623299674, 348.6739635108323228 ) ) ;
#39683=CARTESIAN_POINT ( 'NONE',  ( 792.1044303154645831, -12.45278447660232146, 317.8323909638837677 ) ) ;
#39686=CARTESIAN_POINT ( 'NONE',  ( 778.7502325331095108, -336.3510508353228943, 304.6391490659818828 ) ) ;
#39687=CARTESIAN_POINT ( 'NONE',  ( 800.2193346964446619, -138.9982390220564241, 355.1360043628816925 ) ) ;
#39692=CARTESIAN_POINT ( 'NONE',  ( 774.6858677611749044, -345.7255117493285184, 315.5713283507209894 ) ) ;
#39699=CARTESIAN_POINT ( 'NONE',  ( 802.1676090361156639, -62.63460265842031305, 327.8955696845344505 ) ) ;
#39700=CARTESIAN_POINT ( 'NONE',  ( 787.5531968255692163, -357.8272453906068904, 316.1348686366205811 ) ) ;
#39702=CARTESIAN_POINT ( 'NONE',  ( 787.4397851343537695, -405.7255117493283478, 374.2001403089903988 ) ) ;
#39703=CARTESIAN_POINT ( 'NONE',  ( 776.2433038121456548, -276.8965053807776258, 374.8207195650711014 ) ) ;
#39704=EDGE_CURVE ( 'NONE', #1373, #28817, #529, .T. ) ;
#39711=CARTESIAN_POINT ( 'NONE',  ( 749.2812353651451076, -414.4527844766010389, 323.2262854647983090 ) ) ;
#39717=CARTESIAN_POINT ( 'NONE',  ( 787.5531968255692163, -285.8272453906071178, 316.1348686366205811 ) ) ;
#39718=CARTESIAN_POINT ( 'NONE',  ( 792.1044303154645831, -156.4527844766018916, 317.8323909638837677 ) ) ;
#39721=CARTESIAN_POINT ( 'NONE',  ( 769.1273215169530886, -310.7146871989593251, 317.4527132478988847 ) ) ;
#39723=DIRECTION ( 'NONE',  ( 0.000000000000000000, 0.000000000000000000, 1.000000000000000000 ) ) ;
#39724=CARTESIAN_POINT ( 'NONE',  ( 750.9282345327678740, -40.91815448151695023, 319.8311093483690115 ) ) ;
#39727=CARTESIAN_POINT ( 'NONE',  ( 808.0189434323515343, -206.0891481129653471, 319.0252816721025511 ) ) ;
#39728=CARTESIAN_POINT ( 'NONE',  ( 758.0580252608178853, -126.4527844766019626, 328.0187753319985404 ) ) ;
#39731=CARTESIAN_POINT ( 'NONE',  ( 805.2837595273609850, -26.73633629969882008, 340.5290396650784714 ) ) ;
#39734=CARTESIAN_POINT ( 'NONE',  ( 804.9511171171677688, -413.8055962898681059, 335.8780910478229202 ) ) ;
#39735=ORIENTED_EDGE ( 'NONE', *, *, #10052, .T. ) ;
#39740=CARTESIAN_POINT ( 'NONE',  ( 747.3154664389472828, -235.9874144716868898, 326.4474001241230781 ) ) ;
#39741=CARTESIAN_POINT ( 'NONE',  ( 804.9363028652555840, -40.27096629478405987, 338.2165204200192079 ) ) ;
#39745=CARTESIAN_POINT ( 'NONE',  ( 758.0580252608178853, -222.4527844766016642, 328.0187753319985404 ) ) ;
#39753=CARTESIAN_POINT ( 'NONE',  ( 796.7737145352015204, -284.6346026584196807, 370.7187646348536987 ) ) ;
#39754=CARTESIAN_POINT ( 'NONE',  ( 786.2056067578752163, -11.80559628986942577, 374.4686193811670023 ) ) ;
#39762=CARTESIAN_POINT ( 'NONE',  ( 777.5031285880264704, -334.8164208402376403, 374.9108240113588408 ) ) ;
#39764=CARTESIAN_POINT ( 'NONE',  ( 775.9200461376533440, -359.8055962898683333, 315.3028492785443291 ) ) ;
#39766=CARTESIAN_POINT ( 'NONE',  ( 802.9823548866075953, -145.0999726633347677, 330.0799878456151077 ) ) ;
#39767=CARTESIAN_POINT ( 'NONE',  ( 771.1735550268778070, -57.18005720387489532, 316.3353852180827630 ) ) ;
#39771=CARTESIAN_POINT ( 'NONE',  ( 745.7194118038753459, -277.6454272087889308, 348.7631598425976449 ) ) ;
#39772=CARTESIAN_POINT ( 'NONE',  ( 759.2295555964440155, -208.1692326535051905, 353.9708237608231229 ) ) ;
#39775=CARTESIAN_POINT ( 'NONE',  ( 804.4286716492782716, 6.638124614306706306, 345.3141322388244703 ) ) ;
#39778=CARTESIAN_POINT ( 'NONE',  ( 801.1904061080336987, -44.08914811296584446, 368.3070685750235498 ) ) ;
#39779=CARTESIAN_POINT ( 'NONE',  ( 814.9108240113580450, -112.2709662947838325, 337.5031285880265273 ) ) ;
#39782=CARTESIAN_POINT ( 'NONE',  ( 814.2805881961230625, -385.6454272087888171, 331.2368401574024119 ) ) ;
#39784=CARTESIAN_POINT ( 'NONE',  ( 772.5602148656447525, -369.7255117493284615, 305.7998596910095443 ) ) ;
#39787=CARTESIAN_POINT ( 'NONE',  ( 804.6798772138708955, -423.7255117493281205, 334.6312213355107019 ) ) ;
#39788=CARTESIAN_POINT ( 'NONE',  ( 779.4763451958990572, -200.7363362996982801, 365.0264073115438919 ) ) ;
#39791=CARTESIAN_POINT ( 'NONE',  ( 803.8556311672234642, -105.6237781080509421, 365.6418435158340117 ) ) ;
#39792=CARTESIAN_POINT ( 'NONE',  ( 767.8955696845334842, -432.4527844766009252, 362.1676090361161755 ) ) ;
#39793=CARTESIAN_POINT ( 'NONE',  ( 764.3348316497523456, -166.7146871989598367, 308.6759233522265617 ) ) ;
#39798=CARTESIAN_POINT ( 'NONE',  ( 802.1676090361156639, -254.6346026584196238, 327.8955696845344505 ) ) ;
#39799=CARTESIAN_POINT ( 'NONE',  ( 792.1044303154646968, -252.4527844766015789, 317.8323909638837677 ) ) ;
#39802=CARTESIAN_POINT ( 'NONE',  ( 786.6156483768007774, 22.55804007376682918, 315.5913626894246136 ) ) ;
#39803=ORIENTED_EDGE ( 'NONE', *, *, #8040, .T. ) ;
#39804=CARTESIAN_POINT ( 'NONE',  ( 745.4481719005789273, -195.7255117493290015, 347.5162901302853697 ) ) ;
#39805=CARTESIAN_POINT ( 'NONE',  ( 757.0176451133909268, -253.0999726633345119, 349.9200121543848354 ) ) ;
#39806=CARTESIAN_POINT ( 'NONE',  ( 755.8398074228967971, -379.4419599262318457, 333.4516893846970333 ) ) ;
#39809=CARTESIAN_POINT ( 'NONE',  ( 813.2346286133761168, -221.2601417444142271, 328.9521613784389160 ) ) ;
#39815=CARTESIAN_POINT ( 'NONE',  ( 796.7845633553578182, -249.6237781080505158, 358.5707757039688204 ) ) ;
#39822=CARTESIAN_POINT ( 'NONE',  ( 745.5313806188320314, -159.2817908451529547, 333.7943932421247268 ) ) ;
#39828=CARTESIAN_POINT ( 'NONE',  ( 744.7301800767019131, -28.81642084023863148, 337.4774526936615757 ) ) ;
#39833=CARTESIAN_POINT ( 'NONE',  ( 803.6646147819161570, 6.092670068852159559, 348.8264449731210561 ) ) ;
#39834=CARTESIAN_POINT ( 'NONE',  ( 813.5763878283155464, -267.8272453906071746, 351.1614460488615350 ) ) ;
#39837=CARTESIAN_POINT ( 'NONE',  ( 763.2262854647970016, -272.6346026584196807, 309.2812353651462445 ) ) ;
#39841=CARTESIAN_POINT ( 'NONE',  ( 785.3687786644884454, -323.3618753856923149, 315.3201227861279676 ) ) ;
#39842=CARTESIAN_POINT ( 'NONE',  ( 796.1575198192839480, -78.00906357242591582, 359.4546378042384163 ) ) ;
#39846=CARTESIAN_POINT ( 'NONE',  ( 794.1144889064781864, -154.1692326535053894, 360.9840315886528401 ) ) ;
#39847=CARTESIAN_POINT ( 'NONE',  ( 802.1676090361156639, -350.6346026584192828, 327.8955696845344505 ) ) ;
#39850=CARTESIAN_POINT ( 'NONE',  ( 778.1981804954714335, -154.2709662947836478, 314.8072714833589885 ) ) ;
#39854=CARTESIAN_POINT ( 'NONE',  ( 755.2512626584698410, 16.45630643248849267, 315.2512626584710915 ) ) ;
#39856=CARTESIAN_POINT ( 'NONE',  ( 755.0636971347428243, -340.2709662947831362, 341.7834795799807353 ) ) ;
#39859=CARTESIAN_POINT ( 'NONE',  ( 803.6646147819161570, -449.9073299311463643, 348.8264449731210561 ) ) ;
#39865=CARTESIAN_POINT ( 'NONE',  ( 757.8323909638827445, -2.634602658420536869, 352.1044303154654358 ) ) ;
#39866=CARTESIAN_POINT ( 'NONE',  ( 777.4774526936600978, -226.2709662947834204, 304.7301800767027657 ) ) ;
#39867=CARTESIAN_POINT ( 'NONE',  ( 779.4709603349208464, -168.3510508353234911, 314.7162404726379918 ) ) ;
#39868=PLANE ( 'NONE',  #13723 ) ;
#39874=CARTESIAN_POINT ( 'NONE',  ( 802.2119215644370342, -54.00906357242601530, 367.5423716828165084 ) ) ;
#39882=CARTESIAN_POINT ( 'NONE',  ( 802.9823548866075953, -385.0999726633340856, 330.0799878456151077 ) ) ;
#39886=CARTESIAN_POINT ( 'NONE',  ( 771.3260364891663130, -187.6454272087892434, 306.0683387631859773 ) ) ;
#39888=CARTESIAN_POINT ( 'NONE',  ( 814.5518280994195948, -135.7255117493291152, 332.4837098697145734 ) ) ;
#39892=CARTESIAN_POINT ( 'NONE',  ( 803.6646147819161570, -233.9073299311470180, 348.8264449731210561 ) ) ;
#39893=CARTESIAN_POINT ( 'NONE',  ( 755.5913626894240451, -13.64542720878976390, 346.6156483768012890 ) ) ;
#39897=CARTESIAN_POINT ( 'NONE',  ( 766.5853460496234675, -37.98741447168752927, 372.3518521366060554 ) ) ;
#39899=CARTESIAN_POINT ( 'NONE',  ( 755.0636971347428243, -268.2709662947833067, 341.7834795799807353 ) ) ;
#39903=CARTESIAN_POINT ( 'NONE',  ( 771.1735550268778070, -33.18005720387498769, 316.3353852180827630 ) ) ;
#39905=CARTESIAN_POINT ( 'NONE',  ( 795.6651683502461765, -346.7146871989592682, 371.3240766477733814 ) ) ;
#39909=CARTESIAN_POINT ( 'NONE',  ( 801.9419747391806368, -354.4527844766012095, 351.9812246680014027 ) ) ;
#39915=CARTESIAN_POINT ( 'NONE',  ( 759.9864689768902508, -74.08914811296577341, 354.9819416627836404 ) ) ;
#39916=CARTESIAN_POINT ( 'NONE',  ( 801.5560724626406000, -384.5545181178795247, 326.7756240680316182 ) ) ;
#39918=CARTESIAN_POINT ( 'NONE',  ( 748.9653473494365699, -410.6346026584191691, 356.9462024416520762 ) ) ;
#39919=CARTESIAN_POINT ( 'NONE',  ( 754.0944755984390895, -327.6237781080502600, 364.1009440267246760 ) ) ;
#39925=CARTESIAN_POINT ( 'NONE',  ( 787.4397851343537695, -429.7255117493282910, 374.2001403089903988 ) ) ;
#39931=CARTESIAN_POINT ( 'NONE',  ( 766.0291762391763086, -298.9181544815161828, 360.7704444035551319 ) ) ;
#39932=CARTESIAN_POINT ( 'NONE',  ( 755.0636971347428243, -148.2709662947837330, 341.7834795799807353 ) ) ;
#39935=CARTESIAN_POINT ( 'NONE',  ( 769.1273215169530886, -334.7146871989593251, 317.4527132478988847 ) ) ;
#39936=CARTESIAN_POINT ( 'NONE',  ( 799.9999999999993179, -462.9681489794448339, 309.9999999999998863 ) ) ;
#39939=CARTESIAN_POINT ( 'NONE',  ( 745.1792804349281596, -62.19088175424416676, 343.7566961878542884 ) ) ;
#39942=CARTESIAN_POINT ( 'NONE',  ( 815.2698199232961542, -208.8164208402380666, 342.5225473063383106 ) ) ;
#39943=CARTESIAN_POINT ( 'NONE',  ( 755.5713283507202505, -101.3618753856929544, 334.6858677611754729 ) ) ;
#39945=CARTESIAN_POINT ( 'NONE',  ( 755.5913626894240451, -13.64542720878976390, 346.6156483768012890 ) ) ;
#39948=CARTESIAN_POINT ( 'NONE',  ( 775.9200461376533440, -383.8055962898682765, 315.3028492785443291 ) ) ;
#39955=CARTESIAN_POINT ( 'NONE',  ( 778.7502325331095108, -240.3510508353232069, 304.6391490659818828 ) ) ;
#39956=CARTESIAN_POINT ( 'NONE',  ( 805.1927285166399315, -64.81642084023852135, 341.8018195045277707 ) ) ;
#39957=CARTESIAN_POINT ( 'NONE',  ( 759.9864689768902508, -242.0891481129652618, 354.9819416627836404 ) ) ;
#39961=EDGE_LOOP ( 'NONE', ( #31598, #17843, #6268, #13991, #7922, #24958 ) ) ;
#39965=CARTESIAN_POINT ( 'NONE',  ( 804.7487373415286811, -283.5436935675105019, 364.7487373415288516 ) ) ;
#39966=CARTESIAN_POINT ( 'NONE',  ( 746.7653713866222915, -17.26014174441486659, 351.0478386215610271 ) ) ;
#39972=CARTESIAN_POINT ( 'NONE',  ( 772.4837098697144029, -311.3618753856922581, 374.5518280994205611 ) ) ;
#39975=CARTESIAN_POINT ( 'NONE',  ( 784.1219089521767955, -189.2817908451528979, 315.0488828828318333 ) ) ;
#39976=CARTESIAN_POINT ( 'NONE',  ( 804.6798772138708955, -39.72551174932951312, 334.6312213355107019 ) ) ;
#39977=ORIENTED_EDGE ( 'NONE', *, *, #31202, .F. ) ;
#39981=CARTESIAN_POINT ( 'NONE',  ( 763.2154366446407039, -213.6237781080506011, 321.4292242960311228 ) ) ;
#39985=CARTESIAN_POINT ( 'NONE',  ( 815.2698199232961542, -424.8164208402372992, 342.5225473063383106 ) ) ;
#39990=CARTESIAN_POINT ( 'NONE',  ( 812.7932403749906598, -63.18005720387488822, 327.7687537140311633 ) ) ;
#39991=CARTESIAN_POINT ( 'NONE',  ( 767.6429770376289525, -105.1800572038747248, 306.8695393053162093 ) ) ;
#39993=CARTESIAN_POINT ( 'NONE',  ( 750.9282345327678740, -400.9181544815159555, 319.8311093483690115 ) ) ;
#39994=CARTESIAN_POINT ( 'NONE',  ( 799.9999999999993179, -512.9681489794448908, 329.9999999999999432 ) ) ;
#39995=CARTESIAN_POINT ( 'NONE',  ( 787.5162901302840055, -371.3618753856919739, 305.4481719005792684 ) ) ;
#39997=CARTESIAN_POINT ( 'NONE',  ( 765.8855110935204493, 25.83076734649409545, 319.0159684113471599 ) ) ;
#40001=CARTESIAN_POINT ( 'NONE',  ( 751.2241431872005251, -136.1692326535053894, 359.9636004259367610 ) ) ;
#40002=CARTESIAN_POINT ( 'NONE',  ( 754.8072714833583632, -436.8164208402372992, 338.1981804954721156 ) ) ;
#40007=CARTESIAN_POINT ( 'NONE',  ( 757.8323909638827445, -266.6346026584197375, 352.1044303154654358 ) ) ;
#40008=CARTESIAN_POINT ( 'NONE',  ( 795.1360043628808398, -260.0891481129650629, 360.2193346964456282 ) ) ;
#40011=CARTESIAN_POINT ( 'NONE',  ( 758.6633372737375112, 3.467130982857797417, 326.9102291470432533 ) ) ;
#40013=CARTESIAN_POINT ( 'NONE',  ( 812.7932403749906598, -183.1800572038744974, 327.7687537140311633 ) ) ;
#40014=CARTESIAN_POINT ( 'NONE',  ( 755.3028492785439312, -279.2817908451526137, 335.9200461376539693 ) ) ;
#40015=CARTESIAN_POINT ( 'NONE',  ( 805.0264073115434940, -414.3510508353227237, 339.4763451958999099 ) ) ;
#40016=EDGE_LOOP ( 'NONE', ( #31983, #40574, #27598, #38093 ) ) ;
#40018=VECTOR ( 'NONE', #9855, 1000.000000000000000 ) ;
#40019=CARTESIAN_POINT ( 'NONE',  ( 771.2368401574024119, -205.4419599262324425, 374.2805881961240857 ) ) ;
#40021=ORIENTED_EDGE ( 'NONE', *, *, #8949, .F. ) ;
#40024=CARTESIAN_POINT ( 'NONE',  ( 804.1601925771018387, -271.4419599262321867, 346.5483106153029098 ) ) ;
#40029=VERTEX_POINT ( 'NONE', #37911 ) ;
#40031=CARTESIAN_POINT ( 'NONE',  ( 760.0363995740630116, -178.9181544815165239, 368.7758568127991907 ) ) ;
#40035=CARTESIAN_POINT ( 'NONE',  ( 808.0189434323515343, -14.08914811296595460, 319.0252816721025511 ) ) ;
#40039=CARTESIAN_POINT ( 'NONE',  ( 771.1735550268778070, -33.18005720387498769, 316.3353852180827630 ) ) ;
#40040=CARTESIAN_POINT ( 'NONE',  ( 802.2119215644370342, -270.0090635724253048, 367.5423716828165084 ) ) ;
#40042=CARTESIAN_POINT ( 'NONE',  ( 814.5518280994195948, -255.7255117493287742, 332.4837098697145734 ) ) ;
#40046=CARTESIAN_POINT ( 'NONE',  ( 774.6312213355099630, -359.3618753856920875, 364.6798772138717482 ) ) ;
#40047=CARTESIAN_POINT ( 'NONE',  ( 793.0897708529556667, -78.55451811788046257, 361.3366627262616362 ) ) ;
#40051=CARTESIAN_POINT ( 'NONE',  ( 756.3353852180819104, -389.9073299311465348, 331.1735550268788302 ) ) ;
#40054=CARTESIAN_POINT ( 'NONE',  ( 797.6776695296629214, -163.5436935675109567, 357.6776695296636603 ) ) ;
#40057=CARTESIAN_POINT ( 'NONE',  ( 810.7187646348534145, 5.547215523397618142, 356.7737145352016341 ) ) ;
#40059=CARTESIAN_POINT ( 'NONE',  ( 792.1044303154645831, -348.4527844766012663, 317.8323909638837677 ) ) ;
#40062=CARTESIAN_POINT ( 'NONE',  ( 755.5713283507202505, -437.3618753856919170, 334.6858677611754729 ) ) ;
#40066=ORIENTED_EDGE ( 'NONE', *, *, #25832, .T. ) ;
#40068=CARTESIAN_POINT ( 'NONE',  ( 804.1105419155481968, -459.8272453906066062, 347.6308680596136469 ) ) ;
#40069=CARTESIAN_POINT ( 'NONE',  ( 767.6429770376289525, -225.1800572038743269, 306.8695393053162093 ) ) ;
#40070=CARTESIAN_POINT ( 'NONE',  ( 803.2186876482843445, -151.9874144716871740, 350.0220218866286928 ) ) ;
#40075=CARTESIAN_POINT ( 'NONE',  ( 767.9999999999992042, 205.0000000000000568, 329.9999999999999432 ) ) ;
#40078=CARTESIAN_POINT ( 'NONE',  ( 757.7880784355613741, -42.00906357242603661, 312.4576283171834916 ) ) ;
#40079=CARTESIAN_POINT ( 'NONE',  ( 809.0717654672305343, -76.91815448151683654, 360.1688906516309885 ) ) ;
#40087=CARTESIAN_POINT ( 'NONE',  ( 773.4516893846965786, -403.6454272087884760, 315.8398074228977066 ) ) ;
#40092=CARTESIAN_POINT ( 'NONE',  ( 807.2620300519052989, -192.0090635724255606, 318.0141637701419768 ) ) ;
#40094=CARTESIAN_POINT ( 'NONE',  ( 804.7487373415286811, -139.5436935675110135, 364.7487373415288516 ) ) ;
#40098=CARTESIAN_POINT ( 'NONE',  ( 800.0135310231082713, -206.0891481129653471, 325.0180583372163028 ) ) ;
#40099=CARTESIAN_POINT ( 'NONE',  ( 802.9823548866075953, -25.09997266333519050, 330.0799878456151077 ) ) ;
#40103=CARTESIAN_POINT ( 'NONE',  ( 776.2433038121456548, -36.89650538077844288, 374.8207195650711014 ) ) ;
#40104=CARTESIAN_POINT ( 'NONE',  ( 802.1676090361156639, -302.6346026584196238, 327.8955696845344505 ) ) ;
#40108=CARTESIAN_POINT ( 'NONE',  ( 800.0135310231082713, -38.08914811296587999, 325.0180583372163028 ) ) ;
#40111=CARTESIAN_POINT ( 'NONE',  ( 771.2368401574024119, -349.4419599262320162, 374.2805881961240857 ) ) ;
#40114=CARTESIAN_POINT ( 'NONE',  ( 744.8212110874229666, -426.8965053807771142, 336.2046728542121627 ) ) ;
#40115=CARTESIAN_POINT ( 'NONE',  ( 774.6312213355099630, -335.3618753856920307, 364.6798772138717482 ) ) ;
#40124=CARTESIAN_POINT ( 'NONE',  ( 774.6858677611749044, -57.72551174932945628, 315.5713283507209894 ) ) ;
#40125=CARTESIAN_POINT ( 'NONE',  ( 805.2837595273609850, -362.7363362996977116, 340.5290396650784714 ) ) ;
#40127=CARTESIAN_POINT ( 'NONE',  ( 755.2512626584698410, -439.5436935675101040, 315.2512626584710915 ) ) ;
#40129=CARTESIAN_POINT ( 'NONE',  ( 744.9990715423526808, -330.3510508353229511, 341.2370466360926002 ) ) ;
#40136=CARTESIAN_POINT ( 'NONE',  ( 747.2067596250078623, -411.1800572038738437, 352.2312462859687230 ) ) ;
#40143=CARTESIAN_POINT ( 'NONE',  ( 793.9708237608222134, -310.9181544815160123, 319.2295555964448681 ) ) ;
#40144=CARTESIAN_POINT ( 'NONE',  ( 768.0187753319979720, -176.6346026584199933, 318.0580252608186242 ) ) ;
#40145=ORIENTED_EDGE ( 'NONE', *, *, #27263, .F. ) ;
#40147=CIRCLE ( 'NONE', #9140, 30.00000000000008171 ) ;
#40149=CARTESIAN_POINT ( 'NONE',  ( 755.8398074228967971, -331.4419599262320162, 333.4516893846970333 ) ) ;
#40150=CARTESIAN_POINT ( 'NONE',  ( 811.3240766477731540, -76.37269993606228979, 355.6651683502462902 ) ) ;
#40152=CARTESIAN_POINT ( 'NONE',  ( 756.3353852180819104, -101.9073299311474727, 331.1735550268788302 ) ) ;
#40157=CARTESIAN_POINT ( 'NONE',  ( 773.4516893846965786, -19.64542720878974791, 315.8398074228977066 ) ) ;
#40160=CARTESIAN_POINT ( 'NONE',  ( 763.2154366446407039, -405.6237781080500326, 321.4292242960311228 ) ) ;
#40162=CARTESIAN_POINT ( 'NONE',  ( 773.3843516231979720, -85.44195992623282621, 364.4086373105754433 ) ) ;
#40167=CARTESIAN_POINT ( 'NONE',  ( 761.9338519418445230, -254.5328690171413655, 370.4231160770881957 ) ) ;
#40168=CARTESIAN_POINT ( 'NONE',  ( 803.6646147819162707, -65.90732993114760063, 348.8264449731211130 ) ) ;
#40171=CARTESIAN_POINT ( 'NONE',  ( 785.3687786644884454, -251.3618753856923149, 315.3201227861279676 ) ) ;
#40180=CARTESIAN_POINT ( 'NONE',  ( 787.5162901302840055, -299.3618753856923149, 305.4481719005793252 ) ) ;
#40182=CARTESIAN_POINT ( 'NONE',  ( 758.0141637701419768, -39.07832356259662276, 367.2620300519063790 ) ) ;
#40188=CARTESIAN_POINT ( 'NONE',  ( 768.0187753319979720, -224.6346026584198228, 318.0580252608186242 ) ) ;
#40190=EDGE_LOOP ( 'NONE', ( #33580, #6717 ) ) ;
#40191=CARTESIAN_POINT ( 'NONE',  ( 801.1904061080336987, -332.0891481129649492, 368.3070685750235498 ) ) ;
#40194=CARTESIAN_POINT ( 'NONE',  ( 769.1273215169530886, -358.7146871989592114, 317.4527132478988847 ) ) ;
#40199=CARTESIAN_POINT ( 'NONE',  ( 783.0745993439762742, -200.1908817542436907, 365.1016975059196739 ) ) ;
#40200=CARTESIAN_POINT ( 'NONE',  ( 804.9363028652555840, -40.27096629478405987, 338.2165204200192079 ) ) ;
#40204=CARTESIAN_POINT ( 'NONE',  ( 790.8726784830453198, -226.7146871989596661, 362.5472867521010585 ) ) ;
#40207=CARTESIAN_POINT ( 'NONE',  ( 763.0537975583475827, -432.4527844766008684, 371.0346526505627480 ) ) ;
#40211=CIRCLE ( 'NONE', #6265, 10.00000000000000888 ) ;
#40212=CARTESIAN_POINT ( 'NONE',  ( 745.4481719005789273, -51.72551174932946338, 347.5162901302853129 ) ) ;
#40213=CARTESIAN_POINT ( 'NONE',  ( 745.4481719005789273, -123.7255117493292147, 347.5162901302853129 ) ) ;
#40219=CARTESIAN_POINT ( 'NONE',  ( 749.5768839229115201, -372.5545181178796383, 358.0661480581553064 ) ) ;
#40222=CARTESIAN_POINT ( 'NONE',  ( 796.9462024416508257, -348.4527844766012663, 308.9653473494370246 ) ) ;
#40224=CARTESIAN_POINT ( 'NONE',  ( 803.4237431249931660, -447.1800572038736732, 331.2633955100225194 ) ) ;
#40225=CIRCLE ( 'NONE', #26195, 30.00000000000008171 ) ;
#40228=CARTESIAN_POINT ( 'NONE',  ( 748.3538107759620743, -136.7146871989600072, 355.8262568251490165 ) ) ;
#40229=CARTESIAN_POINT ( 'NONE',  ( 788.8264449731201466, -429.1800572038737300, 363.6646147819170665 ) ) ;
#40231=CARTESIAN_POINT ( 'NONE',  ( 749.8865473780648472, -164.5328690171416781, 322.1177392798429082 ) ) ;
#40235=CARTESIAN_POINT ( 'NONE',  ( 804.4286716492782716, -137.3618753856928265, 345.3141322388244703 ) ) ;
#40238=CARTESIAN_POINT ( 'NONE',  ( 795.1360043628807261, -260.0891481129650060, 360.2193346964456282 ) ) ;
#40239=CARTESIAN_POINT ( 'NONE',  ( 768.0187753319979720, -248.6346026584197659, 318.0580252608186242 ) ) ;
#40242=CARTESIAN_POINT ( 'NONE',  ( 776.9566956441375396, 11.10349461922141145, 364.8461984189686405 ) ) ;
#40247=CARTESIAN_POINT ( 'NONE',  ( 787.5162901302840055, -179.3618753856927128, 305.4481719005793252 ) ) ;
#40249=CARTESIAN_POINT ( 'NONE',  ( 800.9840315886518738, -292.9181544815162397, 354.1144889064786412 ) ) ;
#40250=CARTESIAN_POINT ( 'NONE',  ( 798.7617431975189675, -411.6237781080499758, 323.0428371773161871 ) ) ;
#40258=VECTOR ( 'NONE', #13546, 1000.000000000000000 ) ;
#40259=CARTESIAN_POINT ( 'NONE',  ( 796.7845633553578182, -273.6237781080504305, 358.5707757039688204 ) ) ;
#40265=FACE_BOUND ( 'NONE', #18782, .T. ) ;
#40268=CARTESIAN_POINT ( 'NONE',  ( 788.6739635108323228, -175.6454272087892718, 373.9316612368139090 ) ) ;
#40274=CARTESIAN_POINT ( 'NONE',  ( 767.7687537140311633, -23.90732993114773919, 372.7932403749916830 ) ) ;
#40278=DIRECTION ( 'NONE',  ( 0.000000000000000000, 0.000000000000000000, 1.000000000000000000 ) ) ;
#40279=CARTESIAN_POINT ( 'NONE',  ( 802.1676090361156639, -38.63460265842041252, 327.8955696845344505 ) ) ;
#40280=CARTESIAN_POINT ( 'NONE',  ( 745.1792804349281596, -302.1908817542433781, 343.7566961878542884 ) ) ;
#40281=CARTESIAN_POINT ( 'NONE',  ( 758.8095938919642549, -272.0891481129651197, 311.6929314249763365 ) ) ;
#40285=CARTESIAN_POINT ( 'NONE',  ( 774.6858677611749044, -369.7255117493284615, 315.5713283507209894 ) ) ;
#40286=CARTESIAN_POINT ( 'NONE',  ( 754.7162404726377645, -110.7363362996985501, 339.4709603349214717 ) ) ;
#40291=CARTESIAN_POINT ( 'NONE',  ( 808.7758568127978833, -124.1692326535054463, 320.0363995740631822 ) ) ;
#40292=CARTESIAN_POINT ( 'NONE',  ( 774.6312213355099630, -383.3618753856921444, 364.6798772138717482 ) ) ;
#40297=CARTESIAN_POINT ( 'NONE',  ( 771.1735550268778070, -153.1800572038746395, 316.3353852180827630 ) ) ;
#40300=FACE_BOUND ( 'NONE', #18948, .T. ) ;
#40302=CARTESIAN_POINT ( 'NONE',  ( 785.3687786644884454, -347.3618753856922012, 315.3201227861279676 ) ) ;
#40306=CARTESIAN_POINT ( 'NONE',  ( 774.6312213355099630, -431.3618753856918033, 364.6798772138717482 ) ) ;
#40309=CARTESIAN_POINT ( 'NONE',  ( 759.0252816721024374, -72.99823902205667991, 368.0189434323527280 ) ) ;
#40314=CARTESIAN_POINT ( 'NONE',  ( 797.8594530101008786, 10.45630643248850866, 322.1405469898980982 ) ) ;
#40315=CARTESIAN_POINT ( 'NONE',  ( 772.5602148656447525, -225.7255117493289163, 305.7998596910095443 ) ) ;
#40316=CARTESIAN_POINT ( 'NONE',  ( 773.3843516231979720, -157.4419599262326130, 364.4086373105754433 ) ) ;
#40319=CARTESIAN_POINT ( 'NONE',  ( 798.0661480581538854, -410.5328690171408539, 309.5768839229118043 ) ) ;
#40324=CARTESIAN_POINT ( 'NONE',  ( 755.8990559732751535, -59.46360902697142592, 365.9055244015606831 ) ) ;
#40331=CARTESIAN_POINT ( 'NONE',  ( 791.6690787386836519, -454.6466601436378028, 367.6383479129825673 ) ) ;
#40335=CARTESIAN_POINT ( 'NONE',  ( 805.2837595273609850, -410.7363362996976548, 340.5290396650784714 ) ) ;
#40337=CARTESIAN_POINT ( 'NONE',  ( 804.4086373105744769, -241.6454272087890729, 333.3843516231986541 ) ) ;
#40340=CARTESIAN_POINT ( 'NONE',  ( 752.7379699480933368, -180.0090635724255890, 361.9858362298580232 ) ) ;
#40342=CARTESIAN_POINT ( 'NONE',  ( 814.9108240113580450, -160.2709662947836762, 337.5031285880265273 ) ) ;
#40344=CARTESIAN_POINT ( 'NONE',  ( 799.9999999999993179, -512.9681489794448908, 329.9999999999999432 ) ) ;
#40346=CARTESIAN_POINT ( 'NONE',  ( 771.2633955100217236, -239.9073299311470748, 363.4237431249939618 ) ) ;
#40347=CARTESIAN_POINT ( 'NONE',  ( 757.0176451133909268, -13.09997266333522248, 349.9200121543848354 ) ) ;
#40352=CARTESIAN_POINT ( 'NONE',  ( 772.3691319403857278, -71.26014174441469606, 315.8894580844506663 ) ) ;
#40355=CARTESIAN_POINT ( 'NONE',  ( 800.0135310231082713, -62.08914811296580183, 325.0180583372163028 ) ) ;
#40358=CARTESIAN_POINT ( 'NONE',  ( 756.1443688327750579, -333.6237781080502600, 314.3581564841659315 ) ) ;
#40362=CARTESIAN_POINT ( 'NONE',  ( 756.3353852180819104, -341.9073299311465917, 331.1735550268788302 ) ) ;
#40371=CARTESIAN_POINT ( 'NONE',  ( 794.9819416627830151, -60.99823902205671544, 319.9864689768909898 ) ) ;
#40372=CARTESIAN_POINT ( 'NONE',  ( 802.5472867521000353, -364.3726999360614514, 350.8726784830461156 ) ) ;
#40374=CARTESIAN_POINT ( 'NONE',  ( 796.7737145352015204, -428.6346026584192259, 370.7187646348536987 ) ) ;
#40376=CARTESIAN_POINT ( 'NONE',  ( 773.7943932421234194, -311.8055962898685038, 305.5313806188329409 ) ) ;
#40377=CARTESIAN_POINT ( 'NONE',  ( 795.6651683502461765, -106.7146871989600498, 371.3240766477733814 ) ) ;
#40381=CARTESIAN_POINT ( 'NONE',  ( 754.9967657858570647, -409.5436935675101040, 365.0032342141425374 ) ) ;
#40387=CARTESIAN_POINT ( 'NONE',  ( 801.5560724626406000, -312.5545181178797520, 326.7756240680316182 ) ) ;
#40388=CARTESIAN_POINT ( 'NONE',  ( 755.5713283507202505, -173.3618753856927128, 334.6858677611754729 ) ) ;
#40392=CARTESIAN_POINT ( 'NONE',  ( 812.3518521366052028, -73.09997266333502353, 326.5853460496235243 ) ) ;
#40395=CARTESIAN_POINT ( 'NONE',  ( 805.1927285166397041, -136.8164208402382371, 341.8018195045277707 ) ) ;
#40400=CARTESIAN_POINT ( 'NONE',  ( 800.9840315886518738, -4.918154481517067467, 354.1144889064786412 ) ) ;
#40403=CARTESIAN_POINT ( 'NONE',  ( 789.9200121543843807, -409.9874144716863498, 317.0176451133914384 ) ) ;
#40405=CARTESIAN_POINT ( 'NONE',  ( 779.4709603349208464, -72.35105083532378956, 314.7162404726379918 ) ) ;
#40408=CARTESIAN_POINT ( 'NONE',  ( 773.7943932421234194, -239.8055962898687028, 305.5313806188329409 ) ) ;
#40409=CARTESIAN_POINT ( 'NONE',  ( 800.2193346964446619, -66.99823902205670834, 355.1360043628816925 ) ) ;
#40411=CARTESIAN_POINT ( 'NONE',  ( 754.8072714833581358, -244.8164208402378961, 338.1981804954720587 ) ) ;
#40414=LINE ( 'NONE', #15684, #23175 ) ;
#40417=CARTESIAN_POINT ( 'NONE',  ( 777.5031285880264704, -334.8164208402376403, 374.9108240113588408 ) ) ;
#40418=CARTESIAN_POINT ( 'NONE',  ( 791.1614460488616487, -35.26014174441480264, 373.5763878283158874 ) ) ;
#40426=CARTESIAN_POINT ( 'NONE',  ( 745.4481719005789273, -339.7255117493285184, 347.5162901302853129 ) ) ;
#40430=CARTESIAN_POINT ( 'NONE',  ( 766.9102291470427417, -186.5545181178801215, 318.6633372737382501 ) ) ;
#40431=CARTESIAN_POINT ( 'NONE',  ( 778.2165204200184689, -94.81642084023843609, 364.9363028652563230 ) ) ;
#40435=CARTESIAN_POINT ( 'NONE',  ( 755.8398074228967971, -259.4419599262322436, 333.4516893846970333 ) ) ;
#40438=CARTESIAN_POINT ( 'NONE',  ( 800.9747183278959710, -420.9982390220555999, 311.9810565676471583 ) ) ;
#40442=CARTESIAN_POINT ( 'NONE',  ( 745.0891759886404770, -52.27096629478401724, 342.4968714119734159 ) ) ;
#40443=CARTESIAN_POINT ( 'NONE',  ( 805.0032342141412300, -157.5436935675108998, 314.9967657858571783 ) ) ;
#40446=CARTESIAN_POINT ( 'NONE',  ( 815.2698199232961542, -352.8164208402374129, 342.5225473063383106 ) ) ;
#40449=CARTESIAN_POINT ( 'NONE',  ( 802.7791456095903868, 19.28531280103956647, 329.0155153010375102 ) ) ;
#40452=CARTESIAN_POINT ( 'NONE',  ( 776.2433038121456548, -132.8965053807781374, 374.8207195650711014 ) ) ;
#40453=CARTESIAN_POINT ( 'NONE',  ( 790.0183182880230106, -452.9681489794449476, 362.9048749981275250 ) ) ;
#40458=CARTESIAN_POINT ( 'NONE',  ( 800.2193346964447755, -138.9982390220563957, 355.1360043628815788 ) ) ;
#40461=CARTESIAN_POINT ( 'NONE',  ( 804.4286716492782716, -257.3618753856924286, 345.3141322388244703 ) ) ;
#40462=CARTESIAN_POINT ( 'NONE',  ( 774.6858677611749044, -249.7255117493288594, 315.5713283507209894 ) ) ;
#40465=CARTESIAN_POINT ( 'NONE',  ( 755.8398074228967971, 4.558040073766884248, 333.4516893846970333 ) ) ;
#40469=CARTESIAN_POINT ( 'NONE',  ( 763.0537975583476964, -216.4527844766016926, 371.0346526505628617 ) ) ;
#40470=CARTESIAN_POINT ( 'NONE',  ( 779.4763451958990572, -296.7363362996979390, 365.0264073115438919 ) ) ;
#40471=CARTESIAN_POINT ( 'NONE',  ( 787.6308680596127942, -395.2601417444136587, 364.1105419155492768 ) ) ;
#40472=ORIENTED_EDGE ( 'NONE', *, *, #29510, .F. ) ;
#40479=CARTESIAN_POINT ( 'NONE',  ( 780.5290396650775619, -276.3510508353231785, 365.2837595273619513 ) ) ;
#40485=CARTESIAN_POINT ( 'NONE',  ( 747.6481478633932056, -205.0999726633346256, 353.4146539503763620 ) ) ;
#40491=CARTESIAN_POINT ( 'NONE',  ( 751.9810565676468741, -50.08914811296584446, 360.9747183278973921 ) ) ;
#40495=CARTESIAN_POINT ( 'NONE',  ( 803.4237431249931660, -39.18005720387496638, 331.2633955100225194 ) ) ;
#40497=CARTESIAN_POINT ( 'NONE',  ( 757.7880784355613741, -282.0090635724253048, 312.4576283171834916 ) ) ;
#40498=CARTESIAN_POINT ( 'NONE',  ( 777.5031285880264704, -262.8164208402379245, 374.9108240113588408 ) ) ;
#40503=CARTESIAN_POINT ( 'NONE',  ( 785.3687786644884454, -347.3618753856922012, 315.3201227861279676 ) ) ;
#40504=CARTESIAN_POINT ( 'NONE',  ( 802.9823548866075953, -121.0999726633348956, 330.0799878456151077 ) ) ;
#40508=CARTESIAN_POINT ( 'NONE',  ( 797.6776695296629214, -403.5436935675101608, 357.6776695296636603 ) ) ;
#40512=CARTESIAN_POINT ( 'NONE',  ( 771.2633955100217236, -167.9073299311473022, 363.4237431249939618 ) ) ;
#40513=CARTESIAN_POINT ( 'NONE',  ( 757.8323909638828582, -170.6346026584199933, 352.1044303154654358 ) ) ;
#40517=CARTESIAN_POINT ( 'NONE',  ( 781.7834795799800531, -370.8164208402375834, 315.0636971347436202 ) ) ;
#40522=CARTESIAN_POINT ( 'NONE',  ( 796.9462024416508257, -108.4527844766020053, 308.9653473494370246 ) ) ;
#40529=CARTESIAN_POINT ( 'NONE',  ( 805.0032342141412300, -253.5436935675104735, 314.9967657858571783 ) ) ;
#40530=CARTESIAN_POINT ( 'NONE',  ( 804.9511171171677688, -173.8055962898689302, 335.8780910478229202 ) ) ;
#40537=CARTESIAN_POINT ( 'NONE',  ( 783.7953271457878373, -104.1908817542440175, 375.1787889125761239 ) ) ;
#40543=CARTESIAN_POINT ( 'NONE',  ( 791.8656671112827325, -456.3250812000245560, 367.5545208264068719 ) ) ;
#40546=CARTESIAN_POINT ( 'NONE',  ( 796.1575198192839480, -390.0090635724249069, 359.4546378042384163 ) ) ;
#40554=CARTESIAN_POINT ( 'NONE',  ( 797.8822607201568644, -174.5545181178801784, 370.1134526219340160 ) ) ;
#40556=CARTESIAN_POINT ( 'NONE',  ( 787.4397851343537695, -141.7255117493291721, 374.2001403089903988 ) ) ;
#40560=CARTESIAN_POINT ( 'NONE',  ( 794.9819416627830151, -252.9982390220560831, 319.9864689768909898 ) ) ;
#40561=CARTESIAN_POINT ( 'NONE',  ( 772.4468031744293057, -9.827245390607961539, 363.8651313633793620 ) ) ;
#40566=CARTESIAN_POINT ( 'NONE',  ( 755.0488828828309806, -89.80559628986918597, 344.1219089521771934 ) ) ;
#40570=CARTESIAN_POINT ( 'NONE',  ( 759.9864689768902508, -74.08914811296577341, 354.9819416627836404 ) ) ;
#40573=CARTESIAN_POINT ( 'NONE',  ( 815.1787889125755555, -342.8965053807773984, 343.7953271457877804 ) ) ;
#40574=ORIENTED_EDGE ( 'NONE', *, *, #2646, .F. ) ;
#40575=CARTESIAN_POINT ( 'NONE',  ( 808.7758568127978833, -436.1692326535044231, 320.0363995740631822 ) ) ;
#40577=CARTESIAN_POINT ( 'NONE',  ( 792.1044303154645831, -372.4527844766010958, 317.8323909638837677 ) ) ;
#40584=CARTESIAN_POINT ( 'NONE',  ( 785.3141322388236176, -93.72551174932934259, 364.4286716492789537 ) ) ;
#40585=CARTESIAN_POINT ( 'NONE',  ( 763.0428371773158460, -419.4636090269702891, 358.7617431975195359 ) ) ;
#40586=CARTESIAN_POINT ( 'NONE',  ( 808.0189434323515343, -446.0891481129646081, 319.0252816721025511 ) ) ;
#40587=DIRECTION ( 'NONE',  ( -0.000000000000000000, -1.110223024625155554E-15, 1.000000000000000000 ) ) ;
#40588=CARTESIAN_POINT ( 'NONE',  ( 752.4576283171824116, -333.0783235625956991, 317.7880784355627952 ) ) ;
#40589=CARTESIAN_POINT ( 'NONE',  ( 758.0141637701419768, -111.0783235625964096, 367.2620300519063790 ) ) ;
#40593=CARTESIAN_POINT ( 'NONE',  ( 755.2512626584698410, -439.5436935675101040, 315.2512626584710915 ) ) ;
#40599=CARTESIAN_POINT ( 'NONE',  ( 784.1219089521767955, -285.2817908451526137, 315.0488828828318333 ) ) ;
#40601=CARTESIAN_POINT ( 'NONE',  ( 799.9636004259356241, -262.9181544815162965, 311.2241431872006956 ) ) ;
#40604=CARTESIAN_POINT ( 'NONE',  ( 771.3260364891663130, -91.64542720878951343, 306.0683387631859773 ) ) ;
#40607=CARTESIAN_POINT ( 'NONE',  ( 804.6798772138708955, -159.7255117493291436, 334.6312213355107019 ) ) ;
#40611=CARTESIAN_POINT ( 'NONE',  ( 802.9823548866075953, -25.09997266333519050, 330.0799878456151077 ) ) ;
#40614=CARTESIAN_POINT ( 'NONE',  ( 773.3843516231979720, -421.4419599262317888, 364.4086373105754433 ) ) ;
#40616=CARTESIAN_POINT ( 'NONE',  ( 786.6156483768007774, -73.44195992623286884, 315.5913626894246136 ) ) ;
#40619=CARTESIAN_POINT ( 'NONE',  ( 751.2241431872005251, -256.1692326535049915, 359.9636004259367610 ) ) ;
#40620=CARTESIAN_POINT ( 'NONE',  ( 759.7806653035535192, -78.99823902205665149, 324.8639956371181370 ) ) ;
#40623=CARTESIAN_POINT ( 'NONE',  ( 765.0180583372156207, -240.9982390220561683, 360.0135310231089534 ) ) ;
#40629=CARTESIAN_POINT ( 'NONE',  ( 792.2312462859673587, -323.9073299311468190, 307.2067596250082602 ) ) ;
#40630=CARTESIAN_POINT ( 'NONE',  ( 788.7631598425961101, -49.44195992623295410, 305.7194118038759143 ) ) ;
#40635=CARTESIAN_POINT ( 'NONE',  ( 754.8072714833581358, -196.8164208402380950, 338.1981804954720587 ) ) ;
#40638=CARTESIAN_POINT ( 'NONE',  ( 745.0891759886404770, -340.2709662947831362, 342.4968714119734159 ) ) ;
#40640=CARTESIAN_POINT ( 'NONE',  ( 794.9298647675502707, 16.45630643248849978, 314.4833286358118016 ) ) ;
#40642=CARTESIAN_POINT ( 'NONE',  ( 755.3028492785439312, -207.2817908451527842, 335.9200461376539693 ) ) ;
#40643=CARTESIAN_POINT ( 'NONE',  ( 778.2165204200184689, -70.81642084023850714, 364.9363028652563230 ) ) ;
#40647=CARTESIAN_POINT ( 'NONE',  ( 800.7704444035546203, -244.1692326535050768, 326.0291762391768771 ) ) ;
#40650=CARTESIAN_POINT ( 'NONE',  ( 763.2262854647970016, -416.6346026584192259, 309.2812353651462445 ) ) ;
#40654=CARTESIAN_POINT ( 'NONE',  ( 782.5225473063381969, -70.27096629478397460, 375.2698199232970637 ) ) ;
#40655=CARTESIAN_POINT ( 'NONE',  ( 804.7487373415286811, -139.5436935675110135, 364.7487373415288516 ) ) ;
#40659=CARTESIAN_POINT ( 'NONE',  ( 759.0252816721024374, -360.9982390220557704, 368.0189434323527280 ) ) ;
#40661=CARTESIAN_POINT ( 'NONE',  ( 804.1601925771018387, 16.55804007376685050, 346.5483106153029098 ) ) ;
#40664=CARTESIAN_POINT ( 'NONE',  ( 744.8212110874229666, -138.8965053807781374, 336.2046728542121627 ) ) ;
#40668=CARTESIAN_POINT ( 'NONE',  ( 767.8955696845333705, -144.4527844766018632, 362.1676090361162323 ) ) ;
#40671=CARTESIAN_POINT ( 'NONE',  ( 785.3141322388236176, -285.7255117493286889, 364.4286716492789537 ) ) ;
#40672=CARTESIAN_POINT ( 'NONE',  ( 764.8639956371174549, -248.0891481129651766, 319.7806653035542581 ) ) ;
#40675=CARTESIAN_POINT ( 'NONE',  ( 799.4546378042377910, 14.92167643740321381, 356.1575198192848006 ) ) ;
#40677=ORIENTED_EDGE ( 'NONE', *, *, #44984, .F. ) ;
#40679=CARTESIAN_POINT ( 'NONE',  ( 814.9108240113580450, -208.2709662947835341, 337.5031285880265273 ) ) ;
#40680=CARTESIAN_POINT ( 'NONE',  ( 804.8461984189677878, -314.1908817542433781, 336.9566956441385628 ) ) ;
#40681=CARTESIAN_POINT ( 'NONE',  ( 757.2208543904082489, -400.7146871989590977, 350.9844846989624330 ) ) ;
#40689=CARTESIAN_POINT ( 'NONE',  ( 803.8651313633788504, -293.2601417444139429, 332.4468031744301015 ) ) ;
#40693=ORIENTED_EDGE ( 'NONE', *, *, #8906, .F. ) ;
#40696=CARTESIAN_POINT ( 'NONE',  ( 812.3518521366052028, -217.0999726633345972, 326.5853460496235243 ) ) ;
#40702=CARTESIAN_POINT ( 'NONE',  ( 808.3070685750230950, -42.99823902205675807, 361.1904061080339261 ) ) ;
#40707=CARTESIAN_POINT ( 'NONE',  ( 771.2633955100217236, -47.90732993114767169, 363.4237431249939618 ) ) ;
#40708=CARTESIAN_POINT ( 'NONE',  ( 813.5763878283155464, -315.8272453906070609, 351.1614460488615350 ) ) ;
#40709=CARTESIAN_POINT ( 'NONE',  ( 808.0189434323515343, -254.0891481129652334, 319.0252816721025511 ) ) ;
#40713=CARTESIAN_POINT ( 'NONE',  ( 797.8594530101008786, -373.5436935675101040, 322.1405469898980982 ) ) ;
#40714=CARTESIAN_POINT ( 'NONE',  ( 784.1219089521767955, -117.2817908451530684, 315.0488828828318333 ) ) ;
#40717=DIRECTION ( 'NONE',  ( -1.000000000000000000, 0.000000000000000000, 0.000000000000000000 ) ) ;
#40718=CARTESIAN_POINT ( 'NONE',  ( 788.7366044899766848, -395.9073299311465348, 316.5762568750059813 ) ) ;
#40721=EDGE_CURVE ( 'NONE', #32644, #28582, #7637, .T. ) ;
#40722=CARTESIAN_POINT ( 'NONE',  ( 774.6858677611749044, -177.7255117493290868, 315.5713283507209894 ) ) ;
#40723=CARTESIAN_POINT ( 'NONE',  ( 800.2193346964446619, -162.9982390220563673, 355.1360043628816925 ) ) ;
#40727=CARTESIAN_POINT ( 'NONE',  ( 756.5762568750052424, -363.1800572038739006, 348.7366044899774238 ) ) ;
#40731=CARTESIAN_POINT ( 'NONE',  ( 777.4774526936600978, -106.2709662947838467, 304.7301800767028226 ) ) ;
#40737=CARTESIAN_POINT ( 'NONE',  ( 792.2312462859673587, -251.9073299311470748, 307.2067596250082602 ) ) ;
#40738=CARTESIAN_POINT ( 'NONE',  ( 756.7813123517142913, -211.9874144716869750, 329.9779781133712504 ) ) ;
#40742=ORIENTED_EDGE ( 'NONE', *, *, #2102, .T. ) ;
#40747=CARTESIAN_POINT ( 'NONE',  ( 809.0717654672305343, -100.9181544815167513, 360.1688906516309885 ) ) ;
#40757=CARTESIAN_POINT ( 'NONE',  ( 773.4516893846965786, -451.6454272087884192, 315.8398074228977066 ) ) ;
#40758=AXIS2_PLACEMENT_3D ( 'NONE', #8737, #18454, #43809 ) ;
#40762=CARTESIAN_POINT ( 'NONE',  ( 800.9840315886518738, -244.9181544815162681, 354.1144889064786412 ) ) ;
#40766=CARTESIAN_POINT ( 'NONE',  ( 744.6391490659812007, -206.7363362996982801, 338.7502325331110455 ) ) ;
#40768=CARTESIAN_POINT ( 'NONE',  ( 777.4774526936600978, -154.2709662947836478, 304.7301800767027657 ) ) ;
#40771=CARTESIAN_POINT ( 'NONE',  ( 792.1044303154645831, -252.4527844766015789, 317.8323909638837677 ) ) ;
#40772=CARTESIAN_POINT ( 'NONE',  ( 769.0155153010367712, -10.37269993606250473, 362.7791456095907279 ) ) ;
#40779=CARTESIAN_POINT ( 'NONE',  ( 805.1016975059191054, -102.8965053807782368, 343.0745993439771837 ) ) ;
#40783=CARTESIAN_POINT ( 'NONE',  ( 781.7834795799800531, -58.81642084023854267, 315.0636971347436202 ) ) ;
#40786=CARTESIAN_POINT ( 'NONE',  ( 813.9316612368132837, -391.4419599262317888, 348.6739635108323228 ) ) ;
#40788=CARTESIAN_POINT ( 'NONE',  ( 745.7998596910086917, -5.361875385693257279, 332.5602148656461168 ) ) ;
#40790=CARTESIAN_POINT ( 'NONE',  ( 771.2633955100217236, -383.9073299311466485, 363.4237431249939618 ) ) ;
#40799=CARTESIAN_POINT ( 'NONE',  ( 792.1044303154645831, -84.45278447660206211, 317.8323909638837677 ) ) ;
#40800=CARTESIAN_POINT ( 'NONE',  ( 760.7433823573367135, -396.0090635724249637, 355.9930595647440441 ) ) ;
#40801=CARTESIAN_POINT ( 'NONE',  ( 746.8695393053151292, -437.9073299311464211, 327.6429770376306578 ) ) ;
#40803=CARTESIAN_POINT ( 'NONE',  ( 813.2346286133761168, -317.2601417444139429, 328.9521613784389160 ) ) ;
#40808=CARTESIAN_POINT ( 'NONE',  ( 768.9521613784389729, -9.827245390607961539, 373.2346286133773106 ) ) ;
#40810=FACE_OUTER_BOUND ( 'NONE', #20382, .T. ) ;
#40815=LINE ( 'NONE', #5468, #40018 ) ;
#40818=CARTESIAN_POINT ( 'NONE',  ( 757.4527132478984868, -328.3726999360615650, 329.1273215169538844 ) ) ;
#40819=CARTESIAN_POINT ( 'NONE',  ( 788.7366044899766848, -179.9073299311472454, 316.5762568750059813 ) ) ;
#40821=CARTESIAN_POINT ( 'NONE',  ( 764.1737431748507561, -298.3726999360616787, 371.6461892240376415 ) ) ;
#40824=CARTESIAN_POINT ( 'NONE',  ( 788.6739635108323228, -79.64542720878957027, 373.9316612368139090 ) ) ;
#40827=CARTESIAN_POINT ( 'NONE',  ( 800.0135310231082713, -158.0891481129655176, 325.0180583372163028 ) ) ;
#40833=CARTESIAN_POINT ( 'NONE',  ( 759.0159684113467620, -40.91815448151695023, 325.8855110935213020 ) ) ;
#40836=CARTESIAN_POINT ( 'NONE',  ( 754.9735926884551418, -426.3510508353226669, 340.5236548041000333 ) ) ;
#40840=CARTESIAN_POINT ( 'NONE',  ( 781.2497674668890113, -276.3510508353231785, 375.3608509340180603 ) ) ;
#40841=CARTESIAN_POINT ( 'NONE',  ( 774.6312213355098493, -71.36187538569303968, 364.6798772138717482 ) ) ;
#40844=CARTESIAN_POINT ( 'NONE',  ( 788.8264449731200330, -285.1800572038740711, 363.6646147819171233 ) ) ;
#40851=CARTESIAN_POINT ( 'NONE',  ( 794.9819416627830151, -300.9982390220559409, 319.9864689768909898 ) ) ;
#40852=CARTESIAN_POINT ( 'NONE',  ( 763.2262854647970016, -320.6346026584195670, 309.2812353651462445 ) ) ;
#40853=CARTESIAN_POINT ( 'NONE',  ( 786.2056067578752163, -203.8055962898688449, 374.4686193811670023 ) ) ;
#40854=CARTESIAN_POINT ( 'NONE',  ( 810.1134526219336749, -32.53286901714208312, 357.8822607201570349 ) ) ;
#40860=EDGE_LOOP ( 'NONE', ( #37607, #21538, #27220, #5732 ) ) ;
#40861=CARTESIAN_POINT ( 'NONE',  ( 801.9419747391806368, -210.4527844766016926, 351.9812246680014027 ) ) ;
#40864=CARTESIAN_POINT ( 'NONE',  ( 805.0032342141412300, -373.5436935675101040, 314.9967657858571783 ) ) ;
#40868=CARTESIAN_POINT ( 'NONE',  ( 780.5236548040995785, -188.7363362996983085, 314.9735926884559944 ) ) ;
#40869=CARTESIAN_POINT ( 'NONE',  ( 781.8018195045266339, -70.27096629478397460, 365.1927285166406705 ) ) ;
#40873=CARTESIAN_POINT ( 'NONE',  ( 803.2186876482843445, -271.9874144716868045, 350.0220218866286928 ) ) ;
#40877=CARTESIAN_POINT ( 'NONE',  ( 808.0189434323515343, -446.0891481129646081, 319.0252816721025511 ) ) ;
#40881=CARTESIAN_POINT ( 'NONE',  ( 792.3570229623688874, -93.18005720387481006, 373.1304606946836202 ) ) ;
#40882=CARTESIAN_POINT ( 'NONE',  ( 787.5162901302840055, -155.3618753856927128, 305.4481719005792684 ) ) ;
#40884=LINE ( 'NONE', #37422, #22482 ) ;
#40887=CARTESIAN_POINT ( 'NONE',  ( 772.5602148656447525, -393.7255117493283478, 305.7998596910095443 ) ) ;
#40888=CARTESIAN_POINT ( 'NONE',  ( 745.4481719005789273, -27.72551174932954510, 347.5162901302853697 ) ) ;
#40890=CARTESIAN_POINT ( 'NONE',  ( 758.6633372737375112, 3.467130982857797417, 326.9102291470432533 ) ) ;
#40893=CARTESIAN_POINT ( 'NONE',  ( 807.5423716828161105, -153.0783235625962675, 362.2119215644372048 ) ) ;
#40898=CARTESIAN_POINT ( 'NONE',  ( 755.3201227861273992, -171.7255117493291152, 345.3687786644892981 ) ) ;
#40900=CARTESIAN_POINT ( 'NONE',  ( 795.1360043628808398, -308.0891481129650629, 360.2193346964456282 ) ) ;
#40903=CARTESIAN_POINT ( 'NONE',  ( 796.7845633553578182, -33.62377810805116951, 358.5707757039688204 ) ) ;
#40909=CARTESIAN_POINT ( 'NONE',  ( 804.7487373415286811, -211.5436935675107861, 364.7487373415288516 ) ) ;
#40910=CARTESIAN_POINT ( 'NONE',  ( 804.1105419155481968, -291.8272453906071746, 347.6308680596136469 ) ) ;
#40911=CARTESIAN_POINT ( 'NONE',  ( 800.7704444035546203, -412.1692326535045936, 326.0291762391768771 ) ) ;
#40919=CARTESIAN_POINT ( 'NONE',  ( 765.8855110935204493, -286.1692326535048778, 319.0159684113471599 ) ) ;
#40920=CARTESIAN_POINT ( 'NONE',  ( 792.5472707286114655, -457.8762024727506628, 368.6839859091244307 ) ) ;
#40923=ORIENTED_EDGE ( 'NONE', *, *, #19257, .F. ) ;
#40926=CARTESIAN_POINT ( 'NONE',  ( 773.7305795820266212, -201.2817908451528126, 374.8230680027170365 ) ) ;
#40929=DIRECTION ( 'NONE',  ( 0.000000000000000000, 0.000000000000000000, 1.000000000000000000 ) ) ;
#40931=CARTESIAN_POINT ( 'NONE',  ( 747.2067596250078623, -51.18005720387493085, 352.2312462859687230 ) ) ;
#40934=DIRECTION ( 'NONE',  ( -0.000000000000000000, 1.000000000000000000, -0.000000000000000000 ) ) ;
#40935=CARTESIAN_POINT ( 'NONE',  ( 797.8594530101008786, -61.54369356751124087, 322.1405469898980982 ) ) ;
#40936=CIRCLE ( 'NONE', #11442, 10.00000000000000888 ) ;
#40937=CARTESIAN_POINT ( 'NONE',  ( 748.6759233522253680, -328.3726999360615650, 324.3348316497537098 ) ) ;
#40938=CARTESIAN_POINT ( 'NONE',  ( 800.9747183278959710, -276.9982390220559978, 311.9810565676471583 ) ) ;
#40944=CARTESIAN_POINT ( 'NONE',  ( 800.0135310231082713, -374.0891481129647786, 325.0180583372163028 ) ) ;
#40945=CARTESIAN_POINT ( 'NONE',  ( 786.5483106153019435, -103.6454272087894850, 364.1601925771022366 ) ) ;
#40947=CARTESIAN_POINT ( 'NONE',  ( 795.6651683502461765, -34.71468719896025590, 371.3240766477733814 ) ) ;
#40948=CARTESIAN_POINT ( 'NONE',  ( 778.1981804954715471, -370.2709662947830793, 314.8072714833591021 ) ) ;
#40951=CARTESIAN_POINT ( 'NONE',  ( 793.4146539503750546, -145.9874144716871740, 307.6481478633938877 ) ) ;
#40952=CARTESIAN_POINT ( 'NONE',  ( 785.3141322388236176, -381.7255117493284615, 364.4286716492789537 ) ) ;
#40956=CARTESIAN_POINT ( 'NONE',  ( 762.3223304703356007, -199.5436935675108430, 322.3223304703362828 ) ) ;
#40957=CARTESIAN_POINT ( 'NONE',  ( 756.5762568750052424, -195.1800572038744974, 348.7366044899774238 ) ) ;
#40961=CARTESIAN_POINT ( 'NONE',  ( 800.0135310231082713, -374.0891481129647786, 325.0180583372163028 ) ) ;
#40962=AXIS2_PLACEMENT_3D ( 'NONE', #7075, #10300, #17705 ) ;
#40966=CARTESIAN_POINT ( 'NONE',  ( 782.4968714119720516, -130.8164208402383224, 305.0891759886411023 ) ) ;
#40972=AXIS2_PLACEMENT_3D ( 'NONE', #21359, #35435, #32448 ) ;
#40973=CARTESIAN_POINT ( 'NONE',  ( 759.0252816721024374, -240.9982390220561683, 368.0189434323527280 ) ) ;
#40974=CARTESIAN_POINT ( 'NONE',  ( 789.9200121543843807, -193.9874144716870319, 317.0176451133914384 ) ) ;
#40975=DIRECTION ( 'NONE',  ( 0.9164815115825537539, 0.1263042864341373805, -0.3796167358741193709 ) ) ;
#40986=CARTESIAN_POINT ( 'NONE',  ( 745.5313806188320314, -87.28179084515316788, 333.7943932421247268 ) ) ;
#40994=CARTESIAN_POINT ( 'NONE',  ( 763.0428371773158460, -419.4636090269702891, 358.7617431975195359 ) ) ;
#41002=CIRCLE ( 'NONE', #31431, 20.00000000000001776 ) ;
#41003=CARTESIAN_POINT ( 'NONE',  ( 745.7194118038753459, -205.6454272087891297, 348.7631598425976449 ) ) ;
#41005=CARTESIAN_POINT ( 'NONE',  ( 792.2312462859673587, -155.9073299311473306, 307.2067596250082602 ) ) ;
#41008=CARTESIAN_POINT ( 'NONE',  ( 762.1405469898971887, -265.5436935675106156, 357.8594530101015607 ) ) ;
#41009=CARTESIAN_POINT ( 'NONE',  ( 804.8461984189677878, -50.19088175424420939, 336.9566956441385628 ) ) ;
#41012=CARTESIAN_POINT ( 'NONE',  ( 790.0183182880230106, -452.9681489794449476, 362.9048749981275250 ) ) ;
#41014=CARTESIAN_POINT ( 'NONE',  ( 783.0433043558608688, -96.89650538077825104, 315.1538015810313027 ) ) ;
#41019=CARTESIAN_POINT ( 'NONE',  ( 778.1981804954714335, -58.27096629478398171, 314.8072714833589885 ) ) ;
#41022=CARTESIAN_POINT ( 'NONE',  ( 746.0683387631852383, -379.4419599262318457, 331.3260364891676204 ) ) ;
#41025=CARTESIAN_POINT ( 'NONE',  ( 785.3687786644884454, -371.3618753856919739, 315.3201227861279676 ) ) ;
#41032=CARTESIAN_POINT ( 'NONE',  ( 755.5713283507202505, -101.3618753856929544, 334.6858677611754729 ) ) ;
#41033=CARTESIAN_POINT ( 'NONE',  ( 798.5707757039680246, -413.4636090269704027, 356.7845633553585003 ) ) ;
#41034=CARTESIAN_POINT ( 'NONE',  ( 763.2154366446407039, -93.62377810805098477, 321.4292242960311228 ) ) ;
#41035=CARTESIAN_POINT ( 'NONE',  ( 796.9462024416508257, -444.4527844766009821, 308.9653473494370246 ) ) ;
#41036=CARTESIAN_POINT ( 'NONE',  ( 772.4999999999993179, -462.9681489794447202, 270.0000000000000568 ) ) ;
#41037=CARTESIAN_POINT ( 'NONE',  ( 768.8385539511368734, -359.2601417444137724, 306.4236121716840557 ) ) ;
#41042=CARTESIAN_POINT ( 'NONE',  ( 808.0189434323515343, -446.0891481129646081, 319.0252816721025511 ) ) ;
#41046=ADVANCED_FACE ( 'NONE', ( #38325 ), #2280, .T. ) ;
#41048=CARTESIAN_POINT ( 'NONE',  ( 789.8657795001898876, -452.9681489794449476, 362.9715936389367812 ) ) ;
#41051=CARTESIAN_POINT ( 'NONE',  ( 763.0428371773158460, -323.4636090269706301, 358.7617431975195359 ) ) ;
#41052=CARTESIAN_POINT ( 'NONE',  ( 765.0180583372156207, -192.9982390220562820, 360.0135310231089534 ) ) ;
#41054=CARTESIAN_POINT ( 'NONE',  ( 786.2694204179717872, -309.2817908451525568, 305.1769319972829067 ) ) ;
#41057=CARTESIAN_POINT ( 'NONE',  ( 766.4474001241216001, -115.0999726633348956, 307.3154664389482491 ) ) ;
#41060=CARTESIAN_POINT ( 'NONE',  ( 794.9819416627830151, -156.9982390220564241, 319.9864689768909898 ) ) ;
#41062=CARTESIAN_POINT ( 'NONE',  ( 752.7379699480933368, -420.0090635724249069, 361.9858362298580232 ) ) ;
#41066=CARTESIAN_POINT ( 'NONE',  ( 757.0176451133909268, -37.09997266333514432, 349.9200121543848354 ) ) ;
#41068=DIRECTION ( 'NONE',  ( 0.000000000000000000, 0.000000000000000000, 1.000000000000000000 ) ) ;
#41069=CARTESIAN_POINT ( 'NONE',  ( 756.1443688327750579, 26.37622189194863509, 314.3581564841659315 ) ) ;
#41071=ORIENTED_EDGE ( 'NONE', *, *, #44198, .F. ) ;
#41075=AXIS2_PLACEMENT_3D ( 'NONE', #23693, #26270, #12862 ) ;
#41078=CARTESIAN_POINT ( 'NONE',  ( 746.7653713866222915, -281.2601417444139997, 351.0478386215610271 ) ) ;
#41079=CARTESIAN_POINT ( 'NONE',  ( 768.0187753319979720, -80.63460265842029173, 318.0580252608186242 ) ) ;
#41080=ORIENTED_EDGE ( 'NONE', *, *, #28951, .F. ) ;
#41083=CARTESIAN_POINT ( 'NONE',  ( 804.6798772138708955, -255.7255117493287742, 334.6312213355107019 ) ) ;
#41085=ADVANCED_FACE ( 'NONE', ( #12920 ), #41106, .F. ) ;
#41091=CARTESIAN_POINT ( 'NONE',  ( 804.7487373415286811, -331.5436935675104451, 364.7487373415288516 ) ) ;
#41092=CARTESIAN_POINT ( 'NONE',  ( 815.0009284576459549, -222.3510508353233206, 338.7629533639073429 ) ) ;
#41097=CARTESIAN_POINT ( 'NONE',  ( 755.5713283507202505, -221.3618753856925707, 334.6858677611754729 ) ) ;
#41100=VECTOR ( 'NONE', #6904, 1000.000000000000000 ) ;
#41101=CARTESIAN_POINT ( 'NONE',  ( 796.7737145352015204, -356.6346026584193964, 370.7187646348536987 ) ) ;
#41106=PLANE ( 'NONE',  #22381 ) ;
#41107=CARTESIAN_POINT ( 'NONE',  ( 793.9708237608222134, -214.9181544815164386, 319.2295555964448681 ) ) ;
#41108=CARTESIAN_POINT ( 'NONE',  ( 803.4237431249931660, -87.18005720387481006, 331.2633955100225194 ) ) ;
#41112=CARTESIAN_POINT ( 'NONE',  ( 798.7617431975189675, -243.6237781080504590, 323.0428371773161871 ) ) ;
#41116=CARTESIAN_POINT ( 'NONE',  ( 815.3608509340175488, -2.736336299698892027, 341.2497674668889545 ) ) ;
#41121=CARTESIAN_POINT ( 'NONE',  ( 777.5031285880264704, -94.81642084023843609, 374.9108240113588408 ) ) ;
#41122=CARTESIAN_POINT ( 'NONE',  ( 763.0537975583475827, -144.4527844766018632, 371.0346526505627480 ) ) ;
#41126=CARTESIAN_POINT ( 'NONE',  ( 771.3260364891663130, -427.6454272087885897, 306.0683387631859773 ) ) ;
#41129=CARTESIAN_POINT ( 'NONE',  ( 747.2067596250078623, -387.1800572038738437, 352.2312462859687230 ) ) ;
#41130=CARTESIAN_POINT ( 'NONE',  ( 745.4481719005789273, -3.725511749329622813, 347.5162901302853697 ) ) ;
#41133=CARTESIAN_POINT ( 'NONE',  ( 779.4709603349208464, -24.35105083532392811, 314.7162404726379918 ) ) ;
#41136=CARTESIAN_POINT ( 'NONE',  ( 754.0944755984390895, -159.6237781080508285, 364.1009440267246760 ) ) ;
#41137=CARTESIAN_POINT ( 'NONE',  ( 788.7366044899766848, 12.09267006885214180, 316.5762568750059813 ) ) ;
#41138=VERTEX_POINT ( 'NONE', #27688 ) ;
#41141=CARTESIAN_POINT ( 'NONE',  ( 803.6646147819161570, -161.9073299311472454, 348.8264449731210561 ) ) ;
#41143=CARTESIAN_POINT ( 'NONE',  ( 755.0636971347428243, -292.2709662947831930, 341.7834795799807353 ) ) ;
#41144=CARTESIAN_POINT ( 'NONE',  ( 800.2193346964446619, -282.9982390220559409, 355.1360043628816925 ) ) ;
#41147=CARTESIAN_POINT ( 'NONE',  ( 765.8855110935204493, -22.16923265350575889, 319.0159684113471599 ) ) ;
#41152=CARTESIAN_POINT ( 'NONE',  ( 810.7187646348534145, -210.4527844766016926, 356.7737145352016341 ) ) ;
#41153=CARTESIAN_POINT ( 'NONE',  ( 790.0220218866281812, -295.0999726633343698, 363.2186876482849129 ) ) ;
#41154=CARTESIAN_POINT ( 'NONE',  ( 764.3348316497523456, 25.28531280103955226, 308.6759233522265617 ) ) ;
#41161=CARTESIAN_POINT ( 'NONE',  ( 789.9200121543843807, -313.9874144716866908, 317.0176451133914384 ) ) ;
#41164=CARTESIAN_POINT ( 'NONE',  ( 800.9840315886518738, -124.9181544815167086, 354.1144889064786412 ) ) ;
#41168=CARTESIAN_POINT ( 'NONE',  ( 764.1737431748507561, -202.3726999360618777, 371.6461892240376415 ) ) ;
#41171=CARTESIAN_POINT ( 'NONE',  ( 777.4774526936600978, -34.27096629478407408, 304.7301800767027657 ) ) ;
#41175=CARTESIAN_POINT ( 'NONE',  ( 799.9636004259356241, -334.9181544815160692, 311.2241431872006956 ) ) ;
#41177=CARTESIAN_POINT ( 'NONE',  ( 758.8095938919642549, -296.0891481129650629, 311.6929314249763365 ) ) ;
#41181=CARTESIAN_POINT ( 'NONE',  ( 756.3353852180819104, -389.9073299311465348, 331.1735550268788302 ) ) ;
#41182=CARTESIAN_POINT ( 'NONE',  ( 769.9779781133707957, -115.0999726633348956, 316.7813123517150871 ) ) ;
#41184=CARTESIAN_POINT ( 'NONE',  ( 766.5853460496234675, -61.98741447168745822, 372.3518521366060554 ) ) ;
#41185=CARTESIAN_POINT ( 'NONE',  ( 762.1405469898973024, -361.5436935675103882, 357.8594530101016176 ) ) ;
#41186=CARTESIAN_POINT ( 'NONE',  ( 814.9108240113580450, 7.729033705215793582, 337.5031285880265273 ) ) ;
#41188=CARTESIAN_POINT ( 'NONE',  ( 764.3348316497523456, -142.7146871989599219, 308.6759233522265617 ) ) ;
#41189=CARTESIAN_POINT ( 'NONE',  ( 794.9819416627830151, -444.9982390220554862, 319.9864689768909898 ) ) ;
#41193=CARTESIAN_POINT ( 'NONE',  ( 795.1360043628807261, -188.0891481129653187, 360.2193346964456282 ) ) ;
#41194=CARTESIAN_POINT ( 'NONE',  ( 781.7834795799800531, -202.8164208402380950, 315.0636971347436202 ) ) ;
#41198=CARTESIAN_POINT ( 'NONE',  ( 785.3141322388236176, -381.7255117493284615, 364.4286716492789537 ) ) ;
#41201=CARTESIAN_POINT ( 'NONE',  ( 787.4397851343537695, -117.7255117493292715, 374.2001403089903988 ) ) ;
#41208=CARTESIAN_POINT ( 'NONE',  ( 745.7998596910086917, -269.3618753856924286, 332.5602148656461168 ) ) ;
#41209=CARTESIAN_POINT ( 'NONE',  ( 794.1144889064781864, -178.1692326535052473, 360.9840315886528401 ) ) ;
#41218=CARTESIAN_POINT ( 'NONE',  ( 768.9521613784389729, -105.8272453906076578, 373.2346286133773106 ) ) ;
#41226=CARTESIAN_POINT ( 'NONE',  ( 763.8424801807145741, -426.0090635724247932, 320.5453621957614700 ) ) ;
#41232=CARTESIAN_POINT ( 'NONE',  ( 766.4474001241216001, -211.0999726633346540, 307.3154664389482491 ) ) ;
#41234=CARTESIAN_POINT ( 'NONE',  ( 804.7487373415286811, -187.5436935675108430, 364.7487373415288516 ) ) ;
#41237=CARTESIAN_POINT ( 'NONE',  ( 785.3141322388236176, -261.7255117493288026, 364.4286716492789537 ) ) ;
#41239=CARTESIAN_POINT ( 'NONE',  ( 801.5560724626406000, -48.55451811788057626, 326.7756240680316182 ) ) ;
#41244=CARTESIAN_POINT ( 'NONE',  ( 759.2295555964440155, -88.16923265350555994, 353.9708237608231229 ) ) ;
#41245=CARTESIAN_POINT ( 'NONE',  ( 754.8072714833581358, -340.8164208402376971, 338.1981804954720587 ) ) ;
#41248=CARTESIAN_POINT ( 'NONE',  ( 757.8323909638827445, -74.63460265842032015, 352.1044303154654358 ) ) ;
#41251=CARTESIAN_POINT ( 'NONE',  ( 793.4146539503750546, -385.9874144716864066, 307.6481478633938877 ) ) ;
#41252=ORIENTED_EDGE ( 'NONE', *, *, #20953, .T. ) ;
#41253=CARTESIAN_POINT ( 'NONE',  ( 805.1927285166397041, -304.8164208402376403, 341.8018195045277707 ) ) ;
#41254=CARTESIAN_POINT ( 'NONE',  ( 787.5162901302840055, 12.63812461430668321, 305.4481719005792684 ) ) ;
#41257=CARTESIAN_POINT ( 'NONE',  ( 785.3141322388236176, -381.7255117493284615, 364.4286716492789537 ) ) ;
#41263=CARTESIAN_POINT ( 'NONE',  ( 756.3353852180819104, -101.9073299311474727, 331.1735550268788302 ) ) ;
#41264=CARTESIAN_POINT ( 'NONE',  ( 755.5913626894240451, -421.6454272087885329, 346.6156483768012890 ) ) ;
#41265=CARTESIAN_POINT ( 'NONE',  ( 804.1601925771018387, -103.4419599262327836, 346.5483106153029098 ) ) ;
#41267=FACE_OUTER_BOUND ( 'NONE', #11965, .T. ) ;
#41268=CARTESIAN_POINT ( 'NONE',  ( 808.7758568127978833, -340.1692326535047641, 320.0363995740631822 ) ) ;
#41274=CARTESIAN_POINT ( 'NONE',  ( 813.1304606946830518, -449.9073299311463643, 352.3570229623690580 ) ) ;
#41281=CARTESIAN_POINT ( 'NONE',  ( 793.0897708529556667, -342.5545181178796952, 361.3366627262616362 ) ) ;
#41283=CARTESIAN_POINT ( 'NONE',  ( 760.0363995740630116, -298.9181544815161828, 368.7758568127991907 ) ) ;
#41287=CARTESIAN_POINT ( 'NONE',  ( 744.6391490659812007, -110.7363362996985501, 338.7502325331110455 ) ) ;
#41289=ADVANCED_FACE ( 'NONE', ( #7594 ), #434, .F. ) ;
#41292=CARTESIAN_POINT ( 'NONE',  ( 803.4237431249931660, -135.1800572038746679, 331.2633955100225194 ) ) ;
#41295=CARTESIAN_POINT ( 'NONE',  ( 807.2620300519052989, -432.0090635724247932, 318.0141637701419768 ) ) ;
#41298=CARTESIAN_POINT ( 'NONE',  ( 760.7433823573367135, -36.00906357242605793, 355.9930595647440441 ) ) ;
#41301=CARTESIAN_POINT ( 'NONE',  ( 796.7845633553578182, -417.6237781080499190, 358.5707757039688204 ) ) ;
#41303=CARTESIAN_POINT ( 'NONE',  ( 774.6312213355099630, -263.3618753856924855, 364.6798772138717482 ) ) ;
#41306=CARTESIAN_POINT ( 'NONE',  ( 798.0661480581538854, -266.5328690171413655, 309.5768839229118043 ) ) ;
#41307=CARTESIAN_POINT ( 'NONE',  ( 759.9864689768902508, -98.08914811296568814, 354.9819416627836404 ) ) ;
#41308=ORIENTED_EDGE ( 'NONE', *, *, #39488, .F. ) ;
#41310=CARTESIAN_POINT ( 'NONE',  ( 781.8018195045266339, -262.2709662947831930, 365.1927285166406705 ) ) ;
#41318=CARTESIAN_POINT ( 'NONE',  ( 758.8095938919644823, -344.0891481129648355, 311.6929314249762797 ) ) ;
#41319=CARTESIAN_POINT ( 'NONE',  ( 749.8865473780648472, -260.5328690171413086, 322.1177392798429082 ) ) ;
#41323=CARTESIAN_POINT ( 'NONE',  ( 788.8264449731200330, -261.1800572038741848, 363.6646147819171233 ) ) ;
#41325=CARTESIAN_POINT ( 'NONE',  ( 755.2512626584698410, -367.5436935675102745, 315.2512626584710915 ) ) ;
#41331=CARTESIAN_POINT ( 'NONE',  ( 784.1219089521767955, -213.2817908451527842, 315.0488828828318333 ) ) ;
#41332=CARTESIAN_POINT ( 'NONE',  ( 801.9419747391806368, -90.45278447660209054, 351.9812246680014027 ) ) ;
#41335=CARTESIAN_POINT ( 'NONE',  ( 765.8855110935204493, -262.1692326535049347, 319.0159684113471599 ) ) ;
#41338=CARTESIAN_POINT ( 'NONE',  ( 748.6759233522253680, -16.37269993606248519, 324.3348316497537098 ) ) ;
#41343=CARTESIAN_POINT ( 'NONE',  ( 745.0891759886404770, -100.2709662947838609, 342.4968714119734159 ) ) ;
#41344=CARTESIAN_POINT ( 'NONE',  ( 812.7932403749906598, -135.1800572038746679, 327.7687537140311633 ) ) ;
#41346=DIRECTION ( 'NONE',  ( 0.000000000000000000, 1.000000000000000000, 0.000000000000000000 ) ) ;
#41348=CARTESIAN_POINT ( 'NONE',  ( 766.4474001241216001, -427.0999726633338582, 307.3154664389482491 ) ) ;
#41351=CARTESIAN_POINT ( 'NONE',  ( 777.5031285880264704, -382.8164208402374697, 374.9108240113588408 ) ) ;
#41352=CARTESIAN_POINT ( 'NONE',  ( 805.0032342141413437, -13.54369356751140963, 314.9967657858572352 ) ) ;
#41354=CARTESIAN_POINT ( 'NONE',  ( 789.9200121543843807, -1.987414471687640294, 317.0176451133914384 ) ) ;
#41358=CARTESIAN_POINT ( 'NONE',  ( 781.2497674668890113, -180.3510508353234343, 375.3608509340180603 ) ) ;
#41359=DIRECTION ( 'NONE',  ( 0.000000000000000000, 0.000000000000000000, 1.000000000000000000 ) ) ;
#41360=ADVANCED_FACE ( 'NONE', ( #45487 ), #21221, .T. ) ;
#41361=CARTESIAN_POINT ( 'NONE',  ( 781.2497674668890113, -180.3510508353234343, 375.3608509340180603 ) ) ;
#41366=CARTESIAN_POINT ( 'NONE',  ( 788.7366044899766848, -155.9073299311473306, 316.5762568750059813 ) ) ;
#41368=CARTESIAN_POINT ( 'NONE',  ( 767.8955696845333705, -288.4527844766014937, 362.1676090361162323 ) ) ;
#41369=CARTESIAN_POINT ( 'NONE',  ( 804.9363028652555840, -304.2709662947832499, 338.2165204200192079 ) ) ;
#41372=CARTESIAN_POINT ( 'NONE',  ( 795.9930595647434757, -27.07832356259665474, 320.7433823573372820 ) ) ;
#41375=CARTESIAN_POINT ( 'NONE',  ( 758.8095938919644823, -224.0891481129652902, 311.6929314249762797 ) ) ;
#41376=CARTESIAN_POINT ( 'NONE',  ( 784.1219089521767955, -333.2817908451523863, 315.0488828828318333 ) ) ;
#41377=CARTESIAN_POINT ( 'NONE',  ( 776.9566956441375396, -420.8965053807772279, 364.8461984189686405 ) ) ;
#41384=CARTESIAN_POINT ( 'NONE',  ( 766.7756240680305382, -302.5328690171411949, 361.5560724626415663 ) ) ;
#41387=CARTESIAN_POINT ( 'NONE',  ( 780.5236548040995785, -116.7363362996985217, 314.9735926884559944 ) ) ;
#41388=FACE_OUTER_BOUND ( 'NONE', #5183, .T. ) ;
#41391=CARTESIAN_POINT ( 'NONE',  ( 802.2119215644370342, -198.0090635724255606, 367.5423716828165084 ) ) ;
#41393=CARTESIAN_POINT ( 'NONE',  ( 779.9999999999992042, 16.45630643248849267, 370.0000000000000568 ) ) ;
#41396=CARTESIAN_POINT ( 'NONE',  ( 749.2812353651451076, -54.45278447660219001, 323.2262854647983090 ) ) ;
#41397=CARTESIAN_POINT ( 'NONE',  ( 808.7373736539768743, -452.9681489794446065, 336.0792598452978268 ) ) ;
#41400=CARTESIAN_POINT ( 'NONE',  ( 771.3260364891663130, -307.6454272087888171, 306.0683387631859773 ) ) ;
#41402=CARTESIAN_POINT ( 'NONE',  ( 813.1304606946830518, -305.9073299311467622, 352.3570229623690580 ) ) ;
#41406=CARTESIAN_POINT ( 'NONE',  ( 803.6646147819161570, -401.9073299311463643, 348.8264449731210561 ) ) ;
#41407=CARTESIAN_POINT ( 'NONE',  ( 800.9840315886518738, -172.9181544815165239, 354.1144889064786412 ) ) ;
#41409=CARTESIAN_POINT ( 'NONE',  ( 808.7758568127978833, -52.16923265350567362, 320.0363995740631822 ) ) ;
#41410=CARTESIAN_POINT ( 'NONE',  ( 801.9419747391806368, -378.4527844766011526, 351.9812246680014027 ) ) ;
#41412=CARTESIAN_POINT ( 'NONE',  ( 745.1769319972822814, -137.8055962898690154, 346.2694204179732083 ) ) ;
#41413=CARTESIAN_POINT ( 'NONE',  ( 785.3687786644884454, -443.3618753856917465, 315.3201227861279676 ) ) ;
#41417=CARTESIAN_POINT ( 'NONE',  ( 792.1044303154645831, -204.4527844766016926, 317.8323909638837677 ) ) ;
#41418=CARTESIAN_POINT ( 'NONE',  ( 768.0187753319979720, -176.6346026584199933, 318.0580252608186242 ) ) ;
#41422=CARTESIAN_POINT ( 'NONE',  ( 797.8594530101008786, -397.5436935675100472, 322.1405469898980982 ) ) ;
#41426=CARTESIAN_POINT ( 'NONE',  ( 744.7301800767020268, -100.8164208402383935, 337.4774526936615189 ) ) ;
#41432=CARTESIAN_POINT ( 'NONE',  ( 784.0799538623451781, -203.8055962898688449, 364.6971507214555572 ) ) ;
#41434=DIRECTION ( 'NONE',  ( 0.000000000000000000, 0.000000000000000000, 1.000000000000000000 ) ) ;
#41435=CARTESIAN_POINT ( 'NONE',  ( 779.9999999999992042, -452.9681489794448339, 339.9999999999999432 ) ) ;
#41442=CARTESIAN_POINT ( 'NONE',  ( 778.7629533639073998, -104.7363362996985785, 375.0009284576466371 ) ) ;
#41450=CARTESIAN_POINT ( 'NONE',  ( 757.4527132478984868, -448.3726999360611103, 329.1273215169538844 ) ) ;
#41451=CARTESIAN_POINT ( 'NONE',  ( 802.2119215644370342, -366.0090635724250774, 367.5423716828165084 ) ) ;
#41457=CARTESIAN_POINT ( 'NONE',  ( 760.0363995740630116, -226.9181544815163534, 368.7758568127991907 ) ) ;
#41459=CARTESIAN_POINT ( 'NONE',  ( 813.1304606946830518, -185.9073299311472454, 352.3570229623690580 ) ) ;
#41462=CARTESIAN_POINT ( 'NONE',  ( 757.8323909638827445, -290.6346026584195101, 352.1044303154654358 ) ) ;
#41463=CARTESIAN_POINT ( 'NONE',  ( 766.9102291470427417, -42.55451811788057626, 318.6633372737382501 ) ) ;
#41467=CARTESIAN_POINT ( 'NONE',  ( 764.0069404352550464, -111.0783235625964096, 359.2566176426627180 ) ) ;
#41468=CARTESIAN_POINT ( 'NONE',  ( 767.8955696845333705, -336.4527844766012095, 362.1676090361162323 ) ) ;
#41472=CARTESIAN_POINT ( 'NONE',  ( 804.6798772138708955, -111.7255117493293000, 334.6312213355107019 ) ) ;
#41476=CARTESIAN_POINT ( 'NONE',  ( 805.9055244015594326, -387.6237781080499758, 315.8990559732753240 ) ) ;
#41478=CARTESIAN_POINT ( 'NONE',  ( 768.0187753319979720, -272.6346026584196807, 318.0580252608186242 ) ) ;
#41481=CARTESIAN_POINT ( 'NONE',  ( 755.3201227861273992, -363.7255117493284047, 345.3687786644892981 ) ) ;
#41487=CARTESIAN_POINT ( 'NONE',  ( 788.8264449731200330, -117.1800572038746964, 363.6646147819171233 ) ) ;
#41488=CARTESIAN_POINT ( 'NONE',  ( 755.1538015810308480, -422.1908817542430370, 343.0433043558613804 ) ) ;
#41490=PLANE ( 'NONE',  #18859 ) ;
#41491=CARTESIAN_POINT ( 'NONE',  ( 807.5423716828161105, -345.0783235625956991, 362.2119215644372048 ) ) ;
#41492=CARTESIAN_POINT ( 'NONE',  ( 793.4146539503750546, -121.9874144716872593, 307.6481478633938877 ) ) ;
#41498=CARTESIAN_POINT ( 'NONE',  ( 762.1177392798416577, 5.445481882119263872, 309.8865473780659272 ) ) ;
#41505=CARTESIAN_POINT ( 'NONE',  ( 755.8894580844503253, -327.8272453906069472, 332.3691319403863531 ) ) ;
#41506=ORIENTED_EDGE ( 'NONE', *, *, #15427, .T. ) ;
#41507=CARTESIAN_POINT ( 'NONE',  ( 810.4231160770870019, -312.5545181178797520, 321.9338519418446936 ) ) ;
#41511=CARTESIAN_POINT ( 'NONE',  ( 776.2046728542105711, -116.1908817542440033, 304.8212110874238761 ) ) ;
#41515=CARTESIAN_POINT ( 'NONE',  ( 765.0180583372156207, -168.9982390220563673, 360.0135310231089534 ) ) ;
#41516=ORIENTED_EDGE ( 'NONE', *, *, #17132, .T. ) ;
#41517=CARTESIAN_POINT ( 'NONE',  ( 809.0717654672305343, -436.9181544815157281, 360.1688906516309885 ) ) ;
#41520=CARTESIAN_POINT ( 'NONE',  ( 755.5913626894240451, -37.64542720878968396, 346.6156483768012890 ) ) ;
#41523=CARTESIAN_POINT ( 'NONE',  ( 765.8855110935204493, -430.1692326535043094, 319.0159684113471599 ) ) ;
#41527=CARTESIAN_POINT ( 'NONE',  ( 745.1769319972822814, -281.8055962898686175, 346.2694204179732083 ) ) ;
#41528=CARTESIAN_POINT ( 'NONE',  ( 757.8323909638828582, -98.63460265842023489, 352.1044303154654358 ) ) ;
#41531=CARTESIAN_POINT ( 'NONE',  ( 801.9419747391806368, -282.4527844766014937, 351.9812246680014027 ) ) ;
#41533=CARTESIAN_POINT ( 'NONE',  ( 799.9999999999993179, -512.9681489794448908, 339.9999999999999432 ) ) ;
#41535=ORIENTED_EDGE ( 'NONE', *, *, #18705, .T. ) ;
#41539=CARTESIAN_POINT ( 'NONE',  ( 814.9108240113580450, -352.2709662947830225, 337.5031285880265273 ) ) ;
#41540=CARTESIAN_POINT ( 'NONE',  ( 807.5423716828161105, -249.0783235625959549, 362.2119215644372048 ) ) ;
#41545=CARTESIAN_POINT ( 'NONE',  ( 755.0636971347428243, -244.2709662947834204, 341.7834795799807353 ) ) ;
#41547=CARTESIAN_POINT ( 'NONE',  ( 811.0346526505616112, -350.6346026584192828, 323.0537975583477532 ) ) ;
#41550=CARTESIAN_POINT ( 'NONE',  ( 791.7419236033215384, 16.45630643248850689, 314.5156751397937001 ) ) ;
#41551=DIRECTION ( 'NONE',  ( -1.000000000000000000, 0.000000000000000000, 0.000000000000000000 ) ) ;
#41552=CARTESIAN_POINT ( 'NONE',  ( 800.9840315886518738, -220.9181544815164102, 354.1144889064786412 ) ) ;
#41553=CARTESIAN_POINT ( 'NONE',  ( 767.8955696845333705, -120.4527844766019484, 362.1676090361162323 ) ) ;
#41558=CARTESIAN_POINT ( 'NONE',  ( 759.2295555964440155, -280.1692326535049347, 353.9708237608231229 ) ) ;
#41561=CARTESIAN_POINT ( 'NONE',  ( 809.0717654672305343, -4.918154481517067467, 360.1688906516309885 ) ) ;
#41563=CARTESIAN_POINT ( 'NONE',  ( 777.5031285880264704, -70.81642084023850714, 374.9108240113588408 ) ) ;
#41565=CARTESIAN_POINT ( 'NONE',  ( 772.4837098697144029, -167.3618753856927412, 374.5518280994205611 ) ) ;
#41570=CARTESIAN_POINT ( 'NONE',  ( 744.6391490659812007, -422.7363362996975980, 338.7502325331110455 ) ) ;
#41573=CARTESIAN_POINT ( 'NONE',  ( 747.2067596250078623, -411.1800572038738437, 352.2312462859687230 ) ) ;
#41574=CARTESIAN_POINT ( 'NONE',  ( 787.4397851343537695, -21.72551174932956641, 374.2001403089903988 ) ) ;
#41576=CARTESIAN_POINT ( 'NONE',  ( 796.7845633553578182, -33.62377810805116951, 358.5707757039688204 ) ) ;
#41579=CARTESIAN_POINT ( 'NONE',  ( 744.9990715423526808, -162.3510508353235196, 341.2370466360926002 ) ) ;
#41584=CARTESIAN_POINT ( 'NONE',  ( 758.0580252608178853, -174.4527844766018063, 328.0187753319985404 ) ) ;
#41587=CARTESIAN_POINT ( 'NONE',  ( 803.6646147819162707, -281.9073299311469327, 348.8264449731211130 ) ) ;
#41592=CARTESIAN_POINT ( 'NONE',  ( 760.5453621957607311, -21.07832356259667250, 323.8424801807151425 ) ) ;
#41595=CARTESIAN_POINT ( 'NONE',  ( 745.7998596910086917, -269.3618753856924286, 332.5602148656461168 ) ) ;
#41596=CARTESIAN_POINT ( 'NONE',  ( 779.4763451958990572, -320.7363362996979390, 365.0264073115438919 ) ) ;
#41597=CARTESIAN_POINT ( 'NONE',  ( 789.6640940660590786, -442.9180389616178672, 363.1300863558843162 ) ) ;
#41601=ORIENTED_EDGE ( 'NONE', *, *, #44984, .T. ) ;
#41603=CARTESIAN_POINT ( 'NONE',  ( 786.6156483768007774, -313.4419599262320730, 315.5913626894246136 ) ) ;
#41605=CARTESIAN_POINT ( 'NONE',  ( 775.8780910478218402, -105.2817908451530968, 364.9511171171680530 ) ) ;
#41606=CARTESIAN_POINT ( 'NONE',  ( 757.8323909638827445, -2.634602658420536869, 352.1044303154654358 ) ) ;
#41611=CARTESIAN_POINT ( 'NONE',  ( 815.3608509340175488, -242.7363362996980811, 341.2497674668889545 ) ) ;
#41616=CARTESIAN_POINT ( 'NONE',  ( 813.1304606946830518, -89.90732993114750116, 352.3570229623690580 ) ) ;
#41618=CARTESIAN_POINT ( 'NONE',  ( 809.2691622578233819, -452.9681489794448908, 335.3267997378328005 ) ) ;
#41621=CARTESIAN_POINT ( 'NONE',  ( 814.2805881961230625, -313.6454272087888171, 331.2368401574024119 ) ) ;
#41623=CARTESIAN_POINT ( 'NONE',  ( 811.0346526505616112, -278.6346026584196807, 323.0537975583477532 ) ) ;
#41627=CARTESIAN_POINT ( 'NONE',  ( 778.2165204200184689, -406.8164208402375266, 364.9363028652563230 ) ) ;
#41628=CARTESIAN_POINT ( 'NONE',  ( 793.0897708529556667, -150.5545181178802352, 361.3366627262616362 ) ) ;
#41631=CARTESIAN_POINT ( 'NONE',  ( 798.0661480581538854, -74.53286901714196233, 309.5768839229118043 ) ) ;
#41632=CARTESIAN_POINT ( 'NONE',  ( 800.2193346964446619, -378.9982390220557136, 355.1360043628816925 ) ) ;
#41636=( NAMED_UNIT ( * ) PLANE_ANGLE_UNIT ( ) SI_UNIT ( $, .RADIAN. ) );
#41637=CARTESIAN_POINT ( 'NONE',  ( 752.4576283171824116, -141.0783235625962959, 317.7880784355627952 ) ) ;
#41638=CARTESIAN_POINT ( 'NONE',  ( 781.7834795799800531, -418.8164208402374129, 315.0636971347436202 ) ) ;
#41644=CARTESIAN_POINT ( 'NONE',  ( 800.2193346964447755, -186.9982390220563104, 355.1360043628815788 ) ) ;
#41645=CARTESIAN_POINT ( 'NONE',  ( 774.6858677611749044, -177.7255117493290868, 315.5713283507209894 ) ) ;
#41648=CARTESIAN_POINT ( 'NONE',  ( 767.9999999999992042, 178.9475563372491251, 320.0000000000000000 ) ) ;
#41650=CARTESIAN_POINT ( 'NONE',  ( 774.6312213355099630, -407.3618753856920307, 364.6798772138717482 ) ) ;
#41651=EDGE_LOOP ( 'NONE', ( #27728, #14847, #34203, #7932, #28062 ) ) ;
#41655=CARTESIAN_POINT ( 'NONE',  ( 796.7737145352015204, -140.6346026584201070, 370.7187646348536987 ) ) ;
#41664=CARTESIAN_POINT ( 'NONE',  ( 761.2382568024794409, -207.6237781080506295, 356.9571628226838129 ) ) ;
#41665=CARTESIAN_POINT ( 'NONE',  ( 799.9999999999993179, 205.0000000000000568, 319.9999999999999432 ) ) ;
#41673=CARTESIAN_POINT ( 'NONE',  ( 760.0363995740630116, -130.9181544815166660, 368.7758568127991907 ) ) ;
#41678=EDGE_CURVE ( 'NONE', #56, #5612, #14960, .T. ) ;
#41684=CARTESIAN_POINT ( 'NONE',  ( 783.7953271457878373, -368.1908817542433212, 375.1787889125761239 ) ) ;
#41688=CARTESIAN_POINT ( 'NONE',  ( 803.4237431249931660, 8.819942796124882634, 331.2633955100225194 ) ) ;
#41690=CARTESIAN_POINT ( 'NONE',  ( 745.7194118038753459, -229.6454272087890729, 348.7631598425976449 ) ) ;
#41692=CARTESIAN_POINT ( 'NONE',  ( 800.9747183278959710, -204.9982390220562820, 311.9810565676471583 ) ) ;
#41695=AXIS2_PLACEMENT_3D ( 'NONE', #3746, #31901, #42083 ) ;
#41696=CARTESIAN_POINT ( 'NONE',  ( 794.9819416627830151, -276.9982390220559978, 319.9864689768909898 ) ) ;
#41698=CARTESIAN_POINT ( 'NONE',  ( 793.0897708529556667, -54.55451811788054783, 361.3366627262616362 ) ) ;
#41704=CARTESIAN_POINT ( 'NONE',  ( 776.9566956441375396, -108.8965053807782084, 364.8461984189686405 ) ) ;
#41705=CARTESIAN_POINT ( 'NONE',  ( 765.0180583372156207, -312.9982390220559409, 360.0135310231089534 ) ) ;
#41708=CARTESIAN_POINT ( 'NONE',  ( 801.9419747391806368, -90.45278447660209054, 351.9812246680014027 ) ) ;
#41711=CARTESIAN_POINT ( 'NONE',  ( 776.2433038121456548, -372.8965053807773415, 374.8207195650711014 ) ) ;
#41713=CARTESIAN_POINT ( 'NONE',  ( 801.9419747391806368, -282.4527844766014937, 351.9812246680014027 ) ) ;
#41716=CARTESIAN_POINT ( 'NONE',  ( 785.3141322388236176, -405.7255117493283478, 364.4286716492789537 ) ) ;
#41724=CARTESIAN_POINT ( 'NONE',  ( 785.3687786644884454, -131.3618753856928834, 315.3201227861279676 ) ) ;
#41725=CARTESIAN_POINT ( 'NONE',  ( 773.4516893846965786, -451.6454272087884192, 315.8398074228977066 ) ) ;
#41726=CARTESIAN_POINT ( 'NONE',  ( 803.8651313633788504, -101.2601417444146250, 332.4468031744301015 ) ) ;
#41729=CARTESIAN_POINT ( 'NONE',  ( 786.2056067578752163, -371.8055962898682765, 374.4686193811670023 ) ) ;
#41733=CARTESIAN_POINT ( 'NONE',  ( 793.5525998758768083, -7.099972663335241130, 372.6845335610516941 ) ) ;
#41742=CARTESIAN_POINT ( 'NONE',  ( 760.7433823573367135, -348.0090635724251342, 355.9930595647440441 ) ) ;
#41743=CARTESIAN_POINT ( 'NONE',  ( 814.8207195650702488, -314.1908817542433781, 336.2433038121456548 ) ) ;
#41745=CARTESIAN_POINT ( 'NONE',  ( 767.9999999999992042, 205.0000000000000568, 339.9999999999999432 ) ) ;
#41747=CARTESIAN_POINT ( 'NONE',  ( 783.7953271457878373, -104.1908817542440175, 375.1787889125761239 ) ) ;
#41753=CARTESIAN_POINT ( 'NONE',  ( 788.8264449731200330, -189.1800572038744122, 363.6646147819171233 ) ) ;
#41756=CARTESIAN_POINT ( 'NONE',  ( 747.6481478633932056, -421.0999726633340288, 353.4146539503763620 ) ) ;
#41759=CARTESIAN_POINT ( 'NONE',  ( 787.5531968255692163, -45.82724539060783542, 316.1348686366205811 ) ) ;
#41761=CARTESIAN_POINT ( 'NONE',  ( 799.9999999999993179, -462.9681489794448339, 362.3606797749978909 ) ) ;
#41762=CARTESIAN_POINT ( 'NONE',  ( 744.9990715423526808, 5.648949164675971524, 341.2370466360926002 ) ) ;
#41766=CARTESIAN_POINT ( 'NONE',  ( 747.3154664389472828, -259.9874144716869182, 326.4474001241230781 ) ) ;
#41767=CARTESIAN_POINT ( 'NONE',  ( 755.5713283507202505, -125.3618753856928834, 334.6858677611754729 ) ) ;
#41771=CARTESIAN_POINT ( 'NONE',  ( 757.8323909638827445, -290.6346026584195101, 352.1044303154654358 ) ) ;
#41773=CYLINDRICAL_SURFACE ( 'NONE', #28335, 10.00000000000000888 ) ;
#41775=ORIENTED_EDGE ( 'NONE', *, *, #20676, .T. ) ;
#41777=CARTESIAN_POINT ( 'NONE',  ( 765.0180583372156207, -24.99823902205683268, 360.0135310231089534 ) ) ;
#41780=CARTESIAN_POINT ( 'NONE',  ( 808.0189434323515343, -374.0891481129647786, 319.0252816721025511 ) ) ;
#41781=CARTESIAN_POINT ( 'NONE',  ( 805.9055244015594326, -243.6237781080504590, 315.8990559732753240 ) ) ;
#41786=CARTESIAN_POINT ( 'NONE',  ( 803.4237431249931660, -231.1800572038743553, 331.2633955100225194 ) ) ;
#41788=CARTESIAN_POINT ( 'NONE',  ( 749.2812353651451076, -342.4527844766013231, 323.2262854647983090 ) ) ;
#41791=CARTESIAN_POINT ( 'NONE',  ( 799.9999999999993179, 166.4563064324884465, 319.9999999999999432 ) ) ;
#41793=CARTESIAN_POINT ( 'NONE',  ( 801.5560724626406000, -216.5545181178800931, 326.7756240680316182 ) ) ;
#41794=CARTESIAN_POINT ( 'NONE',  ( 771.2633955100217236, -119.9073299311474443, 363.4237431249939618 ) ) ;
#41798=CARTESIAN_POINT ( 'NONE',  ( 803.2186876482843445, -295.9874144716866908, 350.0220218866286928 ) ) ;
#41802=CARTESIAN_POINT ( 'NONE',  ( 814.2001403089898304, -449.3618753856918602, 347.4397851343538264 ) ) ;
#41804=CARTESIAN_POINT ( 'NONE',  ( 777.4774526936600978, -178.2709662947835625, 304.7301800767027657 ) ) ;
#41805=CARTESIAN_POINT ( 'NONE',  ( 803.6646147819161570, -89.90732993114750116, 348.8264449731210561 ) ) ;
#41811=CARTESIAN_POINT ( 'NONE',  ( 762.1177392798416577, -402.5545181178795247, 309.8865473780659272 ) ) ;
#41814=CARTESIAN_POINT ( 'NONE',  ( 814.2001403089898304, -401.3618753856920307, 347.4397851343538264 ) ) ;
#41815=CARTESIAN_POINT ( 'NONE',  ( 746.8695393053151292, -5.907329931147799584, 327.6429770376306578 ) ) ;
#41818=CARTESIAN_POINT ( 'NONE',  ( 801.3366627262608972, -32.53286901714208312, 353.0897708529566899 ) ) ;
#41821=CARTESIAN_POINT ( 'NONE',  ( 803.8556311672234642, -153.6237781080508000, 365.6418435158340117 ) ) ;
#41822=CARTESIAN_POINT ( 'NONE',  ( 765.0180583372156207, -0.9982390220569063999, 360.0135310231089534 ) ) ;
#41826=CARTESIAN_POINT ( 'NONE',  ( 764.8639956371174549, -152.0891481129655460, 319.7806653035542013 ) ) ;
#41828=CARTESIAN_POINT ( 'NONE',  ( 758.0580252608178853, -294.4527844766013800, 328.0187753319985404 ) ) ;
#41831=CARTESIAN_POINT ( 'NONE',  ( 793.2243759319678702, -26.53286901714210799, 318.4439275373583200 ) ) ;
#41834=CARTESIAN_POINT ( 'NONE',  ( 763.2262854647970016, -248.6346026584197659, 309.2812353651462445 ) ) ;
#41835=CARTESIAN_POINT ( 'NONE',  ( 783.0745993439762742, -344.1908817542433212, 365.1016975059196739 ) ) ;
#41836=CARTESIAN_POINT ( 'NONE',  ( 805.9055244015594326, 20.37622189194865285, 315.8990559732753240 ) ) ;
#41842=CARTESIAN_POINT ( 'NONE',  ( 796.7845633553578182, -321.6237781080502600, 358.5707757039688204 ) ) ;
#41845=CARTESIAN_POINT ( 'NONE',  ( 790.9844846989617508, -118.3726999360621619, 317.2208543904092721 ) ) ;
#41846=CARTESIAN_POINT ( 'NONE',  ( 778.2165204200184689, 1.183579159761269040, 364.9363028652563230 ) ) ;
#41850=CARTESIAN_POINT ( 'NONE',  ( 807.2620300519052989, -240.0090635724253900, 318.0141637701419768 ) ) ;
#41851=CARTESIAN_POINT ( 'NONE',  ( 801.3366627262608972, -200.5328690171415644, 353.0897708529566899 ) ) ;
#41853=CARTESIAN_POINT ( 'NONE',  ( 799.9999999999993179, 166.4563064324884465, 319.9999999999999432 ) ) ;
#41856=CARTESIAN_POINT ( 'NONE',  ( 763.2262854647970016, -80.63460265842029173, 309.2812353651462445 ) ) ;
#41857=CARTESIAN_POINT ( 'NONE',  ( 806.8957046614239061, -452.9681489794451181, 342.6393539086462852 ) ) ;
#41859=DIRECTION ( 'NONE',  ( 1.000000000000000000, -0.000000000000000000, -0.000000000000000000 ) ) ;
#41860=CARTESIAN_POINT ( 'NONE',  ( 810.4231160770870019, -360.5545181178796383, 321.9338519418446936 ) ) ;
#41862=CARTESIAN_POINT ( 'NONE',  ( 751.9810565676468741, -290.0891481129650629, 360.9747183278973921 ) ) ;
#41867=CARTESIAN_POINT ( 'NONE',  ( 759.7806653035534055, -390.9982390220557136, 324.8639956371180801 ) ) ;
#41868=CARTESIAN_POINT ( 'NONE',  ( 780.5236548040995785, -164.7363362996983938, 314.9735926884559944 ) ) ;
#41871=CARTESIAN_POINT ( 'NONE',  ( 744.9990715423526808, -66.35105083532378956, 341.2370466360926002 ) ) ;
#41872=CARTESIAN_POINT ( 'NONE',  ( 771.1735550268780344, -417.1800572038736732, 316.3353852180828198 ) ) ;
#41875=CARTESIAN_POINT ( 'NONE',  ( 800.0135310231082713, -422.0891481129647218, 325.0180583372163028 ) ) ;
#41876=ORIENTED_EDGE ( 'NONE', *, *, #3160, .T. ) ;
#41879=CARTESIAN_POINT ( 'NONE',  ( 758.0580252608178853, -222.4527844766016642, 328.0187753319985404 ) ) ;
#41880=CARTESIAN_POINT ( 'NONE',  ( 755.3201227861273992, -195.7255117493290015, 345.3687786644892981 ) ) ;
#41884=CARTESIAN_POINT ( 'NONE',  ( 767.8955696845333705, -384.4527844766011526, 362.1676090361162323 ) ) ;
#41888=CARTESIAN_POINT ( 'NONE',  ( 814.9108240113580450, -136.2709662947837330, 337.5031285880265273 ) ) ;
#41894=CARTESIAN_POINT ( 'NONE',  ( 805.1016975059191054, -246.8965053807777679, 343.0745993439771837 ) ) ;
#41903=CARTESIAN_POINT ( 'NONE',  ( 745.1792804349281596, -134.1908817542439181, 343.7566961878542884 ) ) ;
#41913=CARTESIAN_POINT ( 'NONE',  ( 812.3518521366052028, -385.0999726633340856, 326.5853460496235243 ) ) ;
#41920=CARTESIAN_POINT ( 'NONE',  ( 766.4474001241216001, -235.0999726633344835, 307.3154664389482491 ) ) ;
#41922=CARTESIAN_POINT ( 'NONE',  ( 767.7687537140311633, -191.9073299311471885, 372.7932403749916830 ) ) ;
#41927=CARTESIAN_POINT ( 'NONE',  ( 755.3201227861273992, -291.7255117493285752, 345.3687786644892981 ) ) ;
#41928=CARTESIAN_POINT ( 'NONE',  ( 799.2566176426618085, -48.00906357242602951, 324.0069404352559559 ) ) ;
#41932=CARTESIAN_POINT ( 'NONE',  ( 766.7756240680305382, -134.5328690171417350, 361.5560724626415663 ) ) ;
#41933=CARTESIAN_POINT ( 'NONE',  ( 788.7366044899766848, -323.9073299311468190, 316.5762568750059813 ) ) ;
#41936=CARTESIAN_POINT ( 'NONE',  ( 771.2633955100217236, -95.90732993114751537, 363.4237431249939618 ) ) ;
#41939=CARTESIAN_POINT ( 'NONE',  ( 815.0009284576459549, -414.3510508353227237, 338.7629533639073429 ) ) ;
#41941=ORIENTED_EDGE ( 'NONE', *, *, #44258, .F. ) ;
#41942=CARTESIAN_POINT ( 'NONE',  ( 788.8264449731200330, -285.1800572038740711, 363.6646147819171233 ) ) ;
#41948=CARTESIAN_POINT ( 'NONE',  ( 800.0135310231082713, -422.0891481129647218, 325.0180583372163028 ) ) ;
#41954=CARTESIAN_POINT ( 'NONE',  ( 804.6798772138708955, -111.7255117493293000, 334.6312213355107019 ) ) ;
#41955=CARTESIAN_POINT ( 'NONE',  ( 775.8780910478218402, -441.2817908451521021, 364.9511171171680530 ) ) ;
#41956=CARTESIAN_POINT ( 'NONE',  ( 787.6308680596127942, -107.2601417444145824, 364.1105419155492768 ) ) ;
#41959=CARTESIAN_POINT ( 'NONE',  ( 815.1787889125755555, -366.8965053807773984, 343.7953271457877804 ) ) ;
#41965=CARTESIAN_POINT ( 'NONE',  ( 749.5768839229115201, -36.55451811788061178, 358.0661480581553064 ) ) ;
#41968=EDGE_CURVE ( 'NONE', #25624, #13889, #40815, .T. ) ;
#41974=CARTESIAN_POINT ( 'NONE',  ( 802.5472867521000353, -364.3726999360614514, 350.8726784830461156 ) ) ;
#41976=CARTESIAN_POINT ( 'NONE',  ( 746.4236121716829757, -351.8272453906068336, 328.8385539511384650 ) ) ;
#41980=CARTESIAN_POINT ( 'NONE',  ( 768.9521613784389729, -105.8272453906076578, 373.2346286133773106 ) ) ;
#41984=CARTESIAN_POINT ( 'NONE',  ( 754.8072714833581358, -172.8164208402381234, 338.1981804954720587 ) ) ;
#41985=CARTESIAN_POINT ( 'NONE',  ( 771.3260364891663130, -427.6454272087885897, 306.0683387631859773 ) ) ;
#41990=CARTESIAN_POINT ( 'NONE',  ( 751.2241431872005251, 7.830767346494148740, 359.9636004259367610 ) ) ;
#41994=CARTESIAN_POINT ( 'NONE',  ( 801.9858362298568863, -315.0783235625957559, 312.7379699480935642 ) ) ;
#41995=CARTESIAN_POINT ( 'NONE',  ( 778.1981804954715471, -130.2709662947837614, 314.8072714833591021 ) ) ;
#41997=CARTESIAN_POINT ( 'NONE',  ( 765.0180583372156207, -312.9982390220559409, 360.0135310231089534 ) ) ;
#42004=CARTESIAN_POINT ( 'NONE',  ( 774.6312213355099630, -23.36187538569318889, 364.6798772138717482 ) ) ;
#42006=CARTESIAN_POINT ( 'NONE',  ( 815.2698199232962679, -376.8164208402375834, 342.5225473063383674 ) ) ;
#42007=CARTESIAN_POINT ( 'NONE',  ( 747.3154664389472828, -235.9874144716868898, 326.4474001241230781 ) ) ;
#42012=CARTESIAN_POINT ( 'NONE',  ( 803.6646147819161570, -257.9073299311469896, 348.8264449731210561 ) ) ;
#42013=CARTESIAN_POINT ( 'NONE',  ( 758.8095938919642549, -392.0891481129648355, 311.6929314249763365 ) ) ;
#42016=PLANE ( 'NONE',  #10114 ) ;
#42018=CARTESIAN_POINT ( 'NONE',  ( 784.1219089521767955, -261.2817908451526705, 315.0488828828318333 ) ) ;
#42019=CARTESIAN_POINT ( 'NONE',  ( 754.8072714833581358, -124.8164208402383508, 338.1981804954720587 ) ) ;
#42023=CARTESIAN_POINT ( 'NONE',  ( 759.2295555964440155, -304.1692326535048210, 353.9708237608231229 ) ) ;
#42025=CARTESIAN_POINT ( 'NONE',  ( 762.1177392798416577, 5.445481882119263872, 309.8865473780659272 ) ) ;
#42027=CARTESIAN_POINT ( 'NONE',  ( 749.2812353651451076, -174.4527844766018063, 323.2262854647983090 ) ) ;
#42028=CARTESIAN_POINT ( 'NONE',  ( 755.0636971347428243, -76.27096629478394618, 341.7834795799807353 ) ) ;
#42031=CARTESIAN_POINT ( 'NONE',  ( 764.1737431748507561, -418.3726999360612808, 371.6461892240376415 ) ) ;
#42034=CARTESIAN_POINT ( 'NONE',  ( 789.9200121543843807, -361.9874144716864635, 317.0176451133914384 ) ) ;
#42035=CARTESIAN_POINT ( 'NONE',  ( 767.6429770376291799, -33.18005720387498769, 306.8695393053162093 ) ) ;
#42038=CARTESIAN_POINT ( 'NONE',  ( 794.1144889064781864, -10.16923265350579442, 360.9840315886528401 ) ) ;
#42042=CARTESIAN_POINT ( 'NONE',  ( 759.8311093483677041, -214.1692326535052189, 310.9282345327691814 ) ) ;
#42043=CARTESIAN_POINT ( 'NONE',  ( 759.7806653035535192, -6.998239022056886860, 324.8639956371181370 ) ) ;
#42046=CARTESIAN_POINT ( 'NONE',  ( 794.9819416627830151, -204.9982390220562820, 319.9864689768909898 ) ) ;
#42048=CARTESIAN_POINT ( 'NONE',  ( 764.8639956371174549, -320.0891481129648923, 319.7806653035542581 ) ) ;
#42051=CARTESIAN_POINT ( 'NONE',  ( 756.1348686366196716, -41.26014174441479554, 347.5531968255698416 ) ) ;
#42053=CARTESIAN_POINT ( 'NONE',  ( 751.6929314249750860, -246.9982390220560831, 318.8095938919659034 ) ) ;
#42054=CARTESIAN_POINT ( 'NONE',  ( 757.0176451133909268, -349.0999726633342561, 349.9200121543848354 ) ) ;
#42055=CARTESIAN_POINT ( 'NONE',  ( 788.7631598425961101, 22.55804007376682918, 305.7194118038759143 ) ) ;
#42060=CARTESIAN_POINT ( 'NONE',  ( 800.9747183278959710, -300.9982390220559409, 311.9810565676471583 ) ) ;
#42061=CARTESIAN_POINT ( 'NONE',  ( 804.9511171171677688, -317.8055962898684470, 335.8780910478229202 ) ) ;
#42063=CARTESIAN_POINT ( 'NONE',  ( 801.5560724626406000, -120.5545181178803205, 326.7756240680316182 ) ) ;
#42064=CARTESIAN_POINT ( 'NONE',  ( 759.7806653035534055, -6.998239022056885972, 324.8639956371180801 ) ) ;
#42068=CARTESIAN_POINT ( 'NONE',  ( 797.8822607201568644, -246.5545181178799510, 370.1134526219340160 ) ) ;
#42069=CARTESIAN_POINT ( 'NONE',  ( 770.0799878456142551, -181.9874144716870887, 362.9823548866085616 ) ) ;
#42073=CARTESIAN_POINT ( 'NONE',  ( 751.9810565676468741, -26.08914811296592262, 360.9747183278973921 ) ) ;
#42074=CARTESIAN_POINT ( 'NONE',  ( 814.9108240113580450, -64.27096629478397460, 337.5031285880265273 ) ) ;
#42075=CARTESIAN_POINT ( 'NONE',  ( 802.3178104526313064, -452.9681489794448339, 352.6268974387025423 ) ) ;
#42078=CARTESIAN_POINT ( 'NONE',  ( 814.4686193811664907, -339.2817908451524431, 346.2056067578752732 ) ) ;
#42080=CARTESIAN_POINT ( 'NONE',  ( 804.7487373415286811, -331.5436935675104451, 364.7487373415288516 ) ) ;
#42083=DIRECTION ( 'NONE',  ( 0.000000000000000000, 0.000000000000000000, -1.000000000000000000 ) ) ;
#42084=CARTESIAN_POINT ( 'NONE',  ( 797.8594530101008786, -397.5436935675100472, 322.1405469898980982 ) ) ;
#42085=CARTESIAN_POINT ( 'NONE',  ( 759.0159684113467620, -160.9181544815165807, 325.8855110935213020 ) ) ;
#42088=CARTESIAN_POINT ( 'NONE',  ( 813.9316612368132837, -79.44195992623286884, 348.6739635108323228 ) ) ;
#42089=CARTESIAN_POINT ( 'NONE',  ( 764.8639956371174549, -392.0891481129647786, 319.7806653035542581 ) ) ;
#42097=CARTESIAN_POINT ( 'NONE',  ( 756.5762568750052424, -219.1800572038744122, 348.7366044899774238 ) ) ;
#42098=CARTESIAN_POINT ( 'NONE',  ( 757.8323909638828582, -242.6346026584197659, 352.1044303154654358 ) ) ;
#42101=DIRECTION ( 'NONE',  ( -1.000000000000000000, -0.000000000000000000, 0.000000000000000000 ) ) ;
#42103=CARTESIAN_POINT ( 'NONE',  ( 771.1735550268778070, -441.1800572038735027, 316.3353852180827630 ) ) ;
#42106=CARTESIAN_POINT ( 'NONE',  ( 787.4397851343537695, -141.7255117493291721, 374.2001403089903988 ) ) ;
#42112=CARTESIAN_POINT ( 'NONE',  ( 770.0799878456142551, -229.9874144716869466, 362.9823548866085616 ) ) ;
#42122=CARTESIAN_POINT ( 'NONE',  ( 811.3240766477731540, -124.3726999360621619, 355.6651683502462902 ) ) ;
#42129=CARTESIAN_POINT ( 'NONE',  ( 814.8207195650702488, -386.1908817542432075, 336.2433038121456548 ) ) ;
#42136=CARTESIAN_POINT ( 'NONE',  ( 783.7953271457878373, -248.1908817542435202, 375.1787889125761239 ) ) ;
#42138=CARTESIAN_POINT ( 'NONE',  ( 814.2001403089898304, -185.3618753856926844, 347.4397851343538264 ) ) ;
#42142=CARTESIAN_POINT ( 'NONE',  ( 754.8072714833581358, -292.8164208402376971, 338.1981804954720587 ) ) ;
#42143=CARTESIAN_POINT ( 'NONE',  ( 766.0291762391763086, -82.91815448151682233, 360.7704444035551319 ) ) ;
#42147=CARTESIAN_POINT ( 'NONE',  ( 757.2208543904082489, -112.7146871989600356, 350.9844846989624330 ) ) ;
#42148=CARTESIAN_POINT ( 'NONE',  ( 774.6858677611749044, -321.7255117493286320, 315.5713283507209894 ) ) ;
#42151=CARTESIAN_POINT ( 'NONE',  ( 762.3223304703356007, -79.54369356751119824, 322.3223304703362828 ) ) ;
#42154=CARTESIAN_POINT ( 'NONE',  ( 815.1787889125755555, -414.8965053807771710, 343.7953271457877804 ) ) ;
#42156=CARTESIAN_POINT ( 'NONE',  ( 800.0135310231082713, -302.0891481129650629, 325.0180583372163028 ) ) ;
#42159=CARTESIAN_POINT ( 'NONE',  ( 803.4237431249931660, -399.1800572038738437, 331.2633955100225194 ) ) ;
#42166=CARTESIAN_POINT ( 'NONE',  ( 759.7806653035534055, -126.9982390220565094, 324.8639956371180801 ) ) ;
#42167=CARTESIAN_POINT ( 'NONE',  ( 790.0220218866281812, -439.0999726633339719, 363.2186876482849129 ) ) ;
#42168=CARTESIAN_POINT ( 'NONE',  ( 757.2208543904082489, -112.7146871989600356, 350.9844846989624330 ) ) ;
#42172=CARTESIAN_POINT ( 'NONE',  ( 812.6845335610512393, -391.9874144716864066, 353.5525998758768651 ) ) ;
#42178=CARTESIAN_POINT ( 'NONE',  ( 781.2370466360911223, -44.73633629969875614, 304.9990715423533629 ) ) ;
#42186=CARTESIAN_POINT ( 'NONE',  ( 780.5236548040995785, -380.7363362996977116, 314.9735926884559944 ) ) ;
#42187=CARTESIAN_POINT ( 'NONE',  ( 814.2805881961230625, -337.6454272087888171, 331.2368401574024119 ) ) ;
#42192=CARTESIAN_POINT ( 'NONE',  ( 781.2370466360911223, -140.7363362996984506, 304.9990715423533629 ) ) ;
#42198=CARTESIAN_POINT ( 'NONE',  ( 762.1405469898971887, -193.5436935675108714, 357.8594530101015607 ) ) ;
#42201=CARTESIAN_POINT ( 'NONE',  ( 750.9282345327678740, -448.9181544815156144, 319.8311093483690115 ) ) ;
#42206=CARTESIAN_POINT ( 'NONE',  ( 810.1134526219336749, -8.532869017142163059, 357.8822607201570349 ) ) ;
#42207=ORIENTED_EDGE ( 'NONE', *, *, #14906, .T. ) ;
#42210=CARTESIAN_POINT ( 'NONE',  ( 800.1688906516307043, -322.1692326535048210, 369.0717654672308186 ) ) ;
#42211=CARTESIAN_POINT ( 'NONE',  ( 805.1927285166399315, -136.8164208402382656, 341.8018195045277707 ) ) ;
#42214=CARTESIAN_POINT ( 'NONE',  ( 757.8323909638827445, -314.6346026584194533, 352.1044303154654358 ) ) ;
#42224=CARTESIAN_POINT ( 'NONE',  ( 814.2001403089898304, -377.3618753856920875, 347.4397851343538264 ) ) ;
#42225=CARTESIAN_POINT ( 'NONE',  ( 751.2241431872005251, -256.1692326535049915, 359.9636004259367610 ) ) ;
#42231=CARTESIAN_POINT ( 'NONE',  ( 791.9812246680005501, -236.6346026584198228, 361.9419747391813189 ) ) ;
#42232=CARTESIAN_POINT ( 'NONE',  ( 813.1304606946830518, -377.9073299311466485, 352.3570229623690580 ) ) ;
#42238=CARTESIAN_POINT ( 'NONE',  ( 790.0220218866281812, -247.0999726633344835, 363.2186876482849129 ) ) ;
#42239=CARTESIAN_POINT ( 'NONE',  ( 797.8594530101008786, -109.5436935675110988, 322.1405469898980982 ) ) ;
#42240=ORIENTED_EDGE ( 'NONE', *, *, #27263, .T. ) ;
#42243=CARTESIAN_POINT ( 'NONE',  ( 779.4709603349208464, -288.3510508353231216, 314.7162404726379918 ) ) ;
#42245=CARTESIAN_POINT ( 'NONE',  ( 766.4474001241216001, -43.09997266333511590, 307.3154664389482491 ) ) ;
#42247=CARTESIAN_POINT ( 'NONE',  ( 796.7737145352015204, -164.6346026584200217, 370.7187646348536987 ) ) ;
#42248=CARTESIAN_POINT ( 'NONE',  ( 774.6312213355099630, -95.36187538569294020, 364.6798772138717482 ) ) ;
#42252=CARTESIAN_POINT ( 'NONE',  ( 793.5525998758768083, -439.0999726633339719, 372.6845335610516941 ) ) ;
#42255=CARTESIAN_POINT ( 'NONE',  ( 755.8398074228967971, -355.4419599262319593, 333.4516893846970333 ) ) ;
#42256=CARTESIAN_POINT ( 'NONE',  ( 787.5162901302840055, -35.36187538569316047, 305.4481719005793252 ) ) ;
#42258=CARTESIAN_POINT ( 'NONE',  ( 772.3691319403857278, -47.26014174441477422, 315.8894580844506663 ) ) ;
#42260=CARTESIAN_POINT ( 'NONE',  ( 798.0661480581538854, -194.5328690171415644, 309.5768839229118043 ) ) ;
#42261=CARTESIAN_POINT ( 'NONE',  ( 801.9419747391806368, -18.45278447660230725, 351.9812246680014027 ) ) ;
#42265=CARTESIAN_POINT ( 'NONE',  ( 802.1676090361156639, -182.6346026584199649, 327.8955696845344505 ) ) ;
#42267=CARTESIAN_POINT ( 'NONE',  ( 791.9812246680005501, -332.6346026584195101, 361.9419747391813189 ) ) ;
#42270=CARTESIAN_POINT ( 'NONE',  ( 757.2208543904082489, -40.71468719896024879, 350.9844846989624330 ) ) ;
#42272=CARTESIAN_POINT ( 'NONE',  ( 813.1304606946831655, -257.9073299311469327, 352.3570229623691716 ) ) ;
#42273=CARTESIAN_POINT ( 'NONE',  ( 815.1787889125755555, -6.896505380778533478, 343.7953271457877804 ) ) ;
#42279=CARTESIAN_POINT ( 'NONE',  ( 801.1904061080336987, -284.0891481129650629, 368.3070685750235498 ) ) ;
#42281=CARTESIAN_POINT ( 'NONE',  ( 784.0799538623451781, -347.8055962898683333, 364.6971507214555572 ) ) ;
#42283=CARTESIAN_POINT ( 'NONE',  ( 802.5472867521000353, -148.3726999360620198, 350.8726784830461156 ) ) ;
#42284=CARTESIAN_POINT ( 'NONE',  ( 774.6312213355099630, 0.6381246143067236254, 364.6798772138717482 ) ) ;
#42285=ORIENTED_EDGE ( 'NONE', *, *, #3156, .F. ) ;
#42288=CARTESIAN_POINT ( 'NONE',  ( 766.4474001241216001, -235.0999726633344835, 307.3154664389482491 ) ) ;
#42289=CARTESIAN_POINT ( 'NONE',  ( 804.9511171171677688, -197.8055962898688733, 335.8780910478229202 ) ) ;
#42292=CARTESIAN_POINT ( 'NONE',  ( 796.1575198192839480, -438.0090635724247932, 359.4546378042384163 ) ) ;
#42294=CARTESIAN_POINT ( 'NONE',  ( 782.4968714119720516, -10.81642084023869543, 305.0891759886411023 ) ) ;
#42295=CARTESIAN_POINT ( 'NONE',  ( 787.4397851343537695, -69.72551174932942786, 374.2001403089903988 ) ) ;
#42299=CARTESIAN_POINT ( 'NONE',  ( 791.0478386215596629, -357.8272453906068904, 306.7653713866226326 ) ) ;
#42301=CARTESIAN_POINT ( 'NONE',  ( 772.4837098697144029, -335.3618753856920307, 374.5518280994205611 ) ) ;
#42305=CARTESIAN_POINT ( 'NONE',  ( 781.7834795799800531, -418.8164208402374129, 315.0636971347436202 ) ) ;
#42306=CARTESIAN_POINT ( 'NONE',  ( 773.4516893846965786, -163.6454272087893003, 315.8398074228977066 ) ) ;
#42309=CARTESIAN_POINT ( 'NONE',  ( 801.9858362298568863, -99.07832356259642381, 312.7379699480935642 ) ) ;
#42310=CARTESIAN_POINT ( 'NONE',  ( 803.6646147819162707, -401.9073299311464211, 348.8264449731211130 ) ) ;
#42312=CARTESIAN_POINT ( 'NONE',  ( 803.8556311672234642, -153.6237781080508000, 365.6418435158340117 ) ) ;
#42317=CARTESIAN_POINT ( 'NONE',  ( 755.0636971347428243, -244.2709662947834204, 341.7834795799807353 ) ) ;
#42318=CARTESIAN_POINT ( 'NONE',  ( 804.4286716492782716, -233.3618753856925423, 345.3141322388244703 ) ) ;
#42320=CARTESIAN_POINT ( 'NONE',  ( 801.1904061080336987, 3.910851887033985896, 368.3070685750235498 ) ) ;
#42323=CARTESIAN_POINT ( 'NONE',  ( 797.8594530101008786, -421.5436935675101040, 322.1405469898980982 ) ) ;
#42327=CARTESIAN_POINT ( 'NONE',  ( 814.5518280994195948, -159.7255117493291436, 332.4837098697145166 ) ) ;
#42333=CARTESIAN_POINT ( 'NONE',  ( 765.8855110935204493, -238.1692326535050768, 319.0159684113471599 ) ) ;
#42344=CARTESIAN_POINT ( 'NONE',  ( 797.8822607201568644, -150.5545181178802352, 370.1134526219340160 ) ) ;
#42350=CARTESIAN_POINT ( 'NONE',  ( 746.4236121716829757, -375.8272453906069472, 328.8385539511384650 ) ) ;
#42354=LINE ( 'NONE', #35421, #12832 ) ;
#42355=CARTESIAN_POINT ( 'NONE',  ( 759.9864689768902508, -2.089148112965993231, 354.9819416627836404 ) ) ;
#42358=CARTESIAN_POINT ( 'NONE',  ( 799.9636004259356241, -262.9181544815162965, 311.2241431872006956 ) ) ;
#42360=CARTESIAN_POINT ( 'NONE',  ( 811.0346526505616112, -206.6346026584198512, 323.0537975583477532 ) ) ;
#42364=CARTESIAN_POINT ( 'NONE',  ( 788.8264449731200330, -285.1800572038740711, 363.6646147819171233 ) ) ;
#42365=CARTESIAN_POINT ( 'NONE',  ( 776.9254006560222479, -92.19088175424406018, 314.8983024940802125 ) ) ;
#42369=CARTESIAN_POINT ( 'NONE',  ( 800.7704444035546203, -124.1692326535054463, 326.0291762391768771 ) ) ;
#42370=CARTESIAN_POINT ( 'NONE',  ( 788.7366044899766848, -347.9073299311467053, 316.5762568750059813 ) ) ;
#42373=CARTESIAN_POINT ( 'NONE',  ( 758.0580252608178853, -78.45278447660211896, 328.0187753319985404 ) ) ;
#42374=CARTESIAN_POINT ( 'NONE',  ( 755.8990559732751535, -395.4636090269705164, 365.9055244015606831 ) ) ;
#42378=CARTESIAN_POINT ( 'NONE',  ( 766.5853460496234675, -421.9874144716863498, 372.3518521366060554 ) ) ;
#42380=CARTESIAN_POINT ( 'NONE',  ( 791.9812246680005501, -332.6346026584195101, 361.9419747391813189 ) ) ;
#42384=CARTESIAN_POINT ( 'NONE',  ( 797.6776695296629214, -403.5436935675101608, 357.6776695296636603 ) ) ;
#42390=CARTESIAN_POINT ( 'NONE',  ( 758.0580252608178853, -126.4527844766019626, 328.0187753319985404 ) ) ;
#42391=CARTESIAN_POINT ( 'NONE',  ( 804.6971507214547046, -435.2817908451521021, 344.0799538623459739 ) ) ;
#42392=CARTESIAN_POINT ( 'NONE',  ( 801.3366627262608972, -128.5328690171417634, 353.0897708529566899 ) ) ;
#42393=DIRECTION ( 'NONE',  ( 0.000000000000000000, 0.000000000000000000, 1.000000000000000000 ) ) ;
#42395=CARTESIAN_POINT ( 'NONE',  ( 815.0009284576459549, -390.3510508353227237, 338.7629533639073429 ) ) ;
#42401=CARTESIAN_POINT ( 'NONE',  ( 754.3581564841646241, -17.46360902697157513, 316.1443688327762516 ) ) ;
#42408=CARTESIAN_POINT ( 'NONE',  ( 787.5531968255692163, -357.8272453906068904, 316.1348686366205811 ) ) ;
#42410=CARTESIAN_POINT ( 'NONE',  ( 768.9521613784389729, -321.8272453906070609, 373.2346286133773106 ) ) ;
#42416=CARTESIAN_POINT ( 'NONE',  ( 746.4236121716829757, -159.8272453906075157, 328.8385539511384650 ) ) ;
#42418=CARTESIAN_POINT ( 'NONE',  ( 782.4968714119720516, -106.8164208402383935, 305.0891759886411023 ) ) ;
#42423=CARTESIAN_POINT ( 'NONE',  ( 778.1981804954714335, -202.2709662947834772, 314.8072714833589885 ) ) ;
#42424=CARTESIAN_POINT ( 'NONE',  ( 801.5560724626406000, -0.5545181178807169209, 326.7756240680316182 ) ) ;
#42429=CARTESIAN_POINT ( 'NONE',  ( 813.9316612368132837, 16.55804007376685050, 348.6739635108323228 ) ) ;
#42435=CARTESIAN_POINT ( 'NONE',  ( 795.6651683502461765, -298.7146871989593251, 371.3240766477733814 ) ) ;
#42436=CARTESIAN_POINT ( 'NONE',  ( 788.7366044899766848, -131.9073299311473875, 316.5762568750059813 ) ) ;
#42439=CARTESIAN_POINT ( 'NONE',  ( 778.2165204200184689, -286.8164208402378677, 364.9363028652563230 ) ) ;
#42441=CARTESIAN_POINT ( 'NONE',  ( 801.1904061080338124, -92.08914811296570235, 368.3070685750236066 ) ) ;
#42449=CARTESIAN_POINT ( 'NONE',  ( 797.8594530101008786, -13.54369356751140785, 322.1405469898980982 ) ) ;
#42452=CARTESIAN_POINT ( 'NONE',  ( 745.0891759886404770, -388.2709662947829656, 342.4968714119734159 ) ) ;
#42453=CARTESIAN_POINT ( 'NONE',  ( 815.0009284576459549, -294.3510508353230648, 338.7629533639073429 ) ) ;
#42454=CARTESIAN_POINT ( 'NONE',  ( 781.2497674668890113, -84.35105083532374692, 375.3608509340180603 ) ) ;
#42464=CARTESIAN_POINT ( 'NONE',  ( 759.9999999999992042, -462.9681489794448339, 370.0000000000000568 ) ) ;
#42469=CARTESIAN_POINT ( 'NONE',  ( 755.1538015810308480, -254.1908817542435770, 343.0433043558613804 ) ) ;
#42470=CARTESIAN_POINT ( 'NONE',  ( 755.3201227861273992, -123.7255117493292147, 345.3687786644892981 ) ) ;
#42474=CARTESIAN_POINT ( 'NONE',  ( 754.9735926884551418, -306.3510508353230648, 340.5236548041000333 ) ) ;
#42477=CARTESIAN_POINT ( 'NONE',  ( 802.2119215644370342, -54.00906357242601530, 367.5423716828165084 ) ) ;
#42480=CARTESIAN_POINT ( 'NONE',  ( 804.7487373415286811, -187.5436935675108430, 364.7487373415288516 ) ) ;
#42481=CARTESIAN_POINT ( 'NONE',  ( 788.8264449731200330, -69.18005720387488111, 363.6646147819171233 ) ) ;
#42485=CARTESIAN_POINT ( 'NONE',  ( 807.2620300519052989, -456.0090635724247932, 318.0141637701419768 ) ) ;
#42488=CARTESIAN_POINT ( 'NONE',  ( 772.3691319403857278, -359.2601417444137724, 315.8894580844506663 ) ) ;
#42490=CARTESIAN_POINT ( 'NONE',  ( 810.7187646348534145, -42.45278447660223264, 356.7737145352016341 ) ) ;
#42493=CARTESIAN_POINT ( 'NONE',  ( 756.1348686366196716, -41.26014174441479554, 347.5531968255698416 ) ) ;
#42495=CARTESIAN_POINT ( 'NONE',  ( 805.9055244015594326, -219.6237781080506295, 315.8990559732753240 ) ) ;
#42496=CARTESIAN_POINT ( 'NONE',  ( 792.1044303154646968, -12.45278447660232324, 317.8323909638837677 ) ) ;
#42500=CARTESIAN_POINT ( 'NONE',  ( 759.9864689768902508, -194.0891481129654039, 354.9819416627836404 ) ) ;
#42504=CARTESIAN_POINT ( 'NONE',  ( 804.9363028652555840, -328.2709662947831362, 338.2165204200192079 ) ) ;
#42506=CARTESIAN_POINT ( 'NONE',  ( 779.9999999999992042, -452.9681489794448339, 339.9999999999999432 ) ) ;
#42508=CARTESIAN_POINT ( 'NONE',  ( 805.1016975059191054, -54.89650538077837183, 343.0745993439771837 ) ) ;
#42511=CARTESIAN_POINT ( 'NONE',  ( 744.7301800767020268, -268.8164208402378677, 337.4774526936615189 ) ) ;
#42512=CARTESIAN_POINT ( 'NONE',  ( 812.6845335610512393, -7.987414471687621642, 353.5525998758768651 ) ) ;
#42518=CARTESIAN_POINT ( 'NONE',  ( 813.1304606946830518, -281.9073299311468759, 352.3570229623690580 ) ) ;
#42520=CARTESIAN_POINT ( 'NONE',  ( 793.2243759319678702, -338.5328690171411381, 318.4439275373583200 ) ) ;
#42523=CARTESIAN_POINT ( 'NONE',  ( 759.0159684113467620, -160.9181544815165807, 325.8855110935213020 ) ) ;
#42524=CARTESIAN_POINT ( 'NONE',  ( 762.3223304703356007, -7.543693567511430942, 322.3223304703362828 ) ) ;
#42528=CARTESIAN_POINT ( 'NONE',  ( 783.0745993439762742, -224.1908817542436623, 365.1016975059196739 ) ) ;
#42529=CARTESIAN_POINT ( 'NONE',  ( 788.6739635108323228, -223.6454272087891013, 373.9316612368139090 ) ) ;
#42530=CARTESIAN_POINT ( 'NONE',  ( 796.7845633553578182, -201.6237781080506863, 358.5707757039688204 ) ) ;
#42533=CARTESIAN_POINT ( 'NONE',  ( 800.2193346964447755, 5.001760977943074948, 355.1360043628815788 ) ) ;
#42538=CARTESIAN_POINT ( 'NONE',  ( 808.3070685750230950, -18.99823902205683979, 361.1904061080339261 ) ) ;
#42539=CARTESIAN_POINT ( 'NONE',  ( 796.9462024416508257, -84.45278447660206211, 308.9653473494370246 ) ) ;
#42543=CARTESIAN_POINT ( 'NONE',  ( 795.8262568251477660, -358.3726999360613945, 308.3538107759623585 ) ) ;
#42545=CARTESIAN_POINT ( 'NONE',  ( 782.4968714119720516, -322.8164208402377540, 305.0891759886411023 ) ) ;
#42551=CARTESIAN_POINT ( 'NONE',  ( 755.3201227861273992, -435.7255117493282341, 345.3687786644892981 ) ) ;
#42552=CARTESIAN_POINT ( 'NONE',  ( 769.0155153010367712, -178.3726999360619629, 362.7791456095907279 ) ) ;
#42555=CARTESIAN_POINT ( 'NONE',  ( 744.9990715423526808, -90.35105083532373271, 341.2370466360926002 ) ) ;
#42556=CARTESIAN_POINT ( 'NONE',  ( 792.1044303154646968, -420.4527844766009821, 317.8323909638837677 ) ) ;
#42563=CARTESIAN_POINT ( 'NONE',  ( 764.8639956371174549, -224.0891481129653187, 319.7806653035542013 ) ) ;
#42564=CARTESIAN_POINT ( 'NONE',  ( 785.3141322388236176, -237.7255117493289163, 364.4286716492789537 ) ) ;
#42566=ORIENTED_EDGE ( 'NONE', *, *, #7470, .F. ) ;
#42570=CARTESIAN_POINT ( 'NONE',  ( 755.0636971347428243, -412.2709662947829088, 341.7834795799807353 ) ) ;
#42575=CARTESIAN_POINT ( 'NONE',  ( 782.5225473063383106, -166.2709662947836478, 375.2698199232970637 ) ) ;
#42576=CARTESIAN_POINT ( 'NONE',  ( 802.5472867521000353, -268.3726999360616787, 350.8726784830461156 ) ) ;
#42578=CARTESIAN_POINT ( 'NONE',  ( 801.9858362298568863, -195.0783235625961538, 312.7379699480935642 ) ) ;
#42583=CARTESIAN_POINT ( 'NONE',  ( 758.6633372737375112, -236.5328690171414792, 326.9102291470432533 ) ) ;
#42586=ORIENTED_EDGE ( 'NONE', *, *, #41968, .T. ) ;
#42590=ORIENTED_EDGE ( 'NONE', *, *, #1301, .T. ) ;
#42598=VECTOR ( 'NONE', #35018, 1000.000000000000000 ) ;
#42603=CARTESIAN_POINT ( 'NONE',  ( 781.8018195045266339, -22.27096629478410250, 365.1927285166406705 ) ) ;
#42605=CARTESIAN_POINT ( 'NONE',  ( 764.1737431748507561, -250.3726999360618208, 371.6461892240376415 ) ) ;
#42607=CARTESIAN_POINT ( 'NONE',  ( 744.7301800767019131, -220.8164208402379529, 337.4774526936615757 ) ) ;
#42610=CARTESIAN_POINT ( 'NONE',  ( 755.5713283507202505, -341.3618753856922012, 334.6858677611754729 ) ) ;
#42611=CARTESIAN_POINT ( 'NONE',  ( 769.9779781133707957, -91.09997266333496668, 316.7813123517150871 ) ) ;
#42612=CARTESIAN_POINT ( 'NONE',  ( 755.1538015810308480, -86.19088175424408860, 343.0433043558613804 ) ) ;
#42616=CARTESIAN_POINT ( 'NONE',  ( 763.2154366446407039, -141.6237781080508569, 321.4292242960311228 ) ) ;
#42617=CARTESIAN_POINT ( 'NONE',  ( 778.2165204200184689, -358.8164208402375834, 364.9363028652563230 ) ) ;
#42620=CARTESIAN_POINT ( 'NONE',  ( 803.4237431249931660, -135.1800572038746679, 331.2633955100225194 ) ) ;
#42623=CARTESIAN_POINT ( 'NONE',  ( 764.3348316497523456, -430.7146871989590409, 308.6759233522265617 ) ) ;
#42625=CARTESIAN_POINT ( 'NONE',  ( 788.7366044899766848, -323.9073299311468190, 316.5762568750059813 ) ) ;
#42629=CARTESIAN_POINT ( 'NONE',  ( 755.3201227861273992, -411.7255117493282910, 345.3687786644892981 ) ) ;
#42634=VECTOR ( 'NONE', #6535, 1000.000000000000000 ) ;
#42636=CARTESIAN_POINT ( 'NONE',  ( 769.9779781133707957, -427.0999726633338582, 316.7813123517150871 ) ) ;
#42637=CARTESIAN_POINT ( 'NONE',  ( 754.9735926884551418, -138.3510508353236048, 340.5236548041000333 ) ) ;
#42640=CARTESIAN_POINT ( 'NONE',  ( 793.4146539503750546, -385.9874144716864066, 307.6481478633938877 ) ) ;
#42645=CARTESIAN_POINT ( 'NONE',  ( 804.1009440267234822, -23.46360902697155026, 314.0944755984392600 ) ) ;
#42652=CARTESIAN_POINT ( 'NONE',  ( 804.8461984189677878, -362.1908817542432644, 336.9566956441385628 ) ) ;
#42653=CARTESIAN_POINT ( 'NONE',  ( 745.1792804349281596, -350.1908817542433212, 343.7566961878542884 ) ) ;
#42657=CARTESIAN_POINT ( 'NONE',  ( 773.7305795820266212, -129.2817908451530400, 374.8230680027170365 ) ) ;
#42659=CARTESIAN_POINT ( 'NONE',  ( 814.9108240113580450, -112.2709662947838325, 337.5031285880265273 ) ) ;
#42663=CARTESIAN_POINT ( 'NONE',  ( 781.7834795799800531, -202.8164208402380950, 315.0636971347436202 ) ) ;
#42664=CARTESIAN_POINT ( 'NONE',  ( 807.2620300519052989, -456.0090635724247932, 318.0141637701419768 ) ) ;
#42669=CARTESIAN_POINT ( 'NONE',  ( 812.6845335610512393, 16.01258552831230375, 353.5525998758768651 ) ) ;
#42672=CARTESIAN_POINT ( 'NONE',  ( 781.2497674668890113, -324.3510508353229511, 375.3608509340180603 ) ) ;
#42673=CARTESIAN_POINT ( 'NONE',  ( 794.9819416627830151, -156.9982390220564241, 319.9864689768909898 ) ) ;
#42675=CARTESIAN_POINT ( 'NONE',  ( 768.0187753319979720, -320.6346026584195670, 318.0580252608186242 ) ) ;
#42677=CARTESIAN_POINT ( 'NONE',  ( 755.2512626584698410, -79.54369356751119824, 315.2512626584710915 ) ) ;
#42681=CARTESIAN_POINT ( 'NONE',  ( 781.7834795799800531, -10.81642084023869543, 315.0636971347436202 ) ) ;
#42682=CARTESIAN_POINT ( 'NONE',  ( 772.5602148656447525, -393.7255117493283478, 305.7998596910095443 ) ) ;
#42683=CARTESIAN_POINT ( 'NONE',  ( 812.6845335610512393, -271.9874144716868045, 353.5525998758768651 ) ) ;
#42684=CARTESIAN_POINT ( 'NONE',  ( 791.1614460488616487, -59.26014174441473870, 373.5763878283158874 ) ) ;
#42688=EDGE_CURVE ( 'NONE', #30209, #16040, #6863, .T. ) ;
#42689=B_SPLINE_CURVE_WITH_KNOTS ( 'NONE', 3,
 ( #31669, #27516, #16914, #41618, #27980, #23590, #20591, #41397, #34686, #27303, #34908, #45554, #17599, #38385, #9974, #17135, #20809, #6278, #41857, #30993, #37921, #6968, #10201, #3273, #42075, #36, #21053, #24279, #30772, #17365, #13449, #13226, #24045, #6734, #6045, #45312 ),
 .UNSPECIFIED., .F., .F.,
 ( 4, 2, 2, 2, 2, 2, 2, 2, 2, 2, 2, 2, 2, 2, 2, 2, 2, 4 ),
 ( 0.0008252806733485880007, 0.001104729680136533072, 0.001384178686924478251, 0.001943076700500593040, 0.002501974714076708045, 0.003060872727652823484, 0.004178668754804788950, 0.005296464781956755283, 0.007532056836260687949, 0.009767648890564618880, 0.01423883299917248421, 0.01871001710778034607, 0.02094560916208429782, 0.02318120121638824610, 0.02765238532499614266, 0.02988797737930003542, 0.03212356943360392819, 0.03659475354221209537 ),
 .UNSPECIFIED. ) ;
#42691=CARTESIAN_POINT ( 'NONE',  ( 792.3570229623688874, -381.1800572038737869, 373.1304606946836202 ) ) ;
#42698=CARTESIAN_POINT ( 'NONE',  ( 766.0291762391763086, -274.9181544815161828, 360.7704444035551319 ) ) ;
#42699=CARTESIAN_POINT ( 'NONE',  ( 759.7806653035534055, -150.9982390220563957, 324.8639956371180801 ) ) ;
#42703=CARTESIAN_POINT ( 'NONE',  ( 776.9566956441375396, -324.8965053807775121, 364.8461984189686405 ) ) ;
#42705=CARTESIAN_POINT ( 'NONE',  ( 815.3608509340175488, -50.73633629969874193, 341.2497674668889545 ) ) ;
#42707=CARTESIAN_POINT ( 'NONE',  ( 781.8018195045266339, -94.27096629478386092, 365.1927285166406705 ) ) ;
#42708=CARTESIAN_POINT ( 'NONE',  ( 799.9999999999993179, 205.0000000000000568, 329.9999999999999432 ) ) ;
#42710=CARTESIAN_POINT ( 'NONE',  ( 745.7194118038753459, -445.6454272087883055, 348.7631598425976449 ) ) ;
#42712=LINE ( 'NONE', #14998, #12128 ) ;
#42713=CARTESIAN_POINT ( 'NONE',  ( 756.1348686366196716, -377.2601417444137724, 347.5531968255698416 ) ) ;
#42714=CARTESIAN_POINT ( 'NONE',  ( 805.0032342141413437, -61.54369356751124798, 314.9967657858572352 ) ) ;
#42716=CARTESIAN_POINT ( 'NONE',  ( 796.7845633553578182, -57.62377810805111267, 358.5707757039688204 ) ) ;
#42718=CARTESIAN_POINT ( 'NONE',  ( 746.7653713866222915, -209.2601417444142839, 351.0478386215610271 ) ) ;
#42719=CARTESIAN_POINT ( 'NONE',  ( 778.2165204200184689, -22.81642084023865280, 364.9363028652563230 ) ) ;
#42723=CARTESIAN_POINT ( 'NONE',  ( 771.2633955100217236, -191.9073299311471885, 363.4237431249939618 ) ) ;
#42725=CARTESIAN_POINT ( 'NONE',  ( 762.1405469898973024, -337.5436935675102745, 357.8594530101016176 ) ) ;
#42729=CARTESIAN_POINT ( 'NONE',  ( 764.0069404352550464, -39.07832356259662276, 359.2566176426627180 ) ) ;
#42731=CARTESIAN_POINT ( 'NONE',  ( 813.1304606946831655, -305.9073299311468190, 352.3570229623691716 ) ) ;
#42733=CARTESIAN_POINT ( 'NONE',  ( 766.5853460496234675, -13.98741447168760033, 372.3518521366060554 ) ) ;
#42738=CARTESIAN_POINT ( 'NONE',  ( 746.8695393053150156, -293.9073299311468759, 327.6429770376306010 ) ) ;
#42740=CARTESIAN_POINT ( 'NONE',  ( 766.7756240680305382, -350.5328690171411381, 361.5560724626415663 ) ) ;
#42744=CARTESIAN_POINT ( 'NONE',  ( 776.9254006560222479, -164.1908817542438612, 314.8983024940802125 ) ) ;
#42745=CARTESIAN_POINT ( 'NONE',  ( 771.2633955100217236, -47.90732993114767169, 363.4237431249939618 ) ) ;
#42749=CARTESIAN_POINT ( 'NONE',  ( 812.3518521366052028, -265.0999726633344267, 326.5853460496235243 ) ) ;
#42751=CARTESIAN_POINT ( 'NONE',  ( 761.2382568024794409, -207.6237781080506295, 356.9571628226838129 ) ) ;
#42753=CARTESIAN_POINT ( 'NONE',  ( 765.0180583372156207, -0.9982390220569063999, 360.0135310231089534 ) ) ;
#42755=CARTESIAN_POINT ( 'NONE',  ( 745.4481719005789273, -3.725511749329622813, 347.5162901302853129 ) ) ;
#42756=CARTESIAN_POINT ( 'NONE',  ( 745.7998596910086917, -125.3618753856928834, 332.5602148656461168 ) ) ;
#42761=CARTESIAN_POINT ( 'NONE',  ( 748.6759233522253680, -352.3726999360614514, 324.3348316497537098 ) ) ;
#42764=CARTESIAN_POINT ( 'NONE',  ( 745.0891759886404770, -340.2709662947831362, 342.4968714119734159 ) ) ;
#42768=CARTESIAN_POINT ( 'NONE',  ( 803.6646147819161570, -425.9073299311463074, 348.8264449731210561 ) ) ;
#42770=CARTESIAN_POINT ( 'NONE',  ( 780.5236548040995785, -188.7363362996983085, 314.9735926884559944 ) ) ;
#42773=CARTESIAN_POINT ( 'NONE',  ( 798.0661480581538854, -98.53286901714187707, 309.5768839229118043 ) ) ;
#42774=CARTESIAN_POINT ( 'NONE',  ( 797.8594530101009923, -421.5436935675101040, 322.1405469898982119 ) ) ;
#42780=CARTESIAN_POINT ( 'NONE',  ( 759.7806653035534055, -222.9982390220561399, 324.8639956371180801 ) ) ;
#42781=CARTESIAN_POINT ( 'NONE',  ( 778.2165204200184689, -214.8164208402380666, 364.9363028652563230 ) ) ;
#42785=CARTESIAN_POINT ( 'NONE',  ( 785.3141322388236176, -429.7255117493282910, 364.4286716492789537 ) ) ;
#42790=CARTESIAN_POINT ( 'NONE',  ( 745.7998596910086917, -173.3618753856927128, 332.5602148656461168 ) ) ;
#42792=CARTESIAN_POINT ( 'NONE',  ( 763.0428371773158460, -251.4636090269709143, 358.7617431975195359 ) ) ;
#42793=CARTESIAN_POINT ( 'NONE',  ( 763.2154366446407039, -381.6237781080500326, 321.4292242960311228 ) ) ;
#42796=CARTESIAN_POINT ( 'NONE',  ( 814.8230680027162407, -197.8055962898688733, 333.7305795820267917 ) ) ;
#42801=CARTESIAN_POINT ( 'NONE',  ( 756.1348686366196716, -233.2601417444141987, 347.5531968255698416 ) ) ;
#42804=EDGE_CURVE ( 'NONE', #13608, #38059, #29679, .T. ) ;
#42808=CARTESIAN_POINT ( 'NONE',  ( 791.7608162188021197, 178.9475563372491251, 320.0000000000000000 ) ) ;
#42811=CARTESIAN_POINT ( 'NONE',  ( 778.7629533639073998, -176.7363362996983369, 375.0009284576466371 ) ) ;
#42816=CARTESIAN_POINT ( 'NONE',  ( 799.9636004259356241, -382.9181544815159555, 311.2241431872006956 ) ) ;
#42821=CARTESIAN_POINT ( 'NONE',  ( 781.8018195045266339, 1.729033705215812011, 365.1927285166406705 ) ) ;
#42822=CARTESIAN_POINT ( 'NONE',  ( 762.1177392798416577, -234.5545181178799794, 309.8865473780659272 ) ) ;
#42824=CARTESIAN_POINT ( 'NONE',  ( 754.9967657858570647, -217.5436935675107293, 365.0032342141425374 ) ) ;
#42827=CARTESIAN_POINT ( 'NONE',  ( 791.9812246680005501, -308.6346026584195670, 361.9419747391813189 ) ) ;
#42828=CARTESIAN_POINT ( 'NONE',  ( 796.1575198192839480, -78.00906357242591582, 359.4546378042384163 ) ) ;
#42829=CARTESIAN_POINT ( 'NONE',  ( 780.5236548040995785, -68.73633629969867798, 314.9735926884559944 ) ) ;
#42833=CARTESIAN_POINT ( 'NONE',  ( 776.9566956441375396, -156.8965053807780805, 364.8461984189686405 ) ) ;
#42834=CARTESIAN_POINT ( 'NONE',  ( 759.9864689768902508, -362.0891481129648923, 354.9819416627836404 ) ) ;
#42837=CARTESIAN_POINT ( 'NONE',  ( 778.1981804954714335, -130.2709662947837899, 314.8072714833589885 ) ) ;
#42840=CARTESIAN_POINT ( 'NONE',  ( 801.9858362298568863, -435.0783235625953580, 312.7379699480935642 ) ) ;
#42842=CARTESIAN_POINT ( 'NONE',  ( 788.8264449731200330, -333.1800572038740142, 363.6646147819171233 ) ) ;
#42845=CARTESIAN_POINT ( 'NONE',  ( 756.5762568750052424, -435.1800572038737869, 348.7366044899774238 ) ) ;
#42851=CARTESIAN_POINT ( 'NONE',  ( 804.9363028652555840, 7.729033705215793582, 338.2165204200192079 ) ) ;
#42852=CARTESIAN_POINT ( 'NONE',  ( 755.8398074228967971, -115.4419599262327409, 333.4516893846970333 ) ) ;
#42855=CARTESIAN_POINT ( 'NONE',  ( 747.3154664389472828, -403.9874144716863498, 326.4474001241230781 ) ) ;
#42860=CARTESIAN_POINT ( 'NONE',  ( 786.2694204179717872, -69.28179084515321051, 305.1769319972829067 ) ) ;
#42868=CARTESIAN_POINT ( 'NONE',  ( 769.0155153010367712, -370.3726999360613377, 362.7791456095907279 ) ) ;
#42869=CARTESIAN_POINT ( 'NONE',  ( 745.5313806188320314, -327.2817908451525000, 333.7943932421247268 ) ) ;
#42873=CARTESIAN_POINT ( 'NONE',  ( 811.3240766477731540, -148.3726999360620198, 355.6651683502462902 ) ) ;
#42875=CARTESIAN_POINT ( 'NONE',  ( 749.2812353651451076, -126.4527844766019626, 323.2262854647983090 ) ) ;
#42879=CARTESIAN_POINT ( 'NONE',  ( 755.3201227861273992, -219.7255117493289447, 345.3687786644892981 ) ) ;
#42880=CARTESIAN_POINT ( 'NONE',  ( 800.9840315886518738, -4.918154481517067467, 354.1144889064786412 ) ) ;
#42884=CARTESIAN_POINT ( 'NONE',  ( 788.7631598425961101, -25.44195992623301450, 305.7194118038759143 ) ) ;
#42888=CARTESIAN_POINT ( 'NONE',  ( 804.6798772138708955, -39.72551174932951312, 334.6312213355107019 ) ) ;
#42891=CARTESIAN_POINT ( 'NONE',  ( 768.8385539511368734, -311.2601417444139429, 306.4236121716840557 ) ) ;
#42892=CARTESIAN_POINT ( 'NONE',  ( 785.3141322388236176, -141.7255117493291721, 364.4286716492789537 ) ) ;
#42894=CARTESIAN_POINT ( 'NONE',  ( 778.2165204200184689, -334.8164208402376403, 364.9363028652563230 ) ) ;
#42897=CARTESIAN_POINT ( 'NONE',  ( 810.7187646348534145, -90.45278447660209054, 356.7737145352016341 ) ) ;
#42901=CARTESIAN_POINT ( 'NONE',  ( 767.8955696845333705, -48.45278447660219712, 362.1676090361162323 ) ) ;
#42902=CARTESIAN_POINT ( 'NONE',  ( 802.9823548866075953, -385.0999726633340856, 330.0799878456151077 ) ) ;
#42904=CARTESIAN_POINT ( 'NONE',  ( 782.5225473063383106, -382.2709662947829088, 375.2698199232970637 ) ) ;
#42905=CARTESIAN_POINT ( 'NONE',  ( 745.1769319972822814, -281.8055962898686175, 346.2694204179732083 ) ) ;
#42906=CARTESIAN_POINT ( 'NONE',  ( 761.9338519418445230, -62.53286901714199786, 370.4231160770881957 ) ) ;
#42913=CARTESIAN_POINT ( 'NONE',  ( 801.1904061080336987, -404.0891481129646081, 368.3070685750235498 ) ) ;
#42919=CARTESIAN_POINT ( 'NONE',  ( 755.5913626894240451, -277.6454272087889308, 346.6156483768012890 ) ) ;
#42920=CARTESIAN_POINT ( 'NONE',  ( 764.8639956371174549, -152.0891481129655460, 319.7806653035542013 ) ) ;
#42924=CARTESIAN_POINT ( 'NONE',  ( 803.8651313633788504, -341.2601417444138292, 332.4468031744301015 ) ) ;
#42926=CARTESIAN_POINT ( 'NONE',  ( 778.7629533639073998, -56.73633629969872771, 375.0009284576466371 ) ) ;
#42929=CARTESIAN_POINT ( 'NONE',  ( 744.7301800767019131, -196.8164208402380950, 337.4774526936615757 ) ) ;
#42930=CARTESIAN_POINT ( 'NONE',  ( 774.6858677611749044, -105.7255117493293000, 315.5713283507209894 ) ) ;
#42933=CARTESIAN_POINT ( 'NONE',  ( 749.5768839229115201, -444.5545181178792973, 358.0661480581553064 ) ) ;
#42936=CARTESIAN_POINT ( 'NONE',  ( 776.9566956441375396, -348.8965053807774552, 364.8461984189686405 ) ) ;
#42937=CARTESIAN_POINT ( 'NONE',  ( 754.9967657858570647, -49.54369356751129772, 365.0032342141425943 ) ) ;
#42939=CARTESIAN_POINT ( 'NONE',  ( 800.7704444035546203, -52.16923265350567362, 326.0291762391768771 ) ) ;
#42942=CARTESIAN_POINT ( 'NONE',  ( 761.9338519418445230, -206.5328690171415360, 370.4231160770881957 ) ) ;
#42943=CARTESIAN_POINT ( 'NONE',  ( 791.9812246680005501, -68.63460265842033436, 361.9419747391813189 ) ) ;
#42946=CARTESIAN_POINT ( 'NONE',  ( 800.2193346964447755, -186.9982390220563104, 355.1360043628815788 ) ) ;
#42948=CARTESIAN_POINT ( 'NONE',  ( 771.1735550268780344, -345.1800572038739574, 316.3353852180828198 ) ) ;
#42953=CARTESIAN_POINT ( 'NONE',  ( 757.2208543904082489, -64.71468719896019195, 350.9844846989624330 ) ) ;
#42955=CARTESIAN_POINT ( 'NONE',  ( 810.7187646348534145, -306.4527844766013800, 356.7737145352016341 ) ) ;
#42956=CARTESIAN_POINT ( 'NONE',  ( 783.7566961878529810, -0.8965053807785533513, 305.1792804349288417 ) ) ;
#42962=CARTESIAN_POINT ( 'NONE',  ( 812.7932403749906598, -303.1800572038740711, 327.7687537140311633 ) ) ;
#42964=CARTESIAN_POINT ( 'NONE',  ( 799.2566176426618085, -216.0090635724255037, 324.0069404352559559 ) ) ;
#42965=CARTESIAN_POINT ( 'NONE',  ( 802.7791456095903868, -364.7146871989592114, 329.0155153010375102 ) ) ;
#42967=CARTESIAN_POINT ( 'NONE',  ( 793.9708237608222134, -166.9181544815165523, 319.2295555964448681 ) ) ;
#42968=CARTESIAN_POINT ( 'NONE',  ( 788.7366044899766848, -59.90732993114762905, 316.5762568750059813 ) ) ;
#42974=CARTESIAN_POINT ( 'NONE',  ( 750.9282345327678740, -256.9181544815163534, 319.8311093483690115 ) ) ;
#42975=CARTESIAN_POINT ( 'NONE',  ( 760.5453621957607311, -213.0783235625960401, 323.8424801807151425 ) ) ;
#42978=CARTESIAN_POINT ( 'NONE',  ( 805.1927285166397041, 7.183579159761247723, 341.8018195045277707 ) ) ;
#42981=CARTESIAN_POINT ( 'NONE',  ( 814.9108240113580450, -16.27096629478413092, 337.5031285880265273 ) ) ;
#42982=CARTESIAN_POINT ( 'NONE',  ( 812.7932403749906598, -111.1800572038747532, 327.7687537140311633 ) ) ;
#42987=CARTESIAN_POINT ( 'NONE',  ( 768.9521613784389729, -393.8272453906067199, 373.2346286133773106 ) ) ;
#42989=CARTESIAN_POINT ( 'NONE',  ( 808.3070685750230950, -330.9982390220558273, 361.1904061080339261 ) ) ;
#42993=CARTESIAN_POINT ( 'NONE',  ( 794.9819416627830151, -444.9982390220554862, 319.9864689768909898 ) ) ;
#42994=CARTESIAN_POINT ( 'NONE',  ( 796.9571628226829034, -191.4636090269709996, 321.2382568024804641 ) ) ;
#42997=CARTESIAN_POINT ( 'NONE',  ( 768.8385539511368734, -95.26014174441461080, 306.4236121716840557 ) ) ;
#42998=CARTESIAN_POINT ( 'NONE',  ( 759.7806653035535192, -438.9982390220554294, 324.8639956371181370 ) ) ;
#43005=CARTESIAN_POINT ( 'NONE',  ( 800.0135310231082713, -278.0891481129651197, 325.0180583372163028 ) ) ;
#43006=CARTESIAN_POINT ( 'NONE',  ( 803.6646147819162707, -233.9073299311470464, 348.8264449731211130 ) ) ;
#43010=CARTESIAN_POINT ( 'NONE',  ( 762.3223304703356007, -439.5436935675101040, 322.3223304703362828 ) ) ;
#43011=ORIENTED_EDGE ( 'NONE', *, *, #3538, .T. ) ;
#43012=CARTESIAN_POINT ( 'NONE',  ( 751.6929314249750860, -174.9982390220563673, 318.8095938919659034 ) ) ;
#43013=CARTESIAN_POINT ( 'NONE',  ( 796.9571628226829034, -263.4636090269708006, 321.2382568024804641 ) ) ;
#43016=CARTESIAN_POINT ( 'NONE',  ( 744.8212110874229666, -234.8965053807777963, 336.2046728542121627 ) ) ;
#43024=CARTESIAN_POINT ( 'NONE',  ( 803.2186876482843445, -247.9874144716867761, 350.0220218866286928 ) ) ;
#43031=CARTESIAN_POINT ( 'NONE',  ( 760.0363995740630116, -154.9181544815165523, 368.7758568127991907 ) ) ;
#43037=CARTESIAN_POINT ( 'NONE',  ( 814.2001403089898304, -17.36187538569322086, 347.4397851343538264 ) ) ;
#43043=CARTESIAN_POINT ( 'NONE',  ( 771.1735550268778070, -9.180057203875058747, 316.3353852180827630 ) ) ;
#43046=CARTESIAN_POINT ( 'NONE',  ( 786.2694204179717872, -285.2817908451526137, 305.1769319972829067 ) ) ;
#43048=CARTESIAN_POINT ( 'NONE',  ( 808.3070685750230950, -234.9982390220561683, 361.1904061080339261 ) ) ;
#43053=CARTESIAN_POINT ( 'NONE',  ( 791.9812246680005501, -332.6346026584195101, 361.9419747391813189 ) ) ;
#43054=CARTESIAN_POINT ( 'NONE',  ( 773.4516893846965786, -91.64542720878951343, 315.8398074228977066 ) ) ;
#43058=CARTESIAN_POINT ( 'NONE',  ( 801.3366627262608972, -152.5328690171416781, 353.0897708529566899 ) ) ;
#43059=CARTESIAN_POINT ( 'NONE',  ( 802.1676090361156639, -374.6346026584192828, 327.8955696845344505 ) ) ;
#43066=CARTESIAN_POINT ( 'NONE',  ( 796.7737145352015204, 3.365397341579444479, 370.7187646348536987 ) ) ;
#43067=ORIENTED_EDGE ( 'NONE', *, *, #11114, .F. ) ;
#43068=CARTESIAN_POINT ( 'NONE',  ( 768.0187753319979720, -320.6346026584195670, 318.0580252608186242 ) ) ;
#43070=CARTESIAN_POINT ( 'NONE',  ( 764.8639956371174549, -440.0891481129644944, 319.7806653035542013 ) ) ;
#43079=CARTESIAN_POINT ( 'NONE',  ( 804.6798772138708955, 8.274488250670337663, 334.6312213355107019 ) ) ;
#43080=CARTESIAN_POINT ( 'NONE',  ( 746.8695393053150156, -221.9073299311470464, 327.6429770376306010 ) ) ;
#43081=CARTESIAN_POINT ( 'NONE',  ( 775.9200461376533440, -143.8055962898690154, 315.3028492785443291 ) ) ;
#43084=CARTESIAN_POINT ( 'NONE',  ( 744.9990715423526808, -378.3510508353227806, 341.2370466360926002 ) ) ;
#43089=CARTESIAN_POINT ( 'NONE',  ( 766.4474001241216001, -67.09997266333506616, 307.3154664389482491 ) ) ;
#43096=FACE_OUTER_BOUND ( 'NONE', #8987, .T. ) ;
#43098=CARTESIAN_POINT ( 'NONE',  ( 793.9708237608222134, -406.9181544815157849, 319.2295555964448681 ) ) ;
#43104=CARTESIAN_POINT ( 'NONE',  ( 752.7379699480933368, -156.0090635724256742, 361.9858362298580232 ) ) ;
#43106=CARTESIAN_POINT ( 'NONE',  ( 772.5602148656447525, -129.7255117493292289, 305.7998596910095443 ) ) ;
#43111=CARTESIAN_POINT ( 'NONE',  ( 794.9819416627830151, -228.9982390220561683, 319.9864689768909898 ) ) ;
#43114=CARTESIAN_POINT ( 'NONE',  ( 771.3260364891663130, -451.6454272087884192, 306.0683387631859773 ) ) ;
#43118=CARTESIAN_POINT ( 'NONE',  ( 749.8865473780648472, -20.53286901714212931, 322.1177392798429082 ) ) ;
#43121=CARTESIAN_POINT ( 'NONE',  ( 800.2193346964447755, -18.99823902205683979, 355.1360043628815788 ) ) ;
#43123=CARTESIAN_POINT ( 'NONE',  ( 813.2346286133761168, -341.2601417444138292, 328.9521613784389160 ) ) ;
#43124=CARTESIAN_POINT ( 'NONE',  ( 797.6776695296629214, -139.5436935675110135, 357.6776695296636603 ) ) ;
#43127=CARTESIAN_POINT ( 'NONE',  ( 761.9338519418445230, -422.5328690171408539, 370.4231160770881957 ) ) ;
#43129=CARTESIAN_POINT ( 'NONE',  ( 764.8639956371174549, -344.0891481129647786, 319.7806653035542013 ) ) ;
#43137=CARTESIAN_POINT ( 'NONE',  ( 781.7834795799800531, -58.81642084023854267, 315.0636971347436202 ) ) ;
#43138=CARTESIAN_POINT ( 'NONE',  ( 776.9254006560222479, -380.1908817542431507, 314.8983024940802125 ) ) ;
#43140=CARTESIAN_POINT ( 'NONE',  ( 751.6929314249750860, -390.9982390220556567, 318.8095938919659034 ) ) ;
#43141=CARTESIAN_POINT ( 'NONE',  ( 758.0141637701419768, -303.0783235625957559, 367.2620300519063790 ) ) ;
#43142=CARTESIAN_POINT ( 'NONE',  ( 801.9858362298568863, -75.07832356259649487, 312.7379699480935642 ) ) ;
#43145=DIRECTION ( 'NONE',  ( -0.000000000000000000, -1.110223024625155554E-15, 1.000000000000000000 ) ) ;
#43149=ORIENTED_EDGE ( 'NONE', *, *, #10566, .F. ) ;
#43150=CARTESIAN_POINT ( 'NONE',  ( 815.2698199232961542, -424.8164208402372992, 342.5225473063383106 ) ) ;
#43152=CARTESIAN_POINT ( 'NONE',  ( 766.1799889109151991, 20.32535068748918050, 313.3728091324376237 ) ) ;
#43157=CARTESIAN_POINT ( 'NONE',  ( 805.2837595273609850, -290.7363362996980527, 340.5290396650784714 ) ) ;
#43158=CARTESIAN_POINT ( 'NONE',  ( 778.2165204200184689, -166.8164208402382087, 364.9363028652563230 ) ) ;
#43161=CARTESIAN_POINT ( 'NONE',  ( 805.0264073115434940, -318.3510508353230080, 339.4763451958999099 ) ) ;
#43164=CARTESIAN_POINT ( 'NONE',  ( 776.2046728542105711, -44.19088175424421649, 304.8212110874238761 ) ) ;
#43167=CARTESIAN_POINT ( 'NONE',  ( 791.9812246680005501, -116.6346026584201780, 361.9419747391813189 ) ) ;
#43170=CARTESIAN_POINT ( 'NONE',  ( 763.8424801807145741, 5.990936427573807954, 320.5453621957614700 ) ) ;
#43173=CARTESIAN_POINT ( 'NONE',  ( 800.7704444035546203, -412.1692326535045936, 326.0291762391768771 ) ) ;
#43178=CARTESIAN_POINT ( 'NONE',  ( 781.2497674668890113, -228.3510508353232922, 375.3608509340180603 ) ) ;
#43179=CARTESIAN_POINT ( 'NONE',  ( 767.8955696845334842, -48.45278447660221133, 362.1676090361161755 ) ) ;
#43183=CARTESIAN_POINT ( 'NONE',  ( 792.1044303154645831, -228.4527844766015789, 317.8323909638837677 ) ) ;
#43189=CARTESIAN_POINT ( 'NONE',  ( 814.5518280994195948, -279.7255117493288026, 332.4837098697145166 ) ) ;
#43190=CARTESIAN_POINT ( 'NONE',  ( 773.7943932421234194, 0.1944037101305369775, 305.5313806188329409 ) ) ;
#43194=ORIENTED_EDGE ( 'NONE', *, *, #26868, .T. ) ;
#43197=CARTESIAN_POINT ( 'NONE',  ( 800.9747183278959710, -324.9982390220559409, 311.9810565676471583 ) ) ;
#43199=CARTESIAN_POINT ( 'NONE',  ( 757.2208543904082489, -352.7146871989593251, 350.9844846989624330 ) ) ;
#43201=CARTESIAN_POINT ( 'NONE',  ( 760.7433823573367135, -156.0090635724256742, 355.9930595647440441 ) ) ;
#43202=CARTESIAN_POINT ( 'NONE',  ( 755.0636971347428243, -52.27096629478401724, 341.7834795799807353 ) ) ;
#43205=AXIS2_PLACEMENT_3D ( 'NONE', #13267, #9571, #23631 ) ;
#43207=CARTESIAN_POINT ( 'NONE',  ( 752.7379699480933368, -276.0090635724253048, 361.9858362298580232 ) ) ;
#43208=CARTESIAN_POINT ( 'NONE',  ( 787.6308680596127942, -227.2601417444141987, 364.1105419155492768 ) ) ;
#43211=CARTESIAN_POINT ( 'NONE',  ( 762.1405469898971887, -1.543693567511449150, 357.8594530101015607 ) ) ;
#43213=CARTESIAN_POINT ( 'NONE',  ( 800.9747183278959710, -36.99823902205679360, 311.9810565676471583 ) ) ;
#43214=CARTESIAN_POINT ( 'NONE',  ( 751.9810565676468741, -98.08914811296568814, 360.9747183278973921 ) ) ;
#43217=CIRCLE ( 'NONE', #15217, 30.00000000000008171 ) ;
#43218=CARTESIAN_POINT ( 'NONE',  ( 812.3518521366052028, -385.0999726633340856, 326.5853460496235243 ) ) ;
#43220=CARTESIAN_POINT ( 'NONE',  ( 810.7187646348534145, -354.4527844766012095, 356.7737145352016341 ) ) ;
#43223=CARTESIAN_POINT ( 'NONE',  ( 779.9999999999992042, 126.4563064324884465, 350.0000000000000000 ) ) ;
#43224=B_SPLINE_CURVE_WITH_KNOTS ( 'NONE', 3,
 ( #23520, #44559, #13379, #13157, #9228, #34387, #38097, #34140, #37622, #9903, #27006, #5974, #30704, #26760, #30932, #2757, #9458, #30234, #6203, #16852, #9677, #12919, #41550, #44326, #2511, #23301, #12681, #5759, #20295, #16616, #23975, #40640, #27236, #20065, #37403, #45026 ),
 .UNSPECIFIED., .F., .F.,
 ( 4, 2, 2, 2, 2, 2, 2, 2, 2, 2, 2, 2, 2, 2, 2, 2, 2, 4 ),
 ( 0.000000000000000000, 0.004405609005296106002, 0.008811218010592212005, 0.01101402251324022814, 0.01321682701588824428, 0.01762243602118459054, 0.01982524052383277668, 0.02202804502648095936, 0.02643365403177701245, 0.02863645853442487593, 0.03083926303707274288, 0.03194066528839652197, 0.03304206753972029759, 0.03359276866538235540, 0.03414346979104441321, 0.03469417091670646408, 0.03496952147953734380, 0.03524487204236821658 ),
 .UNSPECIFIED. ) ;
#43225=CARTESIAN_POINT ( 'NONE',  ( 797.8594530101008786, -421.5436935675101040, 322.1405469898980982 ) ) ;
#43226=CARTESIAN_POINT ( 'NONE',  ( 793.0897708529556667, -174.5545181178801784, 361.3366627262616362 ) ) ;
#43229=CARTESIAN_POINT ( 'NONE',  ( 759.8311093483677041, -94.16923265350555994, 310.9282345327691814 ) ) ;
#43230=CARTESIAN_POINT ( 'NONE',  ( 805.1927285166399315, -424.8164208402373561, 341.8018195045277707 ) ) ;
#43231=CARTESIAN_POINT ( 'NONE',  ( 801.9858362298568863, -171.0783235625962106, 312.7379699480935642 ) ) ;
#43237=CARTESIAN_POINT ( 'NONE',  ( 801.9419747391806368, -258.4527844766016074, 351.9812246680014027 ) ) ;
#43238=CARTESIAN_POINT ( 'NONE',  ( 755.5713283507202505, -269.3618753856924286, 334.6858677611754729 ) ) ;
#43241=CARTESIAN_POINT ( 'NONE',  ( 769.1273215169530886, 25.28531280103955226, 317.4527132478988847 ) ) ;
#43245=CARTESIAN_POINT ( 'NONE',  ( 747.2067596250078623, -195.1800572038744974, 352.2312462859687230 ) ) ;
#43246=CARTESIAN_POINT ( 'NONE',  ( 759.0159684113467620, -256.9181544815163534, 325.8855110935213020 ) ) ;
#43249=CARTESIAN_POINT ( 'NONE',  ( 800.1688906516307043, -202.1692326535051905, 369.0717654672308186 ) ) ;
#43254=CARTESIAN_POINT ( 'NONE',  ( 766.7756240680305382, -254.5328690171413655, 361.5560724626415663 ) ) ;
#43272=CARTESIAN_POINT ( 'NONE',  ( 788.8264449731200330, -21.18005720387502677, 363.6646147819171233 ) ) ;
#43274=CARTESIAN_POINT ( 'NONE',  ( 768.9521613784389729, -297.8272453906070041, 373.2346286133773106 ) ) ;
#43276=CARTESIAN_POINT ( 'NONE',  ( 758.8095938919642549, -224.0891481129653187, 311.6929314249763365 ) ) ;
#43281=CARTESIAN_POINT ( 'NONE',  ( 771.2633955100217236, -311.9073299311468759, 363.4237431249939618 ) ) ;
#43283=CARTESIAN_POINT ( 'NONE',  ( 780.5236548040995785, -92.73633629969860692, 314.9735926884559944 ) ) ;
#43285=VECTOR ( 'NONE', #19674, 1000.000000000000000 ) ;
#43288=CARTESIAN_POINT ( 'NONE',  ( 760.5453621957607311, -141.0783235625962959, 323.8424801807151425 ) ) ;
#43289=CARTESIAN_POINT ( 'NONE',  ( 757.8323909638827445, -362.6346026584194533, 352.1044303154654358 ) ) ;
#43294=CARTESIAN_POINT ( 'NONE',  ( 756.3353852180819104, -149.9073299311473875, 331.1735550268788302 ) ) ;
#43297=CARTESIAN_POINT ( 'NONE',  ( 795.6651683502461765, -442.7146871989589840, 371.3240766477733814 ) ) ;
#43299=CARTESIAN_POINT ( 'NONE',  ( 771.1735550268778070, -321.1800572038740142, 316.3353852180827630 ) ) ;
#43309=CARTESIAN_POINT ( 'NONE',  ( 765.0180583372156207, -0.9982390220569063999, 360.0135310231089534 ) ) ;
#43310=CARTESIAN_POINT ( 'NONE',  ( 789.9200121543843807, -169.9874144716871172, 317.0176451133914384 ) ) ;
#43311=CIRCLE ( 'NONE', #2730, 10.00000000000000888 ) ;
#43314=CARTESIAN_POINT ( 'NONE',  ( 813.2346286133761168, -413.2601417444136018, 328.9521613784389160 ) ) ;
#43320=CARTESIAN_POINT ( 'NONE',  ( 750.9282345327678740, -64.91815448151686496, 319.8311093483690115 ) ) ;
#43331=CARTESIAN_POINT ( 'NONE',  ( 772.4468031744293057, -393.8272453906067199, 363.8651313633793620 ) ) ;
#43335=CARTESIAN_POINT ( 'NONE',  ( 750.9282345327678740, -184.9181544815165239, 319.8311093483690115 ) ) ;
#43337=CARTESIAN_POINT ( 'NONE',  ( 814.9108240113580450, -136.2709662947837330, 337.5031285880265273 ) ) ;
#43341=CARTESIAN_POINT ( 'NONE',  ( 804.4286716492782716, -233.3618753856925423, 345.3141322388244703 ) ) ;
#43342=CARTESIAN_POINT ( 'NONE',  ( 796.1575198192839480, -30.00906357242607925, 359.4546378042384163 ) ) ;
#43348=CARTESIAN_POINT ( 'NONE',  ( 812.6845335610512393, -31.98741447168754348, 353.5525998758768651 ) ) ;
#43351=CARTESIAN_POINT ( 'NONE',  ( 755.0636971347428243, -28.27096629478409540, 341.7834795799807353 ) ) ;
#43353=CARTESIAN_POINT ( 'NONE',  ( 751.2241431872005251, -328.1692326535048210, 359.9636004259367610 ) ) ;
#43354=CARTESIAN_POINT ( 'NONE',  ( 771.2633955100217236, -167.9073299311473022, 363.4237431249939618 ) ) ;
#43358=CARTESIAN_POINT ( 'NONE',  ( 788.7631598425961101, -433.4419599262316183, 305.7194118038759143 ) ) ;
#43360=CARTESIAN_POINT ( 'NONE',  ( 800.0135310231082713, -326.0891481129649492, 325.0180583372163028 ) ) ;
#43368=CARTESIAN_POINT ( 'NONE',  ( 759.7806653035534055, -54.99823902205672255, 324.8639956371180801 ) ) ;
#43369=CARTESIAN_POINT ( 'NONE',  ( 790.9844846989617508, -382.3726999360613945, 317.2208543904092721 ) ) ;
#43371=CARTESIAN_POINT ( 'NONE',  ( 754.9967657858570647, -409.5436935675101608, 365.0032342141425943 ) ) ;
#43373=CARTESIAN_POINT ( 'NONE',  ( 773.7943932421234194, -95.80559628986917176, 305.5313806188329409 ) ) ;
#43378=CARTESIAN_POINT ( 'NONE',  ( 812.7932403749906598, -423.1800572038737300, 327.7687537140311633 ) ) ;
#43385=CARTESIAN_POINT ( 'NONE',  ( 766.9102291470427417, -306.5545181178797520, 318.6633372737382501 ) ) ;
#43386=CARTESIAN_POINT ( 'NONE',  ( 803.6646147819161570, -137.9073299311473875, 348.8264449731210561 ) ) ;
#43389=CARTESIAN_POINT ( 'NONE',  ( 790.8726784830453198, -322.7146871989593819, 362.5472867521010585 ) ) ;
#43392=CARTESIAN_POINT ( 'NONE',  ( 750.9282345327678740, -64.91815448151686496, 319.8311093483690115 ) ) ;
#43393=CARTESIAN_POINT ( 'NONE',  ( 762.1405469898971887, -193.5436935675108714, 357.8594530101015607 ) ) ;
#43395=CARTESIAN_POINT ( 'NONE',  ( 749.2812353651451076, -198.4527844766017495, 323.2262854647983090 ) ) ;
#43396=CARTESIAN_POINT ( 'NONE',  ( 764.8639956371174549, -128.0891481129655176, 319.7806653035542013 ) ) ;
#43399=CARTESIAN_POINT ( 'NONE',  ( 783.0745993439762742, -8.190881754244330182, 365.1016975059196739 ) ) ;
#43402=CARTESIAN_POINT ( 'NONE',  ( 805.0264073115434940, -390.3510508353227237, 339.4763451958999099 ) ) ;
#43407=CARTESIAN_POINT ( 'NONE',  ( 800.1688906516307043, -226.1692326535051052, 369.0717654672308186 ) ) ;
#43408=CARTESIAN_POINT ( 'NONE',  ( 762.1405469898973024, -49.54369356751129772, 357.8594530101016176 ) ) ;
#43410=CARTESIAN_POINT ( 'NONE',  ( 801.9419747391806368, -234.4527844766016358, 351.9812246680014027 ) ) ;
#43417=CARTESIAN_POINT ( 'NONE',  ( 751.9810565676468741, -290.0891481129650629, 360.9747183278973921 ) ) ;
#43418=CARTESIAN_POINT ( 'NONE',  ( 764.3348316497523456, -46.71468719896022748, 308.6759233522265617 ) ) ;
#43424=EDGE_LOOP ( 'NONE', ( #5487, #42285 ) ) ;
#43425=CARTESIAN_POINT ( 'NONE',  ( 782.4968714119720516, -322.8164208402377540, 305.0891759886411023 ) ) ;
#43426=DIRECTION ( 'NONE',  ( 0.000000000000000000, 0.000000000000000000, 1.000000000000000000 ) ) ;
#43428=CARTESIAN_POINT ( 'NONE',  ( 790.0220218866281812, -199.0999726633346825, 363.2186876482849129 ) ) ;
#43429=CARTESIAN_POINT ( 'NONE',  ( 758.0580252608178853, -54.45278447660219001, 328.0187753319985404 ) ) ;
#43433=CARTESIAN_POINT ( 'NONE',  ( 805.1016975059191054, -222.8965053807778531, 343.0745993439771837 ) ) ;
#43436=CARTESIAN_POINT ( 'NONE',  ( 745.7998596910086917, -437.3618753856919170, 332.5602148656461168 ) ) ;
#43440=CARTESIAN_POINT ( 'NONE',  ( 763.2262854647970016, -56.63460265842036279, 309.2812353651462445 ) ) ;
#43441=CARTESIAN_POINT ( 'NONE',  ( 814.5518280994195948, -111.7255117493293000, 332.4837098697145734 ) ) ;
#43445=CARTESIAN_POINT ( 'NONE',  ( 810.4231160770870019, -384.5545181178795247, 321.9338519418446936 ) ) ;
#43447=CARTESIAN_POINT ( 'NONE',  ( 814.2001403089898304, -353.3618753856922012, 347.4397851343538264 ) ) ;
#43449=CARTESIAN_POINT ( 'NONE',  ( 783.0433043558608688, -0.8965053807785533513, 315.1538015810313027 ) ) ;
#43450=CARTESIAN_POINT ( 'NONE',  ( 773.4516893846965786, -187.6454272087892434, 315.8398074228977066 ) ) ;
#43453=CARTESIAN_POINT ( 'NONE',  ( 798.0661480581538854, -122.5328690171417918, 309.5768839229118043 ) ) ;
#43454=CARTESIAN_POINT ( 'NONE',  ( 800.0135310231082713, -446.0891481129646081, 325.0180583372163028 ) ) ;
#43459=CARTESIAN_POINT ( 'NONE',  ( 768.0187753319979720, -248.6346026584197659, 318.0580252608186242 ) ) ;
#43460=CARTESIAN_POINT ( 'NONE',  ( 800.0135310231082713, -254.0891481129652334, 325.0180583372163028 ) ) ;
#43461=DIRECTION ( 'NONE',  ( 1.000000000000000000, 0.000000000000000000, -0.000000000000000000 ) ) ;
#43463=CARTESIAN_POINT ( 'NONE',  ( 773.3843516231979720, 10.55804007376686826, 364.4086373105754433 ) ) ;
#43465=CARTESIAN_POINT ( 'NONE',  ( 744.7301800767020268, -196.8164208402380950, 337.4774526936615189 ) ) ;
#43466=CARTESIAN_POINT ( 'NONE',  ( 755.1538015810308480, -254.1908817542435770, 343.0433043558613804 ) ) ;
#43467=CARTESIAN_POINT ( 'NONE',  ( 795.9930595647434757, -387.0783235625955285, 320.7433823573372820 ) ) ;
#43470=CARTESIAN_POINT ( 'NONE',  ( 812.6845335610512393, -223.9874144716869182, 353.5525998758768651 ) ) ;
#43475=CARTESIAN_POINT ( 'NONE',  ( 763.2154366446407039, -261.6237781080504305, 321.4292242960311228 ) ) ;
#43477=CYLINDRICAL_SURFACE ( 'NONE', #12331, 10.00000000000000888 ) ;
#43482=CARTESIAN_POINT ( 'NONE',  ( 783.7953271457878373, -176.1908817542438328, 375.1787889125761239 ) ) ;
#43488=CARTESIAN_POINT ( 'NONE',  ( 800.9747183278959710, -12.99823902205686821, 311.9810565676471583 ) ) ;
#43492=CARTESIAN_POINT ( 'NONE',  ( 788.7366044899766848, -35.90732993114770011, 316.5762568750059813 ) ) ;
#43493=CARTESIAN_POINT ( 'NONE',  ( 795.8262568251477660, -286.3726999360617356, 308.3538107759623585 ) ) ;
#43495=CARTESIAN_POINT ( 'NONE',  ( 811.0346526505616112, -254.6346026584196238, 323.0537975583477532 ) ) ;
#43498=ORIENTED_EDGE ( 'NONE', *, *, #24740, .T. ) ;
#43499=CARTESIAN_POINT ( 'NONE',  ( 757.8323909638827445, -338.6346026584195101, 352.1044303154654358 ) ) ;
#43500=CARTESIAN_POINT ( 'NONE',  ( 796.1575198192839480, -102.0090635724258448, 359.4546378042384163 ) ) ;
#43504=CARTESIAN_POINT ( 'NONE',  ( 758.0141637701419768, -135.0783235625962959, 367.2620300519063790 ) ) ;
#43505=CARTESIAN_POINT ( 'NONE',  ( 755.3201227861273992, -387.7255117493283478, 345.3687786644892981 ) ) ;
#43506=ORIENTED_EDGE ( 'NONE', *, *, #41678, .T. ) ;
#43508=CARTESIAN_POINT ( 'NONE',  ( 785.3141322388236176, -165.7255117493291152, 364.4286716492789537 ) ) ;
#43509=UNCERTAINTY_MEASURE_WITH_UNIT (LENGTH_MEASURE( 1.000000000000000082E-05 ), #24063, 'distance_accuracy_value', 'NONE');
#43512=CARTESIAN_POINT ( 'NONE',  ( 792.2269492836462632, -443.1233509495419298, 372.8191558162650949 ) ) ;
#43515=CARTESIAN_POINT ( 'NONE',  ( 768.0187753319979720, -368.6346026584193964, 318.0580252608186242 ) ) ;
#43524=CARTESIAN_POINT ( 'NONE',  ( 804.8461984189677878, -458.1908817542429802, 336.9566956441385628 ) ) ;
#43525=CARTESIAN_POINT ( 'NONE',  ( 751.9810565676468741, -218.0891481129653187, 360.9747183278973921 ) ) ;
#43526=CARTESIAN_POINT ( 'NONE',  ( 789.9200121543843807, -145.9874144716871740, 317.0176451133914384 ) ) ;
#43533=CARTESIAN_POINT ( 'NONE',  ( 813.5763878283155464, -75.82724539060775726, 351.1614460488615350 ) ) ;
#43541=CARTESIAN_POINT ( 'NONE',  ( 755.1538015810308480, -398.1908817542431507, 343.0433043558613804 ) ) ;
#43544=CARTESIAN_POINT ( 'NONE',  ( 790.9844846989617508, -238.3726999360617640, 317.2208543904092721 ) ) ;
#43547=CARTESIAN_POINT ( 'NONE',  ( 762.1177392798416577, -186.5545181178801215, 309.8865473780659272 ) ) ;
#43549=CARTESIAN_POINT ( 'NONE',  ( 814.2001403089898304, -161.3618753856927697, 347.4397851343538264 ) ) ;
#43553=CARTESIAN_POINT ( 'NONE',  ( 803.4237431249931660, -207.1800572038744406, 331.2633955100225194 ) ) ;
#43554=CARTESIAN_POINT ( 'NONE',  ( 793.0897708529556667, -30.55451811788062244, 361.3366627262616362 ) ) ;
#43558=CARTESIAN_POINT ( 'NONE',  ( 751.2241431872005251, -40.16923265350570915, 359.9636004259367610 ) ) ;
#43562=CARTESIAN_POINT ( 'NONE',  ( 758.0580252608178853, -30.45278447660226817, 328.0187753319985404 ) ) ;
#43565=CARTESIAN_POINT ( 'NONE',  ( 746.0683387631852383, -331.4419599262320162, 331.3260364891676204 ) ) ;
#43567=CARTESIAN_POINT ( 'NONE',  ( 778.7502325331095108, -432.3510508353226669, 304.6391490659818828 ) ) ;
#43568=EDGE_CURVE ( 'NONE', #34810, #10891, #20900, .T. ) ;
#43569=CARTESIAN_POINT ( 'NONE',  ( 803.6646147819161570, -353.9073299311467053, 348.8264449731210561 ) ) ;
#43578=CARTESIAN_POINT ( 'NONE',  ( 758.0580252608178853, -54.45278447660219001, 328.0187753319985404 ) ) ;
#43579=CARTESIAN_POINT ( 'NONE',  ( 755.1538015810308480, -374.1908817542432075, 343.0433043558613804 ) ) ;
#43581=CARTESIAN_POINT ( 'NONE',  ( 801.1904061080338124, -428.0891481129645513, 368.3070685750236066 ) ) ;
#43582=CARTESIAN_POINT ( 'NONE',  ( 745.1769319972822814, -305.8055962898684470, 346.2694204179732083 ) ) ;
#43583=CARTESIAN_POINT ( 'NONE',  ( 812.6845335610512393, -103.9874144716873161, 353.5525998758768651 ) ) ;
#43590=CARTESIAN_POINT ( 'NONE',  ( 801.1904061080336987, -428.0891481129644944, 368.3070685750235498 ) ) ;
#43597=CARTESIAN_POINT ( 'NONE',  ( 780.5236548040995785, -308.7363362996979390, 314.9735926884559944 ) ) ;
#43598=CARTESIAN_POINT ( 'NONE',  ( 803.6646147819161570, -161.9073299311472454, 348.8264449731210561 ) ) ;
#43602=CARTESIAN_POINT ( 'NONE',  ( 754.8983024940795303, -330.8965053807774552, 336.9254006560228163 ) ) ;
#43604=CARTESIAN_POINT ( 'NONE',  ( 805.6418435158337843, -77.46360902697138329, 363.8556311672236916 ) ) ;
#43606=CARTESIAN_POINT ( 'NONE',  ( 745.0891759886404770, -196.2709662947835909, 342.4968714119734159 ) ) ;
#43607=CARTESIAN_POINT ( 'NONE',  ( 788.7366044899766848, -131.9073299311473875, 316.5762568750059813 ) ) ;
#43612=CARTESIAN_POINT ( 'NONE',  ( 796.9571628226829034, 0.5363909730283709099, 321.2382568024804641 ) ) ;
#43615=CARTESIAN_POINT ( 'NONE',  ( 761.2382568024794409, -399.6237781080500326, 356.9571628226838129 ) ) ;
#43617=CARTESIAN_POINT ( 'NONE',  ( 776.9566956441375396, -84.89650538077830788, 364.8461984189686405 ) ) ;
#43623=CARTESIAN_POINT ( 'NONE',  ( 786.2056067578752163, -251.8055962898686744, 374.4686193811670023 ) ) ;
#43624=CARTESIAN_POINT ( 'NONE',  ( 778.2165204200184689, -46.81642084023858530, 364.9363028652563230 ) ) ;
#43626=CARTESIAN_POINT ( 'NONE',  ( 804.4286716492782716, -233.3618753856925423, 345.3141322388244703 ) ) ;
#43634=CARTESIAN_POINT ( 'NONE',  ( 801.1904061080338124, -284.0891481129651197, 368.3070685750236066 ) ) ;
#43635=CARTESIAN_POINT ( 'NONE',  ( 744.8212110874229666, -18.89650538077849617, 336.2046728542121627 ) ) ;
#43641=CARTESIAN_POINT ( 'NONE',  ( 762.3223304703356007, -223.5436935675107577, 322.3223304703362828 ) ) ;
#43643=ORIENTED_EDGE ( 'NONE', *, *, #44755, .F. ) ;
#43644=CARTESIAN_POINT ( 'NONE',  ( 747.2067596250078623, -315.1800572038740711, 352.2312462859687230 ) ) ;
#43648=CARTESIAN_POINT ( 'NONE',  ( 763.0428371773158460, -179.4636090269710849, 358.7617431975195359 ) ) ;
#43649=CARTESIAN_POINT ( 'NONE',  ( 805.1927285166397041, -64.81642084023852135, 341.8018195045277707 ) ) ;
#43653=CARTESIAN_POINT ( 'NONE',  ( 772.3691319403857278, -239.2601417444141987, 315.8894580844506663 ) ) ;
#43656=CARTESIAN_POINT ( 'NONE',  ( 772.5602148656447525, -417.7255117493283478, 305.7998596910095443 ) ) ;
#43660=CARTESIAN_POINT ( 'NONE',  ( 814.5518280994195948, -63.72551174932939233, 332.4837098697145734 ) ) ;
#43661=CARTESIAN_POINT ( 'NONE',  ( 755.2512626584698410, -103.5436935675111272, 315.2512626584710915 ) ) ;
#43664=CARTESIAN_POINT ( 'NONE',  ( 764.1737431748507561, -394.3726999360613377, 371.6461892240376415 ) ) ;
#43667=CARTESIAN_POINT ( 'NONE',  ( 777.5031285880264704, -358.8164208402375834, 374.9108240113588408 ) ) ;
#43669=CARTESIAN_POINT ( 'NONE',  ( 784.0799538623451781, 12.19440371013049784, 364.6971507214555572 ) ) ;
#43670=AXIS2_PLACEMENT_3D ( 'NONE', #19073, #29250, #25977 ) ;
#43673=CARTESIAN_POINT ( 'NONE',  ( 808.7758568127978833, -124.1692326535054463, 320.0363995740631822 ) ) ;
#43674=CARTESIAN_POINT ( 'NONE',  ( 800.2193346964446619, -426.9982390220555430, 355.1360043628816925 ) ) ;
#43678=CARTESIAN_POINT ( 'NONE',  ( 804.4286716492782716, -113.3618753856929260, 345.3141322388244703 ) ) ;
#43680=CARTESIAN_POINT ( 'NONE',  ( 774.6858677611749044, -249.7255117493288594, 315.5713283507209894 ) ) ;
#43681=CARTESIAN_POINT ( 'NONE',  ( 800.2193346964446619, -258.9982390220561115, 355.1360043628816925 ) ) ;
#43684=CARTESIAN_POINT ( 'NONE',  ( 803.8651313633788504, 18.73985825558501972, 332.4468031744301015 ) ) ;
#43686=CARTESIAN_POINT ( 'NONE',  ( 777.4774526936600978, -178.2709662947835909, 304.7301800767028226 ) ) ;
#43687=CARTESIAN_POINT ( 'NONE',  ( 801.5560724626406000, -312.5545181178797520, 326.7756240680316182 ) ) ;
#43688=CARTESIAN_POINT ( 'NONE',  ( 783.0433043558608688, -408.8965053807772847, 315.1538015810313027 ) ) ;
#43696=CARTESIAN_POINT ( 'NONE',  ( 801.3366627262608972, -272.5328690171413086, 353.0897708529566899 ) ) ;
#43703=CARTESIAN_POINT ( 'NONE',  ( 764.1737431748507561, -178.3726999360619629, 371.6461892240376415 ) ) ;
#43712=CARTESIAN_POINT ( 'NONE',  ( 755.0636971347428243, -28.27096629478409540, 341.7834795799807353 ) ) ;
#43713=CARTESIAN_POINT ( 'NONE',  ( 778.7629533639073998, -296.7363362996979390, 375.0009284576466371 ) ) ;
#43714=CARTESIAN_POINT ( 'NONE',  ( 759.0252816721024374, -264.9982390220561115, 368.0189434323527280 ) ) ;
#43717=VERTEX_POINT ( 'NONE', #21663 ) ;
#43718=CARTESIAN_POINT ( 'NONE',  ( 755.3201227861273992, -363.7255117493284047, 345.3687786644892981 ) ) ;
#43720=CARTESIAN_POINT ( 'NONE',  ( 763.8424801807145741, -138.0090635724257311, 320.5453621957614700 ) ) ;
#43724=CARTESIAN_POINT ( 'NONE',  ( 765.0180583372156207, -384.9982390220556567, 360.0135310231089534 ) ) ;
#43727=CARTESIAN_POINT ( 'NONE',  ( 757.8323909638827445, -170.6346026584199649, 352.1044303154654358 ) ) ;
#43731=CARTESIAN_POINT ( 'NONE',  ( 765.0180583372156207, -360.9982390220557704, 360.0135310231089534 ) ) ;
#43733=CARTESIAN_POINT ( 'NONE',  ( 781.7834795799800531, -442.8164208402372992, 315.0636971347436202 ) ) ;
#43735=CARTESIAN_POINT ( 'NONE',  ( 747.2067596250078623, -99.18005720387478164, 352.2312462859687230 ) ) ;
#43740=CARTESIAN_POINT ( 'NONE',  ( 764.8639956371174549, -8.089148112965974136, 319.7806653035542013 ) ) ;
#43741=CARTESIAN_POINT ( 'NONE',  ( 756.1348686366196716, -161.2601417444143976, 347.5531968255698416 ) ) ;
#43747=CIRCLE ( 'NONE', #20145, 10.00000000000000888 ) ;
#43750=CARTESIAN_POINT ( 'NONE',  ( 755.8990559732751535, -83.46360902697136908, 365.9055244015606831 ) ) ;
#43759=CARTESIAN_POINT ( 'NONE',  ( 790.0220218866281812, -415.0999726633340288, 363.2186876482849129 ) ) ;
#43763=CARTESIAN_POINT ( 'NONE',  ( 814.8207195650702488, -194.1908817542437475, 336.2433038121456548 ) ) ;
#43765=CARTESIAN_POINT ( 'NONE',  ( 759.0252816721024374, -144.9982390220564525, 368.0189434323527280 ) ) ;
#43769=CARTESIAN_POINT ( 'NONE',  ( 762.3223304703356007, -247.5436935675106724, 322.3223304703362828 ) ) ;
#43770=CARTESIAN_POINT ( 'NONE',  ( 799.2566176426618085, -24.00906357242609346, 324.0069404352559559 ) ) ;
#43775=CARTESIAN_POINT ( 'NONE',  ( 757.2208543904082489, -64.71468719896019195, 350.9844846989624330 ) ) ;
#43779=CARTESIAN_POINT ( 'NONE',  ( 771.2633955100217236, -23.90732993114773919, 363.4237431249939618 ) ) ;
#43783=CARTESIAN_POINT ( 'NONE',  ( 811.6461892240364477, -340.7146871989592114, 324.1737431748509835 ) ) ;
#43786=CARTESIAN_POINT ( 'NONE',  ( 791.9812246680005501, -332.6346026584195101, 361.9419747391813189 ) ) ;
#43795=CARTESIAN_POINT ( 'NONE',  ( 754.8072714833581358, -52.81642084023856398, 338.1981804954720587 ) ) ;
#43796=CARTESIAN_POINT ( 'NONE',  ( 780.5236548040995785, -356.7363362996978253, 314.9735926884559944 ) ) ;
#43797=CARTESIAN_POINT ( 'NONE',  ( 814.2001403089898304, -425.3618753856919170, 347.4397851343538264 ) ) ;
#43799=CARTESIAN_POINT ( 'NONE',  ( 749.8865473780648472, -308.5328690171412518, 322.1177392798429082 ) ) ;
#43800=CARTESIAN_POINT ( 'NONE',  ( 800.1688906516307043, -106.1692326535054889, 369.0717654672308186 ) ) ;
#43804=CARTESIAN_POINT ( 'NONE',  ( 745.7998596910086917, -413.3618753856920307, 332.5602148656461168 ) ) ;
#43809=DIRECTION ( 'NONE',  ( 0.000000000000000000, 0.000000000000000000, 1.000000000000000000 ) ) ;
#43811=CARTESIAN_POINT ( 'NONE',  ( 758.4439275373578084, -300.5545181178797520, 353.2243759319684386 ) ) ;
#43815=CARTESIAN_POINT ( 'NONE',  ( 791.0478386215596629, -69.82724539060775726, 306.7653713866226326 ) ) ;
#43819=CARTESIAN_POINT ( 'NONE',  ( 788.7366044899766848, -107.9073299311474727, 316.5762568750059813 ) ) ;
#43824=CARTESIAN_POINT ( 'NONE',  ( 793.9708237608222134, 1.081845518482914104, 319.2295555964448681 ) ) ;
#43827=CARTESIAN_POINT ( 'NONE',  ( 755.0488828828309806, -401.8055962898681059, 344.1219089521771934 ) ) ;
#43833=CARTESIAN_POINT ( 'NONE',  ( 766.5853460496234675, -229.9874144716869466, 372.3518521366060554 ) ) ;
#43834=CARTESIAN_POINT ( 'NONE',  ( 785.3141322388236176, -45.72551174932949181, 364.4286716492789537 ) ) ;
#43838=CARTESIAN_POINT ( 'NONE',  ( 755.5713283507202505, -221.3618753856925707, 334.6858677611754729 ) ) ;
#43841=ADVANCED_FACE ( 'NONE', ( #18224 ), #32300, .F. ) ;
#43849=CARTESIAN_POINT ( 'NONE',  ( 814.9108240113580450, -328.2709662947831362, 337.5031285880265273 ) ) ;
#43850=CARTESIAN_POINT ( 'NONE',  ( 805.9055244015594326, -27.62377810805120149, 315.8990559732753240 ) ) ;
#43855=CARTESIAN_POINT ( 'NONE',  ( 762.3223304703356007, -199.5436935675108430, 322.3223304703362828 ) ) ;
#43858=CARTESIAN_POINT ( 'NONE',  ( 792.3570229623688874, -309.1800572038740711, 373.1304606946836202 ) ) ;
#43859=CIRCLE ( 'NONE', #23942, 30.00000000000008171 ) ;
#43863=DIRECTION ( 'NONE',  ( 0.000000000000000000, 0.000000000000000000, 1.000000000000000000 ) ) ;
#43866=CARTESIAN_POINT ( 'NONE',  ( 755.5913626894240451, -181.6454272087892434, 346.6156483768012890 ) ) ;
#43868=CARTESIAN_POINT ( 'NONE',  ( 762.3223304703356007, -79.54369356751119824, 322.3223304703362828 ) ) ;
#43872=CARTESIAN_POINT ( 'NONE',  ( 755.0488828828309806, -257.8055962898686744, 344.1219089521771934 ) ) ;
#43875=CARTESIAN_POINT ( 'NONE',  ( 792.3570229623688874, -429.1800572038737869, 373.1304606946836202 ) ) ;
#43881=CARTESIAN_POINT ( 'NONE',  ( 787.5162901302840055, -59.36187538569306810, 305.4481719005792684 ) ) ;
#43882=CARTESIAN_POINT ( 'NONE',  ( 755.2512626584698410, -151.5436935675109851, 315.2512626584710915 ) ) ;
#43887=CARTESIAN_POINT ( 'NONE',  ( 811.0346526505616112, -374.6346026584192828, 323.0537975583477532 ) ) ;
#43889=CARTESIAN_POINT ( 'NONE',  ( 756.7813123517142913, 4.012585528312341054, 329.9779781133712504 ) ) ;
#43894=CARTESIAN_POINT ( 'NONE',  ( 812.6845335610512393, -127.9874144716872308, 353.5525998758768651 ) ) ;
#43901=CARTESIAN_POINT ( 'NONE',  ( 805.1927285166397041, -136.8164208402382371, 341.8018195045277707 ) ) ;
#43904=CARTESIAN_POINT ( 'NONE',  ( 778.1981804954714335, -274.2709662947833067, 314.8072714833589885 ) ) ;
#43905=CARTESIAN_POINT ( 'NONE',  ( 756.5762568750052424, -267.1800572038742985, 348.7366044899774238 ) ) ;
#43908=CARTESIAN_POINT ( 'NONE',  ( 789.9200121543843807, 22.01258552831228599, 317.0176451133914384 ) ) ;
#43912=CARTESIAN_POINT ( 'NONE',  ( 812.7932403749906598, -231.1800572038743553, 327.7687537140311633 ) ) ;
#43913=CARTESIAN_POINT ( 'NONE',  ( 766.9102291470427417, -306.5545181178797520, 318.6633372737382501 ) ) ;
#43914=CARTESIAN_POINT ( 'NONE',  ( 803.8651313633788504, -389.2601417444136018, 332.4468031744301015 ) ) ;
#43924=CARTESIAN_POINT ( 'NONE',  ( 761.2382568024794409, -279.6237781080503737, 356.9571628226838129 ) ) ;
#43932=CARTESIAN_POINT ( 'NONE',  ( 804.1009440267234822, -191.4636090269709996, 314.0944755984392600 ) ) ;
#43937=AXIS2_PLACEMENT_3D ( 'NONE', #32468, #135, #24840 ) ;
#43942=DIRECTION ( 'NONE',  ( -1.000000000000000000, -0.000000000000000000, 0.000000000000000000 ) ) ;
#43943=CARTESIAN_POINT ( 'NONE',  ( 768.0187753319979720, -32.63460265842044095, 318.0580252608186242 ) ) ;
#43944=CARTESIAN_POINT ( 'NONE',  ( 793.5525998758768083, -271.0999726633344267, 372.6845335610516941 ) ) ;
#43945=CARTESIAN_POINT ( 'NONE',  ( 745.4481719005789273, -267.7255117493286320, 347.5162901302853129 ) ) ;
#43949=CARTESIAN_POINT ( 'NONE',  ( 774.6858677611749044, -345.7255117493285184, 315.5713283507209894 ) ) ;
#43950=CARTESIAN_POINT ( 'NONE',  ( 801.5560724626406000, -120.5545181178803205, 326.7756240680316182 ) ) ;
#43955=CARTESIAN_POINT ( 'NONE',  ( 767.8955696845333705, -384.4527844766011526, 362.1676090361162323 ) ) ;
#43960=CARTESIAN_POINT ( 'NONE',  ( 803.6646147819161570, -161.9073299311472454, 348.8264449731210561 ) ) ;
#43965=CARTESIAN_POINT ( 'NONE',  ( 795.1360043628807261, -356.0891481129647218, 360.2193346964456282 ) ) ;
#43971=CARTESIAN_POINT ( 'NONE',  ( 763.0537975583476964, -72.45278447660213317, 371.0346526505628617 ) ) ;
#43976=CARTESIAN_POINT ( 'NONE',  ( 747.2067596250078623, -243.1800572038743269, 352.2312462859687230 ) ) ;
#43977=CARTESIAN_POINT ( 'NONE',  ( 795.9930595647434757, -171.0783235625962106, 320.7433823573372820 ) ) ;
#43978=CARTESIAN_POINT ( 'NONE',  ( 767.9999999999992042, 205.0000000000000568, 360.0000000000000000 ) ) ;
#43984=CARTESIAN_POINT ( 'NONE',  ( 766.4474001241216001, -115.0999726633348956, 307.3154664389482491 ) ) ;
#43986=CARTESIAN_POINT ( 'NONE',  ( 759.9999999999992042, 205.0000000000000568, 339.9999999999999432 ) ) ;
#43995=CARTESIAN_POINT ( 'NONE',  ( 758.4439275373578084, -396.5545181178794678, 353.2243759319684386 ) ) ;
#43998=CARTESIAN_POINT ( 'NONE',  ( 804.6971507214547046, -243.2817908451526705, 344.0799538623459739 ) ) ;
#44002=CARTESIAN_POINT ( 'NONE',  ( 791.0478386215596629, -165.8272453906074873, 306.7653713866226326 ) ) ;
#44004=CARTESIAN_POINT ( 'NONE',  ( 744.7301800767019131, -148.8164208402382656, 337.4774526936615757 ) ) ;
#44008=CARTESIAN_POINT ( 'NONE',  ( 805.1927285166397041, -256.8164208402379245, 341.8018195045277707 ) ) ;
#44009=CARTESIAN_POINT ( 'NONE',  ( 760.7433823573367135, -12.00906357242613609, 355.9930595647440441 ) ) ;
#44014=CARTESIAN_POINT ( 'NONE',  ( 757.2208543904082489, -88.71468719896009247, 350.9844846989624330 ) ) ;
#44017=CARTESIAN_POINT ( 'NONE',  ( 778.2165204200184689, -70.81642084023850714, 364.9363028652563230 ) ) ;
#44020=CARTESIAN_POINT ( 'NONE',  ( 756.1443688327750579, -357.6237781080501463, 314.3581564841659315 ) ) ;
#44023=CARTESIAN_POINT ( 'NONE',  ( 755.5713283507202505, -365.3618753856920875, 334.6858677611754729 ) ) ;
#44032=CARTESIAN_POINT ( 'NONE',  ( 803.4237431249931660, -111.1800572038747532, 331.2633955100225194 ) ) ;
#44033=CARTESIAN_POINT ( 'NONE',  ( 804.4086373105744769, -409.6454272087884760, 333.3843516231986541 ) ) ;
#44035=CARTESIAN_POINT ( 'NONE',  ( 787.5162901302840055, -443.3618753856917465, 305.4481719005793252 ) ) ;
#44037=CARTESIAN_POINT ( 'NONE',  ( 746.0683387631852383, -331.4419599262320162, 331.3260364891676204 ) ) ;
#44038=CARTESIAN_POINT ( 'NONE',  ( 815.1787889125755555, -102.8965053807782368, 343.7953271457877804 ) ) ;
#44043=CARTESIAN_POINT ( 'NONE',  ( 748.9653473494363425, -410.6346026584191122, 356.9462024416521331 ) ) ;
#44044=CARTESIAN_POINT ( 'NONE',  ( 779.9999999999990905, 18.49609980828599376, 309.9999999999999432 ) ) ;
#44050=CARTESIAN_POINT ( 'NONE',  ( 763.0428371773158460, -299.4636090269707438, 358.7617431975195359 ) ) ;
#44051=CARTESIAN_POINT ( 'NONE',  ( 771.1735550268778070, -177.1800572038744690, 316.3353852180827630 ) ) ;
#44053=CARTESIAN_POINT ( 'NONE',  ( 747.6481478633932056, -277.0999726633344267, 353.4146539503763620 ) ) ;
#44056=CARTESIAN_POINT ( 'NONE',  ( 748.6759233522253680, -64.37269993606231822, 324.3348316497537098 ) ) ;
#44061=CARTESIAN_POINT ( 'NONE',  ( 759.7806653035534055, -150.9982390220563957, 324.8639956371180801 ) ) ;
#44066=CARTESIAN_POINT ( 'NONE',  ( 769.9779781133707957, -19.09997266333520116, 316.7813123517150871 ) ) ;
#44069=CARTESIAN_POINT ( 'NONE',  ( 787.6308680596127942, -395.2601417444136587, 364.1105419155492768 ) ) ;
#44072=CARTESIAN_POINT ( 'NONE',  ( 791.7608162188021197, 178.9475563372491251, 320.0000000000000000 ) ) ;
#44073=CARTESIAN_POINT ( 'NONE',  ( 788.7631598425961101, -241.4419599262322720, 305.7194118038759143 ) ) ;
#44074=CARTESIAN_POINT ( 'NONE',  ( 762.3223304703356007, -103.5436935675111272, 322.3223304703362828 ) ) ;
#44078=CARTESIAN_POINT ( 'NONE',  ( 755.3201227861273992, -219.7255117493289447, 345.3687786644892981 ) ) ;
#44086=CARTESIAN_POINT ( 'NONE',  ( 749.2812353651451076, -318.4527844766014368, 323.2262854647983090 ) ) ;
#44087=CARTESIAN_POINT ( 'NONE',  ( 778.7502325331095108, -48.35105083532386061, 304.6391490659818828 ) ) ;
#44093=CARTESIAN_POINT ( 'NONE',  ( 755.5713283507202505, -197.3618753856926560, 334.6858677611754729 ) ) ;
#44096=AXIS2_PLACEMENT_3D ( 'NONE', #1422, #29604, #12053 ) ;
#44097=CARTESIAN_POINT ( 'NONE',  ( 767.6429770376289525, -321.1800572038740142, 306.8695393053162093 ) ) ;
#44101=CARTESIAN_POINT ( 'NONE',  ( 798.5707757039680246, -197.4636090269709996, 356.7845633553585003 ) ) ;
#44102=CARTESIAN_POINT ( 'NONE',  ( 757.8323909638827445, -74.63460265842032015, 352.1044303154654358 ) ) ;
#44103=ORIENTED_EDGE ( 'NONE', *, *, #23205, .T. ) ;
#44106=CARTESIAN_POINT ( 'NONE',  ( 786.6156483768007774, -265.4419599262323004, 315.5913626894246136 ) ) ;
#44109=CARTESIAN_POINT ( 'NONE',  ( 787.5162901302840055, -419.3618753856918033, 305.4481719005792684 ) ) ;
#44113=CARTESIAN_POINT ( 'NONE',  ( 755.2512626584698410, -55.54369356751127640, 315.2512626584710915 ) ) ;
#44114=CARTESIAN_POINT ( 'NONE',  ( 808.0189434323515343, -158.0891481129655176, 319.0252816721025511 ) ) ;
#44118=CARTESIAN_POINT ( 'NONE',  ( 815.2698199232961542, -376.8164208402375834, 342.5225473063383106 ) ) ;
#44120=CARTESIAN_POINT ( 'NONE',  ( 793.2243759319678702, 21.46713098285774279, 318.4439275373583200 ) ) ;
#44123=CARTESIAN_POINT ( 'NONE',  ( 814.8230680027162407, -149.8055962898689870, 333.7305795820267917 ) ) ;
#44124=CARTESIAN_POINT ( 'NONE',  ( 794.9819416627830151, 11.00176097794305541, 319.9864689768909898 ) ) ;
#44129=CARTESIAN_POINT ( 'NONE',  ( 762.1405469898971887, -121.5436935675110419, 357.8594530101015607 ) ) ;
#44132=CARTESIAN_POINT ( 'NONE',  ( 778.1981804954714335, -298.2709662947830793, 314.8072714833589885 ) ) ;
#44133=CARTESIAN_POINT ( 'NONE',  ( 759.7806653035535192, -246.9982390220560831, 324.8639956371181370 ) ) ;
#44136=CARTESIAN_POINT ( 'NONE',  ( 769.1273215169530886, 1.285312801039623753, 317.4527132478988847 ) ) ;
#44140=ADVANCED_FACE ( 'NONE', ( #37356 ), #37115, .F. ) ;
#44141=CARTESIAN_POINT ( 'NONE',  ( 801.1904061080338124, -236.0891481129652334, 368.3070685750236066 ) ) ;
#44142=CARTESIAN_POINT ( 'NONE',  ( 802.9823548866075953, -289.0999726633343698, 330.0799878456151077 ) ) ;
#44143=CARTESIAN_POINT ( 'NONE',  ( 758.6633372737375112, -404.5328690171409107, 326.9102291470432533 ) ) ;
#44151=CARTESIAN_POINT ( 'NONE',  ( 764.0069404352550464, -303.0783235625957559, 359.2566176426627180 ) ) ;
#44154=DIRECTION ( 'NONE',  ( 0.000000000000000000, -1.000000000000000000, 0.000000000000000000 ) ) ;
#44158=CARTESIAN_POINT ( 'NONE',  ( 797.8822607201568644, -198.5545181178800647, 370.1134526219340160 ) ) ;
#44159=AXIS2_PLACEMENT_3D ( 'NONE', #23371, #36399, #26232 ) ;
#44165=ADVANCED_FACE ( 'NONE', ( #22808 ), #36901, .T. ) ;
#44166=CARTESIAN_POINT ( 'NONE',  ( 805.0032342141412300, -37.54369356751132614, 314.9967657858571783 ) ) ;
#44170=CARTESIAN_POINT ( 'NONE',  ( 771.1735550268778070, -57.18005720387489532, 316.3353852180827630 ) ) ;
#44171=CARTESIAN_POINT ( 'NONE',  ( 757.7880784355613741, -306.0090635724252479, 312.4576283171834916 ) ) ;
#44172=CARTESIAN_POINT ( 'NONE',  ( 792.2312462859673587, -251.9073299311470748, 307.2067596250082602 ) ) ;
#44176=CARTESIAN_POINT ( 'NONE',  ( 800.2193346964447755, -354.9982390220557704, 355.1360043628815788 ) ) ;
#44177=CARTESIAN_POINT ( 'NONE',  ( 760.7433823573367135, -132.0090635724257595, 355.9930595647440441 ) ) ;
#44182=CARTESIAN_POINT ( 'NONE',  ( 813.9316612368132837, -127.4419599262326983, 348.6739635108323228 ) ) ;
#44183=CARTESIAN_POINT ( 'NONE',  ( 804.4286716492782716, -401.3618753856920307, 345.3141322388244703 ) ) ;
#44184=ORIENTED_EDGE ( 'NONE', *, *, #2106, .F. ) ;
#44188=CARTESIAN_POINT ( 'NONE',  ( 755.5713283507202505, -173.3618753856927128, 334.6858677611754729 ) ) ;
#44189=CARTESIAN_POINT ( 'NONE',  ( 754.8072714833583632, -172.8164208402381519, 338.1981804954721156 ) ) ;
#44191=DIRECTION ( 'NONE',  ( 1.000000000000000000, 0.000000000000000000, -0.000000000000000000 ) ) ;
#44192=ADVANCED_BREP_SHAPE_REPRESENTATION ( '', ( #31946, #26858 ), #27503 ) ;
#44194=CARTESIAN_POINT ( 'NONE',  ( 794.9819416627830151, -348.9982390220558273, 319.9864689768909898 ) ) ;
#44198=EDGE_CURVE ( 'NONE', #22109, #37078, #43747, .T. ) ;
#44201=CARTESIAN_POINT ( 'NONE',  ( 792.2312462859673587, -131.9073299311473875, 307.2067596250082602 ) ) ;
#44204=VERTEX_POINT ( 'NONE', #35024 ) ;
#44206=CARTESIAN_POINT ( 'NONE',  ( 748.9653473494363425, -242.6346026584197659, 356.9462024416521331 ) ) ;
#44207=CARTESIAN_POINT ( 'NONE',  ( 770.0799878456142551, -181.9874144716870887, 362.9823548866085616 ) ) ;
#44210=CARTESIAN_POINT ( 'NONE',  ( 815.0009284576459549, -414.3510508353227237, 338.7629533639073429 ) ) ;
#44216=CARTESIAN_POINT ( 'NONE',  ( 815.3608509340175488, -98.73633629969859271, 341.2497674668889545 ) ) ;
#44225=CARTESIAN_POINT ( 'NONE',  ( 779.4763451958990572, -440.7363362996975980, 365.0264073115438919 ) ) ;
#44226=CARTESIAN_POINT ( 'NONE',  ( 768.9521613784389729, -369.8272453906068904, 373.2346286133773106 ) ) ;
#44229=CARTESIAN_POINT ( 'NONE',  ( 786.5483106153019435, -247.6454272087890160, 364.1601925771022366 ) ) ;
#44234=CARTESIAN_POINT ( 'NONE',  ( 762.1177392798416577, -210.5545181178800647, 309.8865473780659272 ) ) ;
#44236=CARTESIAN_POINT ( 'NONE',  ( 745.7998596910086917, -149.3618753856928265, 332.5602148656461168 ) ) ;
#44239=CARTESIAN_POINT ( 'NONE',  ( 778.2165204200184689, -262.8164208402379245, 364.9363028652563230 ) ) ;
#44240=CARTESIAN_POINT ( 'NONE',  ( 790.0220218866281812, -7.099972663335241130, 363.2186876482849129 ) ) ;
#44246=CARTESIAN_POINT ( 'NONE',  ( 776.9566956441375396, -84.89650538077830788, 364.8461984189686405 ) ) ;
#44250=CARTESIAN_POINT ( 'NONE',  ( 762.1405469898971887, -49.54369356751129061, 357.8594530101015607 ) ) ;
#44253=CARTESIAN_POINT ( 'NONE',  ( 814.8230680027162407, -389.8055962898682765, 333.7305795820267917 ) ) ;
#44254=EDGE_LOOP ( 'NONE', ( #17050, #28713, #5636, #3366, #16719, #17916 ) ) ;
#44255=CARTESIAN_POINT ( 'NONE',  ( 745.4481719005789273, -3.725511749329622813, 347.5162901302853129 ) ) ;
#44257=CARTESIAN_POINT ( 'NONE',  ( 778.2165204200184689, -382.8164208402374697, 364.9363028652563230 ) ) ;
#44258=EDGE_CURVE ( 'NONE', #12793, #10247, #34146, .T. ) ;
#44265=CARTESIAN_POINT ( 'NONE',  ( 804.9363028652555840, -88.27096629478390355, 338.2165204200192079 ) ) ;
#44266=CARTESIAN_POINT ( 'NONE',  ( 793.0897708529556667, -390.5545181178794678, 361.3366627262616362 ) ) ;
#44267=CARTESIAN_POINT ( 'NONE',  ( 808.0189434323515343, -422.0891481129647218, 319.0252816721025511 ) ) ;
#44269=CARTESIAN_POINT ( 'NONE',  ( 798.0661480581538854, -338.5328690171411381, 309.5768839229118043 ) ) ;
#44270=CARTESIAN_POINT ( 'NONE',  ( 798.0661480581538854, -122.5328690171417918, 309.5768839229118043 ) ) ;
#44274=CARTESIAN_POINT ( 'NONE',  ( 746.4236121716829757, -15.82724539060794200, 328.8385539511384650 ) ) ;
#44281=CARTESIAN_POINT ( 'NONE',  ( 798.5707757039680246, -317.4636090269706301, 356.7845633553585003 ) ) ;
#44282=CARTESIAN_POINT ( 'NONE',  ( 756.5762568750052424, -171.1800572038745543, 348.7366044899774238 ) ) ;
#44284=CARTESIAN_POINT ( 'NONE',  ( 773.7305795820266212, -297.2817908451526137, 374.8230680027170365 ) ) ;
#44287=CARTESIAN_POINT ( 'NONE',  ( 799.9636004259356241, -70.91815448151683654, 311.2241431872006956 ) ) ;
#44290=CARTESIAN_POINT ( 'NONE',  ( 767.7687537140311633, -215.9073299311471317, 372.7932403749916830 ) ) ;
#44291=CARTESIAN_POINT ( 'NONE',  ( 803.4237431249931660, -159.1800572038746111, 331.2633955100225194 ) ) ;
#44295=CARTESIAN_POINT ( 'NONE',  ( 769.9779781133707957, -67.09997266333506616, 316.7813123517150871 ) ) ;
#44298=CARTESIAN_POINT ( 'NONE',  ( 758.6633372737375112, -428.5328690171409107, 326.9102291470432533 ) ) ;
#44300=CARTESIAN_POINT ( 'NONE',  ( 802.7791456095903868, -76.71468719896012090, 329.0155153010375102 ) ) ;
#44303=CARTESIAN_POINT ( 'NONE',  ( 788.7631598425961101, -289.4419599262321299, 305.7194118038759143 ) ) ;
#44304=CARTESIAN_POINT ( 'NONE',  ( 756.3353852180820240, -77.90732993114757221, 331.1735550268787733 ) ) ;
#44308=CARTESIAN_POINT ( 'NONE',  ( 804.6798772138708955, -279.7255117493288026, 334.6312213355107019 ) ) ;
#44314=CARTESIAN_POINT ( 'NONE',  ( 810.7187646348534145, -330.4527844766013231, 356.7737145352016341 ) ) ;
#44315=CARTESIAN_POINT ( 'NONE',  ( 754.0944755984390895, -207.6237781080506295, 364.1009440267246760 ) ) ;
#44316=CARTESIAN_POINT ( 'NONE',  ( 748.3538107759620743, -40.71468719896024879, 355.8262568251490165 ) ) ;
#44321=CARTESIAN_POINT ( 'NONE',  ( 781.8018195045266339, -214.2709662947834488, 365.1927285166406705 ) ) ;
#44324=CARTESIAN_POINT ( 'NONE',  ( 800.9747183278959710, -372.9982390220557704, 311.9810565676471583 ) ) ;
#44326=CARTESIAN_POINT ( 'NONE',  ( 792.4730984305310812, 16.45630643248850333, 314.5980907654948169 ) ) ;
#44328=CARTESIAN_POINT ( 'NONE',  ( 769.9779781133707957, -187.0999726633346825, 316.7813123517150871 ) ) ;
#44329=CARTESIAN_POINT ( 'NONE',  ( 758.0580252608178853, -78.45278447660211896, 328.0187753319985404 ) ) ;
#44333=CARTESIAN_POINT ( 'NONE',  ( 772.3691319403857278, -263.2601417444141134, 315.8894580844506663 ) ) ;
#44336=CARTESIAN_POINT ( 'NONE',  ( 808.3070685750230950, -426.9982390220554862, 361.1904061080339261 ) ) ;
#44340=CARTESIAN_POINT ( 'NONE',  ( 767.6429770376289525, -81.18005720387481006, 306.8695393053162093 ) ) ;
#44341=CARTESIAN_POINT ( 'NONE',  ( 746.8695393053150156, -149.9073299311473875, 327.6429770376306010 ) ) ;
#44346=CARTESIAN_POINT ( 'NONE',  ( 758.8095938919642549, -392.0891481129648355, 311.6929314249763365 ) ) ;
#44347=CARTESIAN_POINT ( 'NONE',  ( 796.7737145352015204, -20.63460265842048003, 370.7187646348536987 ) ) ;
#44349=CARTESIAN_POINT ( 'NONE',  ( 770.0799878456142551, 10.01258552831232329, 362.9823548866085616 ) ) ;
#44352=CARTESIAN_POINT ( 'NONE',  ( 812.6845335610512393, -151.9874144716871740, 353.5525998758768651 ) ) ;
#44357=CARTESIAN_POINT ( 'NONE',  ( 804.9363028652555840, -160.2709662947836762, 338.2165204200192079 ) ) ;
#44359=CARTESIAN_POINT ( 'NONE',  ( 795.1360043628807261, -284.0891481129650629, 360.2193346964456282 ) ) ;
#44360=CARTESIAN_POINT ( 'NONE',  ( 800.2193346964446619, -306.9982390220558841, 355.1360043628816925 ) ) ;
#44364=CARTESIAN_POINT ( 'NONE',  ( 803.2186876482843445, -7.987414471687621642, 350.0220218866286928 ) ) ;
#44368=CARTESIAN_POINT ( 'NONE',  ( 748.9653473494365699, -218.6346026584198228, 356.9462024416520762 ) ) ;
#44369=CARTESIAN_POINT ( 'NONE',  ( 801.5560724626406000, -288.5545181178798657, 326.7756240680316182 ) ) ;
#44370=CARTESIAN_POINT ( 'NONE',  ( 793.2243759319678702, -410.5328690171408539, 318.4439275373583200 ) ) ;
#44375=ORIENTED_EDGE ( 'NONE', *, *, #31981, .F. ) ;
#44378=CARTESIAN_POINT ( 'NONE',  ( 803.2186876482843445, -295.9874144716866908, 350.0220218866286928 ) ) ;
#44384=CARTESIAN_POINT ( 'NONE',  ( 809.0717654672305343, -196.9181544815164386, 360.1688906516309885 ) ) ;
#44386=LINE ( 'NONE', #9295, #9716 ) ;
#44389=CARTESIAN_POINT ( 'NONE',  ( 759.0252816721024374, -48.99823902205675807, 368.0189434323527280 ) ) ;
#44393=PLANE ( 'NONE',  #18784 ) ;
#44394=CARTESIAN_POINT ( 'NONE',  ( 797.8594530101008786, -37.54369356751132614, 322.1405469898980982 ) ) ;
#44395=CARTESIAN_POINT ( 'NONE',  ( 781.2370466360911223, -332.7363362996979390, 304.9990715423533629 ) ) ;
#44396=CARTESIAN_POINT ( 'NONE',  ( 792.3570229623688874, -261.1800572038741848, 373.1304606946836202 ) ) ;
#44401=CARTESIAN_POINT ( 'NONE',  ( 803.6646147819161570, -353.9073299311467053, 348.8264449731210561 ) ) ;
#44402=CARTESIAN_POINT ( 'NONE',  ( 804.8461984189677878, -122.1908817542439749, 336.9566956441385628 ) ) ;
#44404=CARTESIAN_POINT ( 'NONE',  ( 756.1443688327750579, -45.62377810805114109, 314.3581564841659315 ) ) ;
#44405=CARTESIAN_POINT ( 'NONE',  ( 781.8018195045267476, -382.2709662947829088, 365.1927285166407273 ) ) ;
#44407=DIRECTION ( 'NONE',  ( -1.000000000000000000, -0.000000000000000000, -0.000000000000000000 ) ) ;
#44408=CARTESIAN_POINT ( 'NONE',  ( 791.9812246680005501, -404.6346026584193396, 361.9419747391813189 ) ) ;
#44411=CARTESIAN_POINT ( 'NONE',  ( 757.8323909638827445, -194.6346026584198796, 352.1044303154654358 ) ) ;
#44412=CARTESIAN_POINT ( 'NONE',  ( 792.1044303154646968, -204.4527844766016926, 317.8323909638837677 ) ) ;
#44418=CARTESIAN_POINT ( 'NONE',  ( 794.9819416627830151, -372.9982390220557704, 319.9864689768909898 ) ) ;
#44422=CARTESIAN_POINT ( 'NONE',  ( 758.8095938919644823, -128.0891481129655745, 311.6929314249762797 ) ) ;
#44428=CARTESIAN_POINT ( 'NONE',  ( 755.2512626584698410, -247.5436935675106724, 315.2512626584710915 ) ) ;
#44429=CARTESIAN_POINT ( 'NONE',  ( 758.6633372737375112, -188.5328690171416497, 326.9102291470432533 ) ) ;
#44439=CARTESIAN_POINT ( 'NONE',  ( 744.6391490659812007, -110.7363362996985501, 338.7502325331110455 ) ) ;
#44446=DIRECTION ( 'NONE',  ( 0.000000000000000000, 0.000000000000000000, -1.000000000000000000 ) ) ;
#44449=CARTESIAN_POINT ( 'NONE',  ( 757.0176451133909268, -421.0999726633340288, 349.9200121543848354 ) ) ;
#44456=DIRECTION ( 'NONE',  ( -1.000000000000000000, -0.000000000000000000, -0.000000000000000000 ) ) ;
#44458=CARTESIAN_POINT ( 'NONE',  ( 749.5768839229115201, -204.5545181178800931, 358.0661480581553064 ) ) ;
#44460=CARTESIAN_POINT ( 'NONE',  ( 759.0252816721024374, -168.9982390220563673, 368.0189434323527280 ) ) ;
#44464=CARTESIAN_POINT ( 'NONE',  ( 781.8018195045266339, -262.2709662947831930, 365.1927285166406705 ) ) ;
#44466=CARTESIAN_POINT ( 'NONE',  ( 790.9844846989617508, -46.37269993606239638, 317.2208543904092721 ) ) ;
#44470=CARTESIAN_POINT ( 'NONE',  ( 803.8651313633788504, -101.2601417444146250, 332.4468031744301015 ) ) ;
#44474=CARTESIAN_POINT ( 'NONE',  ( 795.1360043628807261, -68.08914811296575920, 360.2193346964456282 ) ) ;
#44477=CARTESIAN_POINT ( 'NONE',  ( 814.8230680027162407, -365.8055962898682765, 333.7305795820267917 ) ) ;
#44479=CARTESIAN_POINT ( 'NONE',  ( 792.3570229623688874, 2.819942796124898177, 373.1304606946836202 ) ) ;
#44482=CARTESIAN_POINT ( 'NONE',  ( 765.0180583372156207, -384.9982390220556567, 360.0135310231089534 ) ) ;
#44490=CARTESIAN_POINT ( 'NONE',  ( 754.8072714833581358, -100.8164208402383792, 338.1981804954720587 ) ) ;
#44491=CARTESIAN_POINT ( 'NONE',  ( 755.8894580844503253, -399.8272453906067767, 332.3691319403863531 ) ) ;
#44492=CARTESIAN_POINT ( 'NONE',  ( 798.7617431975189675, -99.62377810805098477, 323.0428371773161871 ) ) ;
#44493=CARTESIAN_POINT ( 'NONE',  ( 749.2812353651451076, -438.4527844766009821, 323.2262854647983090 ) ) ;
#44495=CARTESIAN_POINT ( 'NONE',  ( 749.8865473780648472, -356.5328690171410813, 322.1177392798429082 ) ) ;
#44498=CARTESIAN_POINT ( 'NONE',  ( 786.2694204179717872, 2.718209154846545683, 305.1769319972829067 ) ) ;
#44508=CARTESIAN_POINT ( 'NONE',  ( 779.4763451958990572, -344.7363362996978253, 365.0264073115438919 ) ) ;
#44510=CARTESIAN_POINT ( 'NONE',  ( 764.8639956371174549, -176.0891481129653755, 319.7806653035542013 ) ) ;
#44511=ORIENTED_EDGE ( 'NONE', *, *, #15390, .T. ) ;
#44512=CARTESIAN_POINT ( 'NONE',  ( 788.6739635108323228, -295.6454272087888739, 373.9316612368139090 ) ) ;
#44515=CARTESIAN_POINT ( 'NONE',  ( 747.6481478633932056, -109.0999726633349241, 353.4146539503763620 ) ) ;
#44519=CARTESIAN_POINT ( 'NONE',  ( 804.4286716492782716, -137.3618753856928265, 345.3141322388244703 ) ) ;
#44522=CARTESIAN_POINT ( 'NONE',  ( 799.9636004259356241, -406.9181544815157849, 311.2241431872006956 ) ) ;
#44526=CARTESIAN_POINT ( 'NONE',  ( 800.9840315886518738, -52.91815448151692891, 354.1144889064786412 ) ) ;
#44529=CARTESIAN_POINT ( 'NONE',  ( 790.8726784830453198, -442.7146871989589840, 362.5472867521010585 ) ) ;
#44531=CARTESIAN_POINT ( 'NONE',  ( 803.2186876482843445, -79.98741447168740137, 350.0220218866286928 ) ) ;
#44534=CARTESIAN_POINT ( 'NONE',  ( 758.0141637701419768, -279.0783235625958127, 367.2620300519063790 ) ) ;
#44535=CARTESIAN_POINT ( 'NONE',  ( 765.0180583372156207, -72.99823902205667991, 360.0135310231089534 ) ) ;
#44539=CARTESIAN_POINT ( 'NONE',  ( 756.5762568750052424, -267.1800572038742985, 348.7366044899774238 ) ) ;
#44546=CARTESIAN_POINT ( 'NONE',  ( 746.8695393053151292, -317.9073299311467622, 327.6429770376306578 ) ) ;
#44547=CARTESIAN_POINT ( 'NONE',  ( 776.2433038121456548, -204.8965053807779100, 374.8207195650711014 ) ) ;
#44554=CARTESIAN_POINT ( 'NONE',  ( 754.8072714833581358, -220.8164208402379529, 338.1981804954720587 ) ) ;
#44557=CARTESIAN_POINT ( 'NONE',  ( 767.6429770376289525, -345.1800572038739006, 306.8695393053162093 ) ) ;
#44559=CARTESIAN_POINT ( 'NONE',  ( 763.3756531158825283, 16.45630643248848912, 321.2690078247891847 ) ) ;
#44560=DIRECTION ( 'NONE',  ( 0.000000000000000000, 1.000000000000000000, 0.000000000000000000 ) ) ;
#44561=CARTESIAN_POINT ( 'NONE',  ( 790.9844846989617508, -214.3726999360618493, 317.2208543904092721 ) ) ;
#44562=CARTESIAN_POINT ( 'NONE',  ( 771.2633955100217236, -95.90732993114751537, 363.4237431249939618 ) ) ;
#44566=CARTESIAN_POINT ( 'NONE',  ( 794.1144889064781864, -274.1692326535049915, 360.9840315886528401 ) ) ;
#44570=CARTESIAN_POINT ( 'NONE',  ( 744.6391490659812007, -14.73633629969885384, 338.7502325331110455 ) ) ;
#44575=CARTESIAN_POINT ( 'NONE',  ( 758.8095938919642549, -80.08914811296574499, 311.6929314249763365 ) ) ;
#44576=CARTESIAN_POINT ( 'NONE',  ( 767.6429770376289525, -129.1800572038746111, 306.8695393053162093 ) ) ;
#44580=CARTESIAN_POINT ( 'NONE',  ( 812.3518521366052028, -409.0999726633340288, 326.5853460496235243 ) ) ;
#44583=CARTESIAN_POINT ( 'NONE',  ( 792.3570229623688874, -405.1800572038737300, 373.1304606946836202 ) ) ;
#44584=CARTESIAN_POINT ( 'NONE',  ( 814.9108240113580450, -16.27096629478413092, 337.5031285880265273 ) ) ;
#44587=CARTESIAN_POINT ( 'NONE',  ( 755.0488828828309806, -17.80559628986940979, 344.1219089521771934 ) ) ;
#44588=CIRCLE ( 'NONE', #9177, 10.00000000000000888 ) ;
#44591=CARTESIAN_POINT ( 'NONE',  ( 781.2497674668890113, -156.3510508353235480, 375.3608509340180603 ) ) ;
#44592=CARTESIAN_POINT ( 'NONE',  ( 792.1044303154646968, 11.54721552339759860, 317.8323909638837677 ) ) ;
#44596=CARTESIAN_POINT ( 'NONE',  ( 785.3141322388236176, -165.7255117493291152, 364.4286716492789537 ) ) ;
#44598=CARTESIAN_POINT ( 'NONE',  ( 801.9419747391806368, -306.4527844766013800, 351.9812246680014027 ) ) ;
#44601=CARTESIAN_POINT ( 'NONE',  ( 801.3366627262608972, -8.532869017142163059, 353.0897708529566899 ) ) ;
#44603=AXIS2_PLACEMENT_3D ( 'NONE', #33677, #26732, #13128 ) ;
#44606=CARTESIAN_POINT ( 'NONE',  ( 763.2262854647970016, -224.6346026584198228, 309.2812353651462445 ) ) ;
#44607=CARTESIAN_POINT ( 'NONE',  ( 793.9708237608222134, -286.9181544815161828, 319.2295555964448681 ) ) ;
#44608=CARTESIAN_POINT ( 'NONE',  ( 793.2243759319678702, -434.5328690171407970, 318.4439275373583200 ) ) ;
#44615=CARTESIAN_POINT ( 'NONE',  ( 758.6633372737375112, -308.5328690171412518, 326.9102291470432533 ) ) ;
#44618=CARTESIAN_POINT ( 'NONE',  ( 804.4086373105744769, -121.6454272087894282, 333.3843516231986541 ) ) ;
#44622=CARTESIAN_POINT ( 'NONE',  ( 807.2620300519052989, -192.0090635724255606, 318.0141637701419768 ) ) ;
#44626=CARTESIAN_POINT ( 'NONE',  ( 800.9747183278959710, -60.99823902205671544, 311.9810565676471583 ) ) ;
#44631=CARTESIAN_POINT ( 'NONE',  ( 783.7953271457878373, -320.1908817542434349, 375.1787889125761239 ) ) ;
#44633=CARTESIAN_POINT ( 'NONE',  ( 745.4481719005789273, -291.7255117493285752, 347.5162901302853129 ) ) ;
#44638=VECTOR ( 'NONE', #18618, 1000.000000000000000 ) ;
#44640=CARTESIAN_POINT ( 'NONE',  ( 788.8264449731200330, -357.1800572038739006, 363.6646147819171233 ) ) ;
#44641=CARTESIAN_POINT ( 'NONE',  ( 793.9708237608222134, -118.9181544815167229, 319.2295555964448681 ) ) ;
#44643=CARTESIAN_POINT ( 'NONE',  ( 798.0661480581538854, -50.53286901714203339, 309.5768839229118043 ) ) ;
#44644=CARTESIAN_POINT ( 'NONE',  ( 755.5713283507202505, -365.3618753856920875, 334.6858677611754729 ) ) ;
#44646=CARTESIAN_POINT ( 'NONE',  ( 757.8323909638827445, -434.6346026584190554, 352.1044303154654358 ) ) ;
#44650=CARTESIAN_POINT ( 'NONE',  ( 800.0135310231082713, -182.0891481129654323, 325.0180583372163028 ) ) ;
#44651=CARTESIAN_POINT ( 'NONE',  ( 767.8955696845334842, -192.4527844766017211, 362.1676090361161755 ) ) ;
#44656=CARTESIAN_POINT ( 'NONE',  ( 781.7834795799800531, -394.8164208402374697, 315.0636971347436202 ) ) ;
#44660=CARTESIAN_POINT ( 'NONE',  ( 792.2312462859673587, -107.9073299311474727, 307.2067596250082602 ) ) ;
#44667=CARTESIAN_POINT ( 'NONE',  ( 796.9462024416508257, -252.4527844766015789, 308.9653473494370246 ) ) ;
#44668=CARTESIAN_POINT ( 'NONE',  ( 804.9511171171677688, -197.8055962898688733, 335.8780910478229202 ) ) ;
#44669=CARTESIAN_POINT ( 'NONE',  ( 792.0613484971601110, -458.0032201311295807, 367.4685979341032294 ) ) ;
#44670=DIRECTION ( 'NONE',  ( -0.000000000000000000, -1.110223024625155554E-15, 1.000000000000000000 ) ) ;
#44681=CARTESIAN_POINT ( 'NONE',  ( 752.7379699480933368, -108.0090635724258448, 361.9858362298580232 ) ) ;
#44689=CARTESIAN_POINT ( 'NONE',  ( 758.4439275373578084, -420.5545181178793541, 353.2243759319684386 ) ) ;
#44695=CARTESIAN_POINT ( 'NONE',  ( 764.8639956371174549, 15.91085188703394238, 319.7806653035542013 ) ) ;
#44697=CARTESIAN_POINT ( 'NONE',  ( 755.8990559732751535, -203.4636090269709996, 365.9055244015606831 ) ) ;
#44699=CARTESIAN_POINT ( 'NONE',  ( 767.6429770376289525, -177.1800572038744690, 306.8695393053162093 ) ) ;
#44703=CARTESIAN_POINT ( 'NONE',  ( 795.1360043628807261, -260.0891481129650060, 360.2193346964456282 ) ) ;
#44704=CARTESIAN_POINT ( 'NONE',  ( 773.4516893846965786, -67.64542720878958448, 315.8398074228977066 ) ) ;
#44709=CARTESIAN_POINT ( 'NONE',  ( 770.0799878456142551, -85.98741447168738716, 362.9823548866085616 ) ) ;
#44710=CARTESIAN_POINT ( 'NONE',  ( 759.7806653035534055, -318.9982390220557704, 324.8639956371180801 ) ) ;
#44714=CARTESIAN_POINT ( 'NONE',  ( 801.9419747391806368, -42.45278447660223264, 351.9812246680014027 ) ) ;
#44716=CARTESIAN_POINT ( 'NONE',  ( 767.9999999999992042, 205.0000000000000568, 339.9999999999999432 ) ) ;
#44717=CARTESIAN_POINT ( 'NONE',  ( 764.3348316497523456, -382.7146871989591546, 308.6759233522265617 ) ) ;
#44719=CARTESIAN_POINT ( 'NONE',  ( 797.6776695296629214, -283.5436935675105019, 357.6776695296636603 ) ) ;
#44720=CARTESIAN_POINT ( 'NONE',  ( 763.2262854647970016, 15.36539734157940629, 309.2812353651462445 ) ) ;
#44722=CARTESIAN_POINT ( 'NONE',  ( 756.3353852180819104, -389.9073299311465348, 331.1735550268788302 ) ) ;
#44730=CARTESIAN_POINT ( 'NONE',  ( 759.9864689768902508, -98.08914811296568814, 354.9819416627836404 ) ) ;
#44731=CARTESIAN_POINT ( 'NONE',  ( 798.5707757039680246, -389.4636090269704027, 356.7845633553585003 ) ) ;
#44732=CARTESIAN_POINT ( 'NONE',  ( 800.7704444035546203, -100.1692326535055315, 326.0291762391768771 ) ) ;
#44734=AXIS2_PLACEMENT_3D ( 'NONE', #6779, #13492, #27346 ) ;
#44735=CARTESIAN_POINT ( 'NONE',  ( 808.3070685750232087, -450.9982390220554294, 361.1904061080339829 ) ) ;
#44737=CARTESIAN_POINT ( 'NONE',  ( 815.0009284576459549, -342.3510508353228943, 338.7629533639073429 ) ) ;
#44739=CARTESIAN_POINT ( 'NONE',  ( 746.7653713866222915, -113.2601417444145682, 351.0478386215610271 ) ) ;
#44743=CARTESIAN_POINT ( 'NONE',  ( 813.5763878283155464, -3.827245390607979303, 351.1614460488615350 ) ) ;
#44751=CARTESIAN_POINT ( 'NONE',  ( 776.9254006560222479, -332.1908817542433781, 314.8983024940802125 ) ) ;
#44752=VERTEX_POINT ( 'NONE', #36172 ) ;
#44753=CARTESIAN_POINT ( 'NONE',  ( 793.5525998758768083, -295.0999726633343698, 372.6845335610516941 ) ) ;
#44755=EDGE_CURVE ( 'NONE', #34810, #10697, #18405, .T. ) ;
#44757=CARTESIAN_POINT ( 'NONE',  ( 786.2694204179717872, -93.28179084515315367, 305.1769319972829067 ) ) ;
#44762=CARTESIAN_POINT ( 'NONE',  ( 794.9819416627830151, -132.9982390220564810, 319.9864689768909898 ) ) ;
#44764=CARTESIAN_POINT ( 'NONE',  ( 814.4686193811664907, -411.2817908451521589, 346.2056067578752732 ) ) ;
#44767=CARTESIAN_POINT ( 'NONE',  ( 758.4439275373578084, -36.55451811788061178, 353.2243759319684386 ) ) ;
#44770=CARTESIAN_POINT ( 'NONE',  ( 756.7813123517142913, -427.9874144716862929, 329.9779781133712504 ) ) ;
#44776=CARTESIAN_POINT ( 'NONE',  ( 808.7758568127978833, -292.1692326535048210, 320.0363995740631822 ) ) ;
#44777=CARTESIAN_POINT ( 'NONE',  ( 800.2193346964446619, -90.99823902205662307, 355.1360043628816925 ) ) ;
#44782=CARTESIAN_POINT ( 'NONE',  ( 768.0187753319979720, -272.6346026584196807, 318.0580252608186242 ) ) ;
#44790=CARTESIAN_POINT ( 'NONE',  ( 782.4968714119720516, -322.8164208402377540, 305.0891759886411023 ) ) ;
#44791=CARTESIAN_POINT ( 'NONE',  ( 783.7566961878529810, -264.8965053807776826, 305.1792804349288417 ) ) ;
#44795=CARTESIAN_POINT ( 'NONE',  ( 800.2193346964447755, -234.9982390220561683, 355.1360043628815788 ) ) ;
#44797=CARTESIAN_POINT ( 'NONE',  ( 808.3070685750230950, -354.9982390220557704, 361.1904061080339261 ) ) ;
#44802=CARTESIAN_POINT ( 'NONE',  ( 763.8424801807145741, -210.0090635724255321, 320.5453621957614700 ) ) ;
#44803=CARTESIAN_POINT ( 'NONE',  ( 755.5713283507202505, -77.36187538569302546, 334.6858677611754729 ) ) ;
#44807=CARTESIAN_POINT ( 'NONE',  ( 803.8651313633788504, -245.2601417444141987, 332.4468031744301015 ) ) ;
#44810=CARTESIAN_POINT ( 'NONE',  ( 795.8262568251477660, -22.37269993606246743, 308.3538107759623585 ) ) ;
#44814=CARTESIAN_POINT ( 'NONE',  ( 814.5518280994195948, -87.72551174932937101, 332.4837098697145734 ) ) ;
#44815=CARTESIAN_POINT ( 'NONE',  ( 759.0252816721024374, -144.9982390220564525, 368.0189434323527280 ) ) ;
#44819=CARTESIAN_POINT ( 'NONE',  ( 760.0363995740630116, -418.9181544815157849, 368.7758568127991907 ) ) ;
#44822=CARTESIAN_POINT ( 'NONE',  ( 759.0252816721024374, -408.9982390220556567, 368.0189434323527280 ) ) ;
#44823=CARTESIAN_POINT ( 'NONE',  ( 759.0252816721024374, -24.99823902205683268, 368.0189434323527280 ) ) ;
#44825=CARTESIAN_POINT ( 'NONE',  ( 754.8983024940795303, -18.89650538077849617, 336.9254006560228163 ) ) ;
#44828=CARTESIAN_POINT ( 'NONE',  ( 798.0661480581538854, -170.5328690171416781, 309.5768839229118043 ) ) ;
#44829=CARTESIAN_POINT ( 'NONE',  ( 800.2193346964446619, 5.001760977943074948, 355.1360043628816925 ) ) ;
#44833=CARTESIAN_POINT ( 'NONE',  ( 755.5713283507202505, -149.3618753856928265, 334.6858677611754729 ) ) ;
#44835=CARTESIAN_POINT ( 'NONE',  ( 757.8323909638828582, -290.6346026584196238, 352.1044303154654358 ) ) ;
#44838=CARTESIAN_POINT ( 'NONE',  ( 805.1016975059191054, -6.896505380778533478, 343.0745993439771837 ) ) ;
#44842=CARTESIAN_POINT ( 'NONE',  ( 759.0252816721024374, -216.9982390220562252, 368.0189434323527280 ) ) ;
#44843=CARTESIAN_POINT ( 'NONE',  ( 757.4527132478984868, -352.3726999360614514, 329.1273215169538844 ) ) ;
#44844=CARTESIAN_POINT ( 'NONE',  ( 786.6156483768007774, -433.4419599262316183, 315.5913626894246136 ) ) ;
#44851=CARTESIAN_POINT ( 'NONE',  ( 795.9930595647434757, -291.0783235625957559, 320.7433823573372820 ) ) ;
#44854=CARTESIAN_POINT ( 'NONE',  ( 775.8780910478218402, -129.2817908451530400, 364.9511171171680530 ) ) ;
#44855=LINE ( 'NONE', #5822, #6418 ) ;
#44858=CARTESIAN_POINT ( 'NONE',  ( 788.6739635108323228, -199.6454272087891582, 373.9316612368139090 ) ) ;
#44862=CARTESIAN_POINT ( 'NONE',  ( 763.0537975583475827, -48.45278447660219712, 371.0346526505627480 ) ) ;
#44867=CARTESIAN_POINT ( 'NONE',  ( 814.4686193811664907, -315.2817908451525000, 346.2056067578752732 ) ) ;
#44869=CARTESIAN_POINT ( 'NONE',  ( 745.0891759886404770, -292.2709662947831930, 342.4968714119734159 ) ) ;
#44873=CARTESIAN_POINT ( 'NONE',  ( 788.8264449731200330, -381.1800572038737869, 363.6646147819171233 ) ) ;
#44874=CARTESIAN_POINT ( 'NONE',  ( 804.1105419155481968, -171.8272453906074304, 347.6308680596136469 ) ) ;
#44876=CARTESIAN_POINT ( 'NONE',  ( 812.6845335610512393, -55.98741447168748664, 353.5525998758768651 ) ) ;
#44877=CARTESIAN_POINT ( 'NONE',  ( 804.6798772138710092, -375.7255117493284047, 334.6312213355106451 ) ) ;
#44880=CARTESIAN_POINT ( 'NONE',  ( 746.7653713866222915, -137.2601417444144829, 351.0478386215610271 ) ) ;
#44881=CARTESIAN_POINT ( 'NONE',  ( 759.9864689768902508, -434.0891481129646081, 354.9819416627836404 ) ) ;
#44885=CARTESIAN_POINT ( 'NONE',  ( 785.3687786644884454, -203.3618753856925991, 315.3201227861279676 ) ) ;
#44886=CARTESIAN_POINT ( 'NONE',  ( 804.9363028652555840, -208.2709662947835341, 338.2165204200192079 ) ) ;
#44891=CARTESIAN_POINT ( 'NONE',  ( 771.1735550268778070, -393.1800572038737300, 316.3353852180827630 ) ) ;
#44895=CARTESIAN_POINT ( 'NONE',  ( 805.0032342141413437, -109.5436935675110988, 314.9967657858572352 ) ) ;
#44902=CARTESIAN_POINT ( 'NONE',  ( 755.8398074228967971, -187.4419599262325278, 333.4516893846970333 ) ) ;
#44909=CARTESIAN_POINT ( 'NONE',  ( 787.4999999999992042, -462.9681489794448339, 369.0473750965555837 ) ) ;
#44912=CARTESIAN_POINT ( 'NONE',  ( 811.3240766477731540, -100.3726999360622187, 355.6651683502462902 ) ) ;
#44920=CARTESIAN_POINT ( 'NONE',  ( 800.9840315886518738, -436.9181544815157281, 354.1144889064786412 ) ) ;
#44927=CARTESIAN_POINT ( 'NONE',  ( 768.9521613784389729, -225.8272453906072599, 373.2346286133773106 ) ) ;
#44929=CARTESIAN_POINT ( 'NONE',  ( 777.4774526936600978, -178.2709662947835625, 304.7301800767027657 ) ) ;
#44932=CARTESIAN_POINT ( 'NONE',  ( 774.6312213355099630, -287.3618753856923718, 364.6798772138717482 ) ) ;
#44933=CARTESIAN_POINT ( 'NONE',  ( 772.4468031744293057, -57.82724539060780700, 363.8651313633793620 ) ) ;
#44938=DIRECTION ( 'NONE',  ( 0.000000000000000000, 0.000000000000000000, 1.000000000000000000 ) ) ;
#44939=CARTESIAN_POINT ( 'NONE',  ( 790.8726784830453198, -82.71468719896012090, 362.5472867521010585 ) ) ;
#44940=CARTESIAN_POINT ( 'NONE',  ( 755.3201227861273992, -315.7255117493286320, 345.3687786644892981 ) ) ;
#44945=CARTESIAN_POINT ( 'NONE',  ( 802.1676090361156639, -62.63460265842031305, 327.8955696845344505 ) ) ;
#44948=CARTESIAN_POINT ( 'NONE',  ( 807.5423716828161105, -393.0783235625954717, 362.2119215644372048 ) ) ;
#44950=CARTESIAN_POINT ( 'NONE',  ( 804.6798772138708955, -279.7255117493288026, 334.6312213355107019 ) ) ;
#44951=CARTESIAN_POINT ( 'NONE',  ( 796.9462024416508257, 11.54721552339760038, 308.9653473494370246 ) ) ;
#44953=CARTESIAN_POINT ( 'NONE',  ( 794.9819416627830151, -372.9982390220557704, 319.9864689768909898 ) ) ;
#44959=CARTESIAN_POINT ( 'NONE',  ( 774.6858677611749044, -105.7255117493293000, 315.5713283507209894 ) ) ;
#44960=CARTESIAN_POINT ( 'NONE',  ( 787.5531968255692163, -405.8272453906067199, 316.1348686366205811 ) ) ;
#44961=CARTESIAN_POINT ( 'NONE',  ( 759.2295555964440155, -88.16923265350555994, 353.9708237608231229 ) ) ;
#44963=FACE_OUTER_BOUND ( 'NONE', #25122, .T. ) ;
#44964=CARTESIAN_POINT ( 'NONE',  ( 811.6461892240364477, -364.7146871989592114, 324.1737431748509835 ) ) ;
#44970=CARTESIAN_POINT ( 'NONE',  ( 807.2620300519052989, -0.009063572426172561425, 318.0141637701419768 ) ) ;
#44977=CARTESIAN_POINT ( 'NONE',  ( 786.5483106153019435, -343.6454272087887603, 364.1601925771022366 ) ) ;
#44979=CARTESIAN_POINT ( 'NONE',  ( 815.3608509340175488, -314.7363362996979959, 341.2497674668889545 ) ) ;
#44982=CARTESIAN_POINT ( 'NONE',  ( 748.6759233522253680, -112.3726999360621761, 324.3348316497537098 ) ) ;
#44984=EDGE_CURVE ( 'NONE', #45600, #24990, #33607, .T. ) ;
#44987=CARTESIAN_POINT ( 'NONE',  ( 755.0636971347428243, -172.2709662947836478, 341.7834795799807353 ) ) ;
#44989=CARTESIAN_POINT ( 'NONE',  ( 795.8262568251477660, -430.3726999360611671, 308.3538107759623585 ) ) ;
#44992=CARTESIAN_POINT ( 'NONE',  ( 804.8461984189677878, -50.19088175424420939, 336.9566956441385628 ) ) ;
#44995=CARTESIAN_POINT ( 'NONE',  ( 780.5290396650775619, -420.3510508353225532, 365.2837595273619513 ) ) ;
#45000=CARTESIAN_POINT ( 'NONE',  ( 793.4146539503750546, -289.9874144716866908, 307.6481478633938877 ) ) ;
#45001=CARTESIAN_POINT ( 'NONE',  ( 785.3141322388236176, -93.72551174932934259, 364.4286716492789537 ) ) ;
#45004=CARTESIAN_POINT ( 'NONE',  ( 785.3687786644884454, -275.3618753856923149, 315.3201227861279676 ) ) ;
#45013=CARTESIAN_POINT ( 'NONE',  ( 785.3687786644884454, -299.3618753856922581, 315.3201227861279676 ) ) ;
#45015=CARTESIAN_POINT ( 'NONE',  ( 763.2262854647970016, -368.6346026584193964, 309.2812353651462445 ) ) ;
#45016=CARTESIAN_POINT ( 'NONE',  ( 811.6461892240364477, -268.7146871989595525, 324.1737431748509835 ) ) ;
#45017=CARTESIAN_POINT ( 'NONE',  ( 808.7758568127978833, -52.16923265350567362, 320.0363995740631822 ) ) ;
#45021=CARTESIAN_POINT ( 'NONE',  ( 762.1405469898971887, -241.5436935675106156, 357.8594530101015607 ) ) ;
#45023=CARTESIAN_POINT ( 'NONE',  ( 777.5031285880264704, -358.8164208402375834, 374.9108240113588408 ) ) ;
#45026=CARTESIAN_POINT ( 'NONE',  ( 795.2725662613897839, 16.45630643248849267, 314.1785221222716586 ) ) ;
#45028=CARTESIAN_POINT ( 'NONE',  ( 796.9571628226829034, -215.4636090269709712, 321.2382568024804641 ) ) ;
#45029=CARTESIAN_POINT ( 'NONE',  ( 794.9819416627830151, -132.9982390220564810, 319.9864689768909898 ) ) ;
#45032=CARTESIAN_POINT ( 'NONE',  ( 763.2154366446407039, -309.6237781080502600, 321.4292242960311228 ) ) ;
#45036=CARTESIAN_POINT ( 'NONE',  ( 808.3070685750230950, -450.9982390220554294, 361.1904061080339261 ) ) ;
#45040=CARTESIAN_POINT ( 'NONE',  ( 787.5162901302840055, -83.36187538569296862, 305.4481719005792684 ) ) ;
#45041=CARTESIAN_POINT ( 'NONE',  ( 747.2067596250078623, -171.1800572038745543, 352.2312462859687230 ) ) ;
#45045=CARTESIAN_POINT ( 'NONE',  ( 750.9282345327678740, -424.9181544815158986, 319.8311093483690115 ) ) ;
#45048=CARTESIAN_POINT ( 'NONE',  ( 754.9967657858570647, -409.5436935675101040, 365.0032342141425374 ) ) ;
#45049=CARTESIAN_POINT ( 'NONE',  ( 767.7687537140311633, -23.90732993114773919, 372.7932403749916830 ) ) ;
#45052=CARTESIAN_POINT ( 'NONE',  ( 804.1601925771018387, -7.441959926233078448, 346.5483106153029098 ) ) ;
#45055=CARTESIAN_POINT ( 'NONE',  ( 768.8385539511368734, -167.2601417444143976, 306.4236121716840557 ) ) ;
#45056=CARTESIAN_POINT ( 'NONE',  ( 781.8018195045267476, 1.729033705215812233, 365.1927285166407273 ) ) ;
#45061=CARTESIAN_POINT ( 'NONE',  ( 759.9864689768902508, -170.0891481129654608, 354.9819416627836404 ) ) ;
#45064=CARTESIAN_POINT ( 'NONE',  ( 756.3353852180819104, -293.9073299311468759, 331.1735550268788302 ) ) ;
#45065=CARTESIAN_POINT ( 'NONE',  ( 774.6312213355098493, -311.3618753856923149, 364.6798772138717482 ) ) ;
#45068=CARTESIAN_POINT ( 'NONE',  ( 761.2382568024794409, -15.62377810805123524, 356.9571628226838129 ) ) ;
#45070=( BOUNDED_CURVE ( )  B_SPLINE_CURVE ( 2, ( #27534, #13006, #27318, #9761, #3060, #31235, #45330, #24294, #38400, #6750, #20824, #17384, #31467, #38626, #34007, #2361, #41186, #21070, #35153, #17616, #6985, #31685, #3531, #12945, #19639, #9702, #20090, #23545, #37648, #6227, #23766, #27031, #31171, #12703, #19873, #5545, #23323, #41130, #9482, #9926, #16401, #41815, #16641, #30481, #30255, #10161, #13181, #27262, #24237, #5997, #34165, #45268, #20319, #2082, #2536, #41352, #33733, #23999, #37427, #2781, #44584, #17092, #27476, #26783, #16174, #16873, #30955, #27711, #44347, #37879, #41574, #30729, #5784, #38121, #45049, #34412, #44823, #13404, #6474, #3004, #33951, #40888, #9255, #20550, #2302, #34647, #13627, #10614, #7388, #28387, #39039, #42035, #35091, #14558, #14315, #42256, #7165, #18256, #31631, #11078, #3466, #10381, #4162, #32084, #17559, #31849, #6868, #6691, #42490, #21239, #24690, #38809, #21464, #10856, #14088, #32330, #45510, #6918, #38346, #24457, #28163, #42937, #35319, #31405, #20769, #3697, #17784, #14784, #221, #27939, #38564, #34860, #21690, #684, #13863, #24925, #35542, #20998, #3917, #18012, #455, #3224, #28635, #42714, #25146, #39258, #7613, #35783, #28856, #11304, #17314, #411, #28341, #12346, #22724, #26422, #28816, #26193, #21426, #21200, #7574, #12113, #35502, #43971, #40309, #19259, #39221, #3877, #5173, #14515, #28593, #10812, #33347, #1477, #32041, #641, #42677, #35281, #11263, #21650, #25107, #19050, #35737, #8662, #179, #1690, #36820, #15794, #4116, #18211, #14742, #7121, #11040, #14272, #3658, #32285, #42897, #29884, #25338, #42441, #24885, #17746, #31810, #39454, #21889, #38999, #36604, #4958, #33141, #15577, #29658, #7349, #43735, #17969, #30802, #41426, #34243, #26635, #16031, #13255, #5386, #12559, #30558, #9558, #30112, #40731, #23618, #2618, #44660, #40522, #45122, #44895, #9088, #27333, #5625, #23155, #37264, #22937, #19719, #37726, #33806, #2378, #13480, #2159, #9328, #34492, #41201, #37033, #12776, #16479, #8873, #9775, #16251, #6078, #30328, #20166, #16718, #13021, #19480, #27111, #33576, #16945, #1928, #23844, #37956, #44422, #26855, #6315, #20397, #2852, #40966, #31024, #44201, #23397, #37499, #5859, #19947, #34023, #31487, #24081, #41888, #6541, #24776, #38195, #17164, #10934, #10456, #17637, #41655, #31701, #42106, #45588, #13936, #28232, #68, #3307, #7463, #34715, #10231, #27551, #45350, #21091, #32170, #20842, #20621, #10011, #34941, #28011, #3990, #24533, #13712, #27790, #3073, #25003, #35618, #24311, #35176, #7003, #38416, #6767, #38646, #3552, #14161, #42327, #10691, #17856, #28474, #21318, #38892, #7246, #294, #35393, #3766, #31922, #533, #42575, #14393, #39114, #21536, #18087, #28710, #19210, #18997, #28935, #33089, #25458, #32409, #11376, #42790, #39578, #11833, #43012, #758, #36539, #8152, #29394, #11152, #43686, #25221, #40247, #29609, #33297, #1426, #14858, #25904, #7935, #40013, #15312, #18768, #39333, #4669, #7688, #11616, #8365, #32854, #32626, #29160, #21767, #971, #35862, #36308, #25693, #36766, #4239, #5122, #18329, #15074, #22002, #43245, #39804, #1204, #43465, #36092, #22433, #4457, #18546, #12059, #22215, #4898, #14637, #15528, #26133, #8605, #22670, #20112, #12505, #19429, #23567, #1642, #34187, #8821, #9503, #40679, #9033, #5334, #13204, #41152, #26581, #40909, #23103, #15743, #16663, #23788, #22889, #12967, #30275, #6021, #40469, #44842, #30748, #27282, #44368, #2105, #9276, #6253, #37205, #36981, #29831, #5569, #19661, #37900, #41375, #44606, #33754, #2558, #20341, #19894, #23345, #9723, #12723, #37448, #27056, #16195, #26803, #43912, #5807, #15976, #37671, #12290, #26367, #33521, #1869, #30059, #44141, #33972, #2323, #16421, #30503, #6492, #3489, #28180, #24478, #34435, #39059, #38832, #3025, #7184, #45290, #20570, #31193, #16892, #13426, #24943, #42053, #10401, #7407, #41834, #3246, #28413, #35111, #30973, #6710, #38584, #2801, #21259, #34666, #31647, #13650, #15, #17577, #6940, #45071, #14106, #42272, #10876, #27495, #21022, #10633, #24256, #17112, #35338, #24713, #3714, #27731, #17801, #31867, #238, #10180, #38141, #24022, #9951, #31424, #14335, #42511, #41595, #38364, #20787, #34882, #17336, #45530, #13882, #27957, #25855, #33038, #7877, #35805, #18943, #4402, #21953, #15016, #26067, #29105, #18492, #43189, #4181, #11558, #36039, #1377, #18706, #14800, #39965, #43634, #39753, #25640, #15480, #32568, #8101, #32796, #28875, #25400, #21481, #1150, #43417, #29560, #39522, #35559, #914, #12003, #21708, #11096, #39275, #22163, #36252, #25166, #7630, #4609, #15255, #29344, #3934, #40180, #8310, #11784, #18029, #32110, #475, #22373, #704, #14580, #28654, #36479, #4843, #42731, #42955, #18276, #32350, #11322, #5070, #26531, #30223, #13145, #12907, #5507, #5964, #36710, #20053, #30444, #15689, #22610, #19834, #5746, #30693, #1590, #16140, #44546, #44086, #26311, #26994, #2268, #40852, #1809, #37391, #19161, #44790, #29771, #40629, #33461, #8981, #19603, #12669, #26749, #33245, #33917, #43849, #12231, #37610, #37148, #44314, #27226, #41091, #34131, #23050, #15916, #9446, #19377, #40417, #23510, #8546, #2499, #8769, #16365, #33696, #2045, #16606, #22836, #36930, #5284, #9215, #29999, #12452, #23290, #10577, #41318, #13368, #31368, #10349, #30919, #27440, #24424, #35057, #45476, #9667, #187, #45706, #9890, #14057, #6441, #41539, #38086, #23733, #20520, #38528, #23964, #17528, #34826, #6882, #37844, #24654, #6192, #21207, #38771, #35288, #3431, #2746, #38312, #7129, #20284, #3666, #31601, #16841, #34377, #20958, #6659, #28128, #13832, #13592, #10129, #45015, #27674, #34613, #17277, #17057, #20732, #17753, #2969, #31817, #31134, #41780, #45231, #24203, #3190, #27909, #42006, #42224, #14279, #18440, #29054, #32047, #25114, #4567, #4349, #32294, #42904, #8260, #21658, #1094, #39228, #419, #18658, #28349, #15208, #35509, #35746, #42452, #32518, #11271, #649, #14751, #43140, #866, #4126, #22326, #3884, #42682, #10820, #14524, #18219, #28824, #39462, #35984, #25347, #14969, #7820, #4790, #21899, #17977, #28600, #24892, #11736, #36427, #21433, #11507, #25592, #11049, #7581, #39702, #36203, #32747, #8050, #22114, #29296, #18894, #43371, #25805, #39918, #32989, #39006, #1327, #7357, #19326, #15431, #8932, #29719, #5699, #16317, #9158, #1540, #36665, #33870, #26016, #8725, #5025, #30176, #19115, #33203, #44267, #23231, #5453, #29508, #20009, #19786, #43797, #2223, #26261, #15636, #12178, #43581, #40374, #12625, #22790, #36885, #37337, #5236, #29952, #9395, #16092, #11949, #33410, #37097, #34085, #30399, #1754, #26703, #15861, #40801, #44493, #19547, #40127, #33644, #8490, #12405, #12851, #23003, #26933, #44035, #26485, #41035, #23463, #1997, #40586, #37562, #5919, #22561, #2692, #6144, #37795, #23684, #6390, #44735, #16788, #9843, #20472, #13095, #20234 ),
 .UNSPECIFIED., .F., .T. ) 
 B_SPLINE_CURVE_WITH_KNOTS ( ( 3, 2, 2, 2, 2, 2, 2, 2, 2, 2, 2, 2, 2, 2, 2, 2, 2, 2, 2, 2, 2, 2, 2, 2, 2, 2, 2, 2, 2, 2, 2, 2, 2, 2, 2, 2, 2, 2, 2, 2, 2, 2, 2, 2, 2, 2, 2, 2, 2, 2, 2, 2, 2, 2, 2, 2, 2, 2, 2, 2, 2, 2, 2, 2, 2, 2, 2, 2, 2, 2, 2, 2, 2, 2, 2, 2, 2, 2, 2, 2, 2, 2, 2, 2, 2, 2, 2, 2, 2, 2, 2, 2, 2, 2, 2, 2, 2, 2, 2, 2, 2, 2, 2, 2, 2, 2, 2, 2, 2, 2, 2, 2, 2, 2, 2, 2, 2, 2, 2, 2, 2, 2, 2, 2, 2, 2, 2, 2, 2, 2, 2, 2, 2, 2, 2, 2, 2, 2, 2, 2, 2, 2, 2, 2, 2, 2, 2, 2, 2, 2, 2, 2, 2, 2, 2, 2, 2, 2, 2, 2, 2, 2, 2, 2, 2, 2, 2, 2, 2, 2, 2, 2, 2, 2, 2, 2, 2, 2, 2, 2, 2, 2, 2, 2, 2, 2, 2, 2, 2, 2, 2, 2, 2, 2, 2, 2, 2, 2, 2, 2, 2, 2, 2, 2, 2, 2, 2, 2, 2, 2, 2, 2, 2, 2, 2, 2, 2, 2, 2, 2, 2, 2, 2, 2, 2, 2, 2, 2, 2, 2, 2, 2, 2, 2, 2, 2, 2, 2, 2, 2, 2, 2, 2, 2, 2, 2, 2, 2, 2, 2, 2, 2, 2, 2, 2, 2, 2, 2, 2, 2, 2, 2, 2, 2, 2, 2, 2, 2, 2, 2, 2, 2, 2, 2, 2, 2, 2, 2, 2, 2, 2, 2, 2, 2, 2, 2, 2, 2, 2, 2, 2, 2, 2, 2, 2, 2, 2, 2, 2, 2, 2, 2, 2, 2, 2, 2, 2, 2, 2, 2, 2, 2, 2, 2, 2, 2, 2, 2, 2, 2, 2, 2, 2, 2, 2, 2, 2, 2, 2, 2, 2, 2, 2, 2, 2, 2, 2, 2, 2, 2, 2, 2, 2, 2, 2, 2, 2, 2, 2, 2, 2, 2, 2, 2, 2, 2, 2, 2, 2, 2, 2, 2, 2, 2, 2, 2, 2, 2, 2, 2, 2, 2, 2, 2, 2, 2, 2, 2, 2, 2, 2, 2, 2, 2, 2, 2, 2, 2, 2, 2, 2, 2, 2, 2, 2, 2, 2, 2, 2, 2, 2, 2, 2, 2, 2, 2, 2, 2, 2, 2, 2, 2, 2, 2, 2, 2, 2, 2, 2, 2, 2, 2, 2, 2, 2, 2, 2, 2, 2, 2, 2, 3 ),
 ( 8.755858387967423303E-18, 0.002272727272727281290, 0.004545454545454553907, 0.006818181818181826524, 0.009090909090909099141, 0.01136363636363637263, 0.01363636363636364437, 0.01590909090909091786, 0.01818181818181819134, 0.02045454545454546483, 0.02272727272727273831, 0.02500000000000001180, 0.02727272727272728181, 0.02954545454545455530, 0.03181818181818182184, 0.03409090909090909532, 0.03636363636363636881, 0.03863636363636364229, 0.04090909090909091578, 0.04318181818181818926, 0.04545454545454546275, 0.04772727272727273623, 0.05000000000000000971, 0.05227272727272727626, 0.05454545454545454974, 0.05681818181818182323, 0.05909090909090909671, 0.06136363636363637020, 0.06363636363636364368, 0.06590909090909091717, 0.06818181818181819065, 0.07045454545454546413, 0.07272727272727273762, 0.07500000000000001110, 0.07727272727272728459, 0.07954545454545455807, 0.08181818181818183155, 0.08409090909090910504, 0.08636363636363637852, 0.08863636363636365201, 0.09090909090909092549, 0.09318181818181819898, 0.09545454545454547246, 0.09772727272727274594, 0.1000000000000000194, 0.1022727272727272929, 0.1045454545454545525, 0.1068181818181818260, 0.1090909090909090995, 0.1113636363636363730, 0.1136363636363636465, 0.1159090909090909199, 0.1181818181818181934, 0.1204545454545454669, 0.1227272727272727404, 0.1250000000000000000, 0.1272727272727272596, 0.1295454545454545470, 0.1318181818181818066, 0.1340909090909090939, 0.1363636363636363535, 0.1386363636363636409, 0.1409090909090909005, 0.1431818181818181879, 0.1454545454545454475, 0.1477272727272727348, 0.1499999999999999944, 0.1522727272727272818, 0.1545454545454545414, 0.1568181818181818288, 0.1590909090909090884, 0.1613636363636363757, 0.1636363636363636354, 0.1659090909090909227, 0.1681818181818181823, 0.1704545454545454419, 0.1727272727272727293, 0.1749999999999999889, 0.1772727272727272763, 0.1795454545454545359, 0.1818181818181818232, 0.1840909090909090828, 0.1863636363636363702, 0.1886363636363636298, 0.1909090909090909172, 0.1931818181818181768, 0.1954545454545454641, 0.1977272727272727237, 0.2000000000000000111, 0.2022727272727272707, 0.2045454545454545581, 0.2068181818181818177, 0.2090909090909090773, 0.2113636363636363646, 0.2136363636363636243, 0.2159090909090909116, 0.2181818181818181712, 0.2204545454545454586, 0.2227272727272727182, 0.2250000000000000056, 0.2272727272727272652, 0.2295454545454545525, 0.2318181818181818121, 0.2340909090909090995, 0.2363636363636363591, 0.2386363636363636465, 0.2409090909090909061, 0.2431818181818181934, 0.2454545454545454530, 0.2477272727272727404, 0.2500000000000000000, 0.2522727272727272596, 0.2545454545454545192, 0.2568181818181818343, 0.2590909090909090939, 0.2613636363636363535, 0.2636363636363636131, 0.2659090909090909283, 0.2681818181818181879, 0.2704545454545454475, 0.2727272727272727071, 0.2750000000000000222, 0.2772727272727272818, 0.2795454545454545414, 0.2818181818181818010, 0.2840909090909091161, 0.2863636363636363757, 0.2886363636363636354, 0.2909090909090908950, 0.2931818181818181546, 0.2954545454545454697, 0.2977272727272727293, 0.2999999999999999889, 0.3022727272727272485, 0.3045454545454545636, 0.3068181818181818232, 0.3090909090909090828, 0.3113636363636363424, 0.3136363636363636576, 0.3159090909090909172, 0.3181818181818181768, 0.3204545454545454364, 0.3227272727272727515, 0.3250000000000000111, 0.3272727272727272707, 0.3295454545454545303, 0.3318181818181818454, 0.3340909090909091050, 0.3363636363636363646, 0.3386363636363636243, 0.3409090909090908839, 0.3431818181818181990, 0.3454545454545454586, 0.3477272727272727182, 0.3499999999999999778, 0.3522727272727272929, 0.3545454545454545525, 0.3568181818181818121, 0.3590909090909090717, 0.3613636363636363869, 0.3636363636363636465, 0.3659090909090909061, 0.3681818181818181657, 0.3704545454545454808, 0.3727272727272727404, 0.3749999999999999445, 0.3772727272727272596, 0.3795454545454545192, 0.3818181818181818343, 0.3840909090909090939, 0.3863636363636363535, 0.3886363636363636131, 0.3909090909090909283, 0.3931818181818181879, 0.3954545454545454475, 0.3977272727272727071, 0.4000000000000000222, 0.4022727272727272818, 0.4045454545454545414, 0.4068181818181818010, 0.4090909090909091161, 0.4113636363636363757, 0.4136363636363636354, 0.4159090909090908950, 0.4181818181818181546, 0.4204545454545454697, 0.4227272727272727293, 0.4249999999999999889, 0.4272727272727272485, 0.4295454545454545636, 0.4318181818181818232, 0.4340909090909090828, 0.4363636363636363424, 0.4386363636363636576, 0.4409090909090909172, 0.4431818181818181768, 0.4454545454545454364, 0.4477272727272727515, 0.4500000000000000111, 0.4522727272727272707, 0.4545454545454545303, 0.4568181818181818454, 0.4590909090909091050, 0.4613636363636363646, 0.4636363636363636243, 0.4659090909090908839, 0.4681818181818181990, 0.4704545454545454586, 0.4727272727272727182, 0.4749999999999999778, 0.4772727272727272929, 0.4795454545454545525, 0.4818181818181818121, 0.4840909090909090717, 0.4863636363636363869, 0.4886363636363636465, 0.4909090909090909061, 0.4931818181818181657, 0.4954545454545454808, 0.4977272727272727404, 0.5000000000000000000, 0.5022727272727273151, 0.5045454545454545192, 0.5068181818181818343, 0.5090909090909090384, 0.5113636363636363535, 0.5136363636363636687, 0.5159090909090908728, 0.5181818181818181879, 0.5204545454545455030, 0.5227272727272727071, 0.5250000000000000222, 0.5272727272727272263, 0.5295454545454545414, 0.5318181818181818565, 0.5340909090909090606, 0.5363636363636363757, 0.5386363636363636909, 0.5409090909090908950, 0.5431818181818182101, 0.5454545454545454142, 0.5477272727272727293, 0.5500000000000000444, 0.5522727272727272485, 0.5545454545454545636, 0.5568181818181817677, 0.5590909090909090828, 0.5613636363636363980, 0.5636363636363636020, 0.5659090909090909172, 0.5681818181818182323, 0.5704545454545454364, 0.5727272727272727515, 0.5749999999999999556, 0.5772727272727272707, 0.5795454545454545858, 0.5818181818181817899, 0.5840909090909091050, 0.5863636363636363091, 0.5886363636363636243, 0.5909090909090909394, 0.5931818181818181435, 0.5954545454545454586, 0.5977272727272727737, 0.5999999999999999778, 0.6022727272727272929, 0.6045454545454544970, 0.6068181818181818121, 0.6090909090909091272, 0.6113636363636362203, 0.6136363636363636465, 0.6159090909090909616, 0.6181818181818181657, 0.6204545454545454808, 0.6227272727272726849, 0.6250000000000000000, 0.6272727272727273151, 0.6295454545454546302, 0.6318181818181818343, 0.6340909090909090384, 0.6363636363636363535, 0.6386363636363636687, 0.6409090909090908728, 0.6431818181818181879, 0.6454545454545455030, 0.6477272727272727071, 0.6500000000000000222, 0.6522727272727272263, 0.6545454545454545414, 0.6568181818181818565, 0.6590909090909090606, 0.6613636363636363757, 0.6636363636363636909, 0.6659090909090908950, 0.6681818181818182101, 0.6704545454545454142, 0.6727272727272727293, 0.6750000000000000444, 0.6772727272727272485, 0.6795454545454545636, 0.6818181818181817677, 0.6840909090909090828, 0.6863636363636363980, 0.6886363636363636020, 0.6909090909090909172, 0.6931818181818182323, 0.6954545454545454364, 0.6977272727272727515, 0.6999999999999999556, 0.7022727272727272707, 0.7045454545454545858, 0.7068181818181817899, 0.7090909090909091050, 0.7113636363636363091, 0.7136363636363636243, 0.7159090909090909394, 0.7181818181818181435, 0.7204545454545454586, 0.7227272727272727737, 0.7249999999999999778, 0.7272727272727272929, 0.7295454545454544970, 0.7318181818181818121, 0.7340909090909091272, 0.7363636363636363313, 0.7386363636363636465, 0.7409090909090909616, 0.7431818181818181657, 0.7454545454545454808, 0.7477272727272726849, 0.7499999999999998890, 0.7522727272727273151, 0.7545454545454545192, 0.7568181818181818343, 0.7590909090909090384, 0.7613636363636363535, 0.7636363636363636687, 0.7659090909090908728, 0.7681818181818181879, 0.7704545454545455030, 0.7727272727272727071, 0.7750000000000000222, 0.7772727272727272263, 0.7795454545454545414, 0.7818181818181818565, 0.7840909090909090606, 0.7863636363636363757, 0.7886363636363636909, 0.7909090909090908950, 0.7931818181818182101, 0.7954545454545454142, 0.7977272727272727293, 0.8000000000000000444, 0.8022727272727272485, 0.8045454545454545636, 0.8068181818181817677, 0.8090909090909090828, 0.8113636363636363980, 0.8136363636363636020, 0.8159090909090909172, 0.8181818181818182323, 0.8204545454545454364, 0.8227272727272727515, 0.8249999999999999556, 0.8272727272727272707, 0.8295454545454545858, 0.8318181818181817899, 0.8340909090909091050, 0.8363636363636363091, 0.8386363636363636243, 0.8409090909090909394, 0.8431818181818181435, 0.8454545454545454586, 0.8477272727272727737, 0.8499999999999999778, 0.8522727272727272929, 0.8545454545454544970, 0.8568181818181818121, 0.8590909090909091272, 0.8613636363636363313, 0.8636363636363636465, 0.8659090909090909616, 0.8681818181818181657, 0.8704545454545453698, 0.8727272727272726849, 0.8750000000000000000, 0.8772727272727273151, 0.8795454545454545192, 0.8818181818181818343, 0.8840909090909090384, 0.8863636363636363535, 0.8886363636363637797, 0.8909090909090908728, 0.8931818181818181879, 0.8954545454545455030, 0.8977272727272727071, 0.9000000000000000222, 0.9022727272727272263, 0.9045454545454545414, 0.9068181818181818565, 0.9090909090909090606, 0.9113636363636363757, 0.9136363636363636909, 0.9159090909090908950, 0.9181818181818182101, 0.9204545454545454142, 0.9227272727272727293, 0.9250000000000000444, 0.9272727272727272485, 0.9295454545454545636, 0.9318181818181817677, 0.9340909090909090828, 0.9363636363636363980, 0.9386363636363636020, 0.9409090909090909172, 0.9431818181818182323, 0.9454545454545454364, 0.9477272727272727515, 0.9499999999999999556, 0.9522727272727272707, 0.9545454545454545858, 0.9568181818181817899, 0.9590909090909091050, 0.9613636363636363091, 0.9636363636363636243, 0.9659090909090909394, 0.9681818181818181435, 0.9704545454545454586, 0.9727272727272727737, 0.9749999999999999778, 0.9772727272727272929, 0.9781254700864302487 ),
 .UNSPECIFIED. ) 
 CURVE ( )  GEOMETRIC_REPRESENTATION_ITEM ( )  RATIONAL_B_SPLINE_CURVE ( ( 1.000000000000000000, 0.9898214418809326842, 1.000000000000000000, 0.9898214418809326842, 1.000000000000000000, 0.9898214418809326842, 1.000000000000000000, 0.9898214418809326842, 1.000000000000000000, 0.9898214418809326842, 1.000000000000000000, 0.9898214418809326842, 1.000000000000000000, 0.9898214418809326842, 1.000000000000000000, 0.9898214418809326842, 1.000000000000000000, 0.9898214418809326842, 1.000000000000000000, 0.9898214418809326842, 1.000000000000000000, 0.9898214418809326842, 1.000000000000000000, 0.9898214418809326842, 1.000000000000000000, 0.9898214418809326842, 1.000000000000000000, 0.9898214418809326842, 1.000000000000000000, 0.9898214418809326842, 1.000000000000000000, 0.9898214418809326842, 1.000000000000000000, 0.9898214418809326842, 1.000000000000000000, 0.9898214418809326842, 1.000000000000000000, 0.9898214418809326842, 1.000000000000000000, 0.9898214418809326842, 1.000000000000000000, 0.9898214418809326842, 1.000000000000000000, 0.9898214418809326842, 1.000000000000000000, 0.9898214418809326842, 1.000000000000000000, 0.9898214418809326842, 1.000000000000000000, 0.9898214418809326842, 1.000000000000000000, 0.9898214418809326842, 1.000000000000000000, 0.9898214418809326842, 1.000000000000000000, 0.9898214418809326842, 1.000000000000000000, 0.9898214418809326842, 1.000000000000000000, 0.9898214418809326842, 1.000000000000000000, 0.9898214418809326842, 1.000000000000000000, 0.9898214418809326842, 1.000000000000000000, 0.9898214418809326842, 1.000000000000000000, 0.9898214418809326842, 1.000000000000000000, 0.9898214418809326842, 1.000000000000000000, 0.9898214418809326842, 1.000000000000000000, 0.9898214418809326842, 1.000000000000000000, 0.9898214418809326842, 1.000000000000000000, 0.9898214418809326842, 1.000000000000000000, 0.9898214418809326842, 1.000000000000000000, 0.9898214418809326842, 1.000000000000000000, 0.9898214418809326842, 1.000000000000000000, 0.9898214418809326842, 1.000000000000000000, 0.9898214418809326842, 1.000000000000000000, 0.9898214418809326842, 1.000000000000000000, 0.9898214418809326842, 1.000000000000000000, 0.9898214418809326842, 1.000000000000000000, 0.9898214418809326842, 1.000000000000000000, 0.9898214418809326842, 1.000000000000000000, 0.9898214418809326842, 1.000000000000000000, 0.9898214418809326842, 1.000000000000000000, 0.9898214418809326842, 1.000000000000000000, 0.9898214418809326842, 1.000000000000000000, 0.9898214418809326842, 1.000000000000000000, 0.9898214418809326842, 1.000000000000000000, 0.9898214418809326842, 1.000000000000000000, 0.9898214418809326842, 1.000000000000000000, 0.9898214418809326842, 1.000000000000000000, 0.9898214418809326842, 1.000000000000000000, 0.9898214418809326842, 1.000000000000000000, 0.9898214418809326842, 1.000000000000000000, 0.9898214418809326842, 1.000000000000000000, 0.9898214418809326842, 1.000000000000000000, 0.9898214418809326842, 1.000000000000000000, 0.9898214418809326842, 1.000000000000000000, 0.9898214418809326842, 1.000000000000000000, 0.9898214418809326842, 1.000000000000000000, 0.9898214418809326842, 1.000000000000000000, 0.9898214418809326842, 1.000000000000000000, 0.9898214418809326842, 1.000000000000000000, 0.9898214418809326842, 1.000000000000000000, 0.9898214418809326842, 1.000000000000000000, 0.9898214418809326842, 1.000000000000000000, 0.9898214418809326842, 1.000000000000000000, 0.9898214418809326842, 1.000000000000000000, 0.9898214418809326842, 1.000000000000000000, 0.9898214418809326842, 1.000000000000000000, 0.9898214418809326842, 1.000000000000000000, 0.9898214418809326842, 1.000000000000000000, 0.9898214418809326842, 1.000000000000000000, 0.9898214418809326842, 1.000000000000000000, 0.9898214418809326842, 1.000000000000000000, 0.9898214418809326842, 1.000000000000000000, 0.9898214418809326842, 1.000000000000000000, 0.9898214418809326842, 1.000000000000000000, 0.9898214418809326842, 1.000000000000000000, 0.9898214418809326842, 1.000000000000000000, 0.9898214418809326842, 1.000000000000000000, 0.9898214418809326842, 1.000000000000000000, 0.9898214418809326842, 1.000000000000000000, 0.9898214418809326842, 1.000000000000000000, 0.9898214418809326842, 1.000000000000000000, 0.9898214418809326842, 1.000000000000000000, 0.9898214418809326842, 1.000000000000000000, 0.9898214418809326842, 1.000000000000000000, 0.9898214418809326842, 1.000000000000000000, 0.9898214418809326842, 1.000000000000000000, 0.9898214418809326842, 1.000000000000000000, 0.9898214418809326842, 1.000000000000000000, 0.9898214418809326842, 1.000000000000000000, 0.9898214418809326842, 1.000000000000000000, 0.9898214418809326842, 1.000000000000000000, 0.9898214418809326842, 1.000000000000000000, 0.9898214418809326842, 1.000000000000000000, 0.9898214418809326842, 1.000000000000000000, 0.9898214418809326842, 1.000000000000000000, 0.9898214418809326842, 1.000000000000000000, 0.9898214418809326842, 1.000000000000000000, 0.9898214418809326842, 1.000000000000000000, 0.9898214418809326842, 1.000000000000000000, 0.9898214418809326842, 1.000000000000000000, 0.9898214418809326842, 1.000000000000000000, 0.9898214418809326842, 1.000000000000000000, 0.9898214418809326842, 1.000000000000000000, 0.9898214418809326842, 1.000000000000000000, 0.9898214418809326842, 1.000000000000000000, 0.9898214418809326842, 1.000000000000000000, 0.9898214418809326842, 1.000000000000000000, 0.9898214418809326842, 1.000000000000000000, 0.9898214418809326842, 1.000000000000000000, 0.9898214418809326842, 1.000000000000000000, 0.9898214418809326842, 1.000000000000000000, 0.9898214418809326842, 1.000000000000000000, 0.9898214418809326842, 1.000000000000000000, 0.9898214418809326842, 1.000000000000000000, 0.9898214418809326842, 1.000000000000000000, 0.9898214418809326842, 1.000000000000000000, 0.9898214418809326842, 1.000000000000000000, 0.9898214418809326842, 1.000000000000000000, 0.9898214418809326842, 1.000000000000000000, 0.9898214418809326842, 1.000000000000000000, 0.9898214418809326842, 1.000000000000000000, 0.9898214418809326842, 1.000000000000000000, 0.9898214418809326842, 1.000000000000000000, 0.9898214418809326842, 1.000000000000000000, 0.9898214418809326842, 1.000000000000000000, 0.9898214418809326842, 1.000000000000000000, 0.9898214418809326842, 1.000000000000000000, 0.9898214418809326842, 1.000000000000000000, 0.9898214418809326842, 1.000000000000000000, 0.9898214418809326842, 1.000000000000000000, 0.9898214418809326842, 1.000000000000000000, 0.9898214418809326842, 1.000000000000000000, 0.9898214418809326842, 1.000000000000000000, 0.9898214418809326842, 1.000000000000000000, 0.9898214418809326842, 1.000000000000000000, 0.9898214418809326842, 1.000000000000000000, 0.9898214418809326842, 1.000000000000000000, 0.9898214418809326842, 1.000000000000000000, 0.9898214418809326842, 1.000000000000000000, 0.9898214418809326842, 1.000000000000000000, 0.9898214418809326842, 1.000000000000000000, 0.9898214418809326842, 1.000000000000000000, 0.9898214418809326842, 1.000000000000000000, 0.9898214418809326842, 1.000000000000000000, 0.9898214418809326842, 1.000000000000000000, 0.9898214418809326842, 1.000000000000000000, 0.9898214418809326842, 1.000000000000000000, 0.9898214418809326842, 1.000000000000000000, 0.9898214418809326842, 1.000000000000000000, 0.9898214418809326842, 1.000000000000000000, 0.9898214418809326842, 1.000000000000000000, 0.9898214418809326842, 1.000000000000000000, 0.9898214418809326842, 1.000000000000000000, 0.9898214418809326842, 1.000000000000000000, 0.9898214418809326842, 1.000000000000000000, 0.9898214418809326842, 1.000000000000000000, 0.9898214418809326842, 1.000000000000000000, 0.9898214418809326842, 1.000000000000000000, 0.9898214418809326842, 1.000000000000000000, 0.9898214418809326842, 1.000000000000000000, 0.9898214418809326842, 1.000000000000000000, 0.9898214418809326842, 1.000000000000000000, 0.9898214418809326842, 1.000000000000000000, 0.9898214418809326842, 1.000000000000000000, 0.9898214418809326842, 1.000000000000000000, 0.9898214418809326842, 1.000000000000000000, 0.9898214418809326842, 1.000000000000000000, 0.9898214418809326842, 1.000000000000000000, 0.9898214418809326842, 1.000000000000000000, 0.9898214418809326842, 1.000000000000000000, 0.9898214418809326842, 1.000000000000000000, 0.9898214418809326842, 1.000000000000000000, 0.9898214418809326842, 1.000000000000000000, 0.9898214418809326842, 1.000000000000000000, 0.9898214418809326842, 1.000000000000000000, 0.9898214418809326842, 1.000000000000000000, 0.9898214418809326842, 1.000000000000000000, 0.9898214418809326842, 1.000000000000000000, 0.9898214418809326842, 1.000000000000000000, 0.9898214418809326842, 1.000000000000000000, 0.9898214418809326842, 1.000000000000000000, 0.9898214418809326842, 1.000000000000000000, 0.9898214418809326842, 1.000000000000000000, 0.9898214418809326842, 1.000000000000000000, 0.9898214418809326842, 1.000000000000000000, 0.9898214418809326842, 1.000000000000000000, 0.9898214418809326842, 1.000000000000000000, 0.9898214418809326842, 1.000000000000000000, 0.9898214418809326842, 1.000000000000000000, 0.9898214418809326842, 1.000000000000000000, 0.9898214418809326842, 1.000000000000000000, 0.9898214418809326842, 1.000000000000000000, 0.9898214418809326842, 1.000000000000000000, 0.9898214418809326842, 1.000000000000000000, 0.9898214418809326842, 1.000000000000000000, 0.9898214418809326842, 1.000000000000000000, 0.9898214418809326842, 1.000000000000000000, 0.9898214418809326842, 1.000000000000000000, 0.9898214418809326842, 1.000000000000000000, 0.9898214418809326842, 1.000000000000000000, 0.9898214418809326842, 1.000000000000000000, 0.9898214418809326842, 1.000000000000000000, 0.9898214418809326842, 1.000000000000000000, 0.9898214418809326842, 1.000000000000000000, 0.9898214418809326842, 1.000000000000000000, 0.9898214418809326842, 1.000000000000000000, 0.9898214418809326842, 1.000000000000000000, 0.9898214418809326842, 1.000000000000000000, 0.9898214418809326842, 1.000000000000000000, 0.9898214418809326842, 1.000000000000000000, 0.9898214418809326842, 1.000000000000000000, 0.9898214418809326842, 1.000000000000000000, 0.9898214418809326842, 1.000000000000000000, 0.9898214418809326842, 1.000000000000000000, 0.9898214418809326842, 1.000000000000000000, 0.9898214418809326842, 1.000000000000000000, 0.9898214418809326842, 1.000000000000000000, 0.9898214418809326842, 1.000000000000000000, 0.9898214418809326842, 1.000000000000000000, 0.9898214418809326842, 1.000000000000000000, 0.9898214418809326842, 1.000000000000000000, 0.9898214418809326842, 1.000000000000000000, 0.9898214418809326842, 1.000000000000000000, 0.9898214418809326842, 1.000000000000000000, 0.9898214418809326842, 1.000000000000000000, 0.9898214418809326842, 1.000000000000000000, 0.9898214418809326842, 1.000000000000000000, 0.9898214418809326842, 1.000000000000000000, 0.9898214418809326842, 1.000000000000000000, 0.9898214418809326842, 1.000000000000000000, 0.9898214418809326842, 1.000000000000000000, 0.9898214418809326842, 1.000000000000000000, 0.9898214418809326842, 1.000000000000000000, 0.9898214418809326842, 1.000000000000000000, 0.9898214418809326842, 1.000000000000000000, 0.9898214418809326842, 1.000000000000000000, 0.9898214418809326842, 1.000000000000000000, 0.9898214418809326842, 1.000000000000000000, 0.9898214418809326842, 1.000000000000000000, 0.9898214418809326842, 1.000000000000000000, 0.9898214418809326842, 1.000000000000000000, 0.9898214418809326842, 1.000000000000000000, 0.9898214418809326842, 1.000000000000000000, 0.9898214418809326842, 1.000000000000000000, 0.9898214418809326842, 1.000000000000000000, 0.9898214418809326842, 1.000000000000000000, 0.9898214418809326842, 1.000000000000000000, 0.9898214418809326842, 1.000000000000000000, 0.9898214418809326842, 1.000000000000000000, 0.9898214418809326842, 1.000000000000000000, 0.9898214418809326842, 1.000000000000000000, 0.9898214418809326842, 1.000000000000000000, 0.9898214418809326842, 1.000000000000000000, 0.9898214418809326842, 1.000000000000000000, 0.9898214418809326842, 1.000000000000000000, 0.9898214418809326842, 1.000000000000000000, 0.9898214418809326842, 1.000000000000000000, 0.9898214418809326842, 1.000000000000000000, 0.9898214418809326842, 1.000000000000000000, 0.9898214418809326842, 1.000000000000000000, 0.9898214418809326842, 1.000000000000000000, 0.9898214418809326842, 1.000000000000000000, 0.9898214418809326842, 1.000000000000000000, 0.9898214418809326842, 1.000000000000000000, 0.9898214418809326842, 1.000000000000000000, 0.9898214418809326842, 1.000000000000000000, 0.9898214418809326842, 1.000000000000000000, 0.9898214418809326842, 1.000000000000000000, 0.9898214418809326842, 1.000000000000000000, 0.9898214418809326842, 1.000000000000000000, 0.9898214418809326842, 1.000000000000000000, 0.9898214418809326842, 1.000000000000000000, 0.9898214418809326842, 1.000000000000000000, 0.9898214418809326842, 1.000000000000000000, 0.9898214418809326842, 1.000000000000000000, 0.9898214418809326842, 1.000000000000000000, 0.9898214418809326842, 1.000000000000000000, 0.9898214418809326842, 1.000000000000000000, 0.9898214418809326842, 1.000000000000000000, 0.9898214418809326842, 1.000000000000000000, 0.9898214418809326842, 1.000000000000000000, 0.9898214418809326842, 1.000000000000000000, 0.9898214418809326842, 1.000000000000000000, 0.9898214418809326842, 1.000000000000000000, 0.9898214418809326842, 1.000000000000000000, 0.9898214418809326842, 1.000000000000000000, 0.9898214418809326842, 1.000000000000000000, 0.9898214418809326842, 1.000000000000000000, 0.9898214418809326842, 1.000000000000000000, 0.9898214418809326842, 1.000000000000000000, 0.9898214418809326842, 1.000000000000000000, 0.9898214418809326842, 1.000000000000000000, 0.9898214418809326842, 1.000000000000000000, 0.9898214418809326842, 1.000000000000000000, 0.9898214418809326842, 1.000000000000000000, 0.9898214418809326842, 1.000000000000000000, 0.9898214418809326842, 1.000000000000000000, 0.9898214418809326842, 1.000000000000000000, 0.9898214418809326842, 1.000000000000000000, 0.9898214418809326842, 1.000000000000000000, 0.9898214418809326842, 1.000000000000000000, 0.9898214418809326842, 1.000000000000000000, 0.9898214418809326842, 1.000000000000000000, 0.9898214418809326842, 1.000000000000000000, 0.9898214418809326842, 1.000000000000000000, 0.9898214418809326842, 1.000000000000000000, 0.9898214418809326842, 1.000000000000000000, 0.9898214418809326842, 1.000000000000000000, 0.9898214418809326842, 1.000000000000000000, 0.9898214418809326842, 1.000000000000000000, 0.9898214418809326842, 1.000000000000000000, 0.9898214418809326842, 1.000000000000000000, 0.9898214418809326842, 1.000000000000000000, 0.9898214418809326842, 1.000000000000000000, 0.9898214418809326842, 1.000000000000000000, 0.9898214418809326842, 1.000000000000000000, 0.9898214418809326842, 1.000000000000000000, 0.9898214418809326842, 1.000000000000000000, 0.9898214418809326842, 1.000000000000000000, 0.9898214418809326842, 1.000000000000000000, 0.9898214418809326842, 1.000000000000000000, 0.9898214418809326842, 1.000000000000000000, 0.9898214418809326842, 1.000000000000000000, 0.9898214418809326842, 1.000000000000000000, 0.9898214418809326842, 1.000000000000000000, 0.9898214418809326842, 1.000000000000000000, 0.9898214418809326842, 1.000000000000000000, 0.9898214418809326842, 1.000000000000000000, 0.9898214418809326842, 1.000000000000000000, 0.9898214418809326842, 1.000000000000000000, 0.9898214418809326842, 1.000000000000000000, 0.9898214418809326842, 1.000000000000000000, 0.9898214418809326842, 1.000000000000000000, 0.9898214418809326842, 1.000000000000000000, 0.9898214418809326842, 1.000000000000000000, 0.9898214418809326842, 1.000000000000000000, 0.9898214418809326842, 1.000000000000000000, 0.9898214418809326842, 1.000000000000000000, 0.9898214418809326842, 1.000000000000000000, 0.9898214418809326842, 1.000000000000000000, 0.9898214418809326842, 1.000000000000000000, 0.9898214418809326842, 1.000000000000000000, 0.9898214418809326842, 1.000000000000000000, 0.9898214418809326842, 1.000000000000000000, 0.9898214418809326842, 1.000000000000000000, 0.9898214418809326842, 1.000000000000000000, 0.9898214418809326842, 1.000000000000000000, 0.9898214418809326842, 1.000000000000000000, 0.9898214418809326842, 1.000000000000000000, 0.9898214418809326842, 1.000000000000000000, 0.9898214418809326842, 1.000000000000000000, 0.9898214418809326842, 1.000000000000000000, 0.9898214418809326842, 1.000000000000000000, 0.9898214418809326842, 1.000000000000000000, 0.9898214418809326842, 1.000000000000000000, 0.9898214418809326842, 1.000000000000000000, 0.9898214418809326842, 1.000000000000000000, 0.9898214418809326842, 1.000000000000000000, 0.9898214418809326842, 1.000000000000000000, 0.9898214418809326842, 1.000000000000000000, 0.9898214418809326842, 1.000000000000000000, 0.9898214418809326842, 1.000000000000000000, 0.9898214418809326842, 1.000000000000000000, 0.9898214418809326842, 1.000000000000000000, 0.9898214418809326842, 1.000000000000000000, 0.9898214418809326842, 1.000000000000000000, 0.9898214418809326842, 1.000000000000000000, 0.9898214418809326842, 1.000000000000000000, 0.9898214418809326842, 1.000000000000000000, 0.9898214418809326842, 1.000000000000000000, 0.9898214418809326842, 1.000000000000000000, 0.9898214418809326842, 1.000000000000000000, 0.9898214418809326842, 1.000000000000000000, 0.9898214418809326842, 1.000000000000000000, 0.9898214418809326842, 1.000000000000000000, 0.9898214418809326842, 1.000000000000000000, 0.9898214418809326842, 1.000000000000000000, 0.9898214418809326842, 1.000000000000000000, 0.9898214418809326842, 1.000000000000000000, 0.9898214418809326842, 1.000000000000000000, 0.9898214418809326842, 1.000000000000000000, 0.9898214418809326842, 1.000000000000000000, 0.9898214418809326842, 1.000000000000000000, 0.9898214418809326842, 1.000000000000000000, 0.9898214418809326842, 1.000000000000000000, 0.9898214418809326842, 1.000000000000000000, 0.9898214418809326842, 1.000000000000000000, 0.9898214418809326842, 1.000000000000000000, 0.9898214418809326842, 1.000000000000000000, 0.9898214418809326842, 1.000000000000000000, 0.9898214418809326842, 1.000000000000000000, 0.9898214418809326842, 1.000000000000000000, 0.9898214418809326842, 1.000000000000000000, 0.9898214418809326842, 1.000000000000000000, 0.9898214418809326842, 1.000000000000000000, 0.9898214418809326842, 1.000000000000000000, 0.9898214418809326842, 1.000000000000000000, 0.9898214418809326842, 1.000000000000000000, 0.9898214418809326842, 1.000000000000000000, 0.9898214418809326842, 1.000000000000000000, 0.9898214418809326842, 1.000000000000000000, 0.9898214418809326842, 1.000000000000000000, 0.9898214418809326842, 1.000000000000000000, 0.9898214418809326842, 1.000000000000000000, 0.9898214418809326842, 1.000000000000000000, 0.9898214418809326842, 1.000000000000000000, 0.9898214418809326842, 1.000000000000000000, 0.9898214418809326842, 1.000000000000000000, 0.9898214418809326842, 1.000000000000000000, 0.9898214418809326842, 1.000000000000000000, 0.9898214418809326842, 1.000000000000000000, 0.9898214418809326842, 1.000000000000000000, 0.9898214418809326842, 1.000000000000000000, 0.9898214418809326842, 1.000000000000000000, 0.9898214418809326842, 1.000000000000000000, 0.9898214418809326842, 1.000000000000000000, 0.9898214418809326842, 1.000000000000000000, 0.9898214418809326842, 1.000000000000000000, 0.9898214418809326842, 1.000000000000000000, 0.9961809353924466759, 0.9952277490961531914 ) ) 
 REPRESENTATION_ITEM ( '' )  );
#45071=CARTESIAN_POINT ( 'NONE',  ( 815.2698199232962679, -256.8164208402379245, 342.5225473063383674 ) ) ;
#45072=CARTESIAN_POINT ( 'NONE',  ( 804.1105419155481968, -339.8272453906069472, 347.6308680596136469 ) ) ;
#45073=CARTESIAN_POINT ( 'NONE',  ( 757.2208543904082489, -424.7146871989589840, 350.9844846989624330 ) ) ;
#45078=CARTESIAN_POINT ( 'NONE',  ( 798.7617431975189675, -291.6237781080503169, 323.0428371773161871 ) ) ;
#45079=CARTESIAN_POINT ( 'NONE',  ( 799.9999999999993179, -462.9681489794448339, 370.0000000000000568 ) ) ;
#45081=CARTESIAN_POINT ( 'NONE',  ( 755.8894580844503253, -135.8272453906076009, 332.3691319403863531 ) ) ;
#45082=CARTESIAN_POINT ( 'NONE',  ( 756.3353852180819104, -29.90732993114771787, 331.1735550268788302 ) ) ;
#45085=CARTESIAN_POINT ( 'NONE',  ( 814.2805881961230625, -241.6454272087890729, 331.2368401574024119 ) ) ;
#45090=CARTESIAN_POINT ( 'NONE',  ( 814.5518280994195948, -63.72551174932939233, 332.4837098697145734 ) ) ;
#45091=CARTESIAN_POINT ( 'NONE',  ( 772.4999999999993179, -462.9681489794447771, 310.9526249034443026 ) ) ;
#45094=CARTESIAN_POINT ( 'NONE',  ( 814.8207195650702488, -314.1908817542433781, 336.2433038121456548 ) ) ;
#45096=CARTESIAN_POINT ( 'NONE',  ( 800.9747183278959710, -300.9982390220559409, 311.9810565676471583 ) ) ;
#45101=CARTESIAN_POINT ( 'NONE',  ( 804.9363028652555840, -400.2709662947828519, 338.2165204200192079 ) ) ;
#45102=CARTESIAN_POINT ( 'NONE',  ( 776.9254006560222479, -140.1908817542438896, 314.8983024940802125 ) ) ;
#45105=CARTESIAN_POINT ( 'NONE',  ( 778.7502325331095108, -72.35105083532378956, 304.6391490659818828 ) ) ;
#45106=CARTESIAN_POINT ( 'NONE',  ( 803.4237431249931660, -375.1800572038739574, 331.2633955100225194 ) ) ;
#45109=CARTESIAN_POINT ( 'NONE',  ( 758.0580252608178853, -438.4527844766009821, 328.0187753319985404 ) ) ;
#45113=CARTESIAN_POINT ( 'NONE',  ( 768.0187753319979720, -200.6346026584199365, 318.0580252608186242 ) ) ;
#45114=CARTESIAN_POINT ( 'NONE',  ( 758.0580252608178853, -174.4527844766018063, 328.0187753319985404 ) ) ;
#45119=CARTESIAN_POINT ( 'NONE',  ( 791.9812246680005501, -404.6346026584193396, 361.9419747391813189 ) ) ;
#45122=CARTESIAN_POINT ( 'NONE',  ( 800.9747183278959710, -108.9982390220565804, 311.9810565676471583 ) ) ;
#45128=CARTESIAN_POINT ( 'NONE',  ( 773.3843516231979720, -205.4419599262324425, 364.4086373105754433 ) ) ;
#45129=CARTESIAN_POINT ( 'NONE',  ( 791.7608162188021197, 205.0000000000000568, 339.9999999999999432 ) ) ;
#45133=FACE_OUTER_BOUND ( 'NONE', #23554, .T. ) ;
#45134=PLANE ( 'NONE',  #44734 ) ;
#45136=CARTESIAN_POINT ( 'NONE',  ( 805.6418435158337843, -125.4636090269712412, 363.8556311672236916 ) ) ;
#45144=CARTESIAN_POINT ( 'NONE',  ( 787.5531968255692163, -429.8272453906067199, 316.1348686366205811 ) ) ;
#45149=CARTESIAN_POINT ( 'NONE',  ( 797.8594530101008786, 10.45630643248850866, 322.1405469898980982 ) ) ;
#45151=CARTESIAN_POINT ( 'NONE',  ( 783.7953271457878373, -200.1908817542436907, 375.1787889125761239 ) ) ;
#45153=CARTESIAN_POINT ( 'NONE',  ( 747.2067596250078623, -195.1800572038744974, 352.2312462859687230 ) ) ;
#45156=CARTESIAN_POINT ( 'NONE',  ( 797.8594530101008786, -277.5436935675105019, 322.1405469898980982 ) ) ;
#45157=CARTESIAN_POINT ( 'NONE',  ( 802.9823548866075953, -73.09997266333502353, 330.0799878456151077 ) ) ;
#45161=CARTESIAN_POINT ( 'NONE',  ( 804.9511171171677688, -125.8055962898690581, 335.8780910478229202 ) ) ;
#45162=CARTESIAN_POINT ( 'NONE',  ( 759.7806653035534055, -342.9982390220557136, 324.8639956371180801 ) ) ;
#45165=CARTESIAN_POINT ( 'NONE',  ( 781.7834795799800531, -106.8164208402383935, 315.0636971347436202 ) ) ;
#45170=CARTESIAN_POINT ( 'NONE',  ( 811.6461892240364477, -364.7146871989592114, 324.1737431748509835 ) ) ;
#45171=ORIENTED_EDGE ( 'NONE', *, *, #24906, .F. ) ;
#45172=CARTESIAN_POINT ( 'NONE',  ( 781.7834795799800531, -274.8164208402378108, 315.0636971347436202 ) ) ;
#45174=CARTESIAN_POINT ( 'NONE',  ( 792.1044303154645831, -396.4527844766010389, 317.8323909638837677 ) ) ;
#45180=CARTESIAN_POINT ( 'NONE',  ( 805.1927285166397041, -112.8164208402383508, 341.8018195045277707 ) ) ;
#45181=CARTESIAN_POINT ( 'NONE',  ( 758.6633372737375112, -92.53286901714190549, 326.9102291470432533 ) ) ;
#45184=CARTESIAN_POINT ( 'NONE',  ( 805.9055244015594326, -339.6237781080502600, 315.8990559732753240 ) ) ;
#45185=CARTESIAN_POINT ( 'NONE',  ( 747.3154664389472828, -115.9874144716872877, 326.4474001241230781 ) ) ;
#45190=CARTESIAN_POINT ( 'NONE',  ( 814.4686193811664907, -3.281790845153435221, 346.2056067578752732 ) ) ;
#45197=CARTESIAN_POINT ( 'NONE',  ( 802.5472867521000353, -340.3726999360615082, 350.8726784830461156 ) ) ;
#45198=CARTESIAN_POINT ( 'NONE',  ( 776.2046728542105711, -308.1908817542434349, 304.8212110874238761 ) ) ;
#45201=CARTESIAN_POINT ( 'NONE',  ( 807.2620300519052989, -96.00906357242585898, 318.0141637701419768 ) ) ;
#45205=CARTESIAN_POINT ( 'NONE',  ( 758.0580252608178853, -198.4527844766017495, 328.0187753319985404 ) ) ;
#45207=CARTESIAN_POINT ( 'NONE',  ( 813.5763878283155464, -411.8272453906067199, 351.1614460488615350 ) ) ;
#45210=CARTESIAN_POINT ( 'NONE',  ( 754.7162404726377645, -62.73633629969871350, 339.4709603349214717 ) ) ;
#45213=CARTESIAN_POINT ( 'NONE',  ( 775.9200461376533440, -431.8055962898681059, 315.3028492785443291 ) ) ;
#45218=CARTESIAN_POINT ( 'NONE',  ( 749.8865473780648472, -260.5328690171413086, 322.1177392798429082 ) ) ;
#45219=CARTESIAN_POINT ( 'NONE',  ( 758.0580252608178853, -126.4527844766019626, 328.0187753319985404 ) ) ;
#45222=CARTESIAN_POINT ( 'NONE',  ( 764.8639956371174549, -272.0891481129651197, 319.7806653035542013 ) ) ;
#45224=DIRECTION ( 'NONE',  ( -1.000000000000000000, -0.000000000000000000, 0.000000000000000000 ) ) ;
#45229=CARTESIAN_POINT ( 'NONE',  ( 758.0580252608178853, -30.45278447660226817, 328.0187753319985404 ) ) ;
#45231=CARTESIAN_POINT ( 'NONE',  ( 811.0346526505617248, -374.6346026584193396, 323.0537975583478101 ) ) ;
#45232=CARTESIAN_POINT ( 'NONE',  ( 795.6651683502461765, -250.7146871989595809, 371.3240766477733814 ) ) ;
#45238=CARTESIAN_POINT ( 'NONE',  ( 781.7834795799800531, -250.8164208402379245, 315.0636971347436202 ) ) ;
#45240=CARTESIAN_POINT ( 'NONE',  ( 767.7687537140311633, -359.9073299311467053, 372.7932403749916830 ) ) ;
#45243=DIRECTION ( 'NONE',  ( 0.000000000000000000, 0.000000000000000000, 1.000000000000000000 ) ) ;
#45246=CARTESIAN_POINT ( 'NONE',  ( 776.9254006560222479, -212.1908817542436623, 314.8983024940802125 ) ) ;
#45247=CARTESIAN_POINT ( 'NONE',  ( 759.7806653035534055, -102.9982390220565520, 324.8639956371180801 ) ) ;
#45252=CARTESIAN_POINT ( 'NONE',  ( 754.8983024940795303, -282.8965053807776258, 336.9254006560228163 ) ) ;
#45255=CARTESIAN_POINT ( 'NONE',  ( 768.9521613784389729, -9.827245390607961539, 373.2346286133773106 ) ) ;
#45257=CARTESIAN_POINT ( 'NONE',  ( 763.2262854647970016, -176.6346026584199933, 309.2812353651462445 ) ) ;
#45258=CARTESIAN_POINT ( 'NONE',  ( 756.5762568750052424, -75.18005720387485269, 348.7366044899774238 ) ) ;
#45263=CARTESIAN_POINT ( 'NONE',  ( 812.3518521366052028, -433.0999726633339151, 326.5853460496235243 ) ) ;
#45264=EDGE_CURVE ( 'NONE', #44204, #31386, #15054, .T. ) ;
#45267=CARTESIAN_POINT ( 'NONE',  ( 755.2512626584698410, -391.5436935675101608, 315.2512626584710915 ) ) ;
#45268=CARTESIAN_POINT ( 'NONE',  ( 787.5162901302840055, -11.36187538569323863, 305.4481719005793252 ) ) ;
#45270=CARTESIAN_POINT ( 'NONE',  ( 766.7756240680305382, -14.53286901714214707, 361.5560724626415663 ) ) ;
#45271=EDGE_CURVE ( 'NONE', #38059, #24078, #33374, .T. ) ;
#45274=CARTESIAN_POINT ( 'NONE',  ( 744.9990715423526808, -186.3510508353234343, 341.2370466360926002 ) ) ;
#45275=CARTESIAN_POINT ( 'NONE',  ( 774.6312213355098493, -23.36187538569319244, 364.6798772138717482 ) ) ;
#45276=CARTESIAN_POINT ( 'NONE',  ( 813.9316612368132837, -175.4419599262325562, 348.6739635108323228 ) ) ;
#45280=CARTESIAN_POINT ( 'NONE',  ( 785.3687786644884454, -179.3618753856927128, 315.3201227861279676 ) ) ;
#45282=CARTESIAN_POINT ( 'NONE',  ( 804.6798772138710092, -303.7255117493286889, 334.6312213355106451 ) ) ;
#45284=DIRECTION ( 'NONE',  ( -1.000000000000000000, -0.000000000000000000, -0.000000000000000000 ) ) ;
#45287=CARTESIAN_POINT ( 'NONE',  ( 783.0433043558608688, -0.8965053807785533513, 315.1538015810313027 ) ) ;
#45290=CARTESIAN_POINT ( 'NONE',  ( 745.4481719005789273, -243.7255117493288310, 347.5162901302853697 ) ) ;
#45292=CARTESIAN_POINT ( 'NONE',  ( 755.3028492785439312, -327.2817908451525000, 335.9200461376539693 ) ) ;
#45293=CARTESIAN_POINT ( 'NONE',  ( 790.8726784830453198, -418.7146871989590409, 362.5472867521010585 ) ) ;
#45297=VERTEX_POINT ( 'NONE', #30142 ) ;
#45298=AXIS2_PLACEMENT_3D ( 'NONE', #43986, #26211, #12363 ) ;
#45299=CARTESIAN_POINT ( 'NONE',  ( 804.9511171171677688, -341.8055962898683333, 335.8780910478229202 ) ) ;
#45302=CARTESIAN_POINT ( 'NONE',  ( 773.4516893846965786, -139.6454272087893571, 315.8398074228977066 ) ) ;
#45306=CARTESIAN_POINT ( 'NONE',  ( 755.8990559732751535, -227.4636090269709143, 365.9055244015606831 ) ) ;
#45307=CARTESIAN_POINT ( 'NONE',  ( 772.3691319403857278, -191.2601417444143976, 315.8894580844506663 ) ) ;
#45309=DIRECTION ( 'NONE',  ( 0.000000000000000000, 0.000000000000000000, -1.000000000000000000 ) ) ;
#45311=CARTESIAN_POINT ( 'NONE',  ( 777.4774526936600978, -82.27096629478388934, 304.7301800767027657 ) ) ;
#45312=CARTESIAN_POINT ( 'NONE',  ( 790.0183182880230106, -452.9681489794449476, 362.9048749981275250 ) ) ;
#45317=CARTESIAN_POINT ( 'NONE',  ( 814.8207195650702488, -338.1908817542433212, 336.2433038121456548 ) ) ;
#45320=CARTESIAN_POINT ( 'NONE',  ( 745.7998596910086917, -293.3618753856923718, 332.5602148656461168 ) ) ;
#45324=CARTESIAN_POINT ( 'NONE',  ( 785.3141322388236176, -381.7255117493284615, 364.4286716492789537 ) ) ;
#45325=CARTESIAN_POINT ( 'NONE',  ( 804.6971507214547046, -147.2817908451529547, 344.0799538623459739 ) ) ;
#45328=CARTESIAN_POINT ( 'NONE',  ( 815.0009284576459549, -78.35105083532376113, 338.7629533639073429 ) ) ;
#45329=CARTESIAN_POINT ( 'NONE',  ( 803.6646147819162707, -377.9073299311465917, 348.8264449731211130 ) ) ;
#45330=CARTESIAN_POINT ( 'NONE',  ( 782.4968714119720516, 13.18357915976123174, 305.0891759886411023 ) ) ;
#45332=CARTESIAN_POINT ( 'NONE',  ( 804.6798772138708955, -423.7255117493281205, 334.6312213355107019 ) ) ;
#45337=CARTESIAN_POINT ( 'NONE',  ( 795.1360043628807261, -236.0891481129651766, 360.2193346964456282 ) ) ;
#45338=CARTESIAN_POINT ( 'NONE',  ( 797.8594530101009923, -205.5436935675108145, 322.1405469898982119 ) ) ;
#45344=CARTESIAN_POINT ( 'NONE',  ( 755.5713283507202505, -389.3618753856919739, 334.6858677611754729 ) ) ;
#45350=CARTESIAN_POINT ( 'NONE',  ( 747.2067596250078623, -147.1800572038746395, 352.2312462859687230 ) ) ;
#45353=CARTESIAN_POINT ( 'NONE',  ( 813.9316612368132837, -199.4419599262324709, 348.6739635108323228 ) ) ;
#45359=CARTESIAN_POINT ( 'NONE',  ( 769.1273215169530886, -214.7146871989597230, 317.4527132478988847 ) ) ;
#45368=CARTESIAN_POINT ( 'NONE',  ( 799.9636004259356241, -142.9181544815166376, 311.2241431872006956 ) ) ;
#45374=DIRECTION ( 'NONE',  ( 0.000000000000000000, 0.000000000000000000, 1.000000000000000000 ) ) ;
#45384=CARTESIAN_POINT ( 'NONE',  ( 768.9521613784389729, -249.8272453906072315, 373.2346286133773106 ) ) ;
#45386=CARTESIAN_POINT ( 'NONE',  ( 746.8695393053150156, -173.9073299311472169, 327.6429770376306010 ) ) ;
#45390=CARTESIAN_POINT ( 'NONE',  ( 771.1735550268778070, -297.1800572038740711, 316.3353852180827630 ) ) ;
#45391=CARTESIAN_POINT ( 'NONE',  ( 804.6971507214547046, -51.28179084515328867, 344.0799538623459739 ) ) ;
#45395=DIRECTION ( 'NONE',  ( 0.000000000000000000, 0.000000000000000000, -1.000000000000000000 ) ) ;
#45396=CARTESIAN_POINT ( 'NONE',  ( 803.8651313633788504, -125.2601417444145255, 332.4468031744301015 ) ) ;
#45397=CARTESIAN_POINT ( 'NONE',  ( 768.0187753319979720, -320.6346026584195670, 318.0580252608186242 ) ) ;
#45400=CARTESIAN_POINT ( 'NONE',  ( 800.0135310231082713, -86.08914811296573077, 325.0180583372163028 ) ) ;
#45404=CARTESIAN_POINT ( 'NONE',  ( 746.0683387631852383, -403.4419599262317888, 331.3260364891676204 ) ) ;
#45406=CARTESIAN_POINT ( 'NONE',  ( 804.9363028652555840, -280.2709662947833067, 338.2165204200192079 ) ) ;
#45411=CARTESIAN_POINT ( 'NONE',  ( 795.1360043628807261, -404.0891481129646081, 360.2193346964456282 ) ) ;
#45418=CARTESIAN_POINT ( 'NONE',  ( 800.2193346964447755, -114.9982390220565236, 355.1360043628815788 ) ) ;
#45419=CARTESIAN_POINT ( 'NONE',  ( 787.5531968255692163, -429.8272453906067199, 316.1348686366205811 ) ) ;
#45420=CARTESIAN_POINT ( 'NONE',  ( 803.2186876482843445, -103.9874144716873161, 350.0220218866286928 ) ) ;
#45423=CARTESIAN_POINT ( 'NONE',  ( 811.6461892240364477, -340.7146871989592114, 324.1737431748509835 ) ) ;
#45428=CARTESIAN_POINT ( 'NONE',  ( 745.1792804349281596, -38.19088175424422360, 343.7566961878542884 ) ) ;
#45431=LINE ( 'NONE', #27403, #35828 ) ;
#45438=CARTESIAN_POINT ( 'NONE',  ( 769.9779781133707957, -355.0999726633341993, 316.7813123517150871 ) ) ;
#45439=CARTESIAN_POINT ( 'NONE',  ( 745.7194118038753459, -325.6454272087888739, 348.7631598425976449 ) ) ;
#45443=CARTESIAN_POINT ( 'NONE',  ( 799.9636004259356241, -94.91815448151677970, 311.2241431872006956 ) ) ;
#45448=CARTESIAN_POINT ( 'NONE',  ( 805.1927285166397041, -184.8164208402380950, 341.8018195045277707 ) ) ;
#45450=CARTESIAN_POINT ( 'NONE',  ( 760.0363995740630116, -418.9181544815157849, 368.7758568127991907 ) ) ;
#45455=CARTESIAN_POINT ( 'NONE',  ( 786.2056067578752163, 12.19440371013049784, 374.4686193811670023 ) ) ;
#45459=CARTESIAN_POINT ( 'NONE',  ( 788.7631598425961101, -313.4419599262320730, 305.7194118038759143 ) ) ;
#45460=CARTESIAN_POINT ( 'NONE',  ( 800.0135310231082713, -134.0891481129655745, 325.0180583372163028 ) ) ;
#45463=CARTESIAN_POINT ( 'NONE',  ( 804.4286716492782716, -305.3618753856922581, 345.3141322388244703 ) ) ;
#45467=CARTESIAN_POINT ( 'NONE',  ( 779.9999999999992042, -452.9681489794448339, 339.9999999999999432 ) ) ;
#45472=ORIENTED_EDGE ( 'NONE', *, *, #45271, .T. ) ;
#45473=CARTESIAN_POINT ( 'NONE',  ( 788.7366044899766848, -11.90732993114778182, 316.5762568750059813 ) ) ;
#45476=CARTESIAN_POINT ( 'NONE',  ( 796.9462024416508257, -348.4527844766012095, 308.9653473494370246 ) ) ;
#45477=CARTESIAN_POINT ( 'NONE',  ( 811.6461892240364477, -244.7146871989596093, 324.1737431748509835 ) ) ;
#45482=CARTESIAN_POINT ( 'NONE',  ( 767.8955696845333705, -240.4527844766015221, 362.1676090361162323 ) ) ;
#45483=CARTESIAN_POINT ( 'NONE',  ( 747.2067596250078623, -387.1800572038738437, 352.2312462859687230 ) ) ;
#45487=FACE_OUTER_BOUND ( 'NONE', #14510, .T. ) ;
#45488=CARTESIAN_POINT ( 'NONE',  ( 755.5913626894240451, -229.6454272087890729, 346.6156483768012890 ) ) ;
#45489=CARTESIAN_POINT ( 'NONE',  ( 792.1044303154645831, -108.4527844766019911, 317.8323909638837677 ) ) ;
#45494=CARTESIAN_POINT ( 'NONE',  ( 802.7791456095903868, -292.7146871989594956, 329.0155153010375102 ) ) ;
#45496=CARTESIAN_POINT ( 'NONE',  ( 786.2694204179717872, 2.718209154846545683, 305.1769319972829067 ) ) ;
#45499=CARTESIAN_POINT ( 'NONE',  ( 810.7187646348534145, -186.4527844766017779, 356.7737145352016341 ) ) ;
#45500=CARTESIAN_POINT ( 'NONE',  ( 801.9419747391806368, -66.45278447660216159, 351.9812246680014027 ) ) ;
#45503=LINE ( 'NONE', #23992, #33538 ) ;
#45506=CARTESIAN_POINT ( 'NONE',  ( 795.8262568251477660, -430.3726999360611671, 308.3538107759623585 ) ) ;
#45509=CARTESIAN_POINT ( 'NONE',  ( 764.0069404352550464, -351.0783235625955854, 359.2566176426627180 ) ) ;
#45510=CARTESIAN_POINT ( 'NONE',  ( 777.5031285880264704, -46.81642084023858530, 374.9108240113588408 ) ) ;
#45513=CARTESIAN_POINT ( 'NONE',  ( 756.7813123517142913, -19.98741447168758256, 329.9779781133712504 ) ) ;
#45517=CARTESIAN_POINT ( 'NONE',  ( 814.8230680027162407, -173.8055962898689302, 333.7305795820267917 ) ) ;
#45521=CARTESIAN_POINT ( 'NONE',  ( 797.8594530101008786, -205.5436935675108430, 322.1405469898980982 ) ) ;
#45524=CARTESIAN_POINT ( 'NONE',  ( 759.7806653035535192, -342.9982390220557704, 324.8639956371181370 ) ) ;
#45527=CARTESIAN_POINT ( 'NONE',  ( 780.5290396650775619, -36.35105083532390324, 365.2837595273619513 ) ) ;
#45530=CARTESIAN_POINT ( 'NONE',  ( 758.8095938919644823, -272.0891481129651197, 311.6929314249762797 ) ) ;
#45531=CARTESIAN_POINT ( 'NONE',  ( 755.3028492785439312, -351.2817908451523294, 335.9200461376539693 ) ) ;
#45532=CARTESIAN_POINT ( 'NONE',  ( 769.1273215169530886, -430.7146871989590409, 317.4527132478988847 ) ) ;
#45539=CARTESIAN_POINT ( 'NONE',  ( 749.2812353651451076, -246.4527844766016074, 323.2262854647983090 ) ) ;
#45540=CARTESIAN_POINT ( 'NONE',  ( 765.8855110935204493, -334.1692326535047073, 319.0159684113471599 ) ) ;
#45542=CARTESIAN_POINT ( 'NONE',  ( 776.9254006560222479, -116.1908817542440033, 314.8983024940802125 ) ) ;
#45543=CARTESIAN_POINT ( 'NONE',  ( 805.1927285166397041, -16.81642084023866701, 341.8018195045277707 ) ) ;
#45547=CARTESIAN_POINT ( 'NONE',  ( 763.0428371773158460, -227.4636090269709143, 358.7617431975195359 ) ) ;
#45548=CARTESIAN_POINT ( 'NONE',  ( 814.8207195650702488, -242.1908817542435770, 336.2433038121456548 ) ) ;
#45549=CARTESIAN_POINT ( 'NONE',  ( 799.4546378042377910, -177.0783235625961538, 356.1575198192848006 ) ) ;
#45551=DIRECTION ( 'NONE',  ( 0.000000000000000000, 0.000000000000000000, 1.000000000000000000 ) ) ;
#45553=CARTESIAN_POINT ( 'NONE',  ( 772.5602148656447525, -9.725511749329603717, 305.7998596910095443 ) ) ;
#45554=CARTESIAN_POINT ( 'NONE',  ( 808.2983282543862060, -452.9681489794448908, 337.2950253338145785 ) ) ;
#45557=CARTESIAN_POINT ( 'NONE',  ( 745.7194118038753459, -349.6454272087887603, 348.7631598425976449 ) ) ;
#45559=CARTESIAN_POINT ( 'NONE',  ( 792.2312462859673587, -299.9073299311468759, 307.2067596250082602 ) ) ;
#45564=CARTESIAN_POINT ( 'NONE',  ( 754.8072714833581358, -388.8164208402374129, 338.1981804954720587 ) ) ;
#45566=CARTESIAN_POINT ( 'NONE',  ( 755.3028492785439312, -159.2817908451529547, 335.9200461376539693 ) ) ;
#45569=CARTESIAN_POINT ( 'NONE',  ( 791.1614460488616487, -83.26014174441466764, 373.5763878283158874 ) ) ;
#45570=CARTESIAN_POINT ( 'NONE',  ( 771.1735550268780344, -393.1800572038737869, 316.3353852180828198 ) ) ;
#45573=CARTESIAN_POINT ( 'NONE',  ( 801.9419747391806368, -426.4527844766010389, 351.9812246680014027 ) ) ;
#45575=ORIENTED_EDGE ( 'NONE', *, *, #38557, .F. ) ;
#45577=ADVANCED_FACE ( 'NONE', ( #45619 ), #14452, .F. ) ;
#45580=CARTESIAN_POINT ( 'NONE',  ( 756.5762568750052424, -243.1800572038743269, 348.7366044899774238 ) ) ;
#45581=CARTESIAN_POINT ( 'NONE',  ( 791.9812246680005501, -236.6346026584198228, 361.9419747391813189 ) ) ;
#45585=CARTESIAN_POINT ( 'NONE',  ( 754.8072714833581358, -388.8164208402374129, 338.1981804954720587 ) ) ;
#45588=CARTESIAN_POINT ( 'NONE',  ( 782.5225473063383106, -142.2709662947837330, 375.2698199232970637 ) ) ;
#45590=CARTESIAN_POINT ( 'NONE',  ( 805.9055244015594326, -195.6237781080506863, 315.8990559732753240 ) ) ;
#45592=ORIENTED_EDGE ( 'NONE', *, *, #38840, .T. ) ;
#45597=CARTESIAN_POINT ( 'NONE',  ( 772.3691319403857278, -215.2601417444141987, 315.8894580844506663 ) ) ;
#45600=VERTEX_POINT ( 'NONE', #36601 ) ;
#45606=CARTESIAN_POINT ( 'NONE',  ( 771.3260364891663130, -139.6454272087893571, 306.0683387631859773 ) ) ;
#45614=CARTESIAN_POINT ( 'NONE',  ( 749.5768839229115201, -372.5545181178796383, 358.0661480581553064 ) ) ;
#45619=FACE_OUTER_BOUND ( 'NONE', #22903, .T. ) ;
#45622=CARTESIAN_POINT ( 'NONE',  ( 757.7880784355613741, -258.0090635724253616, 312.4576283171834916 ) ) ;
#45624=CARTESIAN_POINT ( 'NONE',  ( 787.5162901302840055, -179.3618753856927128, 305.4481719005792684 ) ) ;
#45628=CARTESIAN_POINT ( 'NONE',  ( 756.5762568750052424, -291.1800572038741848, 348.7366044899774238 ) ) ;
#45629=CARTESIAN_POINT ( 'NONE',  ( 755.5913626894240451, -85.64542720878952764, 346.6156483768012890 ) ) ;
#45633=CARTESIAN_POINT ( 'NONE',  ( 764.0069404352550464, -135.0783235625962959, 359.2566176426627180 ) ) ;
#45634=CARTESIAN_POINT ( 'NONE',  ( 762.3223304703356007, -319.5436935675104451, 322.3223304703362828 ) ) ;
#45638=CARTESIAN_POINT ( 'NONE',  ( 791.9812246680005501, -92.63460265842026331, 361.9419747391813189 ) ) ;
#45641=CARTESIAN_POINT ( 'NONE',  ( 783.7566961878529810, -408.8965053807772847, 305.1792804349288417 ) ) ;
#45643=CARTESIAN_POINT ( 'NONE',  ( 767.8955696845333705, -288.4527844766014937, 362.1676090361162323 ) ) ;
#45648=CARTESIAN_POINT ( 'NONE',  ( 768.0187753319979720, -392.6346026584193396, 318.0580252608186242 ) ) ;
#45653=CARTESIAN_POINT ( 'NONE',  ( 786.5483106153019435, -439.6454272087884760, 364.1601925771022366 ) ) ;
#45654=CARTESIAN_POINT ( 'NONE',  ( 804.9511171171677688, -125.8055962898690581, 335.8780910478229202 ) ) ;
#45657=CARTESIAN_POINT ( 'NONE',  ( 749.8865473780648472, -404.5328690171409107, 322.1177392798429082 ) ) ;
#45662=CARTESIAN_POINT ( 'NONE',  ( 795.8262568251477660, -46.37269993606239638, 308.3538107759623585 ) ) ;
#45670=CARTESIAN_POINT ( 'NONE',  ( 805.2837595273609850, -362.7363362996977116, 340.5290396650784714 ) ) ;
#45671=CARTESIAN_POINT ( 'NONE',  ( 776.2046728542105711, -332.1908817542433781, 304.8212110874238761 ) ) ;
#45676=CARTESIAN_POINT ( 'NONE',  ( 762.1177392798416577, -138.5545181178802636, 309.8865473780659272 ) ) ;
#45681=CARTESIAN_POINT ( 'NONE',  ( 781.8018195045266339, -190.2709662947835909, 365.1927285166406705 ) ) ;
#45682=CARTESIAN_POINT ( 'NONE',  ( 759.9999999999992042, -512.9681489794448908, 350.0000000000000000 ) ) ;
#45683=CARTESIAN_POINT ( 'NONE',  ( 797.8822607201568644, -462.5545181178792973, 370.1134526219340160 ) ) ;
#45688=CARTESIAN_POINT ( 'NONE',  ( 764.3348316497523456, 1.285312801039623753, 308.6759233522265617 ) ) ;
#45690=CARTESIAN_POINT ( 'NONE',  ( 771.2633955100217236, -263.9073299311469327, 363.4237431249939618 ) ) ;
#45693=CARTESIAN_POINT ( 'NONE',  ( 807.5423716828161105, -321.0783235625956991, 362.2119215644372048 ) ) ;
#45694=CARTESIAN_POINT ( 'NONE',  ( 755.3201227861273992, -123.7255117493292289, 345.3687786644892981 ) ) ;
#45696=CARTESIAN_POINT ( 'NONE',  ( 800.0135310231082713, -302.0891481129650629, 325.0180583372163028 ) ) ;
#45698=CYLINDRICAL_SURFACE ( 'NONE', #9914, 30.00000000000002842 ) ;
#45704=CARTESIAN_POINT ( 'NONE',  ( 805.1927285166397041, -16.81642084023866701, 341.8018195045277707 ) ) ;
#45706=CARTESIAN_POINT ( 'NONE',  ( 808.0189434323515343, -350.0891481129648923, 319.0252816721025511 ) ) ;
#45707=CARTESIAN_POINT ( 'NONE',  ( 778.7502325331095108, -240.3510508353232069, 304.6391490659818828 ) ) ;
#45708=CARTESIAN_POINT ( 'NONE',  ( 800.1688906516307043, -58.16923265350564520, 369.0717654672308186 ) ) ;
#45712=CARTESIAN_POINT ( 'NONE',  ( 803.4237431249931660, -255.1800572038742700, 331.2633955100225194 ) ) ;
#45713=CARTESIAN_POINT ( 'NONE',  ( 811.0346526505616112, -374.6346026584192828, 323.0537975583477532 ) ) ;
#45718=CARTESIAN_POINT ( 'NONE',  ( 800.9840315886518738, -244.9181544815162681, 354.1144889064786412 ) ) ;
#45719=CARTESIAN_POINT ( 'NONE',  ( 774.6312213355099630, -119.3618753856928691, 364.6798772138717482 ) ) ;
#45723=CARTESIAN_POINT ( 'NONE',  ( 755.0488828828309806, -305.8055962898684470, 344.1219089521771934 ) ) ;
#45725=CARTESIAN_POINT ( 'NONE',  ( 780.5290396650775619, -36.35105083532390324, 365.2837595273619513 ) ) ;
#45759=COLOUR_RGB('Grey',0.48,0.52,0.57);
#45760=FILL_AREA_STYLE_COLOUR('',#45759);
#45761=FILL_AREA_STYLE('',(#45760));
#45762=SURFACE_STYLE_FILL_AREA(#45761);
#45763=SURFACE_SIDE_STYLE('',(#45762));
#45764=SURFACE_STYLE_USAGE(.BOTH.,#45763);
#45765=PRESENTATION_STYLE_ASSIGNMENT((#45764));
ENDSEC;
END-ISO-10303-21;
